ISO-10303-21;
HEADER;
FILE_DESCRIPTION (('STEP AP214'),
    '1' );
FILE_NAME ('straight bevel gear(static)_iso_ISO - Straight bevel gear 2M 48GT 49PT 20PA 5FW ---48O25H100MD16.0N.step',
    '2026-10-08T08:02:49',
    ( '' ),
    ( '' ),
    'SwSTEP 2.0',
    'SolidWorks 2026',
    '' );
FILE_SCHEMA (( 'AUTOMOTIVE_DESIGN' ));
ENDSEC;

DATA;
#11=ORIENTED_EDGE ( 'NONE', *, *, #34105, .F. ) ;
#12=CARTESIAN_POINT ( 'NONE',  ( 2.624215991343608501, -38.92973006074533515, 28.09277600149204801 ) ) ;
#15=CARTESIAN_POINT ( 'NONE',  ( 0.9752132459055861124, -16.63533515462550127, -39.55248938404434966 ) ) ;
#20=ORIENTED_EDGE ( 'NONE', *, *, #44663, .F. ) ;
#24=ADVANCED_FACE ( 'NONE', ( #21978 ), #2362, .F. ) ;
#25=CARTESIAN_POINT ( 'NONE',  ( 5.960221823109900008, 10.26751639438343311, 17.77295928189558794 ) ) ;
#27=LINE ( 'NONE', #23853, #11554 ) ;
#29=CARTESIAN_POINT ( 'NONE',  ( 4.956653778116966613, 0.000000000000000000, 0.000000000000000000 ) ) ;
#31=VECTOR ( 'NONE', #37686, 1000.000000000000000 ) ;
#35=CARTESIAN_POINT ( 'NONE',  ( 5.960221823109900008, -10.25807604135609274, -17.77840967225716895 ) ) ;
#48=CARTESIAN_POINT ( 'NONE',  ( 0.5807400328401574052, 47.89582301953903709, 0.5448834511091634747 ) ) ;
#53=CARTESIAN_POINT ( 'NONE',  ( 0.5839879327111927587, 29.08515285004941120, -38.05372318152023325 ) ) ;
#60=VERTEX_POINT ( 'NONE', #12282 ) ;
#63=CARTESIAN_POINT ( 'NONE',  ( 0.9740398440564311811, -11.50548031350412970, -41.33716823241943672 ) ) ;
#64=ORIENTED_EDGE ( 'NONE', *, *, #23685, .F. ) ;
#68=FACE_OUTER_BOUND ( 'NONE', #26695, .T. ) ;
#69=ADVANCED_FACE ( 'NONE', ( #31062 ), #10020, .T. ) ;
#71=CARTESIAN_POINT ( 'NONE',  ( 0.9722240741986376555, 11.66659279944034111, -41.29187377038488194 ) ) ;
#74=ORIENTED_EDGE ( 'NONE', *, *, #24741, .T. ) ;
#77=CARTESIAN_POINT ( 'NONE',  ( 0.9740398440564309590, -34.29238484271514409, -25.79088785829017283 ) ) ;
#79=EDGE_LOOP ( 'NONE', ( #41919, #50694, #26736, #25891 ) ) ;
#84=CARTESIAN_POINT ( 'NONE',  ( 5.981074661064941900, 2.670494474391725159, 20.35019299530689096 ) ) ;
#85=CARTESIAN_POINT ( 'NONE',  ( 1.227938101723757836, -15.63977281655870222, 39.96870412324331312 ) ) ;
#97=CARTESIAN_POINT ( 'NONE',  ( 2.526552050251863690, 17.56110221699880825, -39.22765360404633128 ) ) ;
#101=B_SPLINE_CURVE_WITH_KNOTS ( 'NONE', 3,
 ( #15435, #38953, #58005, #53923, #53312, #29209 ),
 .UNSPECIFIED., .F., .F.,
 ( 4, 2, 4 ),
 ( 0.000000000000000000, 0.0002291966416970781840, 0.0004583932833941563680 ),
 .UNSPECIFIED. ) ;
#103=CARTESIAN_POINT ( 'NONE',  ( 0.9758171775293917882, -42.54062484958058832, 5.606549717954040446 ) ) ;
#106=CARTESIAN_POINT ( 'NONE',  ( 3.270143674763207553, -9.870732238228454136, -9.482922169188068295 ) ) ;
#109=CARTESIAN_POINT ( 'NONE',  ( 5.959547316686252039, -5.315863417546194292, -19.82530672674360517 ) ) ;
#111=CARTESIAN_POINT ( 'NONE',  ( 0.9730545539215883499, 21.01499094264548972, 37.40983423658480689 ) ) ;
#115=CARTESIAN_POINT ( 'NONE',  ( 4.956653778116975495, 26.26162724282373517, 40.28700667097690769 ) ) ;
#124=ORIENTED_EDGE ( 'NONE', *, *, #27240, .T. ) ;
#132=CARTESIAN_POINT ( 'NONE',  ( 0.5834872094924158370, -41.36515088387901784, -24.14431479207734554 ) ) ;
#133=B_SPLINE_CURVE_WITH_KNOTS ( 'NONE', 3,
 ( #55260, #2330, #15845, #26459 ),
 .UNSPECIFIED., .F., .F.,
 ( 4, 4 ),
 ( 0.000000000000000000, 0.004446090762761379864 ),
 .UNSPECIFIED. ) ;
#136=ORIENTED_EDGE ( 'NONE', *, *, #11452, .T. ) ;
#139=CARTESIAN_POINT ( 'NONE',  ( 4.956653778116987930, -47.05699031914942054, -9.917440902361647659 ) ) ;
#147=VERTEX_POINT ( 'NONE', #41411 ) ;
#148=( BOUNDED_SURFACE ( )  B_SPLINE_SURFACE ( 3, 1, ( 
 ( #20134, #29510 ),
 ( #43334, #14815 ),
 ( #19515, #5067 ),
 ( #19828, #43643 ) ),
 .UNSPECIFIED., .F., .F., .F. ) 
 B_SPLINE_SURFACE_WITH_KNOTS ( ( 4, 4 ),
 ( 2, 2 ),
 ( 0.000000000000000000, 1.000000000000000000 ),
 ( 0.000000000000000000, 1.000000000000000000 ),
 .UNSPECIFIED. ) 
 GEOMETRIC_REPRESENTATION_ITEM ( )  RATIONAL_B_SPLINE_SURFACE ( (
 ( 1.000000000000000000, 1.000000000000000000),
 ( 0.9953390228620291325, 0.8624445117761032620),
 ( 0.9953390228620291325, 0.8624445117761032620),
 ( 1.000000000000000000, 1.000000000000000000) ) ) 
 REPRESENTATION_ITEM ( '' )  SURFACE ( )  );
#149=CARTESIAN_POINT ( 'NONE',  ( 0.8557997880470697982, -11.51622788066490166, 46.50333260518556244 ) ) ;
#152=CARTESIAN_POINT ( 'NONE',  ( 1.227938101723756947, 42.65467462194918369, 4.762198645644581951 ) ) ;
#156=ORIENTED_EDGE ( 'NONE', *, *, #13892, .F. ) ;
#168=CARTESIAN_POINT ( 'NONE',  ( 0.5819845901640497976, -47.42480841519684986, -6.701564444318185210 ) ) ;
#169=EDGE_CURVE ( 'NONE', #49553, #36850, #1300, .T. ) ;
#171=CARTESIAN_POINT ( 'NONE',  ( 0.9749527285493309048, 26.34702925571547993, -33.86694354778329341 ) ) ;
#174=ORIENTED_EDGE ( 'NONE', *, *, #46970, .T. ) ;
#175=CARTESIAN_POINT ( 'NONE',  ( 0.5837374860065644988, -18.49670552082923436, -44.18034382476643884 ) ) ;
#176=CARTESIAN_POINT ( 'NONE',  ( 3.783278058412224976, 41.09146792477083920, -12.79810311738810569 ) ) ;
#185=CARTESIAN_POINT ( 'NONE',  ( 0.7056555295713297093, 38.50897360867684682, 28.48870155114923008 ) ) ;
#200=ORIENTED_EDGE ( 'NONE', *, *, #48538, .F. ) ;
#201=CARTESIAN_POINT ( 'NONE',  ( 4.967162193818130511, -32.68434214048149045, -28.07411493385329138 ) ) ;
#202=EDGE_CURVE ( 'NONE', #46227, #38797, #32610, .T. ) ;
#204=CARTESIAN_POINT ( 'NONE',  ( 0.9752570700956801897, 42.57087745267997292, -5.371905812151719140 ) ) ;
#205=CARTESIAN_POINT ( 'NONE',  ( 3.270143674763207553, 4.983712007628229301, 12.74832469035454352 ) ) ;
#212=EDGE_CURVE ( 'NONE', #15210, #7786, #8757, .T. ) ;
#215=ORIENTED_EDGE ( 'NONE', *, *, #7819, .T. ) ;
#222=LINE ( 'NONE', #29992, #19722 ) ;
#225=CIRCLE ( 'NONE', #35287, 43.08621763946400307 ) ;
#230=VECTOR ( 'NONE', #33635, 1000.000000000000000 ) ;
#234=CARTESIAN_POINT ( 'NONE',  ( 0.5807400328401637335, 44.45848844984468684, -17.82553128098359352 ) ) ;
#239=CARTESIAN_POINT ( 'NONE',  ( 0.7057020205115017708, -46.04437542275037032, -13.20843872046536838 ) ) ;
#240=ADVANCED_FACE ( 'NONE', ( #18825 ), #57227, .F. ) ;
#242=CARTESIAN_POINT ( 'NONE',  ( 0.8557997880470690211, -0.9121262075942833114, -47.89938907511595545 ) ) ;
#244=B_SPLINE_CURVE_WITH_KNOTS ( 'NONE', 3,
 ( #37504, #42512, #47202, #27774, #51255, #61267 ),
 .UNSPECIFIED., .F., .F.,
 ( 4, 2, 4 ),
 ( 8.673617379884035472E-19, 0.0002291966416970798374, 0.0004583932833941588075 ),
 .UNSPECIFIED. ) ;
#247=( BOUNDED_SURFACE ( )  B_SPLINE_SURFACE ( 3, 1, ( 
 ( #59221, #21649 ),
 ( #26042, #59538 ),
 ( #16970, #45789 ),
 ( #49843, #50457 ) ),
 .UNSPECIFIED., .F., .F., .F. ) 
 B_SPLINE_SURFACE_WITH_KNOTS ( ( 4, 4 ),
 ( 2, 2 ),
 ( 0.000000000000000000, 1.000000000000000000 ),
 ( 0.000000000000000000, 1.000000000000000000 ),
 .UNSPECIFIED. ) 
 GEOMETRIC_REPRESENTATION_ITEM ( )  RATIONAL_B_SPLINE_SURFACE ( (
 ( 1.000000000000000000, 1.000000000000000000),
 ( 0.7269869731126817891, 0.9931720237060910339),
 ( 0.7269869731126817891, 0.9931720237060910339),
 ( 1.000000000000000000, 1.000000000000000000) ) ) 
 REPRESENTATION_ITEM ( '' )  SURFACE ( )  );
#249=CARTESIAN_POINT ( 'NONE',  ( 0.9722240741986378776, 16.95645453362518040, -39.41582013185131927 ) ) ;
#262=CARTESIAN_POINT ( 'NONE',  ( 0.9757402383260960210, -21.52772413548508368, 37.11731350497348103 ) ) ;
#266=( BOUNDED_SURFACE ( )  B_SPLINE_SURFACE ( 3, 1, ( 
 ( #49830, #53575 ),
 ( #35756, #6889 ),
 ( #40459, #1574 ),
 ( #29792, #1269 ) ),
 .UNSPECIFIED., .F., .F., .F. ) 
 B_SPLINE_SURFACE_WITH_KNOTS ( ( 4, 4 ),
 ( 2, 2 ),
 ( 0.000000000000000000, 1.000000000000000000 ),
 ( 0.000000000000000000, 1.000000000000000000 ),
 .UNSPECIFIED. ) 
 GEOMETRIC_REPRESENTATION_ITEM ( )  RATIONAL_B_SPLINE_SURFACE ( (
 ( 1.000000000000000000, 1.000000000000000000),
 ( 0.7269869731126821222, 0.9931720237060910339),
 ( 0.7269869731126821222, 0.9931720237060910339),
 ( 1.000000000000000000, 1.000000000000000000) ) ) 
 REPRESENTATION_ITEM ( '' )  SURFACE ( )  );
#275=CARTESIAN_POINT ( 'NONE',  ( 0.5850706913938534814, -47.50996714391777687, -6.071602062251110432 ) ) ;
#278=CARTESIAN_POINT ( 'NONE',  ( 1.227938101723748288, -6.439911493064859549, 42.43379953535183802 ) ) ;
#287=CIRCLE ( 'NONE', #35352, 43.08621763946400307 ) ;
#294=CARTESIAN_POINT ( 'NONE',  ( 3.660176727303412036, -4.399934609596269475, -47.83637937224829528 ) ) ;
#298=ORIENTED_EDGE ( 'NONE', *, *, #8490, .F. ) ;
#306=ORIENTED_EDGE ( 'NONE', *, *, #19497, .F. ) ;
#309=ORIENTED_EDGE ( 'NONE', *, *, #7412, .F. ) ;
#310=CARTESIAN_POINT ( 'NONE',  ( 0.9730545539215883499, -16.88610103448528221, -39.44597740938079511 ) ) ;
#311=CARTESIAN_POINT ( 'NONE',  ( 5.974727161628367256, 2.663664384318781941, -20.35137732084673345 ) ) ;
#315=CARTESIAN_POINT ( 'NONE',  ( 0.5837374860065646098, 44.31936661703473135, 18.16107481025614945 ) ) ;
#316=CARTESIAN_POINT ( 'NONE',  ( 1.154321485836934169, -10.30834589251740141, 41.66001465002025128 ) ) ;
#317=ORIENTED_EDGE ( 'NONE', *, *, #60187, .F. ) ;
#337=CARTESIAN_POINT ( 'NONE',  ( 0.5807400328401637335, 41.75144119563886136, 23.47602859900728944 ) ) ;
#345=CARTESIAN_POINT ( 'NONE',  ( 3.407937589446174087, 11.14158115674384142, -7.970324840161847391 ) ) ;
#348=CARTESIAN_POINT ( 'NONE',  ( 0.5839254288179550612, -23.86932519546702380, -41.52446060675850248 ) ) ;
#352=CARTESIAN_POINT ( 'NONE',  ( 0.5839254288179565044, 29.22920395911566160, -37.94310411505115610 ) ) ;
#355=VERTEX_POINT ( 'NONE', #58856 ) ;
#356=CARTESIAN_POINT ( 'NONE',  ( 0.9757892942422815574, 5.651566539685822121, 42.53466646637865267 ) ) ;
#357=DIRECTION ( 'NONE',  ( 0.07836865515943411409, 0.8593913859058514015, 0.5052769534812779906 ) ) ;
#358=AXIS2_PLACEMENT_3D ( 'NONE', #19879, #43697, #29251 ) ;
#368=ORIENTED_EDGE ( 'NONE', *, *, #18760, .F. ) ;
#370=CARTESIAN_POINT ( 'NONE',  ( 2.526464513654347765, -41.81190200959792236, -9.948146339971660979 ) ) ;
#385=CARTESIAN_POINT ( 'NONE',  ( 4.967162193818130511, 14.26841313271336809, -40.65506779172149976 ) ) ;
#386=CARTESIAN_POINT ( 'NONE',  ( 4.967162193818130511, 0.000000000000000000, 0.000000000000000000 ) ) ;
#387=EDGE_CURVE ( 'NONE', #3069, #4945, #35089, .T. ) ;
#391=ADVANCED_FACE ( 'NONE', ( #36552 ), #45224, .F. ) ;
#392=CARTESIAN_POINT ( 'NONE',  ( 4.967162193818132288, 19.45289607368876617, -38.44485641567052880 ) ) ;
#401=ORIENTED_EDGE ( 'NONE', *, *, #17470, .T. ) ;
#405=CARTESIAN_POINT ( 'NONE',  ( 1.088313998177380837, -20.77783415101598763, -37.54798835078477026 ) ) ;
#410=LINE ( 'NONE', #3884, #31382 ) ;
#412=DIRECTION ( 'NONE',  ( 0.000000000000000000, 0.000000000000000000, 1.000000000000000000 ) ) ;
#421=CARTESIAN_POINT ( 'NONE',  ( 5.960721111146673579, -10.26825948882938278, 17.77250458025974567 ) ) ;
#437=VERTEX_POINT ( 'NONE', #22126 ) ;
#439=DIRECTION ( 'NONE',  ( 0.000000000000000000, 0.000000000000000000, 1.000000000000000000 ) ) ;
#444=CARTESIAN_POINT ( 'NONE',  ( 0.6067099128993267421, 37.56352526808347392, -29.71710940500694065 ) ) ;
#445=CARTESIAN_POINT ( 'NONE',  ( 5.860006189529234355, -15.52021937683242570, -45.66786516969946064 ) ) ;
#447=B_SPLINE_CURVE_WITH_KNOTS ( 'NONE', 3,
 ( #26125, #21427, #16736, #35853, #54922, #31132, #50240, #45560, #2614, #40877, #36165, #59942, #17052, #55539, #31763, #50851 ),
 .UNSPECIFIED., .F., .F.,
 ( 4, 3, 3, 3, 3, 4 ),
 ( 1.095097866269904594E-17, 0.0002724568934985561975, 0.0004086836638483808517, 0.0005449104342063608745, 0.0008173270854453682996, 0.001089761613562689442 ),
 .UNSPECIFIED. ) ;
#448=VERTEX_POINT ( 'NONE', #17428 ) ;
#457=B_SPLINE_CURVE_WITH_KNOTS ( 'NONE', 3,
 ( #61646, #61952, #57249, #33493, #52569, #5253, #28771, #46982, #61341, #18456, #47895, #37582, #56652, #54096, #25009, #25303, #35038, #58486, #25614 ),
 .UNSPECIFIED., .F., .F.,
 ( 4, 3, 3, 3, 3, 3, 4 ),
 ( 0.000000000000000000, 0.0002724573126191725029, 0.0004086839781548403999, 0.0005449106435901787757, 0.0006811373090491486390, 0.0008459866663933673144, 0.001010840725717216185 ),
 .UNSPECIFIED. ) ;
#459=COLOUR_RGB ( '', 0.66274510, 0.83137255, 0.94901961) ;
#460=CARTESIAN_POINT ( 'NONE',  ( 5.960221823109900008, 2.673723662181063165, 20.35070456576735509 ) ) ;
#461=VERTEX_POINT ( 'NONE', #18671 ) ;
#465=VECTOR ( 'NONE', #30114, 999.9999999999998863 ) ;
#475=CARTESIAN_POINT ( 'NONE',  ( 0.9754642270333672149, -42.51806607596984833, -5.774842730422477644 ) ) ;
#489=B_SPLINE_CURVE_WITH_KNOTS ( 'NONE', 3,
 ( #45173, #59532, #34830, #7209, #21337, #54832 ),
 .UNSPECIFIED., .F., .F.,
 ( 4, 2, 4 ),
 ( 0.000000000000000000, 0.0002291966416970804880, 0.0004583932833941609759 ),
 .UNSPECIFIED. ) ;
#498=CARTESIAN_POINT ( 'NONE',  ( 0.5809828226811565299, -23.47450554821739743, 41.74875432577639600 ) ) ;
#505=EDGE_CURVE ( 'NONE', #5333, #39487, #51048, .T. ) ;
#507=CARTESIAN_POINT ( 'NONE',  ( 0.8557997880470690211, -28.43566216844996930, 38.55640757422429488 ) ) ;
#508=LINE ( 'NONE', #20561, #47490 ) ;
#519=DIRECTION ( 'NONE',  ( -1.000000000000000000, -0.000000000000000000, -0.000000000000000000 ) ) ;
#520=CARTESIAN_POINT ( 'NONE',  ( 0.5786265663353153954, 47.89572889566446179, -0.7221568112308096588 ) ) ;
#523=CARTESIAN_POINT ( 'NONE',  ( 0.5819845901640490204, -47.54333976522121219, 5.801229454883783276 ) ) ;
#531=ORIENTED_EDGE ( 'NONE', *, *, #50574, .F. ) ;
#534=DIRECTION ( 'NONE',  ( -1.000000000000000000, -0.000000000000000000, -0.000000000000000000 ) ) ;
#551=CONICAL_SURFACE ( 'NONE', #54554, 43.08621763946400307, 1.568696531533066763 ) ;
#557=AXIS2_PLACEMENT_3D ( 'NONE', #18443, #31926, #56946 ) ;
#562=CARTESIAN_POINT ( 'NONE',  ( 0.7057020205115049905, 11.58334423512235922, 46.47981817772228652 ) ) ;
#564=AXIS2_PLACEMENT_3D ( 'NONE', #56138, #46464, #17637 ) ;
#568=ORIENTED_EDGE ( 'NONE', *, *, #7137, .F. ) ;
#575=ORIENTED_EDGE ( 'NONE', *, *, #20466, .T. ) ;
#581=CARTESIAN_POINT ( 'NONE',  ( 0.9754402186311948997, -21.29160191075025210, 37.25324696807224001 ) ) ;
#584=CARTESIAN_POINT ( 'NONE',  ( 5.965394784446458765, 18.95742317323944803, -7.868087674480759297 ) ) ;
#585=EDGE_LOOP ( 'NONE', ( #45645, #16766, #10272, #13377 ) ) ;
#592=CARTESIAN_POINT ( 'NONE',  ( 0.5807400328401574052, -47.55718917606839824, -5.711437504336464244 ) ) ;
#596=AXIS2_PLACEMENT_3D ( 'NONE', #6152, #30291, #11204 ) ;
#606=CARTESIAN_POINT ( 'NONE',  ( 4.956653778116975495, 9.917440902361160937, 47.05699031914952712 ) ) ;
#609=EDGE_CURVE ( 'NONE', #39397, #32445, #6080, .T. ) ;
#613=AXIS2_PLACEMENT_3D ( 'NONE', #47675, #58583, #43615 ) ;
#617=ORIENTED_EDGE ( 'NONE', *, *, #13578, .F. ) ;
#619=CARTESIAN_POINT ( 'NONE',  ( 0.5807400328401574052, 41.20655774452968956, 24.41979442053183647 ) ) ;
#623=CARTESIAN_POINT ( 'NONE',  ( 0.5819845079324652559, 0.4540594263153105992, 47.89381220525411464 ) ) ;
#625=CARTESIAN_POINT ( 'NONE',  ( 1.088313998177384834, 22.12859469727390760, -36.76812638579207260 ) ) ;
#627=EDGE_CURVE ( 'NONE', #10594, #18602, #5314, .T. ) ;
#630=CARTESIAN_POINT ( 'NONE',  ( 0.5809828226811617480, 34.25055090842200656, -33.48000389720580472 ) ) ;
#631=CARTESIAN_POINT ( 'NONE',  ( 0.5786265663353153954, 18.99608782658033590, 43.97352617418621890 ) ) ;
#635=CARTESIAN_POINT ( 'NONE',  ( 0.5839254288179547281, -33.80331890503245518, -33.93171296845874707 ) ) ;
#638=CARTESIAN_POINT ( 'NONE',  ( 0.8551540677456715978, -19.17641535420884580, 43.91216198251532887 ) ) ;
#641=( BOUNDED_SURFACE ( )  B_SPLINE_SURFACE ( 3, 1, ( 
 ( #9444, #9142 ),
 ( #28248, #47991 ),
 ( #4720, #28864 ),
 ( #23866, #14478 ) ),
 .UNSPECIFIED., .F., .F., .F. ) 
 B_SPLINE_SURFACE_WITH_KNOTS ( ( 4, 4 ),
 ( 2, 2 ),
 ( 0.000000000000000000, 1.000000000000000000 ),
 ( 0.000000000000000000, 1.000000000000000000 ),
 .UNSPECIFIED. ) 
 GEOMETRIC_REPRESENTATION_ITEM ( )  RATIONAL_B_SPLINE_SURFACE ( (
 ( 1.000000000000000000, 1.000000000000000000),
 ( 0.9732289882329797637, 0.9999525324661233672),
 ( 0.9732289882329797637, 0.9999525324661233672),
 ( 1.000000000000000000, 1.000000000000000000) ) ) 
 REPRESENTATION_ITEM ( '' )  SURFACE ( )  );
#642=CARTESIAN_POINT ( 'NONE',  ( 0.9745511491811738036, 25.84997388131858997, 34.24777528633291723 ) ) ;
#645=CARTESIAN_POINT ( 'NONE',  ( 3.270143674763207553, 9.482922169188102046, -9.870732238228422162 ) ) ;
#655=CARTESIAN_POINT ( 'NONE',  ( 5.860006189529234355, 26.78264244998154098, -40.11385274514653787 ) ) ;
#657=CARTESIAN_POINT ( 'NONE',  ( 5.960221823109900008, -7.859839668735337348, 18.96108896995701798 ) ) ;
#659=EDGE_CURVE ( 'NONE', #34606, #4050, #44974, .T. ) ;
#661=CIRCLE ( 'NONE', #21651, 48.09070567114147110 ) ;
#670=CARTESIAN_POINT ( 'NONE',  ( 0.5809828226811553087, 34.25055090842153760, 33.48000389720628789 ) ) ;
#677=EDGE_CURVE ( 'NONE', #34340, #5939, #5995, .T. ) ;
#678=CARTESIAN_POINT ( 'NONE',  ( 0.6846871229502899947, 47.37786444808403274, -7.109010606686910982 ) ) ;
#683=CARTESIAN_POINT ( 'NONE',  ( 0.6846871229502932144, -13.23224427737861930, 46.04462816497483146 ) ) ;
#686=ORIENTED_EDGE ( 'NONE', *, *, #27933, .T. ) ;
#688=CARTESIAN_POINT ( 'NONE',  ( 0.9730545539215892381, 25.71816799638828499, -34.34678117142529175 ) ) ;
#690=ADVANCED_FACE ( 'NONE', ( #22057 ), #36431, .F. ) ;
#694=VERTEX_POINT ( 'NONE', #41182 ) ;
#708=CARTESIAN_POINT ( 'NONE',  ( 4.963659409799330291, 14.83726297270336580, -42.22332985082294243 ) ) ;
#716=CARTESIAN_POINT ( 'NONE',  ( 0.7762783648524382851, -38.54028518467400488, -28.45155609988369250 ) ) ;
#721=ORIENTED_EDGE ( 'NONE', *, *, #32659, .F. ) ;
#722=VERTEX_POINT ( 'NONE', #26431 ) ;
#730=DIRECTION ( 'NONE',  ( 0.000000000000000000, 0.000000000000000000, 1.000000000000000000 ) ) ;
#731=CARTESIAN_POINT ( 'NONE',  ( 0.5800708057587392608, 0.6275304576137059609, -47.89175345272231255 ) ) ;
#740=AXIS2_PLACEMENT_3D ( 'NONE', #47734, #42736, #43357 ) ;
#745=FACE_OUTER_BOUND ( 'NONE', #14666, .T. ) ;
#751=FACE_OUTER_BOUND ( 'NONE', #41449, .T. ) ;
#754=( BOUNDED_SURFACE ( )  B_SPLINE_SURFACE ( 3, 1, ( 
 ( #48930, #29199 ),
 ( #58298, #43641 ),
 ( #5979, #683 ),
 ( #20739, #25738 ) ),
 .UNSPECIFIED., .F., .F., .F. ) 
 B_SPLINE_SURFACE_WITH_KNOTS ( ( 4, 4 ),
 ( 2, 2 ),
 ( 0.000000000000000000, 1.000000000000000000 ),
 ( 0.000000000000000000, 1.000000000000000000 ),
 .UNSPECIFIED. ) 
 GEOMETRIC_REPRESENTATION_ITEM ( )  RATIONAL_B_SPLINE_SURFACE ( (
 ( 1.000000000000000000, 1.000000000000000000),
 ( 0.9953390228620291325, 0.8624445117761032620),
 ( 0.9953390228620291325, 0.8624445117761032620),
 ( 1.000000000000000000, 1.000000000000000000) ) ) 
 REPRESENTATION_ITEM ( '' )  SURFACE ( )  );
#755=CARTESIAN_POINT ( 'NONE',  ( 0.9730545539215892381, -11.59290486963536360, 41.31259007387227911 ) ) ;
#761=DIRECTION ( 'NONE',  ( -1.000000000000000000, -0.000000000000000000, -0.000000000000000000 ) ) ;
#764=ORIENTED_EDGE ( 'NONE', *, *, #45036, .T. ) ;
#765=CARTESIAN_POINT ( 'NONE',  ( 1.227938101723748288, 39.96870412324358313, -15.63977281655798812 ) ) ;
#767=CARTESIAN_POINT ( 'NONE',  ( 0.5839879327111929808, -41.52454255611490197, -23.86931774877339762 ) ) ;
#769=VECTOR ( 'NONE', #19028, 1000.000000000000114 ) ;
#783=CARTESIAN_POINT ( 'NONE',  ( 0.8551540677456715978, -7.157691013574052796, -47.37911285756627677 ) ) ;
#787=CARTESIAN_POINT ( 'NONE',  ( 1.227938101723748288, 42.43379953535185933, 6.439911493064710335 ) ) ;
#800=CARTESIAN_POINT ( 'NONE',  ( 0.5827359174754832560, 28.86822142608449226, 38.21848266111678782 ) ) ;
#801=ORIENTED_EDGE ( 'NONE', *, *, #43455, .F. ) ;
#803=ORIENTED_EDGE ( 'NONE', *, *, #32383, .T. ) ;
#805=CARTESIAN_POINT ( 'NONE',  ( 2.624215991343608501, -43.79392271049056262, -19.66774719433024998 ) ) ;
#807=ORIENTED_EDGE ( 'NONE', *, *, #18327, .F. ) ;
#809=CARTESIAN_POINT ( 'NONE',  ( 0.9757402383260950218, 26.18833306844200237, -33.98983788393794470 ) ) ;
#817=VERTEX_POINT ( 'NONE', #56170 ) ;
#818=CARTESIAN_POINT ( 'NONE',  ( 0.5819845901640506858, -24.34012668949516112, 41.25023214430193264 ) ) ;
#826=CARTESIAN_POINT ( 'NONE',  ( 5.981074661064941900, 2.687517936919725958, 20.34795181394749619 ) ) ;
#833=AXIS2_PLACEMENT_3D ( 'NONE', #52167, #23673, #42803 ) ;
#838=FACE_OUTER_BOUND ( 'NONE', #41555, .T. ) ;
#843=CARTESIAN_POINT ( 'NONE',  ( 1.088313998177379949, 30.89087247895970734, -29.78798111128795512 ) ) ;
#848=CARTESIAN_POINT ( 'NONE',  ( -20.00652009675311405, -7.982586356554360663, 0.5445903824078870414 ) ) ;
#853=CARTESIAN_POINT ( 'NONE',  ( 0.8551540677456834771, 29.88829867897813841, 37.45266983663506721 ) ) ;
#854=CARTESIAN_POINT ( 'NONE',  ( 0.5827359174754830340, 47.53228759166454864, -5.891371786504479680 ) ) ;
#857=CARTESIAN_POINT ( 'NONE',  ( 0.8557997880470599172, -44.60232077416698360, 17.48760788519201981 ) ) ;
#865=DIRECTION ( 'NONE',  ( 0.07836865515943411409, -0.5052769534812810992, 0.8593913859058496252 ) ) ;
#874=FACE_OUTER_BOUND ( 'NONE', #59056, .T. ) ;
#879=VECTOR ( 'NONE', #23921, 1000.000000000000227 ) ;
#882=CARTESIAN_POINT ( 'NONE',  ( 0.5836750258453345941, 6.071582023534265460, 47.50958153310754284 ) ) ;
#883=CARTESIAN_POINT ( 'NONE',  ( 0.5838002273316434954, -6.386683873060837513, 47.46823345111867809 ) ) ;
#884=VERTEX_POINT ( 'NONE', #47714 ) ;
#894=CIRCLE ( 'NONE', #35930, 43.08621763946400307 ) ;
#899=CARTESIAN_POINT ( 'NONE',  ( 5.960721111146673579, -2.685391721746187343, 20.34914600876570390 ) ) ;
#901=CARTESIAN_POINT ( 'NONE',  ( 2.624215991343608501, 46.71702075422666667, -11.05657803850996856 ) ) ;
#905=( BOUNDED_SURFACE ( )  B_SPLINE_SURFACE ( 3, 1, ( 
 ( #19570, #11393 ),
 ( #26404, #54580 ),
 ( #11093, #22031 ),
 ( #30476, #49590 ) ),
 .UNSPECIFIED., .F., .F., .F. ) 
 B_SPLINE_SURFACE_WITH_KNOTS ( ( 4, 4 ),
 ( 2, 2 ),
 ( 0.000000000000000000, 1.000000000000000000 ),
 ( 0.000000000000000000, 1.000000000000000000 ),
 .UNSPECIFIED. ) 
 GEOMETRIC_REPRESENTATION_ITEM ( )  RATIONAL_B_SPLINE_SURFACE ( (
 ( 1.000000000000000000, 1.000000000000000000),
 ( 0.9953390228620291325, 0.8624445117760984880),
 ( 0.9953390228620291325, 0.8624445117760984880),
 ( 1.000000000000000000, 1.000000000000000000) ) ) 
 REPRESENTATION_ITEM ( '' )  SURFACE ( )  );
#909=CARTESIAN_POINT ( 'NONE',  ( 3.407937589446174087, -5.663729899985161076, 12.47329436636627165 ) ) ;
#914=( BOUNDED_SURFACE ( )  B_SPLINE_SURFACE ( 3, 1, ( 
 ( #11593, #53245 ),
 ( #5309, #59175 ),
 ( #30365, #48259 ),
 ( #34166, #619 ) ),
 .UNSPECIFIED., .F., .F., .F. ) 
 B_SPLINE_SURFACE_WITH_KNOTS ( ( 4, 4 ),
 ( 2, 2 ),
 ( 0.000000000000000000, 1.000000000000000000 ),
 ( 0.000000000000000000, 1.000000000000000000 ),
 .UNSPECIFIED. ) 
 GEOMETRIC_REPRESENTATION_ITEM ( )  RATIONAL_B_SPLINE_SURFACE ( (
 ( 1.000000000000000000, 1.000000000000000000),
 ( 0.9732289882329797637, 0.9999525324661233672),
 ( 0.9732289882329797637, 0.9999525324661233672),
 ( 1.000000000000000000, 1.000000000000000000) ) ) 
 REPRESENTATION_ITEM ( '' )  SURFACE ( )  );
#918=DIRECTION ( 'NONE',  ( 0.000000000000000000, 0.000000000000000000, 1.000000000000000000 ) ) ;
#922=( BOUNDED_SURFACE ( )  B_SPLINE_SURFACE ( 3, 1, ( 
 ( #61204, #61807 ),
 ( #57111, #27707 ),
 ( #4791, #22697 ),
 ( #32725, #8581 ) ),
 .UNSPECIFIED., .F., .F., .F. ) 
 B_SPLINE_SURFACE_WITH_KNOTS ( ( 4, 4 ),
 ( 2, 2 ),
 ( 0.000000000000000000, 1.000000000000000000 ),
 ( 0.000000000000000000, 1.000000000000000000 ),
 .UNSPECIFIED. ) 
 GEOMETRIC_REPRESENTATION_ITEM ( )  RATIONAL_B_SPLINE_SURFACE ( (
 ( 1.000000000000000000, 1.000000000000000000),
 ( 0.9953390228620291325, 0.8624445117761032620),
 ( 0.9953390228620291325, 0.8624445117761032620),
 ( 1.000000000000000000, 1.000000000000000000) ) ) 
 REPRESENTATION_ITEM ( '' )  SURFACE ( )  );
#924=DIRECTION ( 'NONE',  ( -1.000000000000000000, -0.000000000000000000, -0.000000000000000000 ) ) ;
#925=B_SPLINE_CURVE_WITH_KNOTS ( 'NONE', 3,
 ( #18539, #13233, #27317, #46445, #18240, #32336 ),
 .UNSPECIFIED., .F., .F.,
 ( 4, 2, 4 ),
 ( 3.529906531158615134E-18, 0.0002445244328975386492, 0.0004890488657950738290 ),
 .UNSPECIFIED. ) ;
#929=VERTEX_POINT ( 'NONE', #23904 ) ;
#933=CARTESIAN_POINT ( 'NONE',  ( 1.088908134280554885, -6.374115321932803724, -42.43751564162690926 ) ) ;
#941=DIRECTION ( 'NONE',  ( -1.000000000000000000, -0.000000000000000000, -0.000000000000000000 ) ) ;
#945=CARTESIAN_POINT ( 'NONE',  ( 0.9968887458511664912, 22.02152923727802403, -36.82760690604603582 ) ) ;
#947=EDGE_LOOP ( 'NONE', ( #43971, #42340, #37157, #45668 ) ) ;
#954=ORIENTED_EDGE ( 'NONE', *, *, #11455, .T. ) ;
#962=CARTESIAN_POINT ( 'NONE',  ( 4.956653778116975495, -27.17045123668499684, 39.67974989265029961 ) ) ;
#965=ORIENTED_EDGE ( 'NONE', *, *, #16950, .F. ) ;
#971=CARTESIAN_POINT ( 'NONE',  ( 0.5800708057587357080, 46.09746469244102229, 13.00144577271058388 ) ) ;
#974=CARTESIAN_POINT ( 'NONE',  ( 4.956653778116990594, -3.690426056929668075, -47.94889704119055551 ) ) ;
#985=CARTESIAN_POINT ( 'NONE',  ( 0.5809828226811626362, 29.58751527316234231, -37.66417181417519799 ) ) ;
#989=CARTESIAN_POINT ( 'NONE',  ( 0.9758171775293910111, 5.606549717954186995, 42.54062484958058121 ) ) ;
#992=( BOUNDED_SURFACE ( )  B_SPLINE_SURFACE ( 3, 1, ( 
 ( #421, #14258 ),
 ( #33364, #13635 ),
 ( #19566, #28636 ),
 ( #23948, #56213 ) ),
 .UNSPECIFIED., .F., .F., .F. ) 
 B_SPLINE_SURFACE_WITH_KNOTS ( ( 4, 4 ),
 ( 2, 2 ),
 ( 0.000000000000000000, 1.000000000000000000 ),
 ( 0.000000000000000000, 1.000000000000000000 ),
 .UNSPECIFIED. ) 
 GEOMETRIC_REPRESENTATION_ITEM ( )  RATIONAL_B_SPLINE_SURFACE ( (
 ( 1.000000000000000000, 1.000000000000000000),
 ( 0.9953390228620291325, 0.8624445117760984880),
 ( 0.9953390228620291325, 0.8624445117760984880),
 ( 1.000000000000000000, 1.000000000000000000) ) ) 
 REPRESENTATION_ITEM ( '' )  SURFACE ( )  );
#995=VERTEX_POINT ( 'NONE', #15749 ) ;
#998=( BOUNDED_SURFACE ( )  B_SPLINE_SURFACE ( 3, 1, ( 
 ( #15677, #54781 ),
 ( #21290, #34781 ),
 ( #20676, #49790 ),
 ( #15982, #53845 ) ),
 .UNSPECIFIED., .F., .F., .F. ) 
 B_SPLINE_SURFACE_WITH_KNOTS ( ( 4, 4 ),
 ( 2, 2 ),
 ( 0.000000000000000000, 1.000000000000000000 ),
 ( 0.000000000000000000, 1.000000000000000000 ),
 .UNSPECIFIED. ) 
 GEOMETRIC_REPRESENTATION_ITEM ( )  RATIONAL_B_SPLINE_SURFACE ( (
 ( 1.000000000000000000, 1.000000000000000000),
 ( 0.7269869731126821222, 0.9931720237060910339),
 ( 0.7269869731126821222, 0.9931720237060910339),
 ( 1.000000000000000000, 1.000000000000000000) ) ) 
 REPRESENTATION_ITEM ( '' )  SURFACE ( )  );
#1001=VERTEX_POINT ( 'NONE', #34238 ) ;
#1009=CARTESIAN_POINT ( 'NONE',  ( 4.963659409799330291, -43.79875484948454556, 9.199077662858760718 ) ) ;
#1010=LINE ( 'NONE', #39571, #13026 ) ;
#1012=ORIENTED_EDGE ( 'NONE', *, *, #32338, .T. ) ;
#1016=CARTESIAN_POINT ( 'NONE',  ( 5.958863334805807099, -14.51296551801813095, 14.51469124124454702 ) ) ;
#1018=B_SPLINE_CURVE_WITH_KNOTS ( 'NONE', 3,
 ( #48990, #34593, #49286, #53658, #15796, #29258 ),
 .UNSPECIFIED., .F., .F.,
 ( 4, 2, 4 ),
 ( 8.848046324741092137E-18, 0.0002291978881530155638, 0.0004583957763060222913 ),
 .UNSPECIFIED. ) ;
#1030=ORIENTED_EDGE ( 'NONE', *, *, #26800, .F. ) ;
#1032=DIRECTION ( 'NONE',  ( 0.07836865515943411409, -0.2503967164834464132, -0.9649662368512228472 ) ) ;
#1037=EDGE_CURVE ( 'NONE', #437, #47724, #101, .T. ) ;
#1040=CARTESIAN_POINT ( 'NONE',  ( 5.965394784446460541, -20.35165389555760029, 2.664747781315769615 ) ) ;
#1053=CARTESIAN_POINT ( 'NONE',  ( 0.5834872094924179464, -41.59216540884680313, 23.75111410077694174 ) ) ;
#1060=CARTESIAN_POINT ( 'NONE',  ( 4.960156602257177916, 30.99165383632763238, 34.56254177294278662 ) ) ;
#1069=CARTESIAN_POINT ( 'NONE',  ( 1.227938101723747621, 22.18841447410770940, -36.73927144310489012 ) ) ;
#1071=CARTESIAN_POINT ( 'NONE',  ( 2.624215991343608501, -17.05978231157370928, -44.87417713512106587 ) ) ;
#1075=CARTESIAN_POINT ( 'NONE',  ( 0.9730545539215883499, -39.44597740938048958, -16.88610103448599986 ) ) ;
#1076=CARTESIAN_POINT ( 'NONE',  ( 1.227938101723748288, -25.45152231597034387, -34.55893248994532030 ) ) ;
#1082=CARTESIAN_POINT ( 'NONE',  ( 0.9757402383260936896, 42.53022961222603726, 5.684842778069367775 ) ) ;
#1083=EDGE_LOOP ( 'NONE', ( #44728, #30417, #16495, #59746 ) ) ;
#1086=CARTESIAN_POINT ( 'NONE',  ( 0.9968887458511644928, -0.6574002966411479632, 42.90440775986216693 ) ) ;
#1093=CARTESIAN_POINT ( 'NONE',  ( 5.981074661064941900, 19.82752479807519919, 5.303881226583745168 ) ) ;
#1096=VECTOR ( 'NONE', #56830, 1000.000000000000227 ) ;
#1097=CARTESIAN_POINT ( 'NONE',  ( 5.965394784446460541, -17.78272165951808148, 10.25014670152084229 ) ) ;
#1100=ORIENTED_EDGE ( 'NONE', *, *, #30334, .T. ) ;
#1102=CARTESIAN_POINT ( 'NONE',  ( 0.5832367798473389042, 24.18350431151220192, -41.34221369670658675 ) ) ;
#1106=CARTESIAN_POINT ( 'NONE',  ( 4.967162193818130511, 32.10009971360111791, -28.74031574029977776 ) ) ;
#1114=ORIENTED_EDGE ( 'NONE', *, *, #16102, .T. ) ;
#1117=CARTESIAN_POINT ( 'NONE',  ( 4.956653778117001252, 47.27023054223765541, -8.845409907520457082 ) ) ;
#1118=ADVANCED_FACE ( 'NONE', ( #59873 ), #21225, .F. ) ;
#1121=EDGE_CURVE ( 'NONE', #11901, #16132, #11993, .T. ) ;
#1138=B_SPLINE_CURVE_WITH_KNOTS ( 'NONE', 3,
 ( #1297, #39882, #370, #33930 ),
 .UNSPECIFIED., .F., .F.,
 ( 4, 4 ),
 ( 4.670885906470169154E-18, 0.004050076154993003351 ),
 .UNSPECIFIED. ) ;
#1160=EDGE_LOOP ( 'NONE', ( #10693, #60226, #61947, #6287 ) ) ;
#1165=ORIENTED_EDGE ( 'NONE', *, *, #39795, .T. ) ;
#1167=CARTESIAN_POINT ( 'NONE',  ( 0.8551540677456739292, 44.61036085020975150, -17.49081417858739229 ) ) ;
#1168=( BOUNDED_SURFACE ( )  B_SPLINE_SURFACE ( 3, 1, ( 
 ( #4101, #45834 ),
 ( #3800, #56425 ),
 ( #23241, #50502 ),
 ( #17312, #31716 ) ),
 .UNSPECIFIED., .F., .F., .F. ) 
 B_SPLINE_SURFACE_WITH_KNOTS ( ( 4, 4 ),
 ( 2, 2 ),
 ( 0.000000000000000000, 1.000000000000000000 ),
 ( 0.000000000000000000, 1.000000000000000000 ),
 .UNSPECIFIED. ) 
 GEOMETRIC_REPRESENTATION_ITEM ( )  RATIONAL_B_SPLINE_SURFACE ( (
 ( 1.000000000000000000, 1.000000000000000000),
 ( 0.7269869731126821222, 0.9931720237060910339),
 ( 0.7269869731126821222, 0.9931720237060910339),
 ( 1.000000000000000000, 1.000000000000000000) ) ) 
 REPRESENTATION_ITEM ( '' )  SURFACE ( )  );
#1169=ORIENTED_EDGE ( 'NONE', *, *, #4409, .T. ) ;
#1172=CARTESIAN_POINT ( 'NONE',  ( 0.5819845079324662551, -17.90867223323918367, 44.42187385013357925 ) ) ;
#1178=CARTESIAN_POINT ( 'NONE',  ( 0.5809828226811553087, 6.791453954330313181, 47.41188724015881917 ) ) ;
#1179=CARTESIAN_POINT ( 'NONE',  ( 3.407937589446174087, 9.356405769959053487, 10.00592723328964162 ) ) ;
#1186=( BOUNDED_SURFACE ( )  B_SPLINE_SURFACE ( 3, 1, ( 
 ( #56448, #37376 ),
 ( #13562, #37076 ),
 ( #51750, #61444 ),
 ( #18567, #16256 ) ),
 .UNSPECIFIED., .F., .F., .F. ) 
 B_SPLINE_SURFACE_WITH_KNOTS ( ( 4, 4 ),
 ( 2, 2 ),
 ( 0.000000000000000000, 1.000000000000000000 ),
 ( 0.000000000000000000, 1.000000000000000000 ),
 .UNSPECIFIED. ) 
 GEOMETRIC_REPRESENTATION_ITEM ( )  RATIONAL_B_SPLINE_SURFACE ( (
 ( 1.000000000000000000, 1.000000000000000000),
 ( 0.9953390228620291325, 0.8624445117760984880),
 ( 0.9953390228620291325, 0.8624445117760984880),
 ( 1.000000000000000000, 1.000000000000000000) ) ) 
 REPRESENTATION_ITEM ( '' )  SURFACE ( )  );
#1188=CARTESIAN_POINT ( 'NONE',  ( 5.960221823109900008, 19.82478916873574448, -5.317678907195231730 ) ) ;
#1196=ADVANCED_FACE ( 'NONE', ( #40814 ), #27628, .F. ) ;
#1200=CARTESIAN_POINT ( 'NONE',  ( 1.227938101723748288, 42.91134962331487657, 0.8460948827226649760 ) ) ;
#1202=DIRECTION ( 'NONE',  ( 0.07836865515943412797, 0.7956898808744514717, -0.6006129930017356511 ) ) ;
#1213=DIRECTION ( 'NONE',  ( 0.07836865515943411409, 0.7860872967108141207, 0.6131273243286309294 ) ) ;
#1214=ORIENTED_EDGE ( 'NONE', *, *, #58418, .T. ) ;
#1216=CARTESIAN_POINT ( 'NONE',  ( 5.959547316686252039, -12.49238070347965035, -16.28624005235095495 ) ) ;
#1217=CARTESIAN_POINT ( 'NONE',  ( 0.5839879882012682932, 18.32896541547133040, -44.25011577017253472 ) ) ;
#1221=CARTESIAN_POINT ( 'NONE',  ( 0.9736507210033059634, -37.38294557109051652, 21.06291100879426992 ) ) ;
#1222=CARTESIAN_POINT ( 'NONE',  ( 0.8551540677456739292, -23.16399837394517292, -41.94570365541225954 ) ) ;
#1247=VERTEX_POINT ( 'NONE', #28214 ) ;
#1249=CARTESIAN_POINT ( 'NONE',  ( 0.8557997880470697982, -41.02602466100796619, 24.73961900479237386 ) ) ;
#1252=ORIENTED_EDGE ( 'NONE', *, *, #33947, .F. ) ;
#1254=CARTESIAN_POINT ( 'NONE',  ( 4.960156602257181468, 30.22163187094385961, 35.23783291257178263 ) ) ;
#1256=DIRECTION ( 'NONE',  ( -0.07836865515943411409, 0.6993330359244963601, -0.7104869166656966328 ) ) ;
#1264=EDGE_CURVE ( 'NONE', #57237, #10490, #61347, .T. ) ;
#1266=B_SPLINE_CURVE_WITH_KNOTS ( 'NONE', 3,
 ( #16711, #25173, #12033, #48986, #21096, #40536 ),
 .UNSPECIFIED., .F., .F.,
 ( 4, 2, 4 ),
 ( 3.576224061345498009E-18, 0.0002445244328975361555, 0.0004890488657950687332 ),
 .UNSPECIFIED. ) ;
#1269=CARTESIAN_POINT ( 'NONE',  ( 5.860006189529234355, 15.52021937683276498, 45.66786516969934695 ) ) ;
#1271=CARTESIAN_POINT ( 'NONE',  ( 0.6846871229502932144, 41.91507847151831356, -23.20185915381512842 ) ) ;
#1277=ADVANCED_FACE ( 'NONE', ( #47039 ), #22875, .F. ) ;
#1280=CARTESIAN_POINT ( 'NONE',  ( 0.5809828226811556418, 44.45562576850601744, 17.82437196699697424 ) ) ;
#1297=CARTESIAN_POINT ( 'NONE',  ( 4.967162193818130511, -42.16965968614187688, -8.839793687085657936 ) ) ;
#1300=B_SPLINE_CURVE_WITH_KNOTS ( 'NONE', 3,
 ( #26354, #60468, #2540, #21662, #30425, #40803 ),
 .UNSPECIFIED., .F., .F.,
 ( 4, 2, 4 ),
 ( 1.519276763058329222E-16, 0.0002445252820015159914, 0.0004890505640028799776 ),
 .UNSPECIFIED. ) ;
#1305=CARTESIAN_POINT ( 'NONE',  ( 4.967162193818130511, -42.16965968614200477, 8.839793687085075291 ) ) ;
#1317=CARTESIAN_POINT ( 'NONE',  ( 1.227938101723756947, 41.23019537246726429, -11.92353943227906399 ) ) ;
#1320=VERTEX_POINT ( 'NONE', #5610 ) ;
#1321=CARTESIAN_POINT ( 'NONE',  ( 5.960221823109900008, 14.50993159119790654, 14.51763960716783508 ) ) ;
#1326=ORIENTED_EDGE ( 'NONE', *, *, #58268, .T. ) ;
#1327=ORIENTED_EDGE ( 'NONE', *, *, #14501, .F. ) ;
#1332=CARTESIAN_POINT ( 'NONE',  ( 1.088908134280556439, -33.56490895818185294, 26.73890361625902301 ) ) ;
#1334=EDGE_CURVE ( 'NONE', #1876, #16670, #3758, .T. ) ;
#1337=CARTESIAN_POINT ( 'NONE',  ( 4.967162193818130511, 32.68434214048205888, -28.07411493385260925 ) ) ;
#1340=CARTESIAN_POINT ( 'NONE',  ( 5.959547316686252039, -14.51128755440531393, -14.51632612601523853 ) ) ;
#1344=EDGE_CURVE ( 'NONE', #29077, #21542, #47180, .T. ) ;
#1345=B_SPLINE_CURVE_WITH_KNOTS ( 'NONE', 3,
 ( #57704, #14835, #53023, #10123, #29219, #5397 ),
 .UNSPECIFIED., .F., .F.,
 ( 4, 2, 4 ),
 ( 0.000000000000000000, 0.0002291966416970784280, 0.0004583932833941568559 ),
 .UNSPECIFIED. ) ;
#1346=CARTESIAN_POINT ( 'NONE',  ( 0.8557997880470606944, -17.48760788519184217, -44.60232077416704755 ) ) ;
#1348=CARTESIAN_POINT ( 'NONE',  ( 4.967162193818130511, 35.57684288742009215, -24.30453456948074376 ) ) ;
#1351=( BOUNDED_SURFACE ( )  B_SPLINE_SURFACE ( 3, 1, ( 
 ( #7117, #26244 ),
 ( #58274, #10697 ),
 ( #48589, #24163 ),
 ( #38918, #337 ) ),
 .UNSPECIFIED., .F., .F., .F. ) 
 B_SPLINE_SURFACE_WITH_KNOTS ( ( 4, 4 ),
 ( 2, 2 ),
 ( 0.000000000000000000, 1.000000000000000000 ),
 ( 0.000000000000000000, 1.000000000000000000 ),
 .UNSPECIFIED. ) 
 GEOMETRIC_REPRESENTATION_ITEM ( )  RATIONAL_B_SPLINE_SURFACE ( (
 ( 1.000000000000000000, 1.000000000000000000),
 ( 0.9953390228620291325, 0.8624445117760984880),
 ( 0.9953390228620291325, 0.8624445117760984880),
 ( 1.000000000000000000, 1.000000000000000000) ) ) 
 REPRESENTATION_ITEM ( '' )  SURFACE ( )  );
#1352=CARTESIAN_POINT ( 'NONE',  ( 0.9752570700956798566, -11.32817567195941777, 41.38610171411356475 ) ) ;
#1369=EDGE_CURVE ( 'NONE', #23520, #22992, #25078, .T. ) ;
#1370=CARTESIAN_POINT ( 'NONE',  ( 1.227938101723747621, 6.439911493065174852, -42.43379953535178828 ) ) ;
#1372=CARTESIAN_POINT ( 'NONE',  ( 1.227938101723748288, 41.23019537246709376, 11.92353943227963597 ) ) ;
#1378=EDGE_LOOP ( 'NONE', ( #17663, #16734, #24499, #56689 ) ) ;
#1380=B_SPLINE_CURVE_WITH_KNOTS ( 'NONE', 3,
 ( #57058, #23875, #33291, #47371, #13877, #28257 ),
 .UNSPECIFIED., .F., .F.,
 ( 4, 2, 4 ),
 ( 0.000000000000000000, 0.0002291966416970781298, 0.0004583932833941562596 ),
 .UNSPECIFIED. ) ;
#1384=ORIENTED_EDGE ( 'NONE', *, *, #50407, .F. ) ;
#1385=CARTESIAN_POINT ( 'NONE',  ( 4.960156602257185909, -30.99165383632742277, -34.56254177294303531 ) ) ;
#1392=DIRECTION ( 'NONE',  ( 0.000000000000000000, 0.000000000000000000, 1.000000000000000000 ) ) ;
#1394=CARTESIAN_POINT ( 'NONE',  ( 4.963659409799330291, 13.93274247732021287, 42.53037318521000287 ) ) ;
#1395=VERTEX_POINT ( 'NONE', #57936 ) ;
#1408=EDGE_CURVE ( 'NONE', #2552, #57258, #32199, .T. ) ;
#1410=CARTESIAN_POINT ( 'NONE',  ( 4.956653778116966613, 0.000000000000000000, 0.000000000000000000 ) ) ;
#1412=CARTESIAN_POINT ( 'NONE',  ( 0.5809828226811553087, 46.11980934799357357, -12.92184523170154620 ) ) ;
#1415=CARTESIAN_POINT ( 'NONE',  ( 0.9754642270333692133, 39.70914670678655511, -16.25787253057890425 ) ) ;
#1419=CARTESIAN_POINT ( 'NONE',  ( 0.8551540677456739292, 34.52115452272974494, -33.23105123575864894 ) ) ;
#1423=EDGE_CURVE ( 'NONE', #16132, #8543, #39641, .T. ) ;
#1425=CARTESIAN_POINT ( 'NONE',  ( 0.9730545539215883499, 41.31259007387247095, -11.59290486963463351 ) ) ;
#1429=VECTOR ( 'NONE', #5050, 1000.000000000000114 ) ;
#1433=EDGE_LOOP ( 'NONE', ( #37109, #26749, #12228, #28663 ) ) ;
#1436=CARTESIAN_POINT ( 'NONE',  ( 5.959547316686252039, -16.28624005235090877, -12.49238070347970364 ) ) ;
#1439=CARTESIAN_POINT ( 'NONE',  ( 2.526464513654346433, -42.43615126908562729, 6.809833384818880120 ) ) ;
#1440=CARTESIAN_POINT ( 'NONE',  ( 0.8557997880470606944, -11.51622788066425684, -46.50333260518571876 ) ) ;
#1453=CARTESIAN_POINT ( 'NONE',  ( 4.303969348037258058, 48.06163817123226067, -2.158280495710381608 ) ) ;
#1454=EDGE_LOOP ( 'NONE', ( #41993, #42412, #46073, #34853 ) ) ;
#1455=CARTESIAN_POINT ( 'NONE',  ( 0.5809828226811548646, -46.40184912890831015, -11.86925843957216742 ) ) ;
#1458=EDGE_CURVE ( 'NONE', #22677, #21051, #43417, .T. ) ;
#1464=CARTESIAN_POINT ( 'NONE',  ( 4.303969348037258058, -27.54579249306236832, 39.44373910178601506 ) ) ;
#1473=( BOUNDED_SURFACE ( )  B_SPLINE_SURFACE ( 3, 1, ( 
 ( #21443, #31457 ),
 ( #50556, #7633 ),
 ( #26758, #50866 ),
 ( #12997, #22682 ) ),
 .UNSPECIFIED., .F., .F., .F. ) 
 B_SPLINE_SURFACE_WITH_KNOTS ( ( 4, 4 ),
 ( 2, 2 ),
 ( 0.000000000000000000, 1.000000000000000000 ),
 ( 0.000000000000000000, 1.000000000000000000 ),
 .UNSPECIFIED. ) 
 GEOMETRIC_REPRESENTATION_ITEM ( )  RATIONAL_B_SPLINE_SURFACE ( (
 ( 1.000000000000000000, 1.000000000000000000),
 ( 0.9953390228620291325, 0.8624445117760984880),
 ( 0.9953390228620291325, 0.8624445117760984880),
 ( 1.000000000000000000, 1.000000000000000000) ) ) 
 REPRESENTATION_ITEM ( '' )  SURFACE ( )  );
#1475=CARTESIAN_POINT ( 'NONE',  ( 0.9968887458511658251, -36.82760690604611398, -22.02152923727788902 ) ) ;
#1477=CARTESIAN_POINT ( 'NONE',  ( 3.407937589446178528, -11.14158115674367799, -7.970324840162072988 ) ) ;
#1483=B_SPLINE_CURVE_WITH_KNOTS ( 'NONE', 3,
 ( #61942, #14069, #14371, #9651 ),
 .UNSPECIFIED., .F., .F.,
 ( 4, 4 ),
 ( 1.551583845779545699E-17, 0.005004741218457429280 ),
 .UNSPECIFIED. ) ;
#1486=EDGE_LOOP ( 'NONE', ( #50446, #50345, #15384, #23586 ) ) ;
#1487=CARTESIAN_POINT ( 'NONE',  ( 0.5819845901640493535, 17.90867915372053432, 44.42187107932949885 ) ) ;
#1488=CARTESIAN_POINT ( 'NONE',  ( 1.154321713695928286, -42.90848032340444718, -0.8253077511131137189 ) ) ;
#1489=CARTESIAN_POINT ( 'NONE',  ( 4.963659409799332067, 29.86601237216454052, -33.33129552235055115 ) ) ;
#1494=VERTEX_POINT ( 'NONE', #60587 ) ;
#1502=CARTESIAN_POINT ( 'NONE',  ( 0.8557997880470599172, -47.60865952217002928, 5.347802024197076065 ) ) ;
#1513=FACE_OUTER_BOUND ( 'NONE', #8620, .T. ) ;
#1514=LINE ( 'NONE', #25648, #36695 ) ;
#1515=ORIENTED_EDGE ( 'NONE', *, *, #29580, .T. ) ;
#1518=CARTESIAN_POINT ( 'NONE',  ( 5.965394784446460541, 20.35165389555757898, -2.664747781315902841 ) ) ;
#1519=CARTESIAN_POINT ( 'NONE',  ( 1.227938101723748288, -33.52879263017845091, -26.79402671879361364 ) ) ;
#1522=CARTESIAN_POINT ( 'NONE',  ( 5.965394784446460541, 16.29267539192343150, -12.48356622107660030 ) ) ;
#1523=CARTESIAN_POINT ( 'NONE',  ( 0.9758171775293911221, 16.41489794146178838, -39.64453667157730621 ) ) ;
#1524=ADVANCED_FACE ( 'NONE', ( #28629 ), #5280, .F. ) ;
#1532=VERTEX_POINT ( 'NONE', #14253 ) ;
#1534=CARTESIAN_POINT ( 'NONE',  ( 5.860006189529246790, -3.137522369585184823, -48.13093674595588567 ) ) ;
#1536=ORIENTED_EDGE ( 'NONE', *, *, #14661, .T. ) ;
#1537=FACE_OUTER_BOUND ( 'NONE', #43813, .T. ) ;
#1541=LINE ( 'NONE', #49478, #29332 ) ;
#1552=EDGE_CURVE ( 'NONE', #1853, #34885, #5718, .T. ) ;
#1558=CARTESIAN_POINT ( 'NONE',  ( 0.5839879882012667389, -44.25009266679219877, 18.32902119196551638 ) ) ;
#1564=CARTESIAN_POINT ( 'NONE',  ( 0.9730545539215883499, -42.90536227157002003, 0.5054011016611185125 ) ) ;
#1565=EDGE_LOOP ( 'NONE', ( #14507, #60385, #31317, #56504 ) ) ;
#1574=CARTESIAN_POINT ( 'NONE',  ( 4.303969348037246512, 16.39840148505092543, 45.22910199346979709 ) ) ;
#1578=DIRECTION ( 'NONE',  ( 0.000000000000000000, 0.000000000000000000, 1.000000000000000000 ) ) ;
#1580=CARTESIAN_POINT ( 'NONE',  ( 2.526464513654346433, 15.32058692775046005, -40.15570173027678180 ) ) ;
#1584=CARTESIAN_POINT ( 'NONE',  ( 0.6846871229502899947, 46.49193983736591917, 11.56285438919648811 ) ) ;
#1585=CARTESIAN_POINT ( 'NONE',  ( 5.959828726073459926, 12.49879082830546473, 16.28130559351268758 ) ) ;
#1591=CARTESIAN_POINT ( 'NONE',  ( 3.407937589446178528, -9.356405769959122765, 10.00592723328957767 ) ) ;
#1599=ORIENTED_EDGE ( 'NONE', *, *, #18489, .T. ) ;
#1601=ADVANCED_FACE ( 'NONE', ( #24869 ), #22507, .F. ) ;
#1604=B_SPLINE_CURVE_WITH_KNOTS ( 'NONE', 3,
 ( #31589, #41620, #36311, #41025, #3672, #17496 ),
 .UNSPECIFIED., .F., .F.,
 ( 4, 2, 4 ),
 ( 1.519728548185745998E-16, 0.0002445252820015222798, 0.0004890505640028926628 ),
 .UNSPECIFIED. ) ;
#1606=ADVANCED_FACE ( 'NONE', ( #35512 ), #26517, .F. ) ;
#1609=VERTEX_POINT ( 'NONE', #54571 ) ;
#1612=ORIENTED_EDGE ( 'NONE', *, *, #11387, .T. ) ;
#1613=CARTESIAN_POINT ( 'NONE',  ( 1.227938101723748288, -26.79402671879349640, 33.52879263017854328 ) ) ;
#1623=AXIS2_PLACEMENT_3D ( 'NONE', #6015, #6949, #58966 ) ;
#1626=EDGE_CURVE ( 'NONE', #20568, #57911, #59595, .T. ) ;
#1636=VECTOR ( 'NONE', #1213, 1000.000000000000114 ) ;
#1641=( BOUNDED_SURFACE ( )  B_SPLINE_SURFACE ( 3, 1, ( 
 ( #48627, #48328 ),
 ( #38336, #33017 ),
 ( #34241, #14827 ),
 ( #14522, #61781 ) ),
 .UNSPECIFIED., .F., .F., .F. ) 
 B_SPLINE_SURFACE_WITH_KNOTS ( ( 4, 4 ),
 ( 2, 2 ),
 ( 0.000000000000000000, 1.000000000000000000 ),
 ( 0.000000000000000000, 1.000000000000000000 ),
 .UNSPECIFIED. ) 
 GEOMETRIC_REPRESENTATION_ITEM ( )  RATIONAL_B_SPLINE_SURFACE ( (
 ( 1.000000000000000000, 1.000000000000000000),
 ( 0.7269869731126817891, 0.9931720237060910339),
 ( 0.7269869731126817891, 0.9931720237060910339),
 ( 1.000000000000000000, 1.000000000000000000) ) ) 
 REPRESENTATION_ITEM ( '' )  SURFACE ( )  );
#1647=CARTESIAN_POINT ( 'NONE',  ( 5.958863334805807099, 18.96276366205782438, 7.855954700275686875 ) ) ;
#1656=CARTESIAN_POINT ( 'NONE',  ( 0.9747592971366236814, -25.86343094887205751, 34.23774590565627562 ) ) ;
#1659=DIRECTION ( 'NONE',  ( -0.07439287786467650709, 0.9665813013808178811, 0.2453289374370170028 ) ) ;
#1661=CARTESIAN_POINT ( 'NONE',  ( 0.8557997880470690211, 41.02602466100812961, -24.73961900479208609 ) ) ;
#1670=ORIENTED_EDGE ( 'NONE', *, *, #57983, .T. ) ;
#1673=B_SPLINE_CURVE_WITH_KNOTS ( 'NONE', 3,
 ( #4355, #42621, #18816, #61683, #37943, #56999 ),
 .UNSPECIFIED., .F., .F.,
 ( 4, 2, 4 ),
 ( 9.140795285775094282E-18, 0.0002291978881530184911, 0.0004583957763060278749 ),
 .UNSPECIFIED. ) ;
#1674=ORIENTED_EDGE ( 'NONE', *, *, #61049, .F. ) ;
#1677=EDGE_CURVE ( 'NONE', #17303, #60647, #12024, .T. ) ;
#1679=CARTESIAN_POINT ( 'NONE',  ( 5.959547316686252039, -12.49238070347988483, 16.28624005235077732 ) ) ;
#1684=CARTESIAN_POINT ( 'NONE',  ( 3.660087539127331535, 4.399983418616820074, -47.83637163185228758 ) ) ;
#1687=EDGE_CURVE ( 'NONE', #7406, #7463, #48599, .T. ) ;
#1694=CARTESIAN_POINT ( 'NONE',  ( 0.5834872094924179464, 44.33648115256923461, -18.11905305011470091 ) ) ;
#1697=CARTESIAN_POINT ( 'NONE',  ( 0.8557997880470697982, -17.48760788519248521, 44.60232077416680596 ) ) ;
#1698=EDGE_CURVE ( 'NONE', #24833, #50125, #35120, .T. ) ;
#1704=CARTESIAN_POINT ( 'NONE',  ( 5.958863334805807099, -10.26176968287957258, 17.77634700750911279 ) ) ;
#1705=VECTOR ( 'NONE', #52626, 1000.000000000000114 ) ;
#1707=ORIENTED_EDGE ( 'NONE', *, *, #59461, .F. ) ;
#1708=CARTESIAN_POINT ( 'NONE',  ( 0.7762777257811939169, 33.23866587527477634, 34.49689427664277730 ) ) ;
#1710=CIRCLE ( 'NONE', #42763, 43.08621763946400307 ) ;
#1727=EDGE_CURVE ( 'NONE', #60037, #54442, #34421, .T. ) ;
#1732=CARTESIAN_POINT ( 'NONE',  ( 1.088908134280558881, 41.24246781061832934, -11.85879120571462764 ) ) ;
#1739=EDGE_CURVE ( 'NONE', #28202, #37486, #8089, .T. ) ;
#1753=ORIENTED_EDGE ( 'NONE', *, *, #1423, .T. ) ;
#1754=ORIENTED_EDGE ( 'NONE', *, *, #40398, .F. ) ;
#1763=B_SPLINE_CURVE_WITH_KNOTS ( 'NONE', 3,
 ( #15361, #294, #47944, #4993 ),
 .UNSPECIFIED., .F., .F.,
 ( 4, 4 ),
 ( 0.000000000000000000, 0.004446090762761373792 ),
 .UNSPECIFIED. ) ;
#1766=CARTESIAN_POINT ( 'NONE',  ( 5.974727161628369032, -20.52494643607030156, -0.01551142186642303668 ) ) ;
#1767=ORIENTED_EDGE ( 'NONE', *, *, #22018, .T. ) ;
#1768=CARTESIAN_POINT ( 'NONE',  ( 0.9747592971366243475, 41.36145845824422906, -11.41797089479089777 ) ) ;
#1771=CARTESIAN_POINT ( 'NONE',  ( 5.959547316686252039, -0.003562808153049117858, 20.52562247508876681 ) ) ;
#1772=EDGE_LOOP ( 'NONE', ( #39252, #3865, #33031, #3390 ) ) ;
#1776=CARTESIAN_POINT ( 'NONE',  ( 0.5832366564991504632, -37.83193087518330344, 29.37287047358866943 ) ) ;
#1779=ORIENTED_EDGE ( 'NONE', *, *, #16286, .T. ) ;
#1786=FACE_OUTER_BOUND ( 'NONE', #6546, .T. ) ;
#1787=AXIS2_PLACEMENT_3D ( 'NONE', #1410, #52817, #24318 ) ;
#1789=CARTESIAN_POINT ( 'NONE',  ( 3.783198216974392292, -41.09147814699331036, -12.79806054635177226 ) ) ;
#1792=ORIENTED_EDGE ( 'NONE', *, *, #61263, .F. ) ;
#1794=CARTESIAN_POINT ( 'NONE',  ( -4.473699999999999122, 0.000000000000000000, -47.67072199303260049 ) ) ;
#1799=CARTESIAN_POINT ( 'NONE',  ( 0.5827357941260193908, 18.66407988912490978, 44.10984861950464619 ) ) ;
#1821=CARTESIAN_POINT ( 'NONE',  ( 0.8557997880470697982, -5.347802024197571669, 47.60865952216997243 ) ) ;
#1826=AXIS2_PLACEMENT_3D ( 'NONE', #39226, #20107, #30097 ) ;
#1829=DIRECTION ( 'NONE',  ( 0.07439287786467665975, -0.9868880006907391200, -0.1432402660415254547 ) ) ;
#1831=CARTESIAN_POINT ( 'NONE',  ( 5.958863334805807099, -20.52565293643016275, 0.001220270596100524923 ) ) ;
#1837=CARTESIAN_POINT ( 'NONE',  ( 0.6067375320500729696, 5.548194933740165702, 47.57460111700603278 ) ) ;
#1838=CARTESIAN_POINT ( 'NONE',  ( 0.9756950546413936110, -26.19769393035348060, -33.98259063592748674 ) ) ;
#1843=CARTESIAN_POINT ( 'NONE',  ( 2.624215991343608501, -22.77108897942107291, -42.26352390376119672 ) ) ;
#1844=CARTESIAN_POINT ( 'NONE',  ( 0.5263152470540364281, 5.264429658279185424E-15, 42.88844316795388778 ) ) ;
#1849=VECTOR ( 'NONE', #56074, 1000.000000000000000 ) ;
#1853=VERTEX_POINT ( 'NONE', #10010 ) ;
#1854=CARTESIAN_POINT ( 'NONE',  ( 0.9740398440564310700, 21.81228698783141695, 36.95080095316281898 ) ) ;
#1860=CARTESIAN_POINT ( 'NONE',  ( 0.8557997880470690211, -24.73961900479222820, -41.02602466100805145 ) ) ;
#1864=ORIENTED_EDGE ( 'NONE', *, *, #11045, .T. ) ;
#1867=CARTESIAN_POINT ( 'NONE',  ( 0.5839254288179547281, 33.93171296845886076, -33.80331890503232728 ) ) ;
#1869=CARTESIAN_POINT ( 'NONE',  ( 5.960721111146673579, -7.860635756377761574, -18.96073515164545498 ) ) ;
#1876=VERTEX_POINT ( 'NONE', #55361 ) ;
#1879=CARTESIAN_POINT ( 'NONE',  ( 3.783198216974389627, 20.00646744835666269, 38.10565824507906996 ) ) ;
#1889=CARTESIAN_POINT ( 'NONE',  ( 4.967162193818129623, -32.10009971360051395, -28.74031574030045633 ) ) ;
#1895=CARTESIAN_POINT ( 'NONE',  ( 5.960721111146673579, -17.77250458025999080, 10.26825948882894934 ) ) ;
#1899=CARTESIAN_POINT ( 'NONE',  ( 0.9752570700956795235, 37.27462300504105741, -21.25416333281058101 ) ) ;
#1904=CARTESIAN_POINT ( 'NONE',  ( 4.967162193818130511, -18.65818244221228284, -38.83676580803786749 ) ) ;
#1913=EDGE_CURVE ( 'NONE', #1320, #26290, #14898, .T. ) ;
#1924=ORIENTED_EDGE ( 'NONE', *, *, #2309, .F. ) ;
#1926=CARTESIAN_POINT ( 'NONE',  ( 0.9757892942422831117, -5.549787678908672639, 42.54806590760152574 ) ) ;
#1928=CARTESIAN_POINT ( 'NONE',  ( 5.959547316686252039, -2.682663672454773440, -20.34955788964375856 ) ) ;
#1929=B_SPLINE_CURVE_WITH_KNOTS ( 'NONE', 3,
 ( #55493, #21071, #12621, #6621 ),
 .UNSPECIFIED., .F., .F.,
 ( 4, 4 ),
 ( 0.000000000000000000, 0.004446090762761219402 ),
 .UNSPECIFIED. ) ;
#1935=CARTESIAN_POINT ( 'NONE',  ( 3.783198216974390515, 41.98529422752528006, -9.462293521184431455 ) ) ;
#1949=CARTESIAN_POINT ( 'NONE',  ( 4.967162193818132288, -24.30453456948087521, -35.57684288742000689 ) ) ;
#1953=ORIENTED_EDGE ( 'NONE', *, *, #41986, .T. ) ;
#1960=EDGE_CURVE ( 'NONE', #36040, #30530, #35993, .T. ) ;
#1962=CARTESIAN_POINT ( 'NONE',  ( 4.960156602257182357, 2.524999074837563917, 46.35381625054454702 ) ) ;
#1967=LINE ( 'NONE', #58661, #24922 ) ;
#1972=FACE_OUTER_BOUND ( 'NONE', #29277, .T. ) ;
#1979=ORIENTED_EDGE ( 'NONE', *, *, #19274, .T. ) ;
#1997=VERTEX_POINT ( 'NONE', #61599 ) ;
#2006=VERTEX_POINT ( 'NONE', #47225 ) ;
#2022=B_SPLINE_CURVE_WITH_KNOTS ( 'NONE', 3,
 ( #39689, #29330, #48441, #25252 ),
 .UNSPECIFIED., .F., .F.,
 ( 4, 4 ),
 ( 0.000000000000000000, 0.004444878191957668707 ),
 .UNSPECIFIED. ) ;
#2023=ORIENTED_EDGE ( 'NONE', *, *, #47307, .T. ) ;
#2026=B_SPLINE_CURVE_WITH_KNOTS ( 'NONE', 3,
 ( #32104, #37127, #27388, #55888 ),
 .UNSPECIFIED., .F., .F.,
 ( 4, 4 ),
 ( 4.336808689942017736E-19, 0.004048833967417082152 ),
 .UNSPECIFIED. ) ;
#2035=CARTESIAN_POINT ( 'NONE',  ( 3.660087539127320877, 8.130906407640051015, 47.34518630204115652 ) ) ;
#2039=CARTESIAN_POINT ( 'NONE',  ( 5.960721111146673579, -14.50930005615026808, 14.51823969584074625 ) ) ;
#2052=CARTESIAN_POINT ( 'NONE',  ( 1.154321485836933725, 42.43366804742927911, -6.418927614505664181 ) ) ;
#2054=CARTESIAN_POINT ( 'NONE',  ( 4.967162193818130511, 0.000000000000000000, 0.000000000000000000 ) ) ;
#2060=ORIENTED_EDGE ( 'NONE', *, *, #3949, .T. ) ;
#2067=CARTESIAN_POINT ( 'NONE',  ( 0.5786265663353196143, -0.7221568112309819654, 47.89572889566445468 ) ) ;
#2071=CARTESIAN_POINT ( 'NONE',  ( 0.9740398440564312921, 41.33716823241947935, -11.50548031350398759 ) ) ;
#2072=ORIENTED_EDGE ( 'NONE', *, *, #52458, .F. ) ;
#2075=VERTEX_POINT ( 'NONE', #52208 ) ;
#2077=CARTESIAN_POINT ( 'NONE',  ( 0.8551540677456834771, -28.44084013485144879, 38.56334384152421535 ) ) ;
#2089=CARTESIAN_POINT ( 'NONE',  ( 0.5839880159502364165, -18.37091806000265493, 44.23273844814454492 ) ) ;
#2091=VERTEX_POINT ( 'NONE', #51585 ) ;
#2096=CARTESIAN_POINT ( 'NONE',  ( 0.5839879882012675161, 6.251708210202064464, 47.48620708510744493 ) ) ;
#2100=EDGE_LOOP ( 'NONE', ( #50022, #60282, #17987, #56722 ) ) ;
#2104=CARTESIAN_POINT ( 'NONE',  ( 1.154321485836933725, -0.8253076867715974929, -42.90848031452337352 ) ) ;
#2133=CARTESIAN_POINT ( 'NONE',  ( 0.9758171775293911221, -39.64453667157735595, -16.41489794146167114 ) ) ;
#2138=CARTESIAN_POINT ( 'NONE',  ( 2.624215991343620935, -47.98682984381861871, 1.411420423865310747 ) ) ;
#2140=CARTESIAN_POINT ( 'NONE',  ( 3.270143674763207553, 11.02405647745181305, -8.113405361969396878 ) ) ;
#2141=ORIENTED_EDGE ( 'NONE', *, *, #14391, .T. ) ;
#2144=EDGE_CURVE ( 'NONE', #40793, #41494, #47846, .T. ) ;
#2148=CARTESIAN_POINT ( 'NONE',  ( 4.303969348037246512, -30.97035057417686232, 36.81598326424538925 ) ) ;
#2156=ORIENTED_EDGE ( 'NONE', *, *, #11387, .F. ) ;
#2163=EDGE_CURVE ( 'NONE', #6622, #2619, #47074, .T. ) ;
#2173=CARTESIAN_POINT ( 'NONE',  ( 5.860006189529234355, -47.30296539008831047, 9.426589201135334051 ) ) ;
#2179=CARTESIAN_POINT ( 'NONE',  ( 0.8557997880470697982, 17.48760788519276943, -44.60232077416669227 ) ) ;
#2180=ORIENTED_EDGE ( 'NONE', *, *, #12497, .T. ) ;
#2188=VERTEX_POINT ( 'NONE', #44695 ) ;
#2190=CARTESIAN_POINT ( 'NONE',  ( 0.8557997880470690211, -33.22501220301925429, 34.51495345639537504 ) ) ;
#2191=ADVANCED_FACE ( 'NONE', ( #38768 ), #11718, .F. ) ;
#2195=CARTESIAN_POINT ( 'NONE',  ( 5.860006189529246790, 36.27483683749480292, -31.78942168514526401 ) ) ;
#2197=CARTESIAN_POINT ( 'NONE',  ( 0.9754642270333682141, 37.24735125696685856, -21.30186789325715679 ) ) ;
#2211=CARTESIAN_POINT ( 'NONE',  ( 0.5832367798473397924, 46.19266341874894977, 12.65931911325620263 ) ) ;
#2215=CARTESIAN_POINT ( 'NONE',  ( 1.154321485836933725, -4.782433484301485294, 42.64911658695774577 ) ) ;
#2224=ORIENTED_EDGE ( 'NONE', *, *, #627, .F. ) ;
#2226=CARTESIAN_POINT ( 'NONE',  ( 0.9756354156337463390, -5.729847988735645714, 42.52418499698892873 ) ) ;
#2237=ADVANCED_FACE ( 'NONE', ( #40615 ), #35322, .F. ) ;
#2241=CARTESIAN_POINT ( 'NONE',  ( 5.960221823109900008, -19.82761049839338696, -5.307149561568015095 ) ) ;
#2244=EDGE_LOOP ( 'NONE', ( #57865, #19145, #28472, #20033 ) ) ;
#2248=CARTESIAN_POINT ( 'NONE',  ( 0.5809828226811617480, -37.66417181417530458, -29.58751527316218954 ) ) ;
#2254=CARTESIAN_POINT ( 'NONE',  ( 0.5819845079324655890, -46.37938935563221321, -11.95724301473555684 ) ) ;
#2257=CARTESIAN_POINT ( 'NONE',  ( 0.5800708057587390387, 29.65250565429499474, -37.61306623599811161 ) ) ;
#2261=CARTESIAN_POINT ( 'NONE',  ( 0.9754402186311968981, -16.24692483025446066, 39.71365199966008674 ) ) ;
#2269=CARTESIAN_POINT ( 'NONE',  ( 5.974727161628369032, -2.694421823323069454, 20.34732802718242795 ) ) ;
#2276=CARTESIAN_POINT ( 'NONE',  ( 4.956653778116992370, 14.93973939759951541, -45.71126949320233734 ) ) ;
#2277=CARTESIAN_POINT ( 'NONE',  ( 5.958863334805807099, -2.677925489610788023, 20.35021240744029924 ) ) ;
#2284=CARTESIAN_POINT ( 'NONE',  ( 4.967162193818130511, 0.000000000000000000, 0.000000000000000000 ) ) ;
#2289=CARTESIAN_POINT ( 'NONE',  ( 4.967162193818130511, -43.02067033766017801, -2.375726030843023029 ) ) ;
#2299=DIRECTION ( 'NONE',  ( 0.000000000000000000, 0.000000000000000000, 1.000000000000000000 ) ) ;
#2300=CARTESIAN_POINT ( 'NONE',  ( 0.5850706913938533704, 44.18063951072221585, 18.49682194437980698 ) ) ;
#2302=EDGE_LOOP ( 'NONE', ( #58956, #27585, #54804, #32628 ) ) ;
#2309=EDGE_CURVE ( 'NONE', #32300, #52379, #27136, .T. ) ;
#2312=EDGE_CURVE ( 'NONE', #38360, #25968, #28337, .T. ) ;
#2315=ORIENTED_EDGE ( 'NONE', *, *, #59385, .F. ) ;
#2323=CARTESIAN_POINT ( 'NONE',  ( 0.9752570700956788574, -30.17732761204920422, -30.50353876750662963 ) ) ;
#2326=CARTESIAN_POINT ( 'NONE',  ( 0.9756354156337447847, -21.34128958497355555, -37.22481466014919960 ) ) ;
#2330=CARTESIAN_POINT ( 'NONE',  ( 3.660176727303413813, 30.71420464230624603, -36.93665184075187113 ) ) ;
#2333=B_SPLINE_CURVE_WITH_KNOTS ( 'NONE', 3,
 ( #12190, #49758, #26884, #50074 ),
 .UNSPECIFIED., .F., .F.,
 ( 4, 4 ),
 ( 8.673617379884034509E-19, 0.004050076154992999881 ),
 .UNSPECIFIED. ) ;
#2341=B_SPLINE_CURVE_WITH_KNOTS ( 'NONE', 3,
 ( #43722, #48694, #19282, #53676, #132, #34609, #24586, #10803, #5142, #39021, #767, #29892, #6059, #42786, #38399, #58076 ),
 .UNSPECIFIED., .F., .F.,
 ( 4, 3, 3, 3, 3, 4 ),
 ( 1.250973872328959164E-17, 0.0002724568934985599380, 0.0004086836638483908805, 0.0005449104342063664039, 0.0008173270854453730701, 0.001089761613562692045 ),
 .UNSPECIFIED. ) ;
#2343=CARTESIAN_POINT ( 'NONE',  ( 0.9754402186311964540, 42.90805920318125999, -0.1875553420613088607 ) ) ;
#2344=CARTESIAN_POINT ( 'NONE',  ( 0.9754642270333678811, -5.426415525315535504, -42.56393738774956859 ) ) ;
#2346=CARTESIAN_POINT ( 'NONE',  ( 3.270143674763207553, 13.28976595685398188, -3.277085381512974571 ) ) ;
#2350=CARTESIAN_POINT ( 'NONE',  ( 0.6846871229502899947, -41.91507847151781618, -23.20185915381600950 ) ) ;
#2351=CARTESIAN_POINT ( 'NONE',  ( 0.9722240741986378776, -16.95645453362492105, 39.41582013185140454 ) ) ;
#2355=CARTESIAN_POINT ( 'NONE',  ( 5.959547316686252039, 19.82530672674354832, 5.315863417546399461 ) ) ;
#2356=B_SPLINE_CURVE_WITH_KNOTS ( 'NONE', 3,
 ( #3846, #57377, #47402, #56472, #33315, #52698, #42118, #52083, #47105, #61171, #18288, #9176, #37399, #4152, #18592, #43344 ),
 .UNSPECIFIED., .F., .F.,
 ( 4, 3, 3, 3, 3, 4 ),
 ( 1.040890552917501732E-17, 0.0002724568934985589080, 0.0004086836638483807974, 0.0005449104342063607661, 0.0008173270854453691669, 0.001089761613562693346 ),
 .UNSPECIFIED. ) ;
#2362=( BOUNDED_SURFACE ( )  B_SPLINE_SURFACE ( 3, 1, ( 
 ( #16343, #50171 ),
 ( #31681, #31370 ),
 ( #25737, #11338 ),
 ( #45802, #6916 ) ),
 .UNSPECIFIED., .F., .F., .F. ) 
 B_SPLINE_SURFACE_WITH_KNOTS ( ( 4, 4 ),
 ( 2, 2 ),
 ( 0.000000000000000000, 1.000000000000000000 ),
 ( 0.000000000000000000, 1.000000000000000000 ),
 .UNSPECIFIED. ) 
 GEOMETRIC_REPRESENTATION_ITEM ( )  RATIONAL_B_SPLINE_SURFACE ( (
 ( 1.000000000000000000, 1.000000000000000000),
 ( 0.7269869731126821222, 0.9931720237060910339),
 ( 0.7269869731126821222, 0.9931720237060910339),
 ( 1.000000000000000000, 1.000000000000000000) ) ) 
 REPRESENTATION_ITEM ( '' )  SURFACE ( )  );
#2364=FACE_OUTER_BOUND ( 'NONE', #59481, .T. ) ;
#2368=CARTESIAN_POINT ( 'NONE',  ( 5.960721111146673579, 17.77250458025977764, 10.26825948882932060 ) ) ;
#2372=CARTESIAN_POINT ( 'NONE',  ( 0.8551540677456715978, 44.61036085020950992, 17.49081417858803178 ) ) ;
#2374=ORIENTED_EDGE ( 'NONE', *, *, #58896, .F. ) ;
#2381=VERTEX_POINT ( 'NONE', #18962 ) ;
#2384=VERTEX_POINT ( 'NONE', #38082 ) ;
#2395=CARTESIAN_POINT ( 'NONE',  ( 5.860006189529246790, -26.81109398084734963, 40.09484204000590779 ) ) ;
#2397=CARTESIAN_POINT ( 'NONE',  ( 0.9730545539215883499, 42.60426903087360984, -5.099196237954451760 ) ) ;
#2400=ORIENTED_EDGE ( 'NONE', *, *, #28056, .F. ) ;
#2408=VERTEX_POINT ( 'NONE', #1346 ) ;
#2409=CARTESIAN_POINT ( 'NONE',  ( 5.960221823109900008, -0.005450390361865286269, 20.52559243573973546 ) ) ;
#2419=CARTESIAN_POINT ( 'NONE',  ( 0.5807400328401637335, -46.40483864045154405, 11.87003418057225979 ) ) ;
#2420=LINE ( 'NONE', #16864, #49805 ) ;
#2425=CARTESIAN_POINT ( 'NONE',  ( 5.960721111146673579, -2.672857320903164524, -20.35079619394245043 ) ) ;
#2432=CARTESIAN_POINT ( 'NONE',  ( 2.624215991343608501, 43.79392271049069763, 19.66774719432994090 ) ) ;
#2434=CARTESIAN_POINT ( 'NONE',  ( -48.95476116535499500, 9.797174393178825657E-16, -8.000000000000000000 ) ) ;
#2438=CARTESIAN_POINT ( 'NONE',  ( 0.9757787079277452369, -39.65734351318510420, 16.38386580718278296 ) ) ;
#2441=FACE_OUTER_BOUND ( 'NONE', #14027, .T. ) ;
#2448=LINE ( 'NONE', #11569, #8667 ) ;
#2453=CARTESIAN_POINT ( 'NONE',  ( 0.5809828226811617480, 5.711058609465307967, 47.55412398569209387 ) ) ;
#2457=ORIENTED_EDGE ( 'NONE', *, *, #42273, .T. ) ;
#2458=CARTESIAN_POINT ( 'NONE',  ( 4.967162193818130511, -42.96271701169388280, 3.259922920617591924 ) ) ;
#2459=CARTESIAN_POINT ( 'NONE',  ( 0.6846871229502932144, -34.48177377577859914, 33.25969555998731408 ) ) ;
#2460=CARTESIAN_POINT ( 'NONE',  ( 0.8557997880470599172, 13.27832040216703469, -46.03118133706011861 ) ) ;
#2464=DIRECTION ( 'NONE',  ( 0.07439287786467667363, -0.5100024374914997605, 0.8569499480574931383 ) ) ;
#2477=EDGE_CURVE ( 'NONE', #4518, #45517, #28308, .T. ) ;
#2481=ORIENTED_EDGE ( 'NONE', *, *, #42602, .F. ) ;
#2484=CARTESIAN_POINT ( 'NONE',  ( 0.5809828226811617480, 44.03860873105695362, 18.83114015454715684 ) ) ;
#2485=FACE_OUTER_BOUND ( 'NONE', #29596, .T. ) ;
#2490=CARTESIAN_POINT ( 'NONE',  ( 0.9756354156337453398, 10.97961179198200021, 41.47994205070116891 ) ) ;
#2492=ADVANCED_FACE ( 'NONE', ( #38687 ), #905, .F. ) ;
#2495=ORIENTED_EDGE ( 'NONE', *, *, #56606, .F. ) ;
#2496=EDGE_LOOP ( 'NONE', ( #25039, #40521, #14637, #42290 ) ) ;
#2497=CARTESIAN_POINT ( 'NONE',  ( 0.9757402383260938006, 34.09320464257847050, -26.05362288587330966 ) ) ;
#2504=ORIENTED_EDGE ( 'NONE', *, *, #25635, .F. ) ;
#2506=ORIENTED_EDGE ( 'NONE', *, *, #36413, .F. ) ;
#2507=CARTESIAN_POINT ( 'NONE',  ( 0.5850706913938534814, -33.73916126769474744, 33.99603398296579115 ) ) ;
#2509=CARTESIAN_POINT ( 'NONE',  ( 5.860006189529246790, -36.25227510158441646, -31.81514841426795570 ) ) ;
#2512=CARTESIAN_POINT ( 'NONE',  ( 0.9754642270333673260, 21.60621846558691672, -37.07163437210427048 ) ) ;
#2516=B_SPLINE_CURVE_WITH_KNOTS ( 'NONE', 3,
 ( #58510, #30959, #44473, #1502 ),
 .UNSPECIFIED., .F., .F.,
 ( 4, 4 ),
 ( 0.000000000000000000, 0.004446090762761369455 ),
 .UNSPECIFIED. ) ;
#2527=EDGE_CURVE ( 'NONE', #51919, #39239, #6636, .T. ) ;
#2530=ORIENTED_EDGE ( 'NONE', *, *, #23555, .T. ) ;
#2532=CIRCLE ( 'NONE', #47582, 43.08621763946400307 ) ;
#2533=CARTESIAN_POINT ( 'NONE',  ( 0.8557997880470599172, 44.60232077416710439, -17.48760788519168941 ) ) ;
#2535=CARTESIAN_POINT ( 'NONE',  ( 5.965394784446458765, 5.326334832595374991, 19.82223131420056106 ) ) ;
#2540=CARTESIAN_POINT ( 'NONE',  ( 0.7057020205115013267, -33.27137945725694124, -34.46103118762825801 ) ) ;
#2545=CARTESIAN_POINT ( 'NONE',  ( 0.5807400328401637335, -29.58941477092991335, -37.66660715020896077 ) ) ;
#2552=VERTEX_POINT ( 'NONE', #35523 ) ;
#2562=CARTESIAN_POINT ( 'NONE',  ( 0.5834872094924180574, 44.16273175734639977, 18.53852119651579855 ) ) ;
#2566=CARTESIAN_POINT ( 'NONE',  ( 0.9747592971366227932, 26.37717450293426680, 33.84353661172414007 ) ) ;
#2569=CARTESIAN_POINT ( 'NONE',  ( 0.5839879327111929808, -46.28746210677702067, -12.30864801674759512 ) ) ;
#2572=CARTESIAN_POINT ( 'NONE',  ( 0.8557997880470606944, 29.88293891557523807, -37.44587306708065455 ) ) ;
#2573=AXIS2_PLACEMENT_3D ( 'NONE', #29978, #31216, #50314 ) ;
#2588=CARTESIAN_POINT ( 'NONE',  ( 0.5809828226811617480, -41.74875432577665890, 23.47450554821694979 ) ) ;
#2599=DIRECTION ( 'NONE',  ( -0.07439287786467652097, 0.9161872986448755807, -0.3937848822959269524 ) ) ;
#2605=EDGE_CURVE ( 'NONE', #49867, #47520, #25311, .T. ) ;
#2614=CARTESIAN_POINT ( 'NONE',  ( 0.5839880159502327528, 47.89596769806549048, 0.04537901683497938543 ) ) ;
#2619=VERTEX_POINT ( 'NONE', #18259 ) ;
#2630=DIRECTION ( 'NONE',  ( 0.000000000000000000, 0.000000000000000000, 1.000000000000000000 ) ) ;
#2632=CARTESIAN_POINT ( 'NONE',  ( 0.6067099128993224122, -17.67241243535514883, 44.51753430581932491 ) ) ;
#2634=VERTEX_POINT ( 'NONE', #22644 ) ;
#2637=( BOUNDED_SURFACE ( )  B_SPLINE_SURFACE ( 3, 1, ( 
 ( #2825, #31351 ),
 ( #49837, #26335 ),
 ( #16964, #54505 ),
 ( #7517, #11633 ) ),
 .UNSPECIFIED., .F., .F., .F. ) 
 B_SPLINE_SURFACE_WITH_KNOTS ( ( 4, 4 ),
 ( 2, 2 ),
 ( 0.000000000000000000, 1.000000000000000000 ),
 ( 0.000000000000000000, 1.000000000000000000 ),
 .UNSPECIFIED. ) 
 GEOMETRIC_REPRESENTATION_ITEM ( )  RATIONAL_B_SPLINE_SURFACE ( (
 ( 1.000000000000000000, 1.000000000000000000),
 ( 0.9732289882329797637, 0.9999525324661233672),
 ( 0.9732289882329797637, 0.9999525324661233672),
 ( 1.000000000000000000, 1.000000000000000000) ) ) 
 REPRESENTATION_ITEM ( '' )  SURFACE ( )  );
#2645=ORIENTED_EDGE ( 'NONE', *, *, #58120, .F. ) ;
#2651=CARTESIAN_POINT ( 'NONE',  ( 0.5832366564991520175, 46.19265750221185840, -12.65934068133935853 ) ) ;
#2652=CARTESIAN_POINT ( 'NONE',  ( 0.7056555295713293763, -47.59410019435325268, -5.417452459790225383 ) ) ;
#2656=CARTESIAN_POINT ( 'NONE',  ( 5.959547316686252039, 10.26589671991338548, 17.77392908783937386 ) ) ;
#2658=STYLED_ITEM ( 'NONE', ( #18504 ), #30252 ) ;
#2660=CARTESIAN_POINT ( 'NONE',  ( -16.58656855106744032, -12.39978673513562946, -1.582714324450230192 ) ) ;
#2673=EDGE_CURVE ( 'NONE', #25113, #55855, #10086, .T. ) ;
#2677=CARTESIAN_POINT ( 'NONE',  ( 5.974727161628369032, 17.78288073588502982, -10.24903993264990376 ) ) ;
#2680=CARTESIAN_POINT ( 'NONE',  ( 1.227938101723748288, -0.8460948827228147451, 42.91134962331487657 ) ) ;
#2683=CARTESIAN_POINT ( 'NONE',  ( 0.5839879327111928697, -47.47435452316579330, 6.341736898931764621 ) ) ;
#2686=ORIENTED_EDGE ( 'NONE', *, *, #19180, .F. ) ;
#2694=ORIENTED_EDGE ( 'NONE', *, *, #40398, .T. ) ;
#2695=CARTESIAN_POINT ( 'NONE',  ( 4.967162193818130511, -28.74031574029989855, -32.10009971360102554 ) ) ;
#2696=CARTESIAN_POINT ( 'NONE',  ( 0.5809828226811553087, -44.03860873105708151, 18.83114015454682999 ) ) ;
#2706=CARTESIAN_POINT ( 'NONE',  ( 2.526464513654349098, 25.19161096467279037, -34.82216969498438885 ) ) ;
#2707=CARTESIAN_POINT ( 'NONE',  ( 0.8551540677456834771, 43.91216198251566993, -19.17641535420805354 ) ) ;
#2714=B_SPLINE_CURVE_WITH_KNOTS ( 'NONE', 3,
 ( #14902, #34009, #48394, #47671 ),
 .UNSPECIFIED., .F., .F.,
 ( 4, 4 ),
 ( 8.009840277583554626E-17, 0.005004741218457497802 ),
 .UNSPECIFIED. ) ;
#2715=EDGE_LOOP ( 'NONE', ( #53068, #64, #38704, #39941 ) ) ;
#2717=ORIENTED_EDGE ( 'NONE', *, *, #55538, .T. ) ;
#2721=CARTESIAN_POINT ( 'NONE',  ( 4.967162193818130511, 43.02067033766018511, 2.375726030842731706 ) ) ;
#2728=CARTESIAN_POINT ( 'NONE',  ( 0.7057020205115018818, -7.085441699093939505, 47.37450661940665952 ) ) ;
#2737=CARTESIAN_POINT ( 'NONE',  ( 2.624215991343620935, -46.71702075422643929, -11.05657803851094201 ) ) ;
#2741=CARTESIAN_POINT ( 'NONE',  ( 0.5809828226811617480, -46.40184912890847357, 11.86925843957150128 ) ) ;
#2747=CARTESIAN_POINT ( 'NONE',  ( 0.5850706913938534814, -33.99603398296567036, -33.73916126769486823 ) ) ;
#2761=ORIENTED_EDGE ( 'NONE', *, *, #43531, .T. ) ;
#2762=CARTESIAN_POINT ( 'NONE',  ( 0.5809828226811553087, 11.86925843957232729, -46.40184912890826752 ) ) ;
#2765=CARTESIAN_POINT ( 'NONE',  ( 5.981074661064941900, 20.35019299530688386, -2.670494474391787332 ) ) ;
#2769=FACE_OUTER_BOUND ( 'NONE', #21973, .T. ) ;
#2783=ORIENTED_EDGE ( 'NONE', *, *, #26117, .F. ) ;
#2784=B_SPLINE_CURVE_WITH_KNOTS ( 'NONE', 3,
 ( #52700, #37401, #19521, #9178 ),
 .UNSPECIFIED., .F., .F.,
 ( 4, 4 ),
 ( 1.301042606982605321E-18, 0.004048833967417090826 ),
 .UNSPECIFIED. ) ;
#2794=CARTESIAN_POINT ( 'NONE',  ( 4.960156602257181468, 38.88108289790859828, 25.36362146861398159 ) ) ;
#2798=CARTESIAN_POINT ( 'NONE',  ( 0.5838002273316426072, -44.30203797796952614, 18.20308624554815680 ) ) ;
#2804=CARTESIAN_POINT ( 'NONE',  ( 0.8551540677456739292, -41.94570365541218848, 23.16399837394531858 ) ) ;
#2809=VERTEX_POINT ( 'NONE', #57660 ) ;
#2814=CARTESIAN_POINT ( 'NONE',  ( 0.6846871229502932144, -41.91507847151813593, 23.20185915381541619 ) ) ;
#2818=ORIENTED_EDGE ( 'NONE', *, *, #27002, .T. ) ;
#2820=CARTESIAN_POINT ( 'NONE',  ( 4.967162193818130511, 0.000000000000000000, 0.000000000000000000 ) ) ;
#2825=CARTESIAN_POINT ( 'NONE',  ( 5.959547316686252039, -5.315863417546468739, 19.82530672674353056 ) ) ;
#2828=CARTESIAN_POINT ( 'NONE',  ( 0.8551540677456715978, -44.61036085020962361, 17.49081417858771559 ) ) ;
#2831=ADVANCED_FACE ( 'NONE', ( #16323 ), #24501, .F. ) ;
#2832=( BOUNDED_SURFACE ( )  B_SPLINE_SURFACE ( 3, 1, ( 
 ( #14884, #39304 ),
 ( #10475, #10166 ),
 ( #29570, #48678 ),
 ( #44023, #58362 ) ),
 .UNSPECIFIED., .F., .F., .F. ) 
 B_SPLINE_SURFACE_WITH_KNOTS ( ( 4, 4 ),
 ( 2, 2 ),
 ( 0.000000000000000000, 1.000000000000000000 ),
 ( 0.000000000000000000, 1.000000000000000000 ),
 .UNSPECIFIED. ) 
 GEOMETRIC_REPRESENTATION_ITEM ( )  RATIONAL_B_SPLINE_SURFACE ( (
 ( 1.000000000000000000, 1.000000000000000000),
 ( 0.9953390228620291325, 0.8624445117761032620),
 ( 0.9953390228620291325, 0.8624445117761032620),
 ( 1.000000000000000000, 1.000000000000000000) ) ) 
 REPRESENTATION_ITEM ( '' )  SURFACE ( )  );
#2837=ORIENTED_EDGE ( 'NONE', *, *, #52913, .F. ) ;
#2841=ORIENTED_EDGE ( 'NONE', *, *, #2144, .F. ) ;
#2847=CARTESIAN_POINT ( 'NONE',  ( 0.9752132459055862235, -41.50604997043404154, -10.88033124649664352 ) ) ;
#2852=VERTEX_POINT ( 'NONE', #26339 ) ;
#2858=VERTEX_POINT ( 'NONE', #49840 ) ;
#2869=CARTESIAN_POINT ( 'NONE',  ( 0.5839254288179547281, 44.21529885210830457, 18.41284501069694102 ) ) ;
#2870=ORIENTED_EDGE ( 'NONE', *, *, #7147, .F. ) ;
#2872=ADVANCED_FACE ( 'NONE', ( #31044 ), #41733, .F. ) ;
#2876=CARTESIAN_POINT ( 'NONE',  ( 0.5809828226811548646, -46.40184912890831015, -11.86925843957216742 ) ) ;
#2884=ORIENTED_EDGE ( 'NONE', *, *, #27440, .T. ) ;
#2888=DIRECTION ( 'NONE',  ( -0.07836865515943411409, 0.5052769534812689978, 0.8593913859058567306 ) ) ;
#2890=CIRCLE ( 'NONE', #23925, 43.08621763946400307 ) ;
#2893=CARTESIAN_POINT ( 'NONE',  ( 2.526552050251864134, -42.43615142762120485, -6.809858322089482385 ) ) ;
#2914=CARTESIAN_POINT ( 'NONE',  ( 4.956653778116975495, -14.93973939759918323, 45.71126949320244393 ) ) ;
#2920=CARTESIAN_POINT ( 'NONE',  ( 0.9730545539215883499, 5.099196237955498923, -42.60426903087348194 ) ) ;
#2928=DIRECTION ( 'NONE',  ( -0.07439287786467650709, 0.7991213610169827231, 0.5965490341031292054 ) ) ;
#2931=EDGE_LOOP ( 'NONE', ( #46632, #22151, #51467, #15535 ) ) ;
#2937=ORIENTED_EDGE ( 'NONE', *, *, #56558, .F. ) ;
#2938=CARTESIAN_POINT ( 'NONE',  ( 0.9972139404380323535, -29.87264297738548180, 30.80335716430307613 ) ) ;
#2944=CARTESIAN_POINT ( 'NONE',  ( 0.8557997880470697982, 47.60865952216998664, 5.347802024197403803 ) ) ;
#2945=EDGE_CURVE ( 'NONE', #3160, #38104, #19341, .T. ) ;
#2949=ADVANCED_FACE ( 'NONE', ( #31980 ), #37710, .F. ) ;
#2953=CARTESIAN_POINT ( 'NONE',  ( 1.154321713695926288, -26.77578845938205276, 33.53917066545415082 ) ) ;
#2961=EDGE_CURVE ( 'NONE', #31462, #32300, #59698, .T. ) ;
#2964=CARTESIAN_POINT ( 'NONE',  ( 0.9730545539215883499, -15.95224156741799426, -39.83279466599056917 ) ) ;
#2967=CARTESIAN_POINT ( 'NONE',  ( 0.5786265663353153954, 11.69877690266720371, -46.45062944555881757 ) ) ;
#2972=CARTESIAN_POINT ( 'NONE',  ( 4.967162193818130511, 0.000000000000000000, 0.000000000000000000 ) ) ;
#2974=VECTOR ( 'NONE', #15899, 1000.000000000000000 ) ;
#2977=CARTESIAN_POINT ( 'NONE',  ( 0.6067099128993239665, -0.7089426894587230743, -47.89177823194874861 ) ) ;
#2988=CARTESIAN_POINT ( 'NONE',  ( 4.956653778116982600, -47.05699031914957686, 9.917440902360995736 ) ) ;
#2990=CARTESIAN_POINT ( 'NONE',  ( 4.967162193818130511, -2.375726030842872927, 43.02067033766017801 ) ) ;
#2994=CARTESIAN_POINT ( 'NONE',  ( 0.5800708119828342779, -23.40241990038066078, 41.78924007434317645 ) ) ;
#3004=B_SPLINE_CURVE_WITH_KNOTS ( 'NONE', 3,
 ( #53832, #24736, #39170, #43877 ),
 .UNSPECIFIED., .F., .F.,
 ( 4, 4 ),
 ( 6.505213034913026604E-19, 0.004048833967417084755 ),
 .UNSPECIFIED. ) ;
#3005=CARTESIAN_POINT ( 'NONE',  ( 1.227938101723748288, -6.439911493064859549, 42.43379953535183802 ) ) ;
#3007=CARTESIAN_POINT ( 'NONE',  ( 0.8557997880470599172, -38.55640757422458620, 28.43566216844957140 ) ) ;
#3009=ORIENTED_EDGE ( 'NONE', *, *, #28279, .T. ) ;
#3021=VERTEX_POINT ( 'NONE', #53520 ) ;
#3022=CARTESIAN_POINT ( 'NONE',  ( 0.9730545539215892381, -15.95224156741857691, 39.83279466599033469 ) ) ;
#3028=CARTESIAN_POINT ( 'NONE',  ( 1.227938101723748288, -41.23019537246701560, -11.92353943227992197 ) ) ;
#3036=DIRECTION ( 'NONE',  ( 0.07439287786467665975, -0.9262902123089823414, 0.3693942911085547620 ) ) ;
#3039=ORIENTED_EDGE ( 'NONE', *, *, #38008, .T. ) ;
#3043=EDGE_CURVE ( 'NONE', #26290, #28220, #24107, .T. ) ;
#3045=CARTESIAN_POINT ( 'NONE',  ( 4.956653778116975495, 14.93973939759886704, 45.71126949320255761 ) ) ;
#3046=ORIENTED_EDGE ( 'NONE', *, *, #47425, .T. ) ;
#3049=ORIENTED_EDGE ( 'NONE', *, *, #5210, .F. ) ;
#3050=B_SPLINE_CURVE_WITH_KNOTS ( 'NONE', 3,
 ( #39099, #47554, #4594, #38475 ),
 .UNSPECIFIED., .F., .F.,
 ( 4, 4 ),
 ( 0.000000000000000000, 0.004446090762761381598 ),
 .UNSPECIFIED. ) ;
#3054=LINE ( 'NONE', #56291, #8679 ) ;
#3059=CARTESIAN_POINT ( 'NONE',  ( 0.9757402383260953549, -39.67468066200768817, 16.34189654378420187 ) ) ;
#3063=CARTESIAN_POINT ( 'NONE',  ( 4.967162193818130511, 13.42934394584164082, 40.93989340068615945 ) ) ;
#3069=VERTEX_POINT ( 'NONE', #58215 ) ;
#3070=B_SPLINE_CURVE_WITH_KNOTS ( 'NONE', 3,
 ( #43460, #23404, #38149, #185, #38449, #3964 ),
 .UNSPECIFIED., .F., .F.,
 ( 4, 2, 4 ),
 ( 9.946927139006897773E-18, 0.0002445244328975399502, 0.0004890488657950700343 ),
 .UNSPECIFIED. ) ;
#3074=CARTESIAN_POINT ( 'NONE',  ( 0.9752570700956798566, -39.55341424149096241, -16.63323182627910768 ) ) ;
#3089=CARTESIAN_POINT ( 'NONE',  ( 3.407937589446178528, -4.815089211105147982, 12.82481284928202214 ) ) ;
#3092=VERTEX_POINT ( 'NONE', #10635 ) ;
#3096=CARTESIAN_POINT ( 'NONE',  ( 0.5839880159502348622, -37.97080096460561549, -29.19321933421534254 ) ) ;
#3099=EDGE_LOOP ( 'NONE', ( #48891, #51529, #45073, #20272 ) ) ;
#3106=EDGE_LOOP ( 'NONE', ( #22450, #37626, #44503, #53723 ) ) ;
#3122=VERTEX_POINT ( 'NONE', #2988 ) ;
#3126=CARTESIAN_POINT ( 'NONE',  ( 0.9754642270333666598, -34.14824330022352683, 25.98138239028847352 ) ) ;
#3127=CARTESIAN_POINT ( 'NONE',  ( 4.303969348037258058, -35.51084504003173947, -32.45857549159337907 ) ) ;
#3132=CARTESIAN_POINT ( 'NONE',  ( 0.9756008150404595902, 21.33101788548782096, -37.23069985082522493 ) ) ;
#3134=CARTESIAN_POINT ( 'NONE',  ( 3.407937589446178528, 3.099921468255189883, -13.34359005742686044 ) ) ;
#3148=LINE ( 'NONE', #60770, #1849 ) ;
#3158=CARTESIAN_POINT ( 'NONE',  ( 0.7057020205115055456, -41.05685587925817970, -24.67553336431228672 ) ) ;
#3160=VERTEX_POINT ( 'NONE', #41545 ) ;
#3163=ORIENTED_EDGE ( 'NONE', *, *, #6308, .F. ) ;
#3165=ORIENTED_EDGE ( 'NONE', *, *, #18905, .T. ) ;
#3166=CARTESIAN_POINT ( 'NONE',  ( 0.5850706913938534814, 0.1816364388700339449, 47.89601588673689037 ) ) ;
#3173=CARTESIAN_POINT ( 'NONE',  ( 4.960156602257181468, 44.12083041402485151, -14.43621227656483796 ) ) ;
#3181=B_SPLINE_CURVE_WITH_KNOTS ( 'NONE', 3,
 ( #5499, #33434, #42840, #10537, #29325, #37844 ),
 .UNSPECIFIED., .F., .F.,
 ( 4, 2, 4 ),
 ( 1.509732741315237692E-16, 0.0002445252820015224966, 0.0004890505640028939638 ),
 .UNSPECIFIED. ) ;
#3182=( BOUNDED_SURFACE ( )  B_SPLINE_SURFACE ( 3, 1, ( 
 ( #22452, #45053 ),
 ( #55020, #12150 ),
 ( #31538, #17756 ),
 ( #36883, #50630 ) ),
 .UNSPECIFIED., .F., .F., .F. ) 
 B_SPLINE_SURFACE_WITH_KNOTS ( ( 4, 4 ),
 ( 2, 2 ),
 ( 0.000000000000000000, 1.000000000000000000 ),
 ( 0.000000000000000000, 1.000000000000000000 ),
 .UNSPECIFIED. ) 
 GEOMETRIC_REPRESENTATION_ITEM ( )  RATIONAL_B_SPLINE_SURFACE ( (
 ( 1.000000000000000000, 1.000000000000000000),
 ( 0.7269869731126821222, 0.9931720237060910339),
 ( 0.7269869731126821222, 0.9931720237060910339),
 ( 1.000000000000000000, 1.000000000000000000) ) ) 
 REPRESENTATION_ITEM ( '' )  SURFACE ( )  );
#3187=CARTESIAN_POINT ( 'NONE',  ( 2.526464513654344657, -29.52129845577954370, 31.23609615087167057 ) ) ;
#3193=DIRECTION ( 'NONE',  ( 0.000000000000000000, 0.000000000000000000, 1.000000000000000000 ) ) ;
#3195=CARTESIAN_POINT ( 'NONE',  ( 0.9757402383260953549, -16.49876987395755279, 39.60970160107527960 ) ) ;
#3201=DIRECTION ( 'NONE',  ( -1.000000000000000000, -0.000000000000000000, -0.000000000000000000 ) ) ;
#3213=CARTESIAN_POINT ( 'NONE',  ( 0.8551540677456834771, 38.56334384152430772, 28.44084013485131379 ) ) ;
#3223=EDGE_CURVE ( 'NONE', #21472, #22913, #3541, .T. ) ;
#3240=ORIENTED_EDGE ( 'NONE', *, *, #24431, .T. ) ;
#3246=EDGE_CURVE ( 'NONE', #50327, #2552, #10342, .T. ) ;
#3257=CARTESIAN_POINT ( 'NONE',  ( 4.963659409799330291, 42.22332985082310586, 14.83726297270295014 ) ) ;
#3262=CARTESIAN_POINT ( 'NONE',  ( 0.9758171775293923433, 42.90848549292462621, -0.005919131625146459991 ) ) ;
#3263=CARTESIAN_POINT ( 'NONE',  ( 4.967162193818130511, 0.000000000000000000, 0.000000000000000000 ) ) ;
#3275=CARTESIAN_POINT ( 'NONE',  ( 5.960221823109900008, 20.34928172836730553, -2.684531185214208193 ) ) ;
#3280=EDGE_CURVE ( 'NONE', #5776, #33892, #7309, .T. ) ;
#3281=( BOUNDED_SURFACE ( )  B_SPLINE_SURFACE ( 3, 1, ( 
 ( #51256, #8341 ),
 ( #20540, #805 ),
 ( #52805, #44671 ),
 ( #15846, #59038 ) ),
 .UNSPECIFIED., .F., .F., .F. ) 
 B_SPLINE_SURFACE_WITH_KNOTS ( ( 4, 4 ),
 ( 2, 2 ),
 ( 0.000000000000000000, 1.000000000000000000 ),
 ( 0.000000000000000000, 1.000000000000000000 ),
 .UNSPECIFIED. ) 
 GEOMETRIC_REPRESENTATION_ITEM ( )  RATIONAL_B_SPLINE_SURFACE ( (
 ( 1.000000000000000000, 1.000000000000000000),
 ( 0.7269869731126821222, 0.9931720237060910339),
 ( 0.7269869731126821222, 0.9931720237060910339),
 ( 1.000000000000000000, 1.000000000000000000) ) ) 
 REPRESENTATION_ITEM ( '' )  SURFACE ( )  );
#3282=CARTESIAN_POINT ( 'NONE',  ( 5.965394784446458765, -5.326334832595513546, -19.82223131420052198 ) ) ;
#3287=CARTESIAN_POINT ( 'NONE',  ( 4.967162193818130511, 40.93989340068610261, 13.42934394584178648 ) ) ;
#3288=EDGE_CURVE ( 'NONE', #18299, #23600, #46548, .T. ) ;
#3290=ORIENTED_EDGE ( 'NONE', *, *, #20257, .F. ) ;
#3293=CARTESIAN_POINT ( 'NONE',  ( 0.8557997880470697982, -23.15977007032352475, 41.93815086860250574 ) ) ;
#3302=VERTEX_POINT ( 'NONE', #53668 ) ;
#3311=ORIENTED_EDGE ( 'NONE', *, *, #4533, .T. ) ;
#3322=ORIENTED_EDGE ( 'NONE', *, *, #3588, .F. ) ;
#3333=CARTESIAN_POINT ( 'NONE',  ( 0.9722240741986376555, -11.66659279944005334, 41.29187377038497431 ) ) ;
#3335=EDGE_CURVE ( 'NONE', #44156, #21453, #16910, .T. ) ;
#3344=CARTESIAN_POINT ( 'NONE',  ( 5.974727161628369032, -2.663664384318642497, -20.35137732084675122 ) ) ;
#3346=VERTEX_POINT ( 'NONE', #33997 ) ;
#3347=CARTESIAN_POINT ( 'NONE',  ( 0.9757892942422827787, -30.30456399643813370, 30.37715353261981122 ) ) ;
#3348=CARTESIAN_POINT ( 'NONE',  ( 4.956653778116990594, -39.67974989265022145, -27.17045123668512474 ) ) ;
#3350=CARTESIAN_POINT ( 'NONE',  ( 0.9757787079277443487, 5.639827755377256224, -42.53619983261571491 ) ) ;
#3354=CARTESIAN_POINT ( 'NONE',  ( 1.154321485836933725, -42.64911658695771735, -4.782433484301630955 ) ) ;
#3355=CARTESIAN_POINT ( 'NONE',  ( 5.959547316686252039, 14.51128755440521267, 14.51632612601533801 ) ) ;
#3369=VERTEX_POINT ( 'NONE', #5443 ) ;
#3370=CARTESIAN_POINT ( 'NONE',  ( 5.860006189529246790, -45.66786516969918353, -15.52021937683323927 ) ) ;
#3379=VECTOR ( 'NONE', #26608, 1000.000000000000000 ) ;
#3382=EDGE_CURVE ( 'NONE', #3122, #23289, #61474, .T. ) ;
#3385=CARTESIAN_POINT ( 'NONE',  ( 0.5809828226811553087, -0.5448590168529036104, -47.89273459658654275 ) ) ;
#3389=CARTESIAN_POINT ( 'NONE',  ( 0.5839879327111905383, -29.08515285004915540, 38.05372318152046063 ) ) ;
#3390=ORIENTED_EDGE ( 'NONE', *, *, #39633, .F. ) ;
#3397=ORIENTED_EDGE ( 'NONE', *, *, #10985, .F. ) ;
#3402=CARTESIAN_POINT ( 'NONE',  ( 0.5807400328401574052, 46.40483864045145168, 11.87003418057259907 ) ) ;
#3406=CARTESIAN_POINT ( 'NONE',  ( 5.981074661064941900, 19.82308078259091033, -5.320466518160730907 ) ) ;
#3422=CARTESIAN_POINT ( 'NONE',  ( 4.956653778116949738, 45.71126949320249366, 14.93973939759898606 ) ) ;
#3424=CARTESIAN_POINT ( 'NONE',  ( 0.9730545539215883499, -33.73144377768576874, 26.52009130076758225 ) ) ;
#3427=CARTESIAN_POINT ( 'NONE',  ( 0.9972139404380304661, 22.02214929131140764, 36.82725283858614063 ) ) ;
#3429=EDGE_LOOP ( 'NONE', ( #43825, #41789, #34355, #35485 ) ) ;
#3432=CARTESIAN_POINT ( 'NONE',  ( 0.8551540677456834771, 37.45266983663536564, -29.88829867897776538 ) ) ;
#3436=CARTESIAN_POINT ( 'NONE',  ( 4.967162193818130511, 42.34252806656594004, 7.970725651239941811 ) ) ;
#3441=CARTESIAN_POINT ( 'NONE',  ( 0.5819845901640493535, -28.79568196372244060, -38.27312528999461705 ) ) ;
#3444=CARTESIAN_POINT ( 'NONE',  ( 0.7056555295713298204, 47.89404551051138270, -0.8411712675129686678 ) ) ;
#3449=ORIENTED_EDGE ( 'NONE', *, *, #16572, .T. ) ;
#3451=CARTESIAN_POINT ( 'NONE',  ( 0.8551540677456739292, -24.74404575822804375, 41.03346287276421123 ) ) ;
#3453=( NAMED_UNIT ( * ) SI_UNIT ( $, .STERADIAN. ) SOLID_ANGLE_UNIT ( ) );
#3454=ORIENTED_EDGE ( 'NONE', *, *, #41368, .T. ) ;
#3456=CARTESIAN_POINT ( 'NONE',  ( 4.963659409799332067, -25.25989740981475506, -36.94443854030247110 ) ) ;
#3466=EDGE_LOOP ( 'NONE', ( #6368, #50164, #18863, #18524 ) ) ;
#3485=EDGE_CURVE ( 'NONE', #44988, #9101, #7674, .T. ) ;
#3489=CARTESIAN_POINT ( 'NONE',  ( 4.960156602257181468, -35.23783291257149841, -30.22163187094425396 ) ) ;
#3495=CARTESIAN_POINT ( 'NONE',  ( 5.960221823109900008, -16.28072933292539659, -12.49951306783083638 ) ) ;
#3502=DIRECTION ( 'NONE',  ( -1.000000000000000000, -0.000000000000000000, -0.000000000000000000 ) ) ;
#3509=CARTESIAN_POINT ( 'NONE',  ( 1.227938101723756947, 26.79402671879326547, 33.52879263017872091 ) ) ;
#3510=FACE_OUTER_BOUND ( 'NONE', #37387, .T. ) ;
#3512=CARTESIAN_POINT ( 'NONE',  ( 0.9736507210033060744, -36.93248879681195973, -21.84312502845830295 ) ) ;
#3516=CARTESIAN_POINT ( 'NONE',  ( 0.9756950546413946102, 39.67916378221936213, 16.33093981194336664 ) ) ;
#3519=CARTESIAN_POINT ( 'NONE',  ( 4.956653778116992370, 21.75875759808766929, -42.88673967249108188 ) ) ;
#3520=CARTESIAN_POINT ( 'NONE',  ( 0.5819845901640492425, 23.55368560422342483, 41.70428411658535595 ) ) ;
#3526=CARTESIAN_POINT ( 'NONE',  ( 1.154321485836934169, 4.782433484301801485, -42.64911658695771024 ) ) ;
#3528=ORIENTED_EDGE ( 'NONE', *, *, #29071, .F. ) ;
#3532=EDGE_CURVE ( 'NONE', #44988, #34186, #60871, .T. ) ;
#3533=CARTESIAN_POINT ( 'NONE',  ( 0.5807400328401574052, 44.04145271122565219, 18.83234461715198904 ) ) ;
#3534=CARTESIAN_POINT ( 'NONE',  ( 0.9757402383260955769, -41.46830379850860027, 11.02350435907888482 ) ) ;
#3538=DIRECTION ( 'NONE',  ( 0.000000000000000000, 0.000000000000000000, 1.000000000000000000 ) ) ;
#3541=B_SPLINE_CURVE_WITH_KNOTS ( 'NONE', 3,
 ( #61532, #4515, #32758, #27738, #42475, #18655 ),
 .UNSPECIFIED., .F., .F.,
 ( 4, 2, 4 ),
 ( 8.985151752445514084E-18, 0.0002291978881530154554, 0.0004583957763060219660 ),
 .UNSPECIFIED. ) ;
#3548=FACE_OUTER_BOUND ( 'NONE', #12124, .T. ) ;
#3557=( BOUNDED_SURFACE ( )  B_SPLINE_SURFACE ( 3, 1, ( 
 ( #41394, #61678 ),
 ( #51061, #22575 ),
 ( #8774, #8156 ),
 ( #47016, #51366 ) ),
 .UNSPECIFIED., .F., .F., .F. ) 
 B_SPLINE_SURFACE_WITH_KNOTS ( ( 4, 4 ),
 ( 2, 2 ),
 ( 0.000000000000000000, 1.000000000000000000 ),
 ( 0.000000000000000000, 1.000000000000000000 ),
 .UNSPECIFIED. ) 
 GEOMETRIC_REPRESENTATION_ITEM ( )  RATIONAL_B_SPLINE_SURFACE ( (
 ( 1.000000000000000000, 1.000000000000000000),
 ( 0.9953390228620291325, 0.8624445117760984880),
 ( 0.9953390228620291325, 0.8624445117760984880),
 ( 1.000000000000000000, 1.000000000000000000) ) ) 
 REPRESENTATION_ITEM ( '' )  SURFACE ( )  );
#3562=CARTESIAN_POINT ( 'NONE',  ( 1.227938101723748288, -26.79402671879349640, 33.52879263017854328 ) ) ;
#3565=ORIENTED_EDGE ( 'NONE', *, *, #8765, .F. ) ;
#3569=CARTESIAN_POINT ( 'NONE',  ( 0.7762783648524385072, -44.59086139387527226, -17.50713302551375961 ) ) ;
#3572=CARTESIAN_POINT ( 'NONE',  ( 0.8557997880470599172, 41.02602466100778145, 24.73961900479265807 ) ) ;
#3573=CARTESIAN_POINT ( 'NONE',  ( 0.9722240741986378776, 20.94823706911201100, 37.44729083276432391 ) ) ;
#3584=CARTESIAN_POINT ( 'NONE',  ( 4.967162193818130511, -32.10009971360091896, 28.74031574030002645 ) ) ;
#3587=CARTESIAN_POINT ( 'NONE',  ( 0.5832366564991521285, 12.65934068133983814, 46.19265750221173050 ) ) ;
#3588=EDGE_CURVE ( 'NONE', #46801, #20008, #55869, .T. ) ;
#3595=LINE ( 'NONE', #13044, #23508 ) ;
#3597=EDGE_CURVE ( 'NONE', #56316, #32792, #40561, .T. ) ;
#3604=EDGE_LOOP ( 'NONE', ( #2504, #52252, #52224, #46336 ) ) ;
#3615=CARTESIAN_POINT ( 'NONE',  ( 4.967162193818130511, -38.44485641567084855, 19.45289607368810181 ) ) ;
#3621=ORIENTED_EDGE ( 'NONE', *, *, #27547, .T. ) ;
#3641=CARTESIAN_POINT ( 'NONE',  ( 3.783278058412224087, -43.00370293663099375, 1.726763838446040644 ) ) ;
#3644=ORIENTED_EDGE ( 'NONE', *, *, #27146, .T. ) ;
#3645=CARTESIAN_POINT ( 'NONE',  ( -19.36083530377080564, -12.39979437149483132, -1.582588903604334574 ) ) ;
#3649=CARTESIAN_POINT ( 'NONE',  ( 0.8557997880470690211, 23.15977007032381607, -41.93815086860232810 ) ) ;
#3654=ORIENTED_EDGE ( 'NONE', *, *, #36593, .T. ) ;
#3656=CARTESIAN_POINT ( 'NONE',  ( 0.8551540677456834771, -46.51172240253112733, -11.51835730326528839 ) ) ;
#3658=CARTESIAN_POINT ( 'NONE',  ( 0.7762783648524385072, 19.15108798908314469, 43.90991295203428280 ) ) ;
#3660=B_SPLINE_CURVE_WITH_KNOTS ( 'NONE', 3,
 ( #21259, #40093, #11243, #49755, #59142, #1821 ),
 .UNSPECIFIED., .F., .F.,
 ( 4, 2, 4 ),
 ( 6.149443329761889321E-18, 0.0002445244328975381071, 0.0004890488657950701427 ),
 .UNSPECIFIED. ) ;
#3668=CARTESIAN_POINT ( 'NONE',  ( 5.965394784446460541, 7.841344330024671017, 18.96850062921637559 ) ) ;
#3672=CARTESIAN_POINT ( 'NONE',  ( 0.5800708057587377064, 37.61306623599842425, 29.65250565429455776 ) ) ;
#3673=CARTESIAN_POINT ( 'NONE',  ( 4.956653778116966613, 0.000000000000000000, 0.000000000000000000 ) ) ;
#3676=ORIENTED_EDGE ( 'NONE', *, *, #23344, .T. ) ;
#3685=CARTESIAN_POINT ( 'NONE',  ( 4.956653778116975495, -31.29546495791875316, 36.51451553856407628 ) ) ;
#3690=CARTESIAN_POINT ( 'NONE',  ( 0.6846871229502932144, -33.25969555998718619, -34.48177377577871283 ) ) ;
#3693=CARTESIAN_POINT ( 'NONE',  ( 5.960221823109900008, -12.49951306783101579, 16.28072933292526159 ) ) ;
#3694=CARTESIAN_POINT ( 'NONE',  ( 4.967162193818130511, 0.000000000000000000, 0.000000000000000000 ) ) ;
#3696=CARTESIAN_POINT ( 'NONE',  ( 0.9756354156337445627, 21.34128958497381845, 37.22481466014907170 ) ) ;
#3698=AXIS2_PLACEMENT_3D ( 'NONE', #10382, #19173, #61729 ) ;
#3701=ORIENTED_EDGE ( 'NONE', *, *, #58044, .F. ) ;
#3714=CARTESIAN_POINT ( 'NONE',  ( 5.960721111146673579, 2.685391721746036353, -20.34914600876572521 ) ) ;
#3715=CARTESIAN_POINT ( 'NONE',  ( 4.963659409799330291, 3.403493583737961181, -44.62477100936213503 ) ) ;
#3716=VERTEX_POINT ( 'NONE', #48919 ) ;
#3719=EDGE_LOOP ( 'NONE', ( #57930, #23588, #42017, #58475 ) ) ;
#3720=CARTESIAN_POINT ( 'NONE',  ( 0.9752570700956788574, 34.18150842933915357, -25.93764562640069826 ) ) ;
#3728=CARTESIAN_POINT ( 'NONE',  ( 0.5834872094924170582, 47.45604551759237211, 6.476680342366744725 ) ) ;
#3738=ORIENTED_EDGE ( 'NONE', *, *, #61847, .T. ) ;
#3741=EDGE_CURVE ( 'NONE', #14535, #448, #16332, .T. ) ;
#3744=CARTESIAN_POINT ( 'NONE',  ( 0.5838002273316424962, 6.386683873061191896, -47.46823345111864256 ) ) ;
#3745=CARTESIAN_POINT ( 'NONE',  ( 0.6846871229502932144, -46.04462816497477462, -13.23224427737877562 ) ) ;
#3754=ORIENTED_EDGE ( 'NONE', *, *, #39719, .T. ) ;
#3758=B_SPLINE_CURVE_WITH_KNOTS ( 'NONE', 3,
 ( #19446, #28833, #44206, #19760 ),
 .UNSPECIFIED., .F., .F.,
 ( 4, 4 ),
 ( 0.000000000000000000, 0.005004741218457418872 ),
 .UNSPECIFIED. ) ;
#3759=CARTESIAN_POINT ( 'NONE',  ( 0.000000000000000000, 0.000000000000000000, 0.000000000000000000 ) ) ;
#3760=ORIENTED_EDGE ( 'NONE', *, *, #15720, .T. ) ;
#3762=EDGE_CURVE ( 'NONE', #46350, #8115, #58480, .T. ) ;
#3764=CARTESIAN_POINT ( 'NONE',  ( 4.960156602257181468, -44.12083041402454597, -14.43621227656575101 ) ) ;
#3765=EDGE_LOOP ( 'NONE', ( #15448, #56790, #30990, #9629 ) ) ;
#3769=ORIENTED_EDGE ( 'NONE', *, *, #2945, .F. ) ;
#3782=AXIS2_PLACEMENT_3D ( 'NONE', #29947, #34978, #26168 ) ;
#3790=AXIS2_PLACEMENT_3D ( 'NONE', #48663, #48979, #412 ) ;
#3791=CARTESIAN_POINT ( 'NONE',  ( 0.9754402186311955658, -42.90805920318125288, 0.1875553420610092115 ) ) ;
#3796=CARTESIAN_POINT ( 'NONE',  ( 5.959547316686252039, 10.26589671991338548, 17.77392908783937386 ) ) ;
#3800=CARTESIAN_POINT ( 'NONE',  ( 5.965394784446458765, 14.52385693118982601, 14.50338846149138305 ) ) ;
#3804=VERTEX_POINT ( 'NONE', #41102 ) ;
#3807=CARTESIAN_POINT ( 'NONE',  ( 0.8551540677456834771, -43.91216198251552782, 19.17641535420837684 ) ) ;
#3813=DIRECTION ( 'NONE',  ( 0.000000000000000000, 0.000000000000000000, 1.000000000000000000 ) ) ;
#3815=DIRECTION ( 'NONE',  ( 0.07439287786467665975, -0.9903339163990689809, 0.1170659376278736646 ) ) ;
#3817=B_SPLINE_CURVE_WITH_KNOTS ( 'NONE', 3,
 ( #49254, #6312, #44590, #29843, #40214, #2248 ),
 .UNSPECIFIED., .F., .F.,
 ( 4, 2, 4 ),
 ( 1.509951125874620249E-16, 0.0002445252820015219003, 0.0004890505640028928796 ),
 .UNSPECIFIED. ) ;
#3819=CARTESIAN_POINT ( 'NONE',  ( 1.227938101723747621, 6.439911493065174852, -42.43379953535178828 ) ) ;
#3822=CARTESIAN_POINT ( 'NONE',  ( 3.783278058412224976, 27.54892951149544800, 33.06594414781506686 ) ) ;
#3832=CARTESIAN_POINT ( 'NONE',  ( 0.5809828226811617480, 41.20389530892307306, 24.41822904836939401 ) ) ;
#3833=CARTESIAN_POINT ( 'NONE',  ( 3.407937589446174087, -13.10584870154463744, -3.987184287467924193 ) ) ;
#3841=CARTESIAN_POINT ( 'NONE',  ( 0.5263152470540364281, 0.000000000000000000, -42.88844316795388778 ) ) ;
#3843=CARTESIAN_POINT ( 'NONE',  ( 0.9752132459055865565, -41.38545930839056552, 11.33038172416138067 ) ) ;
#3846=CARTESIAN_POINT ( 'NONE',  ( 0.5809828226811617480, -11.86925843957133786, -46.40184912890851621 ) ) ;
#3856=VERTEX_POINT ( 'NONE', #51066 ) ;
#3857=AXIS2_PLACEMENT_3D ( 'NONE', #13004, #13609, #33032 ) ;
#3858=ORIENTED_EDGE ( 'NONE', *, *, #55941, .T. ) ;
#3865=ORIENTED_EDGE ( 'NONE', *, *, #15052, .F. ) ;
#3873=LINE ( 'NONE', #41511, #12713 ) ;
#3877=CARTESIAN_POINT ( 'NONE',  ( 0.5263152470540364281, 0.000000000000000000, 0.000000000000000000 ) ) ;
#3884=CARTESIAN_POINT ( 'NONE',  ( 3.270143674763207553, 3.277085381513305418, -13.28976595685390016 ) ) ;
#3886=CARTESIAN_POINT ( 'NONE',  ( 1.227938101723747621, 20.72293514920750468, 37.58536632582787007 ) ) ;
#3890=EDGE_CURVE ( 'NONE', #13682, #40152, #17349, .T. ) ;
#3893=DIRECTION ( 'NONE',  ( 0.07439287786467665975, -0.7144194931003113869, 0.6957517427942997434 ) ) ;
#3904=ORIENTED_EDGE ( 'NONE', *, *, #6197, .F. ) ;
#3905=ORIENTED_EDGE ( 'NONE', *, *, #30816, .F. ) ;
#3907=CARTESIAN_POINT ( 'NONE',  ( 2.526552050251861914, -31.23611603144884441, 29.52128340070590085 ) ) ;
#3912=CARTESIAN_POINT ( 'NONE',  ( 0.6067099128993252988, -23.33192673707561227, 41.82996792600769709 ) ) ;
#3918=CARTESIAN_POINT ( 'NONE',  ( 0.9754642270333709897, 41.40054989430073817, 11.27515941577587277 ) ) ;
#3923=( BOUNDED_SURFACE ( )  B_SPLINE_SURFACE ( 3, 1, ( 
 ( #44112, #5219 ),
 ( #38467, #43800 ),
 ( #19980, #39092 ),
 ( #52533, #14658 ) ),
 .UNSPECIFIED., .F., .F., .F. ) 
 B_SPLINE_SURFACE_WITH_KNOTS ( ( 4, 4 ),
 ( 2, 2 ),
 ( 0.000000000000000000, 1.000000000000000000 ),
 ( 0.000000000000000000, 1.000000000000000000 ),
 .UNSPECIFIED. ) 
 GEOMETRIC_REPRESENTATION_ITEM ( )  RATIONAL_B_SPLINE_SURFACE ( (
 ( 1.000000000000000000, 1.000000000000000000),
 ( 0.9732289882329797637, 0.9999525324661233672),
 ( 0.9732289882329797637, 0.9999525324661233672),
 ( 1.000000000000000000, 1.000000000000000000) ) ) 
 REPRESENTATION_ITEM ( '' )  SURFACE ( )  );
#3926=CARTESIAN_POINT ( 'NONE',  ( 4.967162193818130511, -2.375726030842277403, -43.02067033766020643 ) ) ;
#3934=CARTESIAN_POINT ( 'NONE',  ( 5.960721111146673579, 7.860635756377893912, -18.96073515164540879 ) ) ;
#3935=CARTESIAN_POINT ( 'NONE',  ( 0.5832366564991491309, 41.61464700196777500, 23.71163571971538886 ) ) ;
#3941=EDGE_CURVE ( 'NONE', #3856, #8543, #3148, .T. ) ;
#3945=CIRCLE ( 'NONE', #30977, 43.08621763946400307 ) ;
#3948=CARTESIAN_POINT ( 'NONE',  ( 0.5836750258453354823, -47.46217286060748108, -6.431686642655249031 ) ) ;
#3949=EDGE_CURVE ( 'NONE', #3021, #31508, #39791, .T. ) ;
#3953=CARTESIAN_POINT ( 'NONE',  ( 4.956653778116991482, -14.93973939759855263, -45.71126949320266419 ) ) ;
#3960=B_SPLINE_CURVE_WITH_KNOTS ( 'NONE', 3,
 ( #29309, #52181, #23384, #14307, #43129, #33414 ),
 .UNSPECIFIED., .F., .F.,
 ( 4, 2, 4 ),
 ( 7.023086426956682172E-18, 0.0002445244328975370771, 0.0004890488657950671069 ),
 .UNSPECIFIED. ) ;
#3962=CONICAL_SURFACE ( 'NONE', #60003, 43.08621763946400307, 1.568696531533066763 ) ;
#3963=ORIENTED_EDGE ( 'NONE', *, *, #11547, .T. ) ;
#3964=CARTESIAN_POINT ( 'NONE',  ( 0.8557997880470697982, 38.55640757422439435, 28.43566216844983074 ) ) ;
#3967=EDGE_CURVE ( 'NONE', #14355, #59171, #24900, .T. ) ;
#3969=CARTESIAN_POINT ( 'NONE',  ( 4.956653778117001252, 47.94889704119056972, -3.690426056929486887 ) ) ;
#3971=CARTESIAN_POINT ( 'NONE',  ( 0.5839879882012697365, -47.89596766821089346, 3.018602120542737986E-05 ) ) ;
#3978=FACE_OUTER_BOUND ( 'NONE', #18229, .T. ) ;
#3979=CARTESIAN_POINT ( 'NONE',  ( 4.303969348037246512, 8.413118729224734693, -47.36875205922763143 ) ) ;
#3984=VERTEX_POINT ( 'NONE', #4052 ) ;
#3985=CARTESIAN_POINT ( 'NONE',  ( 0.9741495583595157770, 11.48707840139643466, -41.34222751889817005 ) ) ;
#3995=EDGE_CURVE ( 'NONE', #41370, #53492, #1673, .T. ) ;
#3998=CARTESIAN_POINT ( 'NONE',  ( 0.5839879882104919151, -1.006200701304952040E-05, -47.89596766822081264 ) ) ;
#3999=AXIS2_PLACEMENT_3D ( 'NONE', #37277, #47278, #4324 ) ;
#4000=CARTESIAN_POINT ( 'NONE',  ( 5.959547316686252039, 14.51632612601508754, 14.51128755440546314 ) ) ;
#4010=CARTESIAN_POINT ( 'NONE',  ( 4.967162193818130511, 40.65506779172185503, -14.26841313271238221 ) ) ;
#4012=EDGE_CURVE ( 'NONE', #32300, #17561, #55379, .T. ) ;
#4026=CARTESIAN_POINT ( 'NONE',  ( 3.270143674763207553, 13.68510027222513337, 0.2742231296310058686 ) ) ;
#4027=CARTESIAN_POINT ( 'NONE',  ( 5.860006189529234355, 15.48781697582111327, -45.67886430272015730 ) ) ;
#4034=ADVANCED_FACE ( 'NONE', ( #39166 ), #56517, .F. ) ;
#4038=CARTESIAN_POINT ( 'NONE',  ( 0.5800708119828327236, -34.30831427709729553, -33.42085299104054741 ) ) ;
#4041=CARTESIAN_POINT ( 'NONE',  ( 3.660176727303073196, 47.34518114598545679, 8.130955556893987080 ) ) ;
#4047=CARTESIAN_POINT ( 'NONE',  ( 5.960721111146673579, 19.82781442290490403, 5.306302591836648652 ) ) ;
#4050=VERTEX_POINT ( 'NONE', #14423 ) ;
#4052=CARTESIAN_POINT ( 'NONE',  ( 0.5809828226811617480, -41.74875432577665890, 23.47450554821694979 ) ) ;
#4054=B_SPLINE_CURVE_WITH_KNOTS ( 'NONE', 3,
 ( #49275, #24868, #25465, #1337 ),
 .UNSPECIFIED., .F., .F.,
 ( 4, 4 ),
 ( 2.501853776554200607E-17, 0.005004741218457455301 ),
 .UNSPECIFIED. ) ;
#4073=CARTESIAN_POINT ( 'NONE',  ( 0.5838002273316424962, -6.116619957188429879, -47.50378804015151957 ) ) ;
#4076=CARTESIAN_POINT ( 'NONE',  ( 5.960721111146673579, 20.52557019979492026, 0.006321279846891981850 ) ) ;
#4077=ORIENTED_EDGE ( 'NONE', *, *, #31678, .T. ) ;
#4078=FACE_OUTER_BOUND ( 'NONE', #1486, .T. ) ;
#4080=CARTESIAN_POINT ( 'NONE',  ( 4.956653778116966613, 0.000000000000000000, 0.000000000000000000 ) ) ;
#4081=CARTESIAN_POINT ( 'NONE',  ( 5.965394784446458765, -18.95742317323950843, 7.868087674480618965 ) ) ;
#4085=CARTESIAN_POINT ( 'NONE',  ( 4.967162193818130511, -42.96271701169388280, 3.259922920617591924 ) ) ;
#4089=CARTESIAN_POINT ( 'NONE',  ( 0.5819845079324653669, 44.42187385013365031, 17.90867223323903445 ) ) ;
#4096=B_SPLINE_CURVE_WITH_KNOTS ( 'NONE', 3,
 ( #42262, #26906, #61321, #32228 ),
 .UNSPECIFIED., .F., .F.,
 ( 4, 4 ),
 ( 4.336808689942017736E-19, 0.004048833967417085622 ),
 .UNSPECIFIED. ) ;
#4098=CARTESIAN_POINT ( 'NONE',  ( 0.6846871229502932144, -23.20185915381527408, -41.91507847151822119 ) ) ;
#4100=CARTESIAN_POINT ( 'NONE',  ( 4.963659409799330291, 8.262218268421102962, -43.98510776953393986 ) ) ;
#4101=CARTESIAN_POINT ( 'NONE',  ( 5.960721111146673579, 14.51823969584079599, 14.50930005615021656 ) ) ;
#4103=ORIENTED_EDGE ( 'NONE', *, *, #42824, .F. ) ;
#4105=CARTESIAN_POINT ( 'NONE',  ( 2.624215991343620935, -43.79392271049083263, 19.66774719432963892 ) ) ;
#4107=B_SPLINE_CURVE_WITH_KNOTS ( 'NONE', 3,
 ( #18239, #17935, #26697, #32645 ),
 .UNSPECIFIED., .F., .F.,
 ( 4, 4 ),
 ( 7.376145397762941244E-17, 0.005004741218457468312 ),
 .UNSPECIFIED. ) ;
#4118=CARTESIAN_POINT ( 'NONE',  ( 0.9722240750034584211, 33.68410530487908261, -26.58024222649010682 ) ) ;
#4122=CARTESIAN_POINT ( 'NONE',  ( 1.227938101723756947, -33.52879263017882039, 26.79402671879314823 ) ) ;
#4123=LINE ( 'NONE', #38006, #35901 ) ;
#4124=AXIS2_PLACEMENT_3D ( 'NONE', #50604, #51840, #51526 ) ;
#4131=CARTESIAN_POINT ( 'NONE',  ( 0.5832367798473382381, 23.71165515427716031, 41.61463593465314403 ) ) ;
#4134=EDGE_CURVE ( 'NONE', #9388, #59309, #7554, .T. ) ;
#4137=CARTESIAN_POINT ( 'NONE',  ( 4.956653778116480780, -21.75875759808806720, 42.88673967249081898 ) ) ;
#4141=ORIENTED_EDGE ( 'NONE', *, *, #15136, .T. ) ;
#4150=ORIENTED_EDGE ( 'NONE', *, *, #38097, .F. ) ;
#4152=CARTESIAN_POINT ( 'NONE',  ( 0.5827357941260206120, -12.74691551863599059, -46.16863402900294489 ) ) ;
#4160=ORIENTED_EDGE ( 'NONE', *, *, #15560, .F. ) ;
#4171=CARTESIAN_POINT ( 'NONE',  ( 0.9730545539215883499, 6.101350888305258735, -42.47233286818610054 ) ) ;
#4180=CARTESIAN_POINT ( 'NONE',  ( 4.960156602257182357, 46.28683144126601690, -3.546989772329427915 ) ) ;
#4183=CARTESIAN_POINT ( 'NONE',  ( 0.9756008150404585910, -42.52260101821271121, 5.741579752919493629 ) ) ;
#4184=CARTESIAN_POINT ( 'NONE',  ( 5.981074661064941900, 10.26976685693823121, -17.77058762078867460 ) ) ;
#4185=CARTESIAN_POINT ( 'NONE',  ( 5.960721111146673579, -5.318514366755071165, 19.82454228767736382 ) ) ;
#4186=EDGE_CURVE ( 'NONE', #61767, #17579, #41328, .T. ) ;
#4192=ORIENTED_EDGE ( 'NONE', *, *, #22081, .T. ) ;
#4193=LINE ( 'NONE', #33664, #46941 ) ;
#4196=LINE ( 'NONE', #12718, #33024 ) ;
#4197=B_SPLINE_CURVE_WITH_KNOTS ( 'NONE', 3,
 ( #28418, #19055, #33458, #47548, #53147, #9627, #9316, #23733, #19662, #38168, #10255, #43170, #24040, #204, #14970, #19351, #48455, #57522, #5824 ),
 .UNSPECIFIED., .F., .F.,
 ( 4, 3, 3, 3, 3, 3, 4 ),
 ( 5.204170427930420513E-18, 0.0002724573126191753760, 0.0004086839781548465798, 0.0005449106435901828957, 0.0006811373090491458200, 0.0008459866663933683986, 0.001010840725717211848 ),
 .UNSPECIFIED. ) ;
#4219=ORIENTED_EDGE ( 'NONE', *, *, #58747, .F. ) ;
#4220=VERTEX_POINT ( 'NONE', #7036 ) ;
#4224=CARTESIAN_POINT ( 'NONE',  ( 0.5786265663353196143, -17.66171603226047182, -44.52624106864163167 ) ) ;
#4233=ADVANCED_FACE ( 'NONE', ( #30240 ), #52126, .F. ) ;
#4238=CARTESIAN_POINT ( 'NONE',  ( 5.960721111146673579, 20.52557019979492026, -0.006321279846608376246 ) ) ;
#4240=CARTESIAN_POINT ( 'NONE',  ( 3.783198216974394068, -18.05208553945175254, 39.06945274417385860 ) ) ;
#4242=ORIENTED_EDGE ( 'NONE', *, *, #20097, .T. ) ;
#4243=ORIENTED_EDGE ( 'NONE', *, *, #22486, .F. ) ;
#4249=ORIENTED_EDGE ( 'NONE', *, *, #54835, .T. ) ;
#4252=ORIENTED_EDGE ( 'NONE', *, *, #17548, .F. ) ;
#4255=CARTESIAN_POINT ( 'NONE',  ( 0.9754642270333691023, 26.26019354539084105, -33.93430397636383589 ) ) ;
#4267=CARTESIAN_POINT ( 'NONE',  ( 0.9745511491811751359, -30.58068216140355489, 30.09905547141343263 ) ) ;
#4268=CARTESIAN_POINT ( 'NONE',  ( 1.088313998177380615, 42.90642884828985615, 0.7798619649922788888 ) ) ;
#4273=CARTESIAN_POINT ( 'NONE',  ( 0.5839880159502355284, -47.89596769806546206, -0.04537901683531408298 ) ) ;
#4283=CARTESIAN_POINT ( 'NONE',  ( 5.860006189529234355, 9.393028332205414443, -47.30964106197847485 ) ) ;
#4303=CARTESIAN_POINT ( 'NONE',  ( 0.5786265663353196143, -33.35675271369515116, -34.37803667029846366 ) ) ;
#4308=CARTESIAN_POINT ( 'NONE',  ( 0.5832367798473392373, -38.16362489683108805, 28.94059862654978943 ) ) ;
#4315=ORIENTED_EDGE ( 'NONE', *, *, #28635, .T. ) ;
#4320=CARTESIAN_POINT ( 'NONE',  ( 5.959547316686252039, 16.28624005235082350, 12.49238070347981910 ) ) ;
#4324=DIRECTION ( 'NONE',  ( 0.000000000000000000, 0.000000000000000000, -1.000000000000000000 ) ) ;
#4329=CARTESIAN_POINT ( 'NONE',  ( 5.965394784446458765, -19.82972329408682199, -5.298374383010567179 ) ) ;
#4343=CARTESIAN_POINT ( 'NONE',  ( 5.965394784446460541, 0.01447339372453102999, -20.52536205633085231 ) ) ;
#4345=CARTESIAN_POINT ( 'NONE',  ( 5.965394784446458765, -20.35165389555756477, -2.664747781316041841 ) ) ;
#4354=ORIENTED_EDGE ( 'NONE', *, *, #48234, .F. ) ;
#4355=CARTESIAN_POINT ( 'NONE',  ( 1.227938101723756947, -39.96870412324324917, -15.63977281655884077 ) ) ;
#4359=VERTEX_POINT ( 'NONE', #15887 ) ;
#4360=ADVANCED_FACE ( 'NONE', ( #44712 ), #21049, .T. ) ;
#4361=CARTESIAN_POINT ( 'NONE',  ( 0.7762783648524390623, -46.03397615175193636, 13.25585403815104613 ) ) ;
#4364=ORIENTED_EDGE ( 'NONE', *, *, #46286, .F. ) ;
#4368=EDGE_LOOP ( 'NONE', ( #50316, #11596, #32917, #34494 ) ) ;
#4370=CARTESIAN_POINT ( 'NONE',  ( 4.960156602257182357, -15.40604254112674987, 43.79161740034471251 ) ) ;
#4376=CARTESIAN_POINT ( 'NONE',  ( 4.956653778116973719, 27.17045123668471973, 39.67974989265048436 ) ) ;
#4380=CARTESIAN_POINT ( 'NONE',  ( 3.783278058412224087, -12.79810311738825668, -41.09146792477079657 ) ) ;
#4386=CARTESIAN_POINT ( 'NONE',  ( 5.960721111146673579, 2.672857320903303968, -20.35079619394243267 ) ) ;
#4389=CARTESIAN_POINT ( 'NONE',  ( 0.5819845901640485764, -33.54497622115107447, -34.18710267837688832 ) ) ;
#4391=CIRCLE ( 'NONE', #53419, 48.09070567114147110 ) ;
#4392=EDGE_LOOP ( 'NONE', ( #39835, #8337, #19205, #8331 ) ) ;
#4401=ORIENTED_EDGE ( 'NONE', *, *, #61136, .F. ) ;
#4406=CARTESIAN_POINT ( 'NONE',  ( 0.9730545539215883499, 34.34678117142591702, -25.71816799638743944 ) ) ;
#4409=EDGE_CURVE ( 'NONE', #29673, #33762, #33082, .T. ) ;
#4417=CARTESIAN_POINT ( 'NONE',  ( 0.9749527285493296835, 30.54214995146816491, -30.13822974582783232 ) ) ;
#4420=CARTESIAN_POINT ( 'NONE',  ( 0.9757892942422814464, 37.18547544211216405, 21.40977514834397866 ) ) ;
#4422=B_SPLINE_CURVE_WITH_KNOTS ( 'NONE', 3,
 ( #27353, #3526, #56767, #37092, #55852, #2920 ),
 .UNSPECIFIED., .F., .F.,
 ( 4, 2, 4 ),
 ( 9.055522398700297199E-18, 0.0002291978881530152385, 0.0004583957763060214239 ),
 .UNSPECIFIED. ) ;
#4427=ORIENTED_EDGE ( 'NONE', *, *, #61563, .T. ) ;
#4430=CARTESIAN_POINT ( 'NONE',  ( 0.5827357941260193908, 24.26189667805002870, 41.29633147056624409 ) ) ;
#4433=VERTEX_POINT ( 'NONE', #36858 ) ;
#4436=CARTESIAN_POINT ( 'NONE',  ( 3.407937589446174087, -11.14158115674378990, 7.970324840161918445 ) ) ;
#4444=CARTESIAN_POINT ( 'NONE',  ( 0.8557997880470599172, -43.90420959842167292, -19.17299735372055736 ) ) ;
#4448=ORIENTED_EDGE ( 'NONE', *, *, #50872, .F. ) ;
#4451=ADVANCED_FACE ( 'NONE', ( #12738 ), #7024, .T. ) ;
#4453=ORIENTED_EDGE ( 'NONE', *, *, #15942, .F. ) ;
#4459=ORIENTED_EDGE ( 'NONE', *, *, #16402, .F. ) ;
#4460=DIRECTION ( 'NONE',  ( -1.000000000000000000, -0.000000000000000000, -0.000000000000000000 ) ) ;
#4463=CARTESIAN_POINT ( 'NONE',  ( 1.227938101723756947, -41.23019537246717903, 11.92353943227934998 ) ) ;
#4464=CARTESIAN_POINT ( 'NONE',  ( 0.5807400328401574052, -38.33001520688930697, -28.72484455891681421 ) ) ;
#4467=B_SPLINE_CURVE_WITH_KNOTS ( 'NONE', 3,
 ( #17753, #42812, #4240, #22755 ),
 .UNSPECIFIED., .F., .F.,
 ( 4, 4 ),
 ( 8.673617379884035472E-19, 0.004048833967417087357 ),
 .UNSPECIFIED. ) ;
#4476=CARTESIAN_POINT ( 'NONE',  ( 0.8557997880470697982, -5.347802024197571669, 47.60865952216997243 ) ) ;
#4479=VERTEX_POINT ( 'NONE', #34004 ) ;
#4488=EDGE_CURVE ( 'NONE', #30530, #10287, #51603, .T. ) ;
#4489=CARTESIAN_POINT ( 'NONE',  ( 0.9754642270333688803, -42.56393738774954727, 5.426415525315669619 ) ) ;
#4490=CARTESIAN_POINT ( 'NONE',  ( 0.9972139404380270244, -22.02214929131115895, -36.82725283858632537 ) ) ;
#4492=DIRECTION ( 'NONE',  ( 1.000000000000000000, -0.000000000000000000, -0.000000000000000000 ) ) ;
#4494=EDGE_CURVE ( 'NONE', #7287, #36466, #2341, .T. ) ;
#4497=CARTESIAN_POINT ( 'NONE',  ( 0.5850706913938534814, 12.57184842332017460, 46.21698775168649576 ) ) ;
#4498=ORIENTED_EDGE ( 'NONE', *, *, #40509, .F. ) ;
#4501=CARTESIAN_POINT ( 'NONE',  ( 3.660087539127331535, 22.37124151181838627, -42.51124390328609337 ) ) ;
#4502=CARTESIAN_POINT ( 'NONE',  ( 4.303969348037246512, -14.52400616872400896, 45.86537346639053681 ) ) ;
#4510=ADVANCED_FACE ( 'NONE', ( #5450 ), #42110, .F. ) ;
#4512=CARTESIAN_POINT ( 'NONE',  ( 4.967162193818130511, 3.259922920617742914, 42.96271701169386859 ) ) ;
#4515=CARTESIAN_POINT ( 'NONE',  ( 1.154321485836933725, -42.90848031452335221, 0.8253076867717469289 ) ) ;
#4518=VERTEX_POINT ( 'NONE', #28975 ) ;
#4531=ADVANCED_FACE ( 'NONE', ( #48089 ), #59253, .F. ) ;
#4533=EDGE_CURVE ( 'NONE', #37398, #46412, #36099, .T. ) ;
#4536=( BOUNDED_SURFACE ( )  B_SPLINE_SURFACE ( 3, 1, ( 
 ( #15979, #1534 ),
 ( #48860, #30668 ),
 ( #35093, #6846 ),
 ( #11912, #21287 ) ),
 .UNSPECIFIED., .F., .F., .F. ) 
 B_SPLINE_SURFACE_WITH_KNOTS ( ( 4, 4 ),
 ( 2, 2 ),
 ( 0.000000000000000000, 1.000000000000000000 ),
 ( 0.000000000000000000, 1.000000000000000000 ),
 .UNSPECIFIED. ) 
 GEOMETRIC_REPRESENTATION_ITEM ( )  RATIONAL_B_SPLINE_SURFACE ( (
 ( 1.000000000000000000, 1.000000000000000000),
 ( 0.7269869731126817891, 0.9931720237060910339),
 ( 0.7269869731126817891, 0.9931720237060910339),
 ( 1.000000000000000000, 1.000000000000000000) ) ) 
 REPRESENTATION_ITEM ( '' )  SURFACE ( )  );
#4541=CARTESIAN_POINT ( 'NONE',  ( 0.7057020205115025480, -47.89404687311019870, -0.8412108057957802254 ) ) ;
#4542=CARTESIAN_POINT ( 'NONE',  ( 4.956653778116981712, -42.88673967249145846, 21.75875759808692322 ) ) ;
#4546=CARTESIAN_POINT ( 'NONE',  ( 0.9740398440564311811, 0.4145941695173028241, 42.90647580953695694 ) ) ;
#4554=ORIENTED_EDGE ( 'NONE', *, *, #33256, .F. ) ;
#4555=CARTESIAN_POINT ( 'NONE',  ( 0.5837374860065634996, -47.50965286059333437, -6.071555045025093911 ) ) ;
#4565=CARTESIAN_POINT ( 'NONE',  ( 4.956653778116975495, -27.17045123668499684, 39.67974989265029961 ) ) ;
#4567=ORIENTED_EDGE ( 'NONE', *, *, #13268, .F. ) ;
#4572=ORIENTED_EDGE ( 'NONE', *, *, #27146, .F. ) ;
#4587=CARTESIAN_POINT ( 'NONE',  ( 5.974727161628367256, -2.663664384318932932, 20.35137732084671214 ) ) ;
#4592=CARTESIAN_POINT ( 'NONE',  ( 0.9736507210033050752, 11.54000710819872033, -41.32746151989287853 ) ) ;
#4594=CARTESIAN_POINT ( 'NONE',  ( 2.281351352603297133, -32.98025003937392086, -34.83869092251595134 ) ) ;
#4600=VERTEX_POINT ( 'NONE', #54602 ) ;
#4605=CARTESIAN_POINT ( 'NONE',  ( 1.227938101723756947, 42.91134962331487657, -0.8460948827226678626 ) ) ;
#4611=CARTESIAN_POINT ( 'NONE',  ( 0.9756008150404605894, 21.57722292874457892, 37.08855330282507623 ) ) ;
#4612=CARTESIAN_POINT ( 'NONE',  ( 0.5839254288179563934, -38.05364096126336193, 29.08514953649804369 ) ) ;
#4615=ORIENTED_EDGE ( 'NONE', *, *, #48856, .T. ) ;
#4618=ORIENTED_EDGE ( 'NONE', *, *, #33526, .F. ) ;
#4622=CARTESIAN_POINT ( 'NONE',  ( 4.967162193818130511, 0.000000000000000000, 0.000000000000000000 ) ) ;
#4625=CARTESIAN_POINT ( 'NONE',  ( 0.9741495583595159991, 0.3955098476637576299, -42.90659993968958474 ) ) ;
#4639=ORIENTED_EDGE ( 'NONE', *, *, #48856, .F. ) ;
#4644=CARTESIAN_POINT ( 'NONE',  ( 0.9754642270333668819, -21.60621846558666803, 37.07163437210444101 ) ) ;
#4646=( BOUNDED_SURFACE ( )  B_SPLINE_SURFACE ( 3, 1, ( 
 ( #46311, #16879 ),
 ( #17181, #8368 ),
 ( #50978, #17795 ),
 ( #41310, #50069 ) ),
 .UNSPECIFIED., .F., .F., .F. ) 
 B_SPLINE_SURFACE_WITH_KNOTS ( ( 4, 4 ),
 ( 2, 2 ),
 ( 0.000000000000000000, 1.000000000000000000 ),
 ( 0.000000000000000000, 1.000000000000000000 ),
 .UNSPECIFIED. ) 
 GEOMETRIC_REPRESENTATION_ITEM ( )  RATIONAL_B_SPLINE_SURFACE ( (
 ( 1.000000000000000000, 1.000000000000000000),
 ( 0.7269869731126817891, 0.9931720237060910339),
 ( 0.7269869731126817891, 0.9931720237060910339),
 ( 1.000000000000000000, 1.000000000000000000) ) ) 
 REPRESENTATION_ITEM ( '' )  SURFACE ( )  );
#4651=CARTESIAN_POINT ( 'NONE',  ( 0.7056555295713299314, -46.47980662829223775, -11.58338207350448457 ) ) ;
#4660=VECTOR ( 'NONE', #33607, 1000.000000000000114 ) ;
#4663=CARTESIAN_POINT ( 'NONE',  ( 0.5807400328401574052, -41.75144119563869793, -23.47602859900758787 ) ) ;
#4667=CARTESIAN_POINT ( 'NONE',  ( 4.967162193818130511, -2.375726030842872927, 43.02067033766017801 ) ) ;
#4668=CARTESIAN_POINT ( 'NONE',  ( 4.967162193818131399, 18.65818244221258126, 38.83676580803773248 ) ) ;
#4669=AXIS2_PLACEMENT_3D ( 'NONE', #42241, #57511, #14038 ) ;
#4674=CARTESIAN_POINT ( 'NONE',  ( 0.8551540677456834771, 46.03951182599446668, -13.28067116677153692 ) ) ;
#4675=EDGE_CURVE ( 'NONE', #14380, #60198, #4422, .T. ) ;
#4676=CARTESIAN_POINT ( 'NONE',  ( 1.227938101723756947, 42.43379953535195170, -6.439911493064139236 ) ) ;
#4677=CARTESIAN_POINT ( 'NONE',  ( 4.967162193818130511, -7.970725651240091025, 42.34252806656591162 ) ) ;
#4679=CARTESIAN_POINT ( 'NONE',  ( 4.956653778116982600, -47.94889704119054130, 3.690426056929806631 ) ) ;
#4693=CARTESIAN_POINT ( 'NONE',  ( 0.9757892942422820015, -16.46777583825573998, -39.62259979733200765 ) ) ;
#4694=AXIS2_PLACEMENT_3D ( 'NONE', #28379, #10514, #39346 ) ;
#4698=CARTESIAN_POINT ( 'NONE',  ( 0.9730545539215883499, -34.34678117142574649, 25.71816799638765971 ) ) ;
#4702=EDGE_LOOP ( 'NONE', ( #43025, #54070, #21052, #59739 ) ) ;
#4703=CARTESIAN_POINT ( 'NONE',  ( 2.624215991343608501, 38.92973006074551279, -28.09277600149179932 ) ) ;
#4705=CARTESIAN_POINT ( 'NONE',  ( 0.7762777257811899201, -47.60264404062384358, 5.369627942761460382 ) ) ;
#4706=ORIENTED_EDGE ( 'NONE', *, *, #6470, .T. ) ;
#4711=EDGE_CURVE ( 'NONE', #18686, #2381, #41879, .T. ) ;
#4716=CARTESIAN_POINT ( 'NONE',  ( 5.965394784446458765, -10.25014670152127394, 17.78272165951783279 ) ) ;
#4719=CARTESIAN_POINT ( 'NONE',  ( 4.956653778116992370, 31.29546495791903027, -36.51451553856384180 ) ) ;
#4720=CARTESIAN_POINT ( 'NONE',  ( 5.958863334805807099, -16.28335246510375356, 12.49619391867154761 ) ) ;
#4722=DIRECTION ( 'NONE',  ( 0.07836865515943411409, -0.7104869166657137303, 0.6993330359244791516 ) ) ;
#4730=CARTESIAN_POINT ( 'NONE',  ( 5.958863334805807099, -7.855954700275490588, -18.96276366205790964 ) ) ;
#4732=CARTESIAN_POINT ( 'NONE',  ( 0.5850706913938533704, 47.89601588673689037, 0.1816364388702041144 ) ) ;
#4738=CARTESIAN_POINT ( 'NONE',  ( 0.5838002273316438284, 23.82993264414563228, 41.54704836736056706 ) ) ;
#4739=VECTOR ( 'NONE', #5256, 1000.000000000000114 ) ;
#4750=CARTESIAN_POINT ( 'NONE',  ( 0.5809828226811617480, -23.47450554821680413, -41.74875432577673706 ) ) ;
#4754=EDGE_CURVE ( 'NONE', #7287, #11517, #23890, .T. ) ;
#4757=EDGE_LOOP ( 'NONE', ( #54458, #18320, #2400, #20330 ) ) ;
#4760=AXIS2_PLACEMENT_3D ( 'NONE', #34973, #34350, #54035 ) ;
#4767=EDGE_LOOP ( 'NONE', ( #52767, #57020, #53304, #7902 ) ) ;
#4768=EDGE_CURVE ( 'NONE', #55943, #9477, #24497, .T. ) ;
#4771=CARTESIAN_POINT ( 'NONE',  ( 0.9730545539215883499, -39.44597740938072405, 16.88610103448544209 ) ) ;
#4777=B_SPLINE_CURVE_WITH_KNOTS ( 'NONE', 3,
 ( #45613, #36845, #60600, #12409 ),
 .UNSPECIFIED., .F., .F.,
 ( 4, 4 ),
 ( 4.336808689942017255E-19, 0.004048833967417086489 ),
 .UNSPECIFIED. ) ;
#4779=CARTESIAN_POINT ( 'NONE',  ( 3.270143674763207553, 13.60381564321236425, -1.514386915940453271 ) ) ;
#4782=ORIENTED_EDGE ( 'NONE', *, *, #14859, .F. ) ;
#4784=CARTESIAN_POINT ( 'NONE',  ( 4.956653778116991482, -9.917440902360828758, -47.05699031914960528 ) ) ;
#4790=ORIENTED_EDGE ( 'NONE', *, *, #9257, .F. ) ;
#4791=CARTESIAN_POINT ( 'NONE',  ( 5.960221823109900008, 18.96526051813969360, 7.849768660536623699 ) ) ;
#4793=ADVANCED_FACE ( 'NONE', ( #14809 ), #48471, .F. ) ;
#4794=CARTESIAN_POINT ( 'NONE',  ( 1.227938101723756947, -17.20315230597815059, -39.32113113558984452 ) ) ;
#4799=CARTESIAN_POINT ( 'NONE',  ( 0.9752132459055863345, -42.51031254975317353, 5.831562321021412920 ) ) ;
#4800=CARTESIAN_POINT ( 'NONE',  ( 5.960721111146673579, 10.26825948882926021, -17.77250458025982027 ) ) ;
#4819=CARTESIAN_POINT ( 'NONE',  ( 0.8551540677456739292, 0.9122407826482417104, -47.90804413217340141 ) ) ;
#4820=CARTESIAN_POINT ( 'NONE',  ( 0.9968887458511649369, -6.251925120321736529, 42.45154664631704833 ) ) ;
#4821=ORIENTED_EDGE ( 'NONE', *, *, #14084, .F. ) ;
#4823=CARTESIAN_POINT ( 'NONE',  ( 3.270143674763207553, -4.983712007628135154, -12.74832469035458082 ) ) ;
#4837=EDGE_CURVE ( 'NONE', #30729, #45266, #5221, .T. ) ;
#4839=FACE_OUTER_BOUND ( 'NONE', #54239, .T. ) ;
#4848=EDGE_CURVE ( 'NONE', #45517, #57237, #34971, .T. ) ;
#4873=CARTESIAN_POINT ( 'NONE',  ( 0.5836750258453351492, -0.1816059738419740499, 47.89563095930319747 ) ) ;
#4874=CARTESIAN_POINT ( 'NONE',  ( 4.967162193818130511, 0.000000000000000000, 0.000000000000000000 ) ) ;
#4877=CARTESIAN_POINT ( 'NONE',  ( 0.5832367798473387932, -18.07699868820156652, -44.35360901387667099 ) ) ;
#4879=CARTESIAN_POINT ( 'NONE',  ( 1.088313998177380837, 26.73848503423903722, -33.56520876252038477 ) ) ;
#4883=ORIENTED_EDGE ( 'NONE', *, *, #31403, .F. ) ;
#4886=ORIENTED_EDGE ( 'NONE', *, *, #5994, .F. ) ;
#4896=CARTESIAN_POINT ( 'NONE',  ( 0.5832367798473377940, -47.89515946578899985, -0.2724222379465481292 ) ) ;
#4902=CARTESIAN_POINT ( 'NONE',  ( 4.956653778116991482, -31.29546495791826644, -36.51451553856450971 ) ) ;
#4903=DIRECTION ( 'NONE',  ( -0.07439287786467652097, 0.9903339163990674265, 0.1170659376278869457 ) ) ;
#4905=ORIENTED_EDGE ( 'NONE', *, *, #40245, .T. ) ;
#4908=CARTESIAN_POINT ( 'NONE',  ( 5.960721111146673579, -20.52557019979492026, -0.006321279846748652925 ) ) ;
#4911=DIRECTION ( 'NONE',  ( 0.07836865515943411409, -0.3742079063794905847, -0.9240274869783798861 ) ) ;
#4913=CARTESIAN_POINT ( 'NONE',  ( 4.956653778116990594, -35.79382859084093127, -32.11725092155079864 ) ) ;
#4926=ORIENTED_EDGE ( 'NONE', *, *, #42946, .F. ) ;
#4927=ADVANCED_FACE ( 'NONE', ( #42027 ), #28168, .F. ) ;
#4934=EDGE_CURVE ( 'NONE', #44905, #35873, #23219, .T. ) ;
#4938=( BOUNDED_SURFACE ( )  B_SPLINE_SURFACE ( 3, 1, ( 
 ( #23529, #14159 ),
 ( #57328, #4703 ),
 ( #23848, #52337 ),
 ( #19465, #14462 ) ),
 .UNSPECIFIED., .F., .F., .F. ) 
 B_SPLINE_SURFACE_WITH_KNOTS ( ( 4, 4 ),
 ( 2, 2 ),
 ( 0.000000000000000000, 1.000000000000000000 ),
 ( 0.000000000000000000, 1.000000000000000000 ),
 .UNSPECIFIED. ) 
 GEOMETRIC_REPRESENTATION_ITEM ( )  RATIONAL_B_SPLINE_SURFACE ( (
 ( 1.000000000000000000, 1.000000000000000000),
 ( 0.7269869731126821222, 0.9931720237060910339),
 ( 0.7269869731126821222, 0.9931720237060910339),
 ( 1.000000000000000000, 1.000000000000000000) ) ) 
 REPRESENTATION_ITEM ( '' )  SURFACE ( )  );
#4942=FACE_OUTER_BOUND ( 'NONE', #1378, .T. ) ;
#4945=VERTEX_POINT ( 'NONE', #41714 ) ;
#4947=CARTESIAN_POINT ( 'NONE',  ( 0.6846871229502932144, 44.58493949244030574, -17.53234844287693761 ) ) ;
#4954=ORIENTED_EDGE ( 'NONE', *, *, #51336, .F. ) ;
#4956=SURFACE_STYLE_USAGE ( .BOTH. , #56659 ) ;
#4960=CARTESIAN_POINT ( 'NONE',  ( 0.9730545539215883499, -26.52009130076748278, -33.73144377768585400 ) ) ;
#4966=CARTESIAN_POINT ( 'NONE',  ( 0.9730545539215883499, -21.01499094264575618, 37.40983423658466478 ) ) ;
#4978=VERTEX_POINT ( 'NONE', #27899 ) ;
#4979=CARTESIAN_POINT ( 'NONE',  ( 1.227938101723748288, -39.32113113558953899, -17.20315230597885758 ) ) ;
#4981=CARTESIAN_POINT ( 'NONE',  ( 0.5850706913938534814, 29.30134895053053867, 37.88789093229816274 ) ) ;
#4990=ORIENTED_EDGE ( 'NONE', *, *, #17270, .T. ) ;
#4993=CARTESIAN_POINT ( 'NONE',  ( 0.8557997880470599172, -5.347802024196930404, -47.60865952217005059 ) ) ;
#4996=CARTESIAN_POINT ( 'NONE',  ( 0.9972139404380280236, -6.252633471303094659, -42.45145681504347834 ) ) ;
#4997=ORIENTED_EDGE ( 'NONE', *, *, #4186, .F. ) ;
#4998=CARTESIAN_POINT ( 'NONE',  ( 4.956653778116986153, -48.02038484091102077, 2.599733001514167086 ) ) ;
#5009=VECTOR ( 'NONE', #27425, 1000.000000000000114 ) ;
#5013=B_SPLINE_CURVE_WITH_KNOTS ( 'NONE', 3,
 ( #60989, #57197, #28722, #18097, #3658, #13404 ),
 .UNSPECIFIED., .F., .F.,
 ( 4, 2, 4 ),
 ( 7.040638946443416885E-18, 0.0002445244328975361555, 0.0004890488657950652638 ),
 .UNSPECIFIED. ) ;
#5014=CARTESIAN_POINT ( 'NONE',  ( 0.6846871229502899947, 19.12907057981204773, 43.92355552798044016 ) ) ;
#5020=ORIENTED_EDGE ( 'NONE', *, *, #50205, .F. ) ;
#5023=( BOUNDED_SURFACE ( )  B_SPLINE_SURFACE ( 3, 1, ( 
 ( #44777, #15334 ),
 ( #20947, #901 ),
 ( #16248, #58513 ),
 ( #6190, #53814 ) ),
 .UNSPECIFIED., .F., .F., .F. ) 
 B_SPLINE_SURFACE_WITH_KNOTS ( ( 4, 4 ),
 ( 2, 2 ),
 ( 0.000000000000000000, 1.000000000000000000 ),
 ( 0.000000000000000000, 1.000000000000000000 ),
 .UNSPECIFIED. ) 
 GEOMETRIC_REPRESENTATION_ITEM ( )  RATIONAL_B_SPLINE_SURFACE ( (
 ( 1.000000000000000000, 1.000000000000000000),
 ( 0.7269869731126821222, 0.9931720237060910339),
 ( 0.7269869731126821222, 0.9931720237060910339),
 ( 1.000000000000000000, 1.000000000000000000) ) ) 
 REPRESENTATION_ITEM ( '' )  SURFACE ( )  );
#5024=CLOSED_SHELL ( 'NONE', ( #54890, #37656, #19044, #6905, #59239, #60975, #59537, #39181, #4451, #17461, #49863, #60996, #22437, #54355, #7740, #60328, #60028, #15212, #19187, #69, #60294, #27393, #11311, #4360, #22571, #44176, #27324, #42489, #26440, #15604, #28674, #24531, #41241, #23283, #14422, #25542, #25460, #31331, #9949, #39417, #30842, #46764, #55420, #38500, #18972, #51607, #55899, #12000, #18055, #8170, #12556, #56600, #8700, #25819, #59590, #33598, #18849, #41000, #36603, #11904, #28356, #20853, #690, #28326, #391, #14112, #15261, #43799, #47576, #2872, #54371, #17333, #20533, #19453, #15352, #48615, #22640, #2831, #55286, #28983, #55234, #50485, #50302, #61224, #37240, #20528, #11989, #55931, #12226, #20723, #61579, #27740, #59517, #53509, #26925, #5619, #4034, #41323, #57245, #48179, #19601, #26568, #30055, #10485, #17125, #61488, #14431, #6344, #49982, #36023, #4233, #27584, #37449, #48698, #44890, #1118, #13966, #19880, #29834, #22886, #59599, #1196, #36258, #17108, #29284, #55428, #35764, #10913, #49089, #14738, #58841, #38109, #44384, #8053, #42380, #47004, #28543, #32194, #4927, #20654, #14910, #46813, #60483, #53518, #35176, #18402, #23758, #60797, #38621, #54202, #5230, #32281, #22398, #41668, #25307, #58801, #1601, #25360, #22936, #37295, #23936, #49315, #37245, #10700, #56501, #25170, #8200, #7623, #36244, #33666, #34888, #33978, #58405, #14256, #29916, #56724, #5761, #22357, #60645, #1277, #14883, #54933, #57615, #1524, #2492, #7830, #14865, #29058, #42417, #2191, #2949, #12571, #31406, #52108, #30409, #43512, #1606, #57711, #51884, #29353, #8081, #58319, #43599, #46110, #25876, #61662, #61145, #23923, #40589, #55223, #7453, #19970, #46977, #24, #5696, #14509, #28619, #43325, #5195, #34425, #25739, #27502, #49522, #4510, #55076, #22428, #22731, #48802, #22058, #4531, #24904, #21311, #61111, #24382, #45561, #61680, #19525, #6034, #34374, #39963, #56771, #7717, #27660, #11916, #19377, #28226, #11469, #12259, #23161, #23706, #54573, #29991, #30890, #42328, #29019, #29034, #30068, #57384, #48170, #29448, #24196, #54958, #19603, #54639, #53641, #22506, #49203, #57589, #29245, #36481, #54558, #16978, #28219, #47080, #4793, #13678, #10401, #8775, #12961, #20157, #28031, #2237, #50982, #46149, #58217, #51776, #19444, #240, #10784, #53137, #54997, #18630, #23910, #26371, #21940, #51770, #35240, #15101, #52581, #23862, #51108 ) ) ;
#5026=CARTESIAN_POINT ( 'NONE',  ( 4.967162193818130511, 28.07411493385295032, 32.68434214048178177 ) ) ;
#5030=CARTESIAN_POINT ( 'NONE',  ( 4.960156602257181468, -26.21519897043455316, 38.31207700265944993 ) ) ;
#5033=VERTEX_POINT ( 'NONE', #24740 ) ;
#5042=DIRECTION ( 'NONE',  ( 0.07836865515943411409, -0.3887811538706257286, 0.9179910502197319300 ) ) ;
#5043=CARTESIAN_POINT ( 'NONE',  ( -16.13943151895728434, -7.933737026945285820, 1.058406808655014908 ) ) ;
#5050=DIRECTION ( 'NONE',  ( -0.07439287786467650709, -0.9262902123089744588, -0.3693942911085744685 ) ) ;
#5058=CARTESIAN_POINT ( 'NONE',  ( 0.9756008150404595902, 5.741579752919638402, 42.52260101821268279 ) ) ;
#5060=B_SPLINE_CURVE_WITH_KNOTS ( 'NONE', 3,
 ( #30310, #29695, #48495, #40069, #34417, #15315, #883, #15619, #20020, #39130, #10923, #48811, #5864, #20617, #30007, #25012 ),
 .UNSPECIFIED., .F., .F.,
 ( 4, 3, 3, 3, 3, 4 ),
 ( 1.040890552917501732E-17, 0.0002724568934985577696, 0.0004086836638483818274, 0.0005449104342063615250, 0.0008173270854453666733, 0.001089761613562689659 ),
 .UNSPECIFIED. ) ;
#5064=CARTESIAN_POINT ( 'NONE',  ( 0.9757402383260944667, -11.02350435907874449, -41.46830379850865711 ) ) ;
#5067=CARTESIAN_POINT ( 'NONE',  ( 0.6846871229502932144, 28.47437962186126370, 38.52803883689310283 ) ) ;
#5069=EDGE_CURVE ( 'NONE', #61163, #21206, #29861, .T. ) ;
#5078=CARTESIAN_POINT ( 'NONE',  ( 0.9757402383260935785, -33.98983788393805128, -26.18833306844188513 ) ) ;
#5081=CARTESIAN_POINT ( 'NONE',  ( 5.959547316686252039, 18.96183906913543282, -7.858107265727552360 ) ) ;
#5085=CARTESIAN_POINT ( 'NONE',  ( 0.9722240750034570889, -41.29187379046131667, 11.66659272802842473 ) ) ;
#5086=CARTESIAN_POINT ( 'NONE',  ( 2.624215991343620935, -7.662883702704355926, -47.39206852872464992 ) ) ;
#5092=CARTESIAN_POINT ( 'NONE',  ( 4.967162193818130511, 0.000000000000000000, 0.000000000000000000 ) ) ;
#5103=CARTESIAN_POINT ( 'NONE',  ( 1.227938101723747621, -20.72293514920724533, -37.58536632582800507 ) ) ;
#5106=DIRECTION ( 'NONE',  ( 0.07439287786467664587, 0.2708295585865134192, -0.9597484305373181757 ) ) ;
#5111=CARTESIAN_POINT ( 'NONE',  ( 0.8557997880470599172, 0.9121262075952832893, -47.89938907511592703 ) ) ;
#5112=EDGE_CURVE ( 'NONE', #2075, #50613, #39993, .T. ) ;
#5120=CARTESIAN_POINT ( 'NONE',  ( 4.956653778116975495, -39.67974989265057673, 27.17045123668458828 ) ) ;
#5126=CARTESIAN_POINT ( 'NONE',  ( 0.5809828226811544205, 47.55412398569205834, 5.711058609465488267 ) ) ;
#5132=FACE_OUTER_BOUND ( 'NONE', #51188, .T. ) ;
#5138=CARTESIAN_POINT ( 'NONE',  ( 5.860006189529234355, 31.81514841426757911, 36.25227510158474331 ) ) ;
#5139=ORIENTED_EDGE ( 'NONE', *, *, #1037, .T. ) ;
#5142=CARTESIAN_POINT ( 'NONE',  ( 0.5839880159502347512, -41.45643525694588760, -23.98728323041091670 ) ) ;
#5143=ORIENTED_EDGE ( 'NONE', *, *, #43272, .T. ) ;
#5144=VERTEX_POINT ( 'NONE', #11903 ) ;
#5157=B_SPLINE_CURVE_WITH_KNOTS ( 'NONE', 3,
 ( #51746, #3822, #60524, #3509 ),
 .UNSPECIFIED., .F., .F.,
 ( 4, 4 ),
 ( 1.734723475976807094E-18, 0.004050076154993005086 ),
 .UNSPECIFIED. ) ;
#5166=EDGE_CURVE ( 'NONE', #34686, #38949, #56817, .T. ) ;
#5172=CARTESIAN_POINT ( 'NONE',  ( 0.5819845079324652559, 29.51613512130382588, 37.72030202710084978 ) ) ;
#5173=EDGE_LOOP ( 'NONE', ( #7417, #2870, #13833, #22426 ) ) ;
#5191=CARTESIAN_POINT ( 'NONE',  ( 0.9736507210033069626, 39.81239086052237042, -16.00326134587874094 ) ) ;
#5195=ADVANCED_FACE ( 'NONE', ( #15972 ), #53752, .F. ) ;
#5199=FACE_OUTER_BOUND ( 'NONE', #4757, .T. ) ;
#5209=CARTESIAN_POINT ( 'NONE',  ( 0.5809828226811617480, -37.66417181417530458, -29.58751527316218954 ) ) ;
#5210=EDGE_CURVE ( 'NONE', #34340, #16449, #53815, .T. ) ;
#5216=CARTESIAN_POINT ( 'NONE',  ( 1.227938101723748288, -33.52879263017845091, -26.79402671879361364 ) ) ;
#5219=CARTESIAN_POINT ( 'NONE',  ( 0.5807400328401574052, 47.55718917606843377, 5.711437504336132953 ) ) ;
#5221=B_SPLINE_CURVE_WITH_KNOTS ( 'NONE', 3,
 ( #49852, #2215, #40480, #21041, #26050, #35151 ),
 .UNSPECIFIED., .F., .F.,
 ( 4, 2, 4 ),
 ( 8.848046324741092137E-18, 0.0002291978881530156722, 0.0004583957763060225081 ),
 .UNSPECIFIED. ) ;
#5223=CARTESIAN_POINT ( 'NONE',  ( 4.967162193818130511, 32.10009971360111791, -28.74031574029977776 ) ) ;
#5226=CARTESIAN_POINT ( 'NONE',  ( 3.783278058412226308, -7.325100730114020742, -42.41041238787302348 ) ) ;
#5228=VERTEX_POINT ( 'NONE', #55690 ) ;
#5229=CARTESIAN_POINT ( 'NONE',  ( 4.967162193818130511, 0.000000000000000000, 0.000000000000000000 ) ) ;
#5230=ADVANCED_FACE ( 'NONE', ( #36943 ), #21769, .F. ) ;
#5231=CARTESIAN_POINT ( 'NONE',  ( 0.5839880159502353063, 47.49213420504723615, -6.206687493267210698 ) ) ;
#5247=CONICAL_SURFACE ( 'NONE', #54244, 43.08621763946400307, 1.568696531533066763 ) ;
#5253=CARTESIAN_POINT ( 'NONE',  ( 0.9756008150404594792, 34.12792951168108857, 26.00810955565524907 ) ) ;
#5256=DIRECTION ( 'NONE',  ( 0.07439287786467665975, -0.6957517427943072930, -0.7144194931003039484 ) ) ;
#5257=CARTESIAN_POINT ( 'NONE',  ( 5.959828726073459926, 16.28130559351247442, 12.49879082830573829 ) ) ;
#5264=CARTESIAN_POINT ( 'NONE',  ( 0.5809828226811617480, 38.32755012159184815, -28.72298383114449294 ) ) ;
#5267=ORIENTED_EDGE ( 'NONE', *, *, #24619, .T. ) ;
#5276=ORIENTED_EDGE ( 'NONE', *, *, #15235, .T. ) ;
#5280=( BOUNDED_SURFACE ( )  B_SPLINE_SURFACE ( 3, 1, ( 
 ( #57120, #34275 ),
 ( #6029, #53351 ),
 ( #9842, #14560 ),
 ( #48980, #33360 ) ),
 .UNSPECIFIED., .F., .F., .F. ) 
 B_SPLINE_SURFACE_WITH_KNOTS ( ( 4, 4 ),
 ( 2, 2 ),
 ( 0.000000000000000000, 1.000000000000000000 ),
 ( 0.000000000000000000, 1.000000000000000000 ),
 .UNSPECIFIED. ) 
 GEOMETRIC_REPRESENTATION_ITEM ( )  RATIONAL_B_SPLINE_SURFACE ( (
 ( 1.000000000000000000, 1.000000000000000000),
 ( 0.7269869731126821222, 0.9931720237060910339),
 ( 0.7269869731126821222, 0.9931720237060910339),
 ( 1.000000000000000000, 1.000000000000000000) ) ) 
 REPRESENTATION_ITEM ( '' )  SURFACE ( )  );
#5292=CARTESIAN_POINT ( 'NONE',  ( 0.5809828226811617480, 18.83114015454759738, -44.03860873105676177 ) ) ;
#5296=( BOUNDED_SURFACE ( )  B_SPLINE_SURFACE ( 3, 1, ( 
 ( #38558, #24746 ),
 ( #33543, #57925 ),
 ( #10035, #30054 ),
 ( #29133, #43886 ) ),
 .UNSPECIFIED., .F., .F., .F. ) 
 B_SPLINE_SURFACE_WITH_KNOTS ( ( 4, 4 ),
 ( 2, 2 ),
 ( 0.000000000000000000, 1.000000000000000000 ),
 ( 0.000000000000000000, 1.000000000000000000 ),
 .UNSPECIFIED. ) 
 GEOMETRIC_REPRESENTATION_ITEM ( )  RATIONAL_B_SPLINE_SURFACE ( (
 ( 1.000000000000000000, 1.000000000000000000),
 ( 0.9953390228620291325, 0.8624445117760984880),
 ( 0.9953390228620291325, 0.8624445117760984880),
 ( 1.000000000000000000, 1.000000000000000000) ) ) 
 REPRESENTATION_ITEM ( '' )  SURFACE ( )  );
#5297=CARTESIAN_POINT ( 'NONE',  ( 0.9757402383260929124, -37.20221273948027374, 21.38067434779568998 ) ) ;
#5307=ORIENTED_EDGE ( 'NONE', *, *, #30077, .T. ) ;
#5309=CARTESIAN_POINT ( 'NONE',  ( 5.958863334805807099, -17.77512673691311917, -10.26388325355081221 ) ) ;
#5310=ORIENTED_EDGE ( 'NONE', *, *, #42602, .T. ) ;
#5312=EDGE_CURVE ( 'NONE', #5855, #1320, #59162, .T. ) ;
#5314=B_SPLINE_CURVE_WITH_KNOTS ( 'NONE', 3,
 ( #35242, #34312, #49314, #25821 ),
 .UNSPECIFIED., .F., .F.,
 ( 4, 4 ),
 ( 5.421010862427522170E-19, 0.004444878191957670442 ),
 .UNSPECIFIED. ) ;
#5316=CARTESIAN_POINT ( 'NONE',  ( 4.303969348037246512, -39.44373910178629927, 27.54579249306195976 ) ) ;
#5322=B_SPLINE_CURVE_WITH_KNOTS ( 'NONE', 3,
 ( #1249, #48273, #24456, #43594 ),
 .UNSPECIFIED., .F., .F.,
 ( 4, 4 ),
 ( 0.000000000000000000, 0.004444878191957677381 ),
 .UNSPECIFIED. ) ;
#5326=CARTESIAN_POINT ( 'NONE',  ( 0.5838002273316424962, -33.77111476497751852, -33.96372661229970902 ) ) ;
#5331=EDGE_LOOP ( 'NONE', ( #58794, #29130, #686, #46241 ) ) ;
#5333=VERTEX_POINT ( 'NONE', #48702 ) ;
#5334=CARTESIAN_POINT ( 'NONE',  ( 4.956653778116982600, -45.35992544608539845, 15.97476558431867844 ) ) ;
#5341=CARTESIAN_POINT ( 'NONE',  ( 0.5836750258453344831, -44.18029554260620984, -18.49664649301237773 ) ) ;
#5343=EDGE_CURVE ( 'NONE', #42745, #57673, #57590, .T. ) ;
#5351=EDGE_CURVE ( 'NONE', #45517, #47841, #10590, .T. ) ;
#5352=EDGE_CURVE ( 'NONE', #44883, #52969, #40458, .T. ) ;
#5353=CARTESIAN_POINT ( 'NONE',  ( 0.9730545539215892381, 39.83279466599039154, 15.95224156741843835 ) ) ;
#5367=CARTESIAN_POINT ( 'NONE',  ( 0.8551540677456715978, 47.37911285756630519, -7.157691013573887595 ) ) ;
#5368=CARTESIAN_POINT ( 'NONE',  ( 0.6846871229502899947, 37.47592888575288583, -29.84551600520595116 ) ) ;
#5370=( BOUNDED_SURFACE ( )  B_SPLINE_SURFACE ( 3, 1, ( 
 ( #6098, #59349 ),
 ( #21157, #34343 ),
 ( #53418, #39671 ),
 ( #34644, #6710 ) ),
 .UNSPECIFIED., .F., .F., .F. ) 
 B_SPLINE_SURFACE_WITH_KNOTS ( ( 4, 4 ),
 ( 2, 2 ),
 ( 0.000000000000000000, 1.000000000000000000 ),
 ( 0.000000000000000000, 1.000000000000000000 ),
 .UNSPECIFIED. ) 
 GEOMETRIC_REPRESENTATION_ITEM ( )  RATIONAL_B_SPLINE_SURFACE ( (
 ( 1.000000000000000000, 1.000000000000000000),
 ( 0.7269869731126821222, 0.9931720237060910339),
 ( 0.7269869731126821222, 0.9931720237060910339),
 ( 1.000000000000000000, 1.000000000000000000) ) ) 
 REPRESENTATION_ITEM ( '' )  SURFACE ( )  );
#5371=ORIENTED_EDGE ( 'NONE', *, *, #10985, .T. ) ;
#5373=LINE ( 'NONE', #54218, #20571 ) ;
#5375=( BOUNDED_SURFACE ( )  B_SPLINE_SURFACE ( 3, 1, ( 
 ( #26070, #54543 ),
 ( #27301, #31081 ),
 ( #2241, #11674 ),
 ( #46429, #12299 ) ),
 .UNSPECIFIED., .F., .F., .F. ) 
 B_SPLINE_SURFACE_WITH_KNOTS ( ( 4, 4 ),
 ( 2, 2 ),
 ( 0.000000000000000000, 1.000000000000000000 ),
 ( 0.000000000000000000, 1.000000000000000000 ),
 .UNSPECIFIED. ) 
 GEOMETRIC_REPRESENTATION_ITEM ( )  RATIONAL_B_SPLINE_SURFACE ( (
 ( 1.000000000000000000, 1.000000000000000000),
 ( 0.9953390228620291325, 0.8624445117761032620),
 ( 0.9953390228620291325, 0.8624445117761032620),
 ( 1.000000000000000000, 1.000000000000000000) ) ) 
 REPRESENTATION_ITEM ( '' )  SURFACE ( )  );
#5376=CARTESIAN_POINT ( 'NONE',  ( 1.227938101723756947, 25.45152231597106507, -34.55893248994479450 ) ) ;
#5390=CARTESIAN_POINT ( 'NONE',  ( 0.9756008150404610335, -34.12792951168087541, -26.00810955565548355 ) ) ;
#5391=ORIENTED_EDGE ( 'NONE', *, *, #53261, .T. ) ;
#5392=ORIENTED_EDGE ( 'NONE', *, *, #30491, .T. ) ;
#5397=CARTESIAN_POINT ( 'NONE',  ( 1.227938101723748288, -30.94118573761333479, 29.74462687941215222 ) ) ;
#5411=ORIENTED_EDGE ( 'NONE', *, *, #22486, .T. ) ;
#5412=CARTESIAN_POINT ( 'NONE',  ( 5.860006189529246790, -40.09484204000580831, -26.81109398084748818 ) ) ;
#5430=AXIS2_PLACEMENT_3D ( 'NONE', #23512, #52940, #52316 ) ;
#5434=CARTESIAN_POINT ( 'NONE',  ( 3.407937589446174087, 13.34359005742693682, -3.099921468254863921 ) ) ;
#5435=CARTESIAN_POINT ( 'NONE',  ( 0.5807400328401574052, -29.58941477092990979, -37.66660715020896077 ) ) ;
#5436=CARTESIAN_POINT ( 'NONE',  ( 0.9736507210033062965, -11.54000710819843256, 41.32746151989296379 ) ) ;
#5443=CARTESIAN_POINT ( 'NONE',  ( 0.5809828226811617480, -0.5448590168535863976, 47.89273459658653564 ) ) ;
#5450=FACE_OUTER_BOUND ( 'NONE', #585, .T. ) ;
#5454=CARTESIAN_POINT ( 'NONE',  ( 4.967162193818129623, 40.65506779172164897, 14.26841313271295952 ) ) ;
#5456=CARTESIAN_POINT ( 'NONE',  ( 0.9730545539215883499, -34.34678117142538412, -25.71816799638815354 ) ) ;
#5457=CARTESIAN_POINT ( 'NONE',  ( 1.154321713695927398, -10.30834583266701898, -41.66001467525153856 ) ) ;
#5463=CARTESIAN_POINT ( 'NONE',  ( 0.9730545539215883499, 42.60426903087353878, 5.099196237955034405 ) ) ;
#5464=VERTEX_POINT ( 'NONE', #27672 ) ;
#5465=ORIENTED_EDGE ( 'NONE', *, *, #8672, .F. ) ;
#5484=CARTESIAN_POINT ( 'NONE',  ( 0.5839254288179547281, 24.02657516616565303, -41.43367229384560346 ) ) ;
#5485=VERTEX_POINT ( 'NONE', #4444 ) ;
#5488=CARTESIAN_POINT ( 'NONE',  ( 0.9752132459055854463, 25.93579301218408162, -34.18286753639614517 ) ) ;
#5494=PLANE ( 'NONE',  #4760 ) ;
#5496=CARTESIAN_POINT ( 'NONE',  ( 0.9757787079277434605, 39.65734351318527473, -16.38386580718250229 ) ) ;
#5499=CARTESIAN_POINT ( 'NONE',  ( 0.8557997880470606944, -24.73961900479280374, 41.02602466100771039 ) ) ;
#5502=CARTESIAN_POINT ( 'NONE',  ( -16.13875996306990146, -12.45778025494542618, 1.057258788294430429 ) ) ;
#5505=CARTESIAN_POINT ( 'NONE',  ( 1.227938101723756947, -22.18841447410693846, -36.73927144310534487 ) ) ;
#5512=CARTESIAN_POINT ( 'NONE',  ( 5.958863334805807099, 19.82657410201442971, -5.311251202228647550 ) ) ;
#5517=CARTESIAN_POINT ( 'NONE',  ( 0.5819845079324658110, -11.95724301473539519, 46.37938935563227005 ) ) ;
#5529=CARTESIAN_POINT ( 'NONE',  ( 1.227938101723756947, -6.439911493064287562, -42.43379953535192328 ) ) ;
#5531=FACE_OUTER_BOUND ( 'NONE', #36176, .T. ) ;
#5543=EDGE_CURVE ( 'NONE', #40624, #9646, #47989, .T. ) ;
#5548=( BOUNDED_SURFACE ( )  B_SPLINE_SURFACE ( 3, 1, ( 
 ( #54379, #11501 ),
 ( #1766, #1453 ),
 ( #20588, #44427 ),
 ( #39720, #30586 ) ),
 .UNSPECIFIED., .F., .F., .F. ) 
 B_SPLINE_SURFACE_WITH_KNOTS ( ( 4, 4 ),
 ( 2, 2 ),
 ( 0.000000000000000000, 1.000000000000000000 ),
 ( 0.000000000000000000, 1.000000000000000000 ),
 .UNSPECIFIED. ) 
 GEOMETRIC_REPRESENTATION_ITEM ( )  RATIONAL_B_SPLINE_SURFACE ( (
 ( 1.000000000000000000, 1.000000000000000000),
 ( 0.7269869731126817891, 0.9931720237060910339),
 ( 0.7269869731126817891, 0.9931720237060910339),
 ( 1.000000000000000000, 1.000000000000000000) ) ) 
 REPRESENTATION_ITEM ( '' )  SURFACE ( )  );
#5555=DIRECTION ( 'NONE',  ( -0.07439287786467650709, -0.7991213610169786152, -0.5965490341031348676 ) ) ;
#5556=CARTESIAN_POINT ( 'NONE',  ( 5.974727161628367256, 17.78288073588488416, 10.24903993265015423 ) ) ;
#5574=ORIENTED_EDGE ( 'NONE', *, *, #17839, .T. ) ;
#5576=CARTESIAN_POINT ( 'NONE',  ( 0.7762777257811882548, -38.54028505510738967, 28.45155622761415160 ) ) ;
#5586=CARTESIAN_POINT ( 'NONE',  ( 5.959547316686252039, 20.35048796920733238, 2.675599016784604434 ) ) ;
#5587=ORIENTED_EDGE ( 'NONE', *, *, #35112, .F. ) ;
#5592=AXIS2_PLACEMENT_3D ( 'NONE', #386, #19233, #28302 ) ;
#5593=ORIENTED_EDGE ( 'NONE', *, *, #17929, .F. ) ;
#5602=CARTESIAN_POINT ( 'NONE',  ( 1.227938101723756947, -26.79402671879305231, -33.52879263017890565 ) ) ;
#5610=CARTESIAN_POINT ( 'NONE',  ( 4.956653778116975495, -20.77844580450591394, 43.37017594958047084 ) ) ;
#5612=EDGE_CURVE ( 'NONE', #10214, #23349, #33312, .T. ) ;
#5619=ADVANCED_FACE ( 'NONE', ( #29818 ), #148, .F. ) ;
#5620=CARTESIAN_POINT ( 'NONE',  ( 0.5839879882012684043, 33.86754218494344570, -33.86758487442367027 ) ) ;
#5627=ORIENTED_EDGE ( 'NONE', *, *, #10195, .F. ) ;
#5631=EDGE_CURVE ( 'NONE', #36040, #33551, #50961, .T. ) ;
#5633=ORIENTED_EDGE ( 'NONE', *, *, #13123, .T. ) ;
#5634=DIRECTION ( 'NONE',  ( -0.07836865515943411409, -0.5052769534812628915, -0.8593913859058602833 ) ) ;
#5646=CARTESIAN_POINT ( 'NONE',  ( 0.5809828226811617480, 46.40184912890855884, -11.86925843957117799 ) ) ;
#5648=FACE_OUTER_BOUND ( 'NONE', #23532, .T. ) ;
#5649=CARTESIAN_POINT ( 'NONE',  ( 5.981074661064941900, -0.008585178657475886835, -20.52466374824937034 ) ) ;
#5650=CARTESIAN_POINT ( 'NONE',  ( 3.660087539127337752, 45.87884541725766496, -14.24113226412002930 ) ) ;
#5654=EDGE_CURVE ( 'NONE', #21051, #44755, #60963, .T. ) ;
#5666=ORIENTED_EDGE ( 'NONE', *, *, #23767, .T. ) ;
#5667=CARTESIAN_POINT ( 'NONE',  ( 0.9757402383260935785, 5.516496958497070224, 42.55239275983112179 ) ) ;
#5669=EDGE_LOOP ( 'NONE', ( #31084, #25212, #60089, #35318 ) ) ;
#5686=CARTESIAN_POINT ( 'NONE',  ( 3.407937589446174087, -12.82481284928207010, 4.815089211105012978 ) ) ;
#5687=VERTEX_POINT ( 'NONE', #58938 ) ;
#5693=CARTESIAN_POINT ( 'NONE',  ( 4.967162193818130511, 0.000000000000000000, 0.000000000000000000 ) ) ;
#5695=FACE_OUTER_BOUND ( 'NONE', #40980, .T. ) ;
#5696=ADVANCED_FACE ( 'NONE', ( #39559 ), #8579, .F. ) ;
#5704=CARTESIAN_POINT ( 'NONE',  ( 0.5809828226811617480, -46.11980934799329646, -12.92184523170252497 ) ) ;
#5708=ORIENTED_EDGE ( 'NONE', *, *, #59120, .F. ) ;
#5716=CARTESIAN_POINT ( 'NONE',  ( 0.7057020205115017708, 0.8412108057959468699, -47.89404687311022002 ) ) ;
#5718=LINE ( 'NONE', #57731, #19116 ) ;
#5726=CARTESIAN_POINT ( 'NONE',  ( 1.227938101723757836, -15.63977281655870222, 39.96870412324331312 ) ) ;
#5738=CARTESIAN_POINT ( 'NONE',  ( 1.154321713695928509, 10.30834583266730320, 41.66001467525142488 ) ) ;
#5740=B_SPLINE_CURVE_WITH_KNOTS ( 'NONE', 3,
 ( #23702, #42832, #20546, #39061, #29317, #44079 ),
 .UNSPECIFIED., .F., .F.,
 ( 4, 2, 4 ),
 ( 7.040638946443416885E-18, 0.0002445244328975376734, 0.0004890488657950682995 ),
 .UNSPECIFIED. ) ;
#5745=B_SPLINE_CURVE_WITH_KNOTS ( 'NONE', 3,
 ( #21031, #35452, #35767, #11967 ),
 .UNSPECIFIED., .F., .F.,
 ( 4, 4 ),
 ( 0.000000000000000000, 0.004446090762761352976 ),
 .UNSPECIFIED. ) ;
#5748=DIRECTION ( 'NONE',  ( 0.000000000000000000, 0.000000000000000000, 1.000000000000000000 ) ) ;
#5754=CARTESIAN_POINT ( 'NONE',  ( 4.960156602257177916, -45.62767441207045493, -8.553784487773349099 ) ) ;
#5756=CARTESIAN_POINT ( 'NONE',  ( 1.227938101723748288, -39.32113113558953899, -17.20315230597885758 ) ) ;
#5759=CARTESIAN_POINT ( 'NONE',  ( 0.9730545539215883499, -10.61654491617534291, -41.57420493492396929 ) ) ;
#5761=ADVANCED_FACE ( 'NONE', ( #25426 ), #47378, .F. ) ;
#5763=CARTESIAN_POINT ( 'NONE',  ( 0.9757787079277435716, 42.53619983261577886, 5.639827755376784602 ) ) ;
#5768=CARTESIAN_POINT ( 'NONE',  ( 0.9730545539215883499, -0.5054011016615761465, 42.90536227157002003 ) ) ;
#5775=CARTESIAN_POINT ( 'NONE',  ( 0.5809828226811617480, -11.86925843957133786, -46.40184912890851621 ) ) ;
#5776=VERTEX_POINT ( 'NONE', #61092 ) ;
#5778=CARTESIAN_POINT ( 'NONE',  ( 1.227938101723756947, 10.28900963485438425, -41.66816631169181306 ) ) ;
#5780=CARTESIAN_POINT ( 'NONE',  ( 0.5838002273316424962, 29.04904228829611412, 38.08117724016815231 ) ) ;
#5782=CARTESIAN_POINT ( 'NONE',  ( 0.5807400328401574052, -47.89582301953904420, 0.5448834511088260779 ) ) ;
#5784=CARTESIAN_POINT ( 'NONE',  ( 0.8557997880470690211, 47.89938907511594124, -0.9121262075947851322 ) ) ;
#5785=CARTESIAN_POINT ( 'NONE',  ( 0.5819845901640494645, 24.34012668949545244, -41.25023214430176210 ) ) ;
#5804=CARTESIAN_POINT ( 'NONE',  ( 1.227938101723748288, 42.43379953535185933, 6.439911493064710335 ) ) ;
#5815=CARTESIAN_POINT ( 'NONE',  ( 4.960156602257180580, -30.22163187094364645, -35.23783291257201711 ) ) ;
#5819=CARTESIAN_POINT ( 'NONE',  ( 0.5839879327111936469, -12.30864801674743525, 46.28746210677709882 ) ) ;
#5824=CARTESIAN_POINT ( 'NONE',  ( 0.9730545539215883499, 42.60426903087360984, -5.099196237954451760 ) ) ;
#5829=AXIS2_PLACEMENT_3D ( 'NONE', #25402, #26031, #1578 ) ;
#5840=CARTESIAN_POINT ( 'NONE',  ( 1.088313998177382169, -33.56520876252045582, -26.73848503423889156 ) ) ;
#5843=CIRCLE ( 'NONE', #43791, 48.09070567114147110 ) ;
#5844=CARTESIAN_POINT ( 'NONE',  ( 0.8557997880470690211, 0.9121262075946178216, 47.89938907511594124 ) ) ;
#5848=CARTESIAN_POINT ( 'NONE',  ( 0.8557997880470697982, -47.37054680076710866, 7.156447707085535903 ) ) ;
#5855=VERTEX_POINT ( 'NONE', #41114 ) ;
#5860=VECTOR ( 'NONE', #19628, 999.9999999999998863 ) ;
#5861=CARTESIAN_POINT ( 'NONE',  ( 0.6067375320500766334, 41.12099578548248502, 24.55990317723871641 ) ) ;
#5863=CARTESIAN_POINT ( 'NONE',  ( 0.5839880159502333079, 6.206687493267690314, 47.49213420504721483 ) ) ;
#5864=CARTESIAN_POINT ( 'NONE',  ( 0.5832366564991514624, -5.981458972434077204, 47.52097076201149406 ) ) ;
#5872=DIRECTION ( 'NONE',  ( -1.000000000000000000, -0.000000000000000000, -0.000000000000000000 ) ) ;
#5877=VECTOR ( 'NONE', #30955, 1000.000000000000114 ) ;
#5882=CARTESIAN_POINT ( 'NONE',  ( 5.960721111146673579, -18.96557324978281756, -7.848955554238449928 ) ) ;
#5884=FACE_OUTER_BOUND ( 'NONE', #42609, .T. ) ;
#5902=ORIENTED_EDGE ( 'NONE', *, *, #38511, .F. ) ;
#5903=B_SPLINE_CURVE_WITH_KNOTS ( 'NONE', 3,
 ( #5848, #58473, #24998, #57546 ),
 .UNSPECIFIED., .F., .F.,
 ( 4, 4 ),
 ( 4.336808689942017736E-19, 0.004444878191957681718 ),
 .UNSPECIFIED. ) ;
#5905=CARTESIAN_POINT ( 'NONE',  ( 0.9749527285493306827, 16.68386601451091877, -39.53206838353028729 ) ) ;
#5906=( BOUNDED_SURFACE ( )  B_SPLINE_SURFACE ( 3, 1, ( 
 ( #56028, #46658 ),
 ( #13146, #27533 ),
 ( #8728, #27843 ),
 ( #46975, #42576 ) ),
 .UNSPECIFIED., .F., .F., .F. ) 
 B_SPLINE_SURFACE_WITH_KNOTS ( ( 4, 4 ),
 ( 2, 2 ),
 ( 0.000000000000000000, 1.000000000000000000 ),
 ( 0.000000000000000000, 1.000000000000000000 ),
 .UNSPECIFIED. ) 
 GEOMETRIC_REPRESENTATION_ITEM ( )  RATIONAL_B_SPLINE_SURFACE ( (
 ( 1.000000000000000000, 1.000000000000000000),
 ( 0.9732289882329797637, 0.9999525324661233672),
 ( 0.9732289882329797637, 0.9999525324661233672),
 ( 1.000000000000000000, 1.000000000000000000) ) ) 
 REPRESENTATION_ITEM ( '' )  SURFACE ( )  );
#5911=EDGE_CURVE ( 'NONE', #8227, #45383, #61393, .T. ) ;
#5926=CARTESIAN_POINT ( 'NONE',  ( 5.958863334805807099, 5.311251202228851831, -19.82657410201437642 ) ) ;
#5928=ORIENTED_EDGE ( 'NONE', *, *, #609, .F. ) ;
#5935=EDGE_CURVE ( 'NONE', #12599, #35558, #31440, .T. ) ;
#5939=VERTEX_POINT ( 'NONE', #4679 ) ;
#5943=DIRECTION ( 'NONE',  ( 0.07836865515943410021, -0.6993330359244864791, -0.7104869166657064028 ) ) ;
#5950=CARTESIAN_POINT ( 'NONE',  ( 0.6067375320500720814, -5.548194933739853063, -47.57460111700608962 ) ) ;
#5954=CARTESIAN_POINT ( 'NONE',  ( 1.227938101723748288, -42.65467462194921922, 4.762198645644287076 ) ) ;
#5957=CARTESIAN_POINT ( 'NONE',  ( -16.91888867401740981, -7.790380955814590891, -1.820995958802028580 ) ) ;
#5963=CARTESIAN_POINT ( 'NONE',  ( 5.960221823109900008, 12.49951306783067828, 16.28072933292552094 ) ) ;
#5964=EDGE_CURVE ( 'NONE', #21601, #29768, #59839, .T. ) ;
#5979=CARTESIAN_POINT ( 'NONE',  ( 5.960221823109900008, 5.307149561568086149, -19.82761049839337275 ) ) ;
#5980=EDGE_CURVE ( 'NONE', #37398, #11505, #45657, .T. ) ;
#5982=DIRECTION ( 'NONE',  ( -1.000000000000000000, -0.000000000000000000, -0.000000000000000000 ) ) ;
#5984=ORIENTED_EDGE ( 'NONE', *, *, #38359, .T. ) ;
#5990=CARTESIAN_POINT ( 'NONE',  ( 0.8557997880470599172, 34.51495345639595058, -33.22501220301865033 ) ) ;
#5994=EDGE_CURVE ( 'NONE', #35714, #10097, #10474, .T. ) ;
#5995=CIRCLE ( 'NONE', #41087, 48.09070567114147110 ) ;
#6003=CARTESIAN_POINT ( 'NONE',  ( 4.303969348037246512, 36.81598326424549583, 30.97035057417673443 ) ) ;
#6005=B_SPLINE_CURVE_WITH_KNOTS ( 'NONE', 3,
 ( #1069, #53376, #38705, #20205 ),
 .UNSPECIFIED., .F., .F.,
 ( 4, 4 ),
 ( 0.000000000000000000, 0.004048833967417084755 ),
 .UNSPECIFIED. ) ;
#6009=EDGE_CURVE ( 'NONE', #694, #41370, #48628, .T. ) ;
#6015=CARTESIAN_POINT ( 'NONE',  ( 4.956653778116966613, 0.000000000000000000, 0.000000000000000000 ) ) ;
#6023=CARTESIAN_POINT ( 'NONE',  ( 4.967162193818130511, 13.42934394584221280, -40.93989340068594629 ) ) ;
#6026=CARTESIAN_POINT ( 'NONE',  ( 4.303969348037258058, 47.36875205922783749, -8.413118729223581838 ) ) ;
#6029=CARTESIAN_POINT ( 'NONE',  ( 5.965394784446458765, 20.35165389555754700, 2.664747781316183506 ) ) ;
#6031=CARTESIAN_POINT ( 'NONE',  ( 5.981074661064941900, -2.687517936920148731, 20.34795181394743935 ) ) ;
#6034=ADVANCED_FACE ( 'NONE', ( #49473 ), #4536, .F. ) ;
#6037=CARTESIAN_POINT ( 'NONE',  ( 0.5827359174754831450, -41.65957726278053030, 23.63273677570900233 ) ) ;
#6039=DIRECTION ( 'NONE',  ( 0.07439287786467665975, -0.9665813013808213228, 0.2453289374370035691 ) ) ;
#6046=CARTESIAN_POINT ( 'NONE',  ( 5.960221823109900008, 10.25807604135597195, 17.77840967225723645 ) ) ;
#6057=CARTESIAN_POINT ( 'NONE',  ( 0.5839879882104920261, 5.827794150371782279E-15, 47.89596766822081264 ) ) ;
#6058=CARTESIAN_POINT ( 'NONE',  ( 3.660176727303411148, 25.63023984566702751, -40.62966184289462745 ) ) ;
#6059=CARTESIAN_POINT ( 'NONE',  ( 0.5832366564991500191, -41.61464700196760447, -23.71163571971566597 ) ) ;
#6062=EDGE_CURVE ( 'NONE', #14241, #8188, #44199, .T. ) ;
#6072=VERTEX_POINT ( 'NONE', #40415 ) ;
#6075=ORIENTED_EDGE ( 'NONE', *, *, #31773, .T. ) ;
#6076=CARTESIAN_POINT ( 'NONE',  ( 2.526464513654346433, 20.43088802552616912, -37.81242626108676319 ) ) ;
#6077=FACE_OUTER_BOUND ( 'NONE', #53310, .T. ) ;
#6080=B_SPLINE_CURVE_WITH_KNOTS ( 'NONE', 3,
 ( #30503, #39327, #1684, #11124 ),
 .UNSPECIFIED., .F., .F.,
 ( 4, 4 ),
 ( 0.000000000000000000, 0.004444878191957688657 ),
 .UNSPECIFIED. ) ;
#6081=ORIENTED_EDGE ( 'NONE', *, *, #17734, .F. ) ;
#6082=CARTESIAN_POINT ( 'NONE',  ( 5.860006189529234355, -45.67886430272019993, -15.48781697582095163 ) ) ;
#6098=CARTESIAN_POINT ( 'NONE',  ( 5.960721111146673579, -20.34914600876577140, 2.685391721745692628 ) ) ;
#6105=CARTESIAN_POINT ( 'NONE',  ( 1.227938101723748288, 34.55893248994541267, -25.45152231597022308 ) ) ;
#6106=ORIENTED_EDGE ( 'NONE', *, *, #9476, .F. ) ;
#6111=CARTESIAN_POINT ( 'NONE',  ( 0.8551540677456715978, -5.348818140991227210, 47.61725548905988603 ) ) ;
#6115=B_SPLINE_CURVE_WITH_KNOTS ( 'NONE', 3,
 ( #7330, #12384, #16769, #12085 ),
 .UNSPECIFIED., .F., .F.,
 ( 4, 4 ),
 ( 9.054276140135500350E-17, 0.005004741218457489996 ),
 .UNSPECIFIED. ) ;
#6116=DIRECTION ( 'NONE',  ( 0.000000000000000000, 0.000000000000000000, 1.000000000000000000 ) ) ;
#6121=EDGE_CURVE ( 'NONE', #40624, #26674, #35716, .T. ) ;
#6126=VERTEX_POINT ( 'NONE', #45725 ) ;
#6127=CARTESIAN_POINT ( 'NONE',  ( 0.5827359174754828119, -12.74690115177639704, 46.16863801597760641 ) ) ;
#6131=CARTESIAN_POINT ( 'NONE',  ( 1.227938101723756947, -25.45152231597080927, 34.55893248994497924 ) ) ;
#6136=ORIENTED_EDGE ( 'NONE', *, *, #51257, .T. ) ;
#6139=EDGE_CURVE ( 'NONE', #9802, #4518, #46962, .T. ) ;
#6143=EDGE_CURVE ( 'NONE', #58875, #58301, #23234, .T. ) ;
#6144=CARTESIAN_POINT ( 'NONE',  ( 5.959547316686252039, -0.003562808152765507049, -20.52562247508876681 ) ) ;
#6145=ORIENTED_EDGE ( 'NONE', *, *, #28499, .T. ) ;
#6149=CARTESIAN_POINT ( 'NONE',  ( 0.5807400328401574052, 0.5448834511096651845, -47.89582301953902999 ) ) ;
#6152=CARTESIAN_POINT ( 'NONE',  ( 4.956653778116966613, 0.000000000000000000, 0.000000000000000000 ) ) ;
#6156=B_SPLINE_CURVE_WITH_KNOTS ( 'NONE', 3,
 ( #38992, #57123, #58047, #14255 ),
 .UNSPECIFIED., .F., .F.,
 ( 4, 4 ),
 ( 4.848699518061080308E-18, 0.004050076154993002484 ),
 .UNSPECIFIED. ) ;
#6166=CARTESIAN_POINT ( 'NONE',  ( 4.303969348037246512, -40.54345935592760952, -25.89994482339412230 ) ) ;
#6167=CARTESIAN_POINT ( 'NONE',  ( 1.227938101723748288, -41.66816631169199070, 10.28900963485366127 ) ) ;
#6170=DIRECTION ( 'NONE',  ( 0.000000000000000000, 0.000000000000000000, 1.000000000000000000 ) ) ;
#6190=CARTESIAN_POINT ( 'NONE',  ( 5.981074661064941900, -19.82308078259094586, 5.320466518160593239 ) ) ;
#6191=CARTESIAN_POINT ( 'NONE',  ( 0.9747592971366227932, -39.51726118357604634, 16.71904224817891915 ) ) ;
#6197=EDGE_CURVE ( 'NONE', #50125, #14535, #38901, .T. ) ;
#6198=CARTESIAN_POINT ( 'NONE',  ( 0.5819845901640494645, -23.55368560422314417, -41.70428411658551227 ) ) ;
#6209=ORIENTED_EDGE ( 'NONE', *, *, #32067, .F. ) ;
#6211=CARTESIAN_POINT ( 'NONE',  ( 2.281351352603290472, -30.23585463601401813, 37.24546109640808567 ) ) ;
#6221=VERTEX_POINT ( 'NONE', #32233 ) ;
#6237=ORIENTED_EDGE ( 'NONE', *, *, #28089, .T. ) ;
#6241=CARTESIAN_POINT ( 'NONE',  ( 0.6067099128993237445, 47.38952184036240567, -6.954009037735675136 ) ) ;
#6249=CARTESIAN_POINT ( 'NONE',  ( -17.97369999999976642, -12.32233744059949210, -2.099999999999997424 ) ) ;
#6252=CARTESIAN_POINT ( 'NONE',  ( 0.5807400328401574052, -34.25275203086258813, 33.48217046439099676 ) ) ;
#6260=B_SPLINE_CURVE_WITH_KNOTS ( 'NONE', 3,
 ( #4966, #48220, #33824, #10009, #581, #28477, #47601, #57271, #43226, #24403, #262, #42606, #4644, #9372, #15026, #28794, #43856, #19410, #52904 ),
 .UNSPECIFIED., .F., .F.,
 ( 4, 3, 3, 3, 3, 3, 4 ),
 ( 3.469446951953614189E-18, 0.0002724573126191867601, 0.0004086839781548543861, 0.0005449106435901867988, 0.0006811373090491506990, 0.0008459866663933788070, 0.001010840725717216185 ),
 .UNSPECIFIED. ) ;
#6272=B_SPLINE_CURVE_WITH_KNOTS ( 'NONE', 3,
 ( #4512, #61832, #33376, #43087 ),
 .UNSPECIFIED., .F., .F.,
 ( 4, 4 ),
 ( 0.000000000000000000, 0.005004741218457417137 ),
 .UNSPECIFIED. ) ;
#6277=CARTESIAN_POINT ( 'NONE',  ( 4.963659409799330291, -8.262218268420191691, -43.98510776953418855 ) ) ;
#6285=( BOUNDED_SURFACE ( )  B_SPLINE_SURFACE ( 3, 1, ( 
 ( #49557, #49250 ),
 ( #6613, #45209 ),
 ( #1016, #44902 ),
 ( #53620, #35488 ) ),
 .UNSPECIFIED., .F., .F., .F. ) 
 B_SPLINE_SURFACE_WITH_KNOTS ( ( 4, 4 ),
 ( 2, 2 ),
 ( 0.000000000000000000, 1.000000000000000000 ),
 ( 0.000000000000000000, 1.000000000000000000 ),
 .UNSPECIFIED. ) 
 GEOMETRIC_REPRESENTATION_ITEM ( )  RATIONAL_B_SPLINE_SURFACE ( (
 ( 1.000000000000000000, 1.000000000000000000),
 ( 0.9732289882329797637, 0.9999525324661233672),
 ( 0.9732289882329797637, 0.9999525324661233672),
 ( 1.000000000000000000, 1.000000000000000000) ) ) 
 REPRESENTATION_ITEM ( '' )  SURFACE ( )  );
#6286=ORIENTED_EDGE ( 'NONE', *, *, #26117, .T. ) ;
#6287=ORIENTED_EDGE ( 'NONE', *, *, #15288, .F. ) ;
#6296=AXIS2_PLACEMENT_3D ( 'NONE', #35588, #29623, #54647 ) ;
#6300=LINE ( 'NONE', #7240, #44785 ) ;
#6307=ORIENTED_EDGE ( 'NONE', *, *, #14591, .T. ) ;
#6308=EDGE_CURVE ( 'NONE', #5144, #46408, #24667, .T. ) ;
#6309=B_SPLINE_CURVE_WITH_KNOTS ( 'NONE', 3,
 ( #36127, #10759, #3489, #22940 ),
 .UNSPECIFIED., .F., .F.,
 ( 4, 4 ),
 ( 0.000000000000000000, 0.005004741218457367698 ),
 .UNSPECIFIED. ) ;
#6311=ORIENTED_EDGE ( 'NONE', *, *, #28635, .F. ) ;
#6312=CARTESIAN_POINT ( 'NONE',  ( 0.7762777257811898091, -37.45705273430986892, -29.86325207275917393 ) ) ;
#6316=CARTESIAN_POINT ( 'NONE',  ( 5.974727161628367256, -17.78288073588495877, -10.24903993265002633 ) ) ;
#6323=CARTESIAN_POINT ( 'NONE',  ( 0.9722240750034578660, 39.41582016107722097, -16.95645446544443047 ) ) ;
#6332=CARTESIAN_POINT ( 'NONE',  ( 5.958863334805807099, -14.51469124124469978, -14.51296551801798174 ) ) ;
#6336=CARTESIAN_POINT ( 'NONE',  ( 4.956653778116970166, -27.17045123668450657, -39.67974989265067620 ) ) ;
#6339=CIRCLE ( 'NONE', #58401, 43.08621763946400307 ) ;
#6344=ADVANCED_FACE ( 'NONE', ( #25593 ), #6541, .F. ) ;
#6349=CARTESIAN_POINT ( 'NONE',  ( 0.5800708119828335008, 41.16171018093194078, -24.48933355903722386 ) ) ;
#6351=ORIENTED_EDGE ( 'NONE', *, *, #50228, .F. ) ;
#6362=ORIENTED_EDGE ( 'NONE', *, *, #31765, .F. ) ;
#6368=ORIENTED_EDGE ( 'NONE', *, *, #3335, .F. ) ;
#6376=CARTESIAN_POINT ( 'NONE',  ( 0.5827359174754830340, 44.38786494726119969, -17.99288944686844616 ) ) ;
#6382=CARTESIAN_POINT ( 'NONE',  ( 4.303969348037246512, -45.86537346639047996, -14.52400616872417061 ) ) ;
#6388=CARTESIAN_POINT ( 'NONE',  ( 0.5809828226811617480, -46.40184912890847357, 11.86925843957150128 ) ) ;
#6391=ORIENTED_EDGE ( 'NONE', *, *, #26437, .F. ) ;
#6394=EDGE_CURVE ( 'NONE', #57497, #1853, #26822, .T. ) ;
#6397=EDGE_CURVE ( 'NONE', #30001, #15923, #26893, .T. ) ;
#6399=CARTESIAN_POINT ( 'NONE',  ( 1.088313998177381947, -39.93881167962110368, 15.69908095455140362 ) ) ;
#6407=CARTESIAN_POINT ( 'NONE',  ( 0.9752570700956805227, 39.72995844664877296, -16.20701641182873587 ) ) ;
#6412=CARTESIAN_POINT ( 'NONE',  ( -16.58512404506131688, -12.39995699298779286, 1.581313323489840661 ) ) ;
#6416=B_SPLINE_CURVE_WITH_KNOTS ( 'NONE', 3,
 ( #48052, #19864, #9831, #20463, #6323, #30157 ),
 .UNSPECIFIED., .F., .F.,
 ( 4, 2, 4 ),
 ( 9.948699630566629781E-18, 0.0002291978881530141272, 0.0004583957763060183340 ),
 .UNSPECIFIED. ) ;
#6423=CARTESIAN_POINT ( 'NONE',  ( 4.963659409799330291, 19.36487359954752918, -40.34793212403946683 ) ) ;
#6425=ORIENTED_EDGE ( 'NONE', *, *, #16646, .T. ) ;
#6426=ORIENTED_EDGE ( 'NONE', *, *, #30182, .T. ) ;
#6428=FACE_OUTER_BOUND ( 'NONE', #2931, .T. ) ;
#6429=CARTESIAN_POINT ( 'NONE',  ( 0.5850706913938534814, 38.10903744847141894, 29.01314519953811555 ) ) ;
#6437=CIRCLE ( 'NONE', #24447, 43.08621763946400307 ) ;
#6441=B_SPLINE_CURVE_WITH_KNOTS ( 'NONE', 3,
 ( #17471, #59439, #46005, #21552, #16546, #40378 ),
 .UNSPECIFIED., .F., .F.,
 ( 4, 2, 4 ),
 ( 1.497543825688427252E-16, 0.0002445252820015178345, 0.0004890505640028859407 ),
 .UNSPECIFIED. ) ;
#6442=FACE_OUTER_BOUND ( 'NONE', #21551, .T. ) ;
#6446=CARTESIAN_POINT ( 'NONE',  ( 4.967162193818130511, 42.34252806656603241, -7.970725651239366272 ) ) ;
#6448=CARTESIAN_POINT ( 'NONE',  ( 0.9757892942422814464, 41.43309903783670478, -11.15510465568958409 ) ) ;
#6455=CARTESIAN_POINT ( 'NONE',  ( 0.5837374860065643878, 41.38807031854345553, -24.10515569139005621 ) ) ;
#6464=VECTOR ( 'NONE', #57841, 1000.000000000000227 ) ;
#6467=ORIENTED_EDGE ( 'NONE', *, *, #37077, .F. ) ;
#6470=EDGE_CURVE ( 'NONE', #33914, #42943, #44776, .T. ) ;
#6478=ORIENTED_EDGE ( 'NONE', *, *, #26678, .F. ) ;
#6484=DIRECTION ( 'NONE',  ( -0.07836865515943411409, 0.2656332009267315386, 0.9608836331491552585 ) ) ;
#6488=CARTESIAN_POINT ( 'NONE',  ( 0.8557997880470606944, -28.43566216844945771, -38.55640757422467857 ) ) ;
#6495=LINE ( 'NONE', #58825, #34730 ) ;
#6505=CARTESIAN_POINT ( 'NONE',  ( 5.959547316686252039, -20.52562247508876681, -0.003562808152834123603 ) ) ;
#6506=DIRECTION ( 'NONE',  ( -0.07836865515943412797, -0.1379401902675499447, -0.9873352307081186829 ) ) ;
#6508=ORIENTED_EDGE ( 'NONE', *, *, #20731, .F. ) ;
#6511=CARTESIAN_POINT ( 'NONE',  ( 0.9736507210033074067, -25.76216842460672751, -34.31386771842686301 ) ) ;
#6515=CARTESIAN_POINT ( 'NONE',  ( 5.974727161628369032, 20.52494643607030156, 0.01551142186656635953 ) ) ;
#6516=CARTESIAN_POINT ( 'NONE',  ( 5.965394784446458765, 10.27521535480962100, 17.76824826579358430 ) ) ;
#6527=FACE_OUTER_BOUND ( 'NONE', #2100, .T. ) ;
#6533=CIRCLE ( 'NONE', #49577, 48.09070567114147110 ) ;
#6536=CARTESIAN_POINT ( 'NONE',  ( 4.963659409799331179, -14.83726297270249006, -42.22332985082326928 ) ) ;
#6539=ORIENTED_EDGE ( 'NONE', *, *, #41623, .T. ) ;
#6541=( BOUNDED_SURFACE ( )  B_SPLINE_SURFACE ( 3, 1, ( 
 ( #49397, #44730 ),
 ( #7080, #25910 ),
 ( #11506, #35017 ),
 ( #45044, #49708 ) ),
 .UNSPECIFIED., .F., .F., .F. ) 
 B_SPLINE_SURFACE_WITH_KNOTS ( ( 4, 4 ),
 ( 2, 2 ),
 ( 0.000000000000000000, 1.000000000000000000 ),
 ( 0.000000000000000000, 1.000000000000000000 ),
 .UNSPECIFIED. ) 
 GEOMETRIC_REPRESENTATION_ITEM ( )  RATIONAL_B_SPLINE_SURFACE ( (
 ( 1.000000000000000000, 1.000000000000000000),
 ( 0.7269869731126817891, 0.9931720237060910339),
 ( 0.7269869731126817891, 0.9931720237060910339),
 ( 1.000000000000000000, 1.000000000000000000) ) ) 
 REPRESENTATION_ITEM ( '' )  SURFACE ( )  );
#6542=VERTEX_POINT ( 'NONE', #13362 ) ;
#6545=CARTESIAN_POINT ( 'NONE',  ( 5.960221823109900008, -7.859839668735083329, -18.96108896995712101 ) ) ;
#6546=EDGE_LOOP ( 'NONE', ( #24452, #48553, #3046, #47023 ) ) ;
#6547=EDGE_CURVE ( 'NONE', #59254, #34686, #13357, .T. ) ;
#6555=CARTESIAN_POINT ( 'NONE',  ( 1.227938101723747621, 20.72293514920750468, 37.58536632582787007 ) ) ;
#6557=LINE ( 'NONE', #645, #50562 ) ;
#6564=VERTEX_POINT ( 'NONE', #32781 ) ;
#6573=DIRECTION ( 'NONE',  ( -0.07439287786467650709, 0.2708295585865068689, 0.9597484305373201741 ) ) ;
#6588=CARTESIAN_POINT ( 'NONE',  ( 2.526552050251863690, -15.32056541070812905, -40.15571433620802111 ) ) ;
#6606=CARTESIAN_POINT ( 'NONE',  ( 2.526552050251863246, 41.81191169914609418, -9.948123361606407755 ) ) ;
#6608=VECTOR ( 'NONE', #3036, 1000.000000000000114 ) ;
#6613=CARTESIAN_POINT ( 'NONE',  ( 5.958863334805807099, -14.51469124124489873, 14.51296551801777923 ) ) ;
#6616=ORIENTED_EDGE ( 'NONE', *, *, #7104, .T. ) ;
#6617=EDGE_CURVE ( 'NONE', #57884, #23449, #38784, .T. ) ;
#6618=ORIENTED_EDGE ( 'NONE', *, *, #48321, .T. ) ;
#6619=CARTESIAN_POINT ( 'NONE',  ( 0.5807400328401574052, -23.47602859900744576, 41.75144119563878320 ) ) ;
#6621=CARTESIAN_POINT ( 'NONE',  ( 0.8557997880470606944, -17.48760788519184217, -44.60232077416704755 ) ) ;
#6622=VERTEX_POINT ( 'NONE', #46889 ) ;
#6628=ORIENTED_EDGE ( 'NONE', *, *, #33756, .T. ) ;
#6634=CARTESIAN_POINT ( 'NONE',  ( 0.7762777257811892540, -17.50713318242604899, -44.59086130178268803 ) ) ;
#6636=B_SPLINE_CURVE_WITH_KNOTS ( 'NONE', 3,
 ( #31421, #31110, #21097, #36449, #30174, #50520 ),
 .UNSPECIFIED., .F., .F.,
 ( 4, 2, 4 ),
 ( 8.148123767742043513E-18, 0.0002291978881530167564, 0.0004583957763060253271 ),
 .UNSPECIFIED. ) ;
#6642=CARTESIAN_POINT ( 'NONE',  ( 0.7762777257811878107, -28.45155622761403436, -38.54028505510749625 ) ) ;
#6643=CARTESIAN_POINT ( 'NONE',  ( 0.7762783648524373969, -41.03453896757959285, 24.71864151483699601 ) ) ;
#6657=ORIENTED_EDGE ( 'NONE', *, *, #627, .T. ) ;
#6666=VERTEX_POINT ( 'NONE', #37808 ) ;
#6686=ORIENTED_EDGE ( 'NONE', *, *, #37009, .F. ) ;
#6693=CARTESIAN_POINT ( 'NONE',  ( 0.5834872094924161701, 12.61552836343356354, -46.20467604622288604 ) ) ;
#6695=ORIENTED_EDGE ( 'NONE', *, *, #17492, .T. ) ;
#6697=EDGE_CURVE ( 'NONE', #15210, #26085, #10869, .T. ) ;
#6698=CARTESIAN_POINT ( 'NONE',  ( 4.967162193818130511, 0.000000000000000000, 0.000000000000000000 ) ) ;
#6708=VECTOR ( 'NONE', #22834, 1000.000000000000114 ) ;
#6710=CARTESIAN_POINT ( 'NONE',  ( 5.860006189529234355, 48.12869875779313134, -3.171667470662035804 ) ) ;
#6718=CARTESIAN_POINT ( 'NONE',  ( 0.5819845079324672543, 38.27312975753810065, 28.79567599618773244 ) ) ;
#6721=CARTESIAN_POINT ( 'NONE',  ( 5.965394784446458765, -14.50338846149142924, 14.52385693118977450 ) ) ;
#6724=CARTESIAN_POINT ( 'NONE',  ( 4.967162193818130511, 0.000000000000000000, 0.000000000000000000 ) ) ;
#6735=VERTEX_POINT ( 'NONE', #34320 ) ;
#6738=CARTESIAN_POINT ( 'NONE',  ( 5.965394784446460541, -14.52385693119012799, 14.50338846149107930 ) ) ;
#6775=CARTESIAN_POINT ( 'NONE',  ( 0.9730545539215883499, 16.88610103448558064, 39.44597740938066721 ) ) ;
#6780=CARTESIAN_POINT ( 'NONE',  ( 0.5834872094924176134, -18.53852119651595842, 44.16273175734635004 ) ) ;
#6781=CIRCLE ( 'NONE', #9807, 8.000000000000000000 ) ;
#6788=CARTESIAN_POINT ( 'NONE',  ( 5.860006189529234355, 48.13093674595585014, 3.137522369585681759 ) ) ;
#6793=CARTESIAN_POINT ( 'NONE',  ( 0.5809828226811553087, 18.83114015454698631, 44.03860873105701046 ) ) ;
#6809=CARTESIAN_POINT ( 'NONE',  ( 0.8551540677456715978, 43.91216198251539993, 19.17641535420869658 ) ) ;
#6811=CARTESIAN_POINT ( 'NONE',  ( 0.5850706913938533704, 44.31965802246131858, -18.16120156791832585 ) ) ;
#6818=B_SPLINE_CURVE_WITH_KNOTS ( 'NONE', 3,
 ( #61751, #56755, #51434, #8222, #9155, #27340, #46467, #18890, #56143, #57061, #38010, #13881, #28261, #52061, #22964, #8528, #14190, #3512, #33295 ),
 .UNSPECIFIED., .F., .F.,
 ( 4, 3, 3, 3, 3, 3, 4 ),
 ( 0.000000000000000000, 0.0002724573126191728281, 0.0004086839781548461462, 0.0005449106435901787757, 0.0006811373090491435432, 0.0008459866663933707839, 0.001010840725717218570 ),
 .UNSPECIFIED. ) ;
#6823=B_SPLINE_CURVE_WITH_KNOTS ( 'NONE', 3,
 ( #12983, #17355, #45880, #60238 ),
 .UNSPECIFIED., .F., .F.,
 ( 4, 4 ),
 ( 2.385244779468109755E-18, 0.004444878191957686922 ),
 .UNSPECIFIED. ) ;
#6827=FACE_OUTER_BOUND ( 'NONE', #40406, .T. ) ;
#6832=CARTESIAN_POINT ( 'NONE',  ( 0.9756008150404590351, -39.69644259322195978, -16.28894658522374073 ) ) ;
#6835=EDGE_CURVE ( 'NONE', #53201, #2091, #28322, .T. ) ;
#6836=ORIENTED_EDGE ( 'NONE', *, *, #56353, .T. ) ;
#6838=CARTESIAN_POINT ( 'NONE',  ( 0.9756354156337460060, 16.54067710771413857, -39.59221474545846320 ) ) ;
#6839=CARTESIAN_POINT ( 'NONE',  ( 0.5263152470540364281, 0.000000000000000000, 0.000000000000000000 ) ) ;
#6840=( BOUNDED_SURFACE ( )  B_SPLINE_SURFACE ( 3, 1, ( 
 ( #18990, #33390 ),
 ( #38106, #4224 ),
 ( #56853, #33701 ),
 ( #28359, #57151 ) ),
 .UNSPECIFIED., .F., .F., .F. ) 
 B_SPLINE_SURFACE_WITH_KNOTS ( ( 4, 4 ),
 ( 2, 2 ),
 ( 0.000000000000000000, 1.000000000000000000 ),
 ( 0.000000000000000000, 1.000000000000000000 ),
 .UNSPECIFIED. ) 
 GEOMETRIC_REPRESENTATION_ITEM ( )  RATIONAL_B_SPLINE_SURFACE ( (
 ( 1.000000000000000000, 1.000000000000000000),
 ( 0.9953390228620291325, 0.8624445117761032620),
 ( 0.9953390228620291325, 0.8624445117761032620),
 ( 1.000000000000000000, 1.000000000000000000) ) ) 
 REPRESENTATION_ITEM ( '' )  SURFACE ( )  );
#6845=AXIS2_PLACEMENT_3D ( 'NONE', #32994, #52067, #27966 ) ;
#6846=CARTESIAN_POINT ( 'NONE',  ( 2.624215991343620935, -1.411420423865143325, -47.98682984381862582 ) ) ;
#6849=ORIENTED_EDGE ( 'NONE', *, *, #50669, .T. ) ;
#6853=ORIENTED_EDGE ( 'NONE', *, *, #54148, .T. ) ;
#6875=EDGE_CURVE ( 'NONE', #13708, #10594, #34331, .T. ) ;
#6880=LINE ( 'NONE', #53569, #57685 ) ;
#6881=CARTESIAN_POINT ( 'NONE',  ( -20.07378285010853602, -12.50001391881583501, 0.1374748271822699153 ) ) ;
#6882=ORIENTED_EDGE ( 'NONE', *, *, #58747, .T. ) ;
#6884=ORIENTED_EDGE ( 'NONE', *, *, #33125, .F. ) ;
#6889=CARTESIAN_POINT ( 'NONE',  ( 2.624215991343608501, 17.05978231157404323, 44.87417713512093798 ) ) ;
#6895=CARTESIAN_POINT ( 'NONE',  ( 5.960221823109900008, 20.35070456576734443, -2.673723662181125338 ) ) ;
#6901=EDGE_CURVE ( 'NONE', #8188, #28286, #45543, .T. ) ;
#6905=ADVANCED_FACE ( 'NONE', ( #47043 ), #18830, .T. ) ;
#6908=CARTESIAN_POINT ( 'NONE',  ( 0.5819845901640492425, 46.14435291605029477, 12.83441129068549813 ) ) ;
#6916=CARTESIAN_POINT ( 'NONE',  ( 5.860006189529234355, -26.81109398084681317, -40.09484204000627017 ) ) ;
#6919=ORIENTED_EDGE ( 'NONE', *, *, #21014, .F. ) ;
#6921=CARTESIAN_POINT ( 'NONE',  ( 5.959547316686252039, 12.49238070347954555, 16.28624005235103311 ) ) ;
#6937=LINE ( 'NONE', #45508, #52531 ) ;
#6940=ORIENTED_EDGE ( 'NONE', *, *, #12526, .F. ) ;
#6942=CARTESIAN_POINT ( 'NONE',  ( 5.959547316686252039, 10.25972575517530139, -17.77749189599207114 ) ) ;
#6944=EDGE_CURVE ( 'NONE', #14392, #41383, #25331, .T. ) ;
#6949=DIRECTION ( 'NONE',  ( -1.000000000000000000, -0.000000000000000000, -0.000000000000000000 ) ) ;
#6950=CARTESIAN_POINT ( 'NONE',  ( 0.7057020205115069889, 29.82342581815259308, -37.48480537461301054 ) ) ;
#6951=VECTOR ( 'NONE', #24331, 1000.000000000000114 ) ;
#6959=CARTESIAN_POINT ( 'NONE',  ( 0.5850706913938533704, -44.18063951072207374, -18.49682194438010896 ) ) ;
#6961=CARTESIAN_POINT ( 'NONE',  ( 4.967162193818131399, -42.34252806656588319, -7.970725651240238463 ) ) ;
#6963=CARTESIAN_POINT ( 'NONE',  ( 0.5809828226811553087, 0.5448590168532381206, 47.89273459658653564 ) ) ;
#6974=FACE_OUTER_BOUND ( 'NONE', #43433, .T. ) ;
#6978=CARTESIAN_POINT ( 'NONE',  ( 3.660176727303405375, -46.85282580473587899, 10.60619300811855403 ) ) ;
#6981=EDGE_CURVE ( 'NONE', #47520, #46817, #20077, .T. ) ;
#6983=VERTEX_POINT ( 'NONE', #57941 ) ;
#6986=CARTESIAN_POINT ( 'NONE',  ( 0.5786265663353153954, -13.09387673186302870, -46.07681357296498703 ) ) ;
#6989=ORIENTED_EDGE ( 'NONE', *, *, #1739, .F. ) ;
#6993=CARTESIAN_POINT ( 'NONE',  ( 4.967162193818131399, -3.259922920618036901, 42.96271701169384016 ) ) ;
#6995=VERTEX_POINT ( 'NONE', #19451 ) ;
#7000=CARTESIAN_POINT ( 'NONE',  ( 0.9736507210033064075, 42.48017254354723349, 6.046964561328082688 ) ) ;
#7011=CARTESIAN_POINT ( 'NONE',  ( 0.9757787079277437936, -30.31292661677473887, -30.36877398309933440 ) ) ;
#7013=B_SPLINE_CURVE_WITH_KNOTS ( 'NONE', 3,
 ( #20025, #1487, #39757, #25622, #39137, #35356, #58810, #44759, #10611, #11227, #30316, #54412, #49737, #1799, #40073, #6793 ),
 .UNSPECIFIED., .F., .F.,
 ( 4, 3, 3, 3, 3, 4 ),
 ( 1.250973872328959318E-17, 0.0002724568934985550049, 0.0004086836638483800927, 0.0005449104342063564293, 0.0008173270854453635291, 0.001089761613562688575 ),
 .UNSPECIFIED. ) ;
#7014=( BOUNDED_SURFACE ( )  B_SPLINE_SURFACE ( 3, 1, ( 
 ( #39085, #14341 ),
 ( #5512, #33449 ),
 ( #14651, #47537 ),
 ( #38459, #9618 ) ),
 .UNSPECIFIED., .F., .F., .F. ) 
 B_SPLINE_SURFACE_WITH_KNOTS ( ( 4, 4 ),
 ( 2, 2 ),
 ( 0.000000000000000000, 1.000000000000000000 ),
 ( 0.000000000000000000, 1.000000000000000000 ),
 .UNSPECIFIED. ) 
 GEOMETRIC_REPRESENTATION_ITEM ( )  RATIONAL_B_SPLINE_SURFACE ( (
 ( 1.000000000000000000, 1.000000000000000000),
 ( 0.9732289882329797637, 0.9999525324661233672),
 ( 0.9732289882329797637, 0.9999525324661233672),
 ( 1.000000000000000000, 1.000000000000000000) ) ) 
 REPRESENTATION_ITEM ( '' )  SURFACE ( )  );
#7015=CARTESIAN_POINT ( 'NONE',  ( 4.967162193818130511, 19.45289607368822615, 38.44485641567079881 ) ) ;
#7017=B_SPLINE_CURVE_WITH_KNOTS ( 'NONE', 3,
 ( #38996, #58052, #4501, #32743 ),
 .UNSPECIFIED., .F., .F.,
 ( 4, 4 ),
 ( 7.589415207398531038E-19, 0.004444878191957689524 ),
 .UNSPECIFIED. ) ;
#7019=VERTEX_POINT ( 'NONE', #37864 ) ;
#7022=CARTESIAN_POINT ( 'NONE',  ( 0.6067375320500720814, 33.36326114377818897, 34.36594163291719894 ) ) ;
#7024=CONICAL_SURFACE ( 'NONE', #50073, 43.08621763946400307, 1.568696531533066763 ) ;
#7033=VECTOR ( 'NONE', #16353, 1000.000000000000000 ) ;
#7034=CARTESIAN_POINT ( 'NONE',  ( 0.9740398440564311811, 42.90647580953695694, -0.4145941695174525932 ) ) ;
#7036=CARTESIAN_POINT ( 'NONE',  ( 4.967162193818130511, 36.06913038482799294, 23.56777426397191277 ) ) ;
#7045=CARTESIAN_POINT ( 'NONE',  ( 5.959547316686252039, -17.77749189599224877, 10.25972575517499052 ) ) ;
#7054=ORIENTED_EDGE ( 'NONE', *, *, #41406, .F. ) ;
#7059=ORIENTED_EDGE ( 'NONE', *, *, #29923, .F. ) ;
#7061=CARTESIAN_POINT ( 'NONE',  ( 0.5819845079324663661, -47.42480735454290652, 6.701571823032553610 ) ) ;
#7062=CARTESIAN_POINT ( 'NONE',  ( 4.967162193818130511, 0.000000000000000000, 0.000000000000000000 ) ) ;
#7065=EDGE_LOOP ( 'NONE', ( #18356, #4618, #54164, #30424 ) ) ;
#7068=LINE ( 'NONE', #40641, #35246 ) ;
#7069=CARTESIAN_POINT ( 'NONE',  ( 5.981074661064941900, 7.862380442164140781, -18.95903134304781190 ) ) ;
#7075=EDGE_LOOP ( 'NONE', ( #36120, #35842, #58112, #6391 ) ) ;
#7078=CARTESIAN_POINT ( 'NONE',  ( 0.9749527285493314599, 41.51939261707898510, -10.82939760924460515 ) ) ;
#7080=CARTESIAN_POINT ( 'NONE',  ( 5.974727161628369032, -5.297264154380800782, -19.82959049719573841 ) ) ;
#7081=CARTESIAN_POINT ( 'NONE',  ( 5.958863334805807099, -0.001220270596312466932, 20.52565293643016275 ) ) ;
#7085=CARTESIAN_POINT ( 'NONE',  ( 3.783278058412225864, 31.62921638229668275, 29.18720354295055230 ) ) ;
#7087=CARTESIAN_POINT ( 'NONE',  ( 0.7762783648524406166, -33.23866576554864594, 34.49689442177335508 ) ) ;
#7093=CARTESIAN_POINT ( 'NONE',  ( 5.960721111146673579, -14.50930005615026808, 14.51823969584074625 ) ) ;
#7104=EDGE_CURVE ( 'NONE', #41282, #21198, #40231, .T. ) ;
#7111=CARTESIAN_POINT ( 'NONE',  ( 5.959547316686252039, -19.82530672674365846, 5.315863417545987346 ) ) ;
#7115=CARTESIAN_POINT ( 'NONE',  ( 2.281351352603284699, -28.15073776031340813, -38.84542754822352606 ) ) ;
#7117=CARTESIAN_POINT ( 'NONE',  ( 5.960721111146673579, -17.77250458025985225, -10.26825948882919626 ) ) ;
#7118=CARTESIAN_POINT ( 'NONE',  ( 4.956653778116982600, -47.94889704119054130, 3.690426056929806631 ) ) ;
#7120=FACE_OUTER_BOUND ( 'NONE', #52594, .T. ) ;
#7127=CARTESIAN_POINT ( 'NONE',  ( 4.956653778116994147, 39.67974989265076857, -27.17045123668430406 ) ) ;
#7128=CARTESIAN_POINT ( 'NONE',  ( 5.958863334805807099, -2.677925489610497589, -20.35021240744034188 ) ) ;
#7137=EDGE_CURVE ( 'NONE', #54529, #461, #35004, .T. ) ;
#7143=CARTESIAN_POINT ( 'NONE',  ( 0.9740398440564319582, 39.48175649279257726, -16.80263250099845251 ) ) ;
#7147=EDGE_CURVE ( 'NONE', #31029, #51225, #23010, .T. ) ;
#7150=EDGE_CURVE ( 'NONE', #3346, #9975, #47862, .T. ) ;
#7157=ORIENTED_EDGE ( 'NONE', *, *, #6835, .T. ) ;
#7170=CARTESIAN_POINT ( 'NONE',  ( 0.6067375320500711933, 43.97491060910887484, 18.98242280073580801 ) ) ;
#7172=CARTESIAN_POINT ( 'NONE',  ( 4.967162193818131399, -38.83676580803778933, 18.65818244221244981 ) ) ;
#7174=EDGE_LOOP ( 'NONE', ( #44984, #46257, #4077, #44569 ) ) ;
#7177=CARTESIAN_POINT ( 'NONE',  ( 0.5819845901640493535, -44.42187107932956280, 17.90867915372037444 ) ) ;
#7178=ORIENTED_EDGE ( 'NONE', *, *, #49712, .F. ) ;
#7181=CARTESIAN_POINT ( 'NONE',  ( 0.9756008150404602564, 33.95486284030262425, -26.23365443298883193 ) ) ;
#7189=EDGE_CURVE ( 'NONE', #461, #26377, #2784, .T. ) ;
#7196=CARTESIAN_POINT ( 'NONE',  ( 5.959547316686252039, 14.51632612601528827, -14.51128755440526241 ) ) ;
#7197=CARTESIAN_POINT ( 'NONE',  ( 4.967162193818130511, -18.65818244221228284, -38.83676580803786749 ) ) ;
#7198=DIRECTION ( 'NONE',  ( 0.000000000000000000, 0.000000000000000000, 1.000000000000000000 ) ) ;
#7203=CARTESIAN_POINT ( 'NONE',  ( 0.9758171775293931205, 21.44911662810702779, -37.16279804060109626 ) ) ;
#7209=CARTESIAN_POINT ( 'NONE',  ( 1.088313998177382613, -37.54798835078475605, 20.77783415101614395 ) ) ;
#7211=CARTESIAN_POINT ( 'NONE',  ( 1.227938101723748288, 26.79402671879374864, -33.52879263017835143 ) ) ;
#7213=( BOUNDED_SURFACE ( )  B_SPLINE_SURFACE ( 3, 1, ( 
 ( #32509, #22180 ),
 ( #32200, #41307 ),
 ( #51584, #36918 ),
 ( #27799, #40695 ) ),
 .UNSPECIFIED., .F., .F., .F. ) 
 B_SPLINE_SURFACE_WITH_KNOTS ( ( 4, 4 ),
 ( 2, 2 ),
 ( 0.000000000000000000, 1.000000000000000000 ),
 ( 0.000000000000000000, 1.000000000000000000 ),
 .UNSPECIFIED. ) 
 GEOMETRIC_REPRESENTATION_ITEM ( )  RATIONAL_B_SPLINE_SURFACE ( (
 ( 1.000000000000000000, 1.000000000000000000),
 ( 0.9953390228620291325, 0.8624445117761032620),
 ( 0.9953390228620291325, 0.8624445117761032620),
 ( 1.000000000000000000, 1.000000000000000000) ) ) 
 REPRESENTATION_ITEM ( '' )  SURFACE ( )  );
#7219=FACE_OUTER_BOUND ( 'NONE', #61459, .T. ) ;
#7221=ORIENTED_EDGE ( 'NONE', *, *, #24978, .T. ) ;
#7223=B_SPLINE_CURVE_WITH_KNOTS ( 'NONE', 3,
 ( #23768, #23156, #19090, #28151, #13774, #32881 ),
 .UNSPECIFIED., .F., .F.,
 ( 4, 2, 4 ),
 ( 7.040638946443416885E-18, 0.0002445244328975369145, 0.0004890488657950667816 ),
 .UNSPECIFIED. ) ;
#7226=ORIENTED_EDGE ( 'NONE', *, *, #4134, .F. ) ;
#7228=EDGE_CURVE ( 'NONE', #9581, #6735, #38007, .T. ) ;
#7229=CARTESIAN_POINT ( 'NONE',  ( 0.9730545539215883499, -41.31259007387222226, -11.59290486963550393 ) ) ;
#7232=CARTESIAN_POINT ( 'NONE',  ( 5.959547316686252039, 20.35048796920736791, -2.675599016784323769 ) ) ;
#7233=ORIENTED_EDGE ( 'NONE', *, *, #42224, .F. ) ;
#7235=CARTESIAN_POINT ( 'NONE',  ( 0.9740398440564311811, -5.189371650077155174, 42.59352035928885982 ) ) ;
#7240=CARTESIAN_POINT ( 'NONE',  ( 3.407937589446178528, 13.69123696618924413, -0.4592810312472460077 ) ) ;
#7245=CARTESIAN_POINT ( 'NONE',  ( 0.5809828226811617480, 18.83114015454759738, -44.03860873105676177 ) ) ;
#7247=B_SPLINE_CURVE_WITH_KNOTS ( 'NONE', 3,
 ( #7669, #20867, #44396, #11472 ),
 .UNSPECIFIED., .F., .F.,
 ( 4, 4 ),
 ( 0.000000000000000000, 0.004048833967417086489 ),
 .UNSPECIFIED. ) ;
#7257=CARTESIAN_POINT ( 'NONE',  ( 4.967162193818130511, -28.74031574030035685, 32.10009971360062764 ) ) ;
#7259=EDGE_CURVE ( 'NONE', #10228, #61052, #14588, .T. ) ;
#7270=CARTESIAN_POINT ( 'NONE',  ( 5.958863334805807099, 18.96369761673808441, 7.853699934219964263 ) ) ;
#7287=VERTEX_POINT ( 'NONE', #33622 ) ;
#7289=CARTESIAN_POINT ( 'NONE',  ( 0.8557997880470606944, -13.27832040216671317, 46.03118133706021808 ) ) ;
#7291=ORIENTED_EDGE ( 'NONE', *, *, #55562, .F. ) ;
#7301=( BOUNDED_SURFACE ( )  B_SPLINE_SURFACE ( 3, 1, ( 
 ( #28483, #19123 ),
 ( #28800, #61674 ),
 ( #38535, #52912 ),
 ( #8768, #13802 ) ),
 .UNSPECIFIED., .F., .F., .F. ) 
 B_SPLINE_SURFACE_WITH_KNOTS ( ( 4, 4 ),
 ( 2, 2 ),
 ( 0.000000000000000000, 1.000000000000000000 ),
 ( 0.000000000000000000, 1.000000000000000000 ),
 .UNSPECIFIED. ) 
 GEOMETRIC_REPRESENTATION_ITEM ( )  RATIONAL_B_SPLINE_SURFACE ( (
 ( 1.000000000000000000, 1.000000000000000000),
 ( 0.9732289882329797637, 0.9999525324661233672),
 ( 0.9732289882329797637, 0.9999525324661233672),
 ( 1.000000000000000000, 1.000000000000000000) ) ) 
 REPRESENTATION_ITEM ( '' )  SURFACE ( )  );
#7307=AXIS2_PLACEMENT_3D ( 'NONE', #2284, #11402, #55526 ) ;
#7309=B_SPLINE_CURVE_WITH_KNOTS ( 'NONE', 3,
 ( #52450, #3907, #9545, #28655 ),
 .UNSPECIFIED., .F., .F.,
 ( 4, 4 ),
 ( 1.734723475976807094E-18, 0.004048833967417083887 ),
 .UNSPECIFIED. ) ;
#7313=CARTESIAN_POINT ( 'NONE',  ( 0.5800708119828338338, 13.00144522946658476, 46.09746484493482654 ) ) ;
#7320=ORIENTED_EDGE ( 'NONE', *, *, #32748, .F. ) ;
#7321=CARTESIAN_POINT ( 'NONE',  ( 0.9756354156337444516, -30.24859376089802510, -30.43287766742280098 ) ) ;
#7325=DIRECTION ( 'NONE',  ( -1.000000000000000000, -0.000000000000000000, -0.000000000000000000 ) ) ;
#7330=CARTESIAN_POINT ( 'NONE',  ( 4.956653778116987041, -47.94889704119048446, -3.690426056930470988 ) ) ;
#7335=CARTESIAN_POINT ( 'NONE',  ( 4.956653778116971054, 42.88673967249130925, 21.75875759808722876 ) ) ;
#7336=CARTESIAN_POINT ( 'NONE',  ( 3.783278058412225864, 38.10568111914503930, 20.00643011788468328 ) ) ;
#7337=B_SPLINE_CURVE_WITH_KNOTS ( 'NONE', 3,
 ( #12278, #9090, #13820, #51375, #4361, #9393 ),
 .UNSPECIFIED., .F., .F.,
 ( 4, 2, 4 ),
 ( 8.805430561888389713E-18, 0.0002445244328975372397, 0.0004890488657950656974 ),
 .UNSPECIFIED. ) ;
#7340=CARTESIAN_POINT ( 'NONE',  ( 4.956653778116990594, -20.77844580450529577, -43.37017594958076927 ) ) ;
#7341=CARTESIAN_POINT ( 'NONE',  ( 0.5819845901640493535, 46.37938751183699537, -11.95725023767309203 ) ) ;
#7349=DIRECTION ( 'NONE',  ( 0.000000000000000000, 0.000000000000000000, 1.000000000000000000 ) ) ;
#7354=VECTOR ( 'NONE', #38808, 1000.000000000000114 ) ;
#7361=CARTESIAN_POINT ( 'NONE',  ( 0.9730545539215883499, -41.31259007387222226, -11.59290486963550393 ) ) ;
#7383=CARTESIAN_POINT ( 'NONE',  ( 1.227938101723756947, -33.52879263017882039, 26.79402671879314823 ) ) ;
#7404=CARTESIAN_POINT ( 'NONE',  ( 0.9730545539215883499, -36.90443313492315980, -21.89037132892475057 ) ) ;
#7406=VERTEX_POINT ( 'NONE', #21288 ) ;
#7412=EDGE_CURVE ( 'NONE', #3302, #8164, #10359, .T. ) ;
#7417=ORIENTED_EDGE ( 'NONE', *, *, #20767, .F. ) ;
#7425=CARTESIAN_POINT ( 'NONE',  ( 4.956653778116990594, -32.11725092155016625, -35.79382859084151391 ) ) ;
#7428=CARTESIAN_POINT ( 'NONE',  ( 5.965394784446460541, 19.82223131420046869, 5.326334832595717828 ) ) ;
#7433=CARTESIAN_POINT ( 'NONE',  ( 0.8557997880470697982, -47.37054680076710866, 7.156447707085535903 ) ) ;
#7434=CARTESIAN_POINT ( 'NONE',  ( 2.281351352603289584, -19.56575819747254741, 43.80196780981711413 ) ) ;
#7438=CIRCLE ( 'NONE', #57421, 43.08621763946400307 ) ;
#7451=CARTESIAN_POINT ( 'NONE',  ( 0.9972139404380313543, -25.59643345733252318, 34.43899251299762199 ) ) ;
#7453=ADVANCED_FACE ( 'NONE', ( #56321 ), #32579, .F. ) ;
#7454=CARTESIAN_POINT ( 'NONE',  ( 0.6067099128993201917, 17.67241243535543305, -44.51753430581923254 ) ) ;
#7455=CARTESIAN_POINT ( 'NONE',  ( 4.303969348037246512, -22.16169334783807443, -42.70173985163840058 ) ) ;
#7463=VERTEX_POINT ( 'NONE', #42267 ) ;
#7464=CARTESIAN_POINT ( 'NONE',  ( 0.5839879882074149320, -2.012401402563926455E-05, -47.89596766821756546 ) ) ;
#7467=ORIENTED_EDGE ( 'NONE', *, *, #33673, .F. ) ;
#7468=CARTESIAN_POINT ( 'NONE',  ( 4.956653778116989706, -42.88673967249116004, -21.75875759808752008 ) ) ;
#7472=B_SPLINE_CURVE_WITH_KNOTS ( 'NONE', 3,
 ( #28374, #47495, #32789, #19004, #9572, #18684 ),
 .UNSPECIFIED., .F., .F.,
 ( 4, 2, 4 ),
 ( 3.476216610979977084E-18, 0.0002291966416970803253, 0.0004583932833941571812 ),
 .UNSPECIFIED. ) ;
#7476=CARTESIAN_POINT ( 'NONE',  ( 0.5837374860065643878, -38.10878877974126056, -29.01294733976400408 ) ) ;
#7482=CARTESIAN_POINT ( 'NONE',  ( 3.270143674763207553, -9.482922169188032768, 9.870732238228487887 ) ) ;
#7484=VECTOR ( 'NONE', #19976, 1000.000000000000000 ) ;
#7488=CARTESIAN_POINT ( 'NONE',  ( 4.956653778116975495, -39.67974989265057673, 27.17045123668458828 ) ) ;
#7490=CARTESIAN_POINT ( 'NONE',  ( 4.303969348037258058, -4.133486515473634881, 47.93217632892346813 ) ) ;
#7493=EDGE_LOOP ( 'NONE', ( #55188, #46058, #60252, #24923 ) ) ;
#7498=ORIENTED_EDGE ( 'NONE', *, *, #47425, .F. ) ;
#7502=ORIENTED_EDGE ( 'NONE', *, *, #24386, .F. ) ;
#7505=DIRECTION ( 'NONE',  ( -0.07836865515943411409, 0.2503967164834599024, -0.9649662368512192945 ) ) ;
#7515=CARTESIAN_POINT ( 'NONE',  ( 4.967162193818130511, 36.06913038482799294, 23.56777426397191277 ) ) ;
#7517=CARTESIAN_POINT ( 'NONE',  ( 5.959547316686252039, -5.308980600728594013, 19.82715097195153220 ) ) ;
#7520=CARTESIAN_POINT ( 'NONE',  ( 0.5807400328401637335, 46.40483864045145168, 11.87003418057259374 ) ) ;
#7536=EDGE_CURVE ( 'NONE', #46801, #6622, #55156, .T. ) ;
#7538=ORIENTED_EDGE ( 'NONE', *, *, #20951, .T. ) ;
#7547=ORIENTED_EDGE ( 'NONE', *, *, #50417, .T. ) ;
#7551=B_SPLINE_CURVE_WITH_KNOTS ( 'NONE', 3,
 ( #21728, #26115, #41475, #40868, #55530, #50842 ),
 .UNSPECIFIED., .F., .F.,
 ( 4, 2, 4 ),
 ( 0.000000000000000000, 0.0002291966416970789701, 0.0004583932833941579401 ),
 .UNSPECIFIED. ) ;
#7554=B_SPLINE_CURVE_WITH_KNOTS ( 'NONE', 3,
 ( #58529, #45404, #58845, #1837, #25652, #2453 ),
 .UNSPECIFIED., .F., .F.,
 ( 4, 2, 4 ),
 ( 1.500335247250105340E-16, 0.0002445252820015200571, 0.0004890505640028900607 ),
 .UNSPECIFIED. ) ;
#7558=ORIENTED_EDGE ( 'NONE', *, *, #4186, .T. ) ;
#7563=VERTEX_POINT ( 'NONE', #24369 ) ;
#7566=CARTESIAN_POINT ( 'NONE',  ( 0.9745511491811745808, -42.90705396078544709, -0.3405614984925067756 ) ) ;
#7568=CARTESIAN_POINT ( 'NONE',  ( 0.9754642270333685472, 25.98138239028857654, 34.14824330022339183 ) ) ;
#7569=B_SPLINE_CURVE_WITH_KNOTS ( 'NONE', 3,
 ( #60295, #42471, #8002, #41857 ),
 .UNSPECIFIED., .F., .F.,
 ( 4, 4 ),
 ( 0.000000000000000000, 0.004446090762761378996 ),
 .UNSPECIFIED. ) ;
#7572=DIRECTION ( 'NONE',  ( -1.000000000000000000, -0.000000000000000000, -0.000000000000000000 ) ) ;
#7576=AXIS2_PLACEMENT_3D ( 'NONE', #24361, #534, #19669 ) ;
#7581=CARTESIAN_POINT ( 'NONE',  ( 0.9736507210033072957, -16.83559693395292101, 39.46762617149627772 ) ) ;
#7588=CARTESIAN_POINT ( 'NONE',  ( 3.270143674763207553, 12.53844339339234715, 5.490410281242826152 ) ) ;
#7606=CARTESIAN_POINT ( 'NONE',  ( 4.967162193818130511, 0.000000000000000000, 0.000000000000000000 ) ) ;
#7608=ORIENTED_EDGE ( 'NONE', *, *, #37077, .T. ) ;
#7618=EDGE_CURVE ( 'NONE', #41383, #58552, #38657, .T. ) ;
#7623=ADVANCED_FACE ( 'NONE', ( #54385 ), #34583, .F. ) ;
#7626=FACE_OUTER_BOUND ( 'NONE', #23273, .T. ) ;
#7630=ORIENTED_EDGE ( 'NONE', *, *, #41755, .T. ) ;
#7631=CARTESIAN_POINT ( 'NONE',  ( 1.227938101723748288, -0.8460948827228147451, 42.91134962331487657 ) ) ;
#7633=CARTESIAN_POINT ( 'NONE',  ( 0.6846871229502899947, -33.25969555998767646, 34.48177377577824387 ) ) ;
#7635=DIRECTION ( 'NONE',  ( -1.000000000000000000, -0.000000000000000000, -0.000000000000000000 ) ) ;
#7637=LINE ( 'NONE', #25836, #10390 ) ;
#7639=CARTESIAN_POINT ( 'NONE',  ( 0.9752132459055852243, -30.50512806189389892, -30.17566824627277100 ) ) ;
#7642=CARTESIAN_POINT ( 'NONE',  ( 0.9736507210033050752, -21.06291100879414913, -37.38294557109060179 ) ) ;
#7643=EDGE_LOOP ( 'NONE', ( #12045, #43094, #54229, #46907 ) ) ;
#7654=CARTESIAN_POINT ( 'NONE',  ( 0.5850706913938533704, -29.30134895053080868, 37.88789093229795668 ) ) ;
#7656=CARTESIAN_POINT ( 'NONE',  ( 0.5800708119828335008, -47.56394195701282968, -5.628966929618236748 ) ) ;
#7661=CARTESIAN_POINT ( 'NONE',  ( 0.5800708057587371513, -18.90714313908690869, 44.00606528161381448 ) ) ;
#7664=B_SPLINE_CURVE_WITH_KNOTS ( 'NONE', 3,
 ( #47925, #9378, #52911, #4651, #42928, #14719 ),
 .UNSPECIFIED., .F., .F.,
 ( 4, 2, 4 ),
 ( 7.040638946443416885E-18, 0.0002445244328975378903, 0.0004890488657950687332 ),
 .UNSPECIFIED. ) ;
#7666=CARTESIAN_POINT ( 'NONE',  ( 0.5809828226811553087, 11.86925843957232729, -46.40184912890826752 ) ) ;
#7668=CARTESIAN_POINT ( 'NONE',  ( 0.6067099128993221901, -13.08009036336170539, -46.07641759122979863 ) ) ;
#7669=CARTESIAN_POINT ( 'NONE',  ( 1.227938101723748288, -4.762198645644156514, -42.65467462194923343 ) ) ;
#7671=CARTESIAN_POINT ( 'NONE',  ( 0.6846871229502932144, -47.60345020167355301, 5.395516691087021144 ) ) ;
#7674=B_SPLINE_CURVE_WITH_KNOTS ( 'NONE', 3,
 ( #3519, #27657, #41786, #13889 ),
 .UNSPECIFIED., .F., .F.,
 ( 4, 4 ),
 ( 7.757919228897728493E-18, 0.005004741218457420607 ),
 .UNSPECIFIED. ) ;
#7693=B_SPLINE_CURVE_WITH_KNOTS ( 'NONE', 3,
 ( #50451, #59531, #23416, #40465 ),
 .UNSPECIFIED., .F., .F.,
 ( 4, 4 ),
 ( 0.000000000000000000, 0.005004741218457412801 ),
 .UNSPECIFIED. ) ;
#7706=ORIENTED_EDGE ( 'NONE', *, *, #6394, .T. ) ;
#7715=CARTESIAN_POINT ( 'NONE',  ( 2.526464513654347321, 31.23609615087176294, 29.52129845577943001 ) ) ;
#7717=ADVANCED_FACE ( 'NONE', ( #59405 ), #22134, .F. ) ;
#7722=EDGE_LOOP ( 'NONE', ( #58392, #56760, #41324, #59807 ) ) ;
#7740=ADVANCED_FACE ( 'NONE', ( #13363 ), #10549, .T. ) ;
#7747=CARTESIAN_POINT ( 'NONE',  ( 0.9756354156337455619, -30.43287766742269085, 30.24859376089808904 ) ) ;
#7753=CARTESIAN_POINT ( 'NONE',  ( 3.407937589446178528, 7.970324840162117397, -11.14158115674364957 ) ) ;
#7756=CARTESIAN_POINT ( 'NONE',  ( 0.9757892942422816684, -39.62259979733192239, 16.46777583825590341 ) ) ;
#7757=DIRECTION ( 'NONE',  ( -0.07836865515943412797, -0.7860872967108227805, 0.6131273243286198271 ) ) ;
#7761=VECTOR ( 'NONE', #48882, 1000.000000000000114 ) ;
#7762=DIRECTION ( 'NONE',  ( -1.000000000000000000, -0.000000000000000000, -0.000000000000000000 ) ) ;
#7766=CARTESIAN_POINT ( 'NONE',  ( 0.5809828226811617480, -28.72298383114462439, -38.32755012159175578 ) ) ;
#7767=CARTESIAN_POINT ( 'NONE',  ( 0.8557997880470697982, -47.89938907511594834, 0.9121262075944505110 ) ) ;
#7772=CARTESIAN_POINT ( 'NONE',  ( 1.154321485836933281, 37.57248783354771859, 20.73950273457856142 ) ) ;
#7786=VERTEX_POINT ( 'NONE', #3926 ) ;
#7791=ORIENTED_EDGE ( 'NONE', *, *, #40509, .T. ) ;
#7799=CARTESIAN_POINT ( 'NONE',  ( 0.5827357941260210561, -38.21849163199656374, -28.86820951701472993 ) ) ;
#7800=ORIENTED_EDGE ( 'NONE', *, *, #31282, .F. ) ;
#7803=CARTESIAN_POINT ( 'NONE',  ( 0.8557997880470606944, 43.90420959842181503, 19.17299735372024827 ) ) ;
#7805=CARTESIAN_POINT ( 'NONE',  ( 4.956653778116996811, 45.35992544608552635, -15.97476558431834626 ) ) ;
#7807=CARTESIAN_POINT ( 'NONE',  ( 5.959547316686252039, -19.82715097195158194, -5.308980600728387067 ) ) ;
#7808=CARTESIAN_POINT ( 'NONE',  ( 5.960721111146673579, -14.51823969584089902, -14.50930005615011709 ) ) ;
#7810=CARTESIAN_POINT ( 'NONE',  ( 0.9756008150404602564, 11.24277293639989317, 41.40938772927936640 ) ) ;
#7813=VERTEX_POINT ( 'NONE', #3615 ) ;
#7816=CARTESIAN_POINT ( 'NONE',  ( 0.9749527285493304607, 34.21468599366747299, -25.89384247702535902 ) ) ;
#7818=CARTESIAN_POINT ( 'NONE',  ( 2.526552050251863246, 20.43086833796958146, 37.81244156770998188 ) ) ;
#7819=EDGE_CURVE ( 'NONE', #10490, #42439, #36252, .T. ) ;
#7830=ADVANCED_FACE ( 'NONE', ( #12757 ), #24137, .F. ) ;
#7835=LINE ( 'NONE', #46087, #45634 ) ;
#7837=VECTOR ( 'NONE', #47602, 1000.000000000000114 ) ;
#7839=CARTESIAN_POINT ( 'NONE',  ( 0.5809828226811553087, 41.20389530892342833, -24.41822904836879715 ) ) ;
#7840=CARTESIAN_POINT ( 'NONE',  ( 0.9756950546413940550, 37.11135009583556865, -21.53795086961224570 ) ) ;
#7846=B_SPLINE_CURVE_WITH_KNOTS ( 'NONE', 3,
 ( #38100, #57145, #444, #47785, #19588, #57444 ),
 .UNSPECIFIED., .F., .F.,
 ( 4, 2, 4 ),
 ( 1.271478423208939840E-17, 0.0002445244328975392997, 0.0004890488657950658059 ),
 .UNSPECIFIED. ) ;
#7854=CARTESIAN_POINT ( 'NONE',  ( 5.960721111146673579, -18.96557324978293124, 7.848955554238177257 ) ) ;
#7855=B_SPLINE_CURVE_WITH_KNOTS ( 'NONE', 3,
 ( #11867, #17780, #51272, #8355, #46602, #3649 ),
 .UNSPECIFIED., .F., .F.,
 ( 4, 2, 4 ),
 ( 1.261454201589629882E-17, 0.0002445244328975406550, 0.0004890488657950686248 ),
 .UNSPECIFIED. ) ;
#7856=CARTESIAN_POINT ( 'NONE',  ( 3.407937589446178528, -13.63405474014707686, -1.331713209622645833 ) ) ;
#7857=ORIENTED_EDGE ( 'NONE', *, *, #8000, .T. ) ;
#7864=CARTESIAN_POINT ( 'NONE',  ( 4.963659409799330291, 43.79875484948460951, -9.199077662858449855 ) ) ;
#7868=CIRCLE ( 'NONE', #1826, 43.08621763946400307 ) ;
#7875=ORIENTED_EDGE ( 'NONE', *, *, #11583, .T. ) ;
#7878=CARTESIAN_POINT ( 'NONE',  ( 0.9757402383260944667, 16.34189654378434398, 39.67468066200765264 ) ) ;
#7884=EDGE_LOOP ( 'NONE', ( #25736, #19842, #3769, #35817 ) ) ;
#7888=CARTESIAN_POINT ( 'NONE',  ( 1.227938101723756947, 22.18841447410719780, 36.73927144310519566 ) ) ;
#7894=ORIENTED_EDGE ( 'NONE', *, *, #27677, .F. ) ;
#7898=DIRECTION ( 'NONE',  ( 0.000000000000000000, 0.000000000000000000, 1.000000000000000000 ) ) ;
#7899=EDGE_CURVE ( 'NONE', #9596, #8039, #22226, .T. ) ;
#7902=ORIENTED_EDGE ( 'NONE', *, *, #37074, .F. ) ;
#7904=CARTESIAN_POINT ( 'NONE',  ( 5.959547316686252039, -16.28190225198610008, -12.49803383497744136 ) ) ;
#7918=CARTESIAN_POINT ( 'NONE',  ( 5.959547316686252039, 5.315863417546055736, 19.82530672674364070 ) ) ;
#7921=CARTESIAN_POINT ( 'NONE',  ( 1.154321485836933947, 42.64911658695776708, 4.782433484301333415 ) ) ;
#7928=ORIENTED_EDGE ( 'NONE', *, *, #5980, .T. ) ;
#7935=ORIENTED_EDGE ( 'NONE', *, *, #46789, .F. ) ;
#7940=VECTOR ( 'NONE', #15419, 1000.000000000000000 ) ;
#7943=B_SPLINE_CURVE_WITH_KNOTS ( 'NONE', 3,
 ( #51531, #13664, #51846, #18363, #61243, #22739, #56850, #37475, #8017, #33085, #28357, #36546, #3918, #32451, #32768, #23057, #8309, #17735, #56238 ),
 .UNSPECIFIED., .F., .F.,
 ( 4, 3, 3, 3, 3, 3, 4 ),
 ( 1.734723475976807094E-18, 0.0002724573126191767855, 0.0004086839781548472846, 0.0005449106435901813778, 0.0006811373090491514579, 0.0008459866663933718681, 0.001010840725717217052 ),
 .UNSPECIFIED. ) ;
#7957=VECTOR ( 'NONE', #27671, 1000.000000000000227 ) ;
#7959=CARTESIAN_POINT ( 'NONE',  ( 0.5839879327111913154, 44.21534283185629022, -18.41291455875256489 ) ) ;
#7960=CARTESIAN_POINT ( 'NONE',  ( 0.9730545539215883499, 16.88610103448558064, 39.44597740938066721 ) ) ;
#7961=FACE_OUTER_BOUND ( 'NONE', #43830, .T. ) ;
#7971=DIRECTION ( 'NONE',  ( -0.07836865515943411409, -0.9649662368512201827, -0.2503967164834565162 ) ) ;
#7975=FACE_OUTER_BOUND ( 'NONE', #39087, .T. ) ;
#7982=CARTESIAN_POINT ( 'NONE',  ( 2.281351352603282479, 40.87339198768997051, 25.11567449372724425 ) ) ;
#7986=CARTESIAN_POINT ( 'NONE',  ( 2.281448460670567613, 7.562315317391745673, 47.37344300043614709 ) ) ;
#7988=CARTESIAN_POINT ( 'NONE',  ( 0.8557997880470606944, -19.17299735372040459, 43.90420959842174398 ) ) ;
#7992=EDGE_CURVE ( 'NONE', #60545, #2852, #34872, .T. ) ;
#7994=CARTESIAN_POINT ( 'NONE',  ( 0.8557997880470599172, -41.02602466100761802, -24.73961900479294584 ) ) ;
#8000=EDGE_CURVE ( 'NONE', #42030, #46817, #32656, .T. ) ;
#8002=CARTESIAN_POINT ( 'NONE',  ( 2.281351352603294913, 34.83869092251607213, -32.98025003937380717 ) ) ;
#8005=ORIENTED_EDGE ( 'NONE', *, *, #16560, .F. ) ;
#8017=CARTESIAN_POINT ( 'NONE',  ( 0.9758171775293909000, 41.44794628856080720, 11.09981579996821566 ) ) ;
#8021=CARTESIAN_POINT ( 'NONE',  ( 0.5807400328401637335, 47.55718917606843377, 5.711437504336126736 ) ) ;
#8028=CARTESIAN_POINT ( 'NONE',  ( 3.660176727303400934, -35.27264088192902136, 32.61164548483952785 ) ) ;
#8029=CARTESIAN_POINT ( 'NONE',  ( 5.959547316686252039, 20.35048796920733238, 2.675599016784604434 ) ) ;
#8030=ORIENTED_EDGE ( 'NONE', *, *, #27516, .F. ) ;
#8032=CARTESIAN_POINT ( 'NONE',  ( 2.624215991343608501, -47.98682984381860450, -1.411420423865975993 ) ) ;
#8033=CARTESIAN_POINT ( 'NONE',  ( 2.281351352603299354, 38.84542754822361132, -28.15073776031326602 ) ) ;
#8034=CARTESIAN_POINT ( 'NONE',  ( 5.974727161628369032, -18.96851388233664082, 7.840226266082205520 ) ) ;
#8038=CARTESIAN_POINT ( 'NONE',  ( 0.5838002273316446056, 41.41085122398249041, 24.06583301632217697 ) ) ;
#8039=VERTEX_POINT ( 'NONE', #45892 ) ;
#8041=VECTOR ( 'NONE', #56086, 1000.000000000000227 ) ;
#8047=CONICAL_SURFACE ( 'NONE', #3999, 42.88844316795388778, 0.04450589592585932341 ) ;
#8051=CARTESIAN_POINT ( 'NONE',  ( 5.974727161628367256, -20.52494643607030156, 0.01551142186642607071 ) ) ;
#8053=ADVANCED_FACE ( 'NONE', ( #60874 ), #49757, .F. ) ;
#8055=CARTESIAN_POINT ( 'NONE',  ( 0.8557997880470599172, 17.48760788519217257, 44.60232077416692675 ) ) ;
#8065=EDGE_LOOP ( 'NONE', ( #61323, #16368, #47865, #8270 ) ) ;
#8066=EDGE_CURVE ( 'NONE', #31261, #929, #43881, .T. ) ;
#8067=( BOUNDED_SURFACE ( )  B_SPLINE_SURFACE ( 3, 1, ( 
 ( #55641, #54714 ),
 ( #2409, #35965 ),
 ( #40984, #17154 ),
 ( #35653, #30305 ) ),
 .UNSPECIFIED., .F., .F., .F. ) 
 B_SPLINE_SURFACE_WITH_KNOTS ( ( 4, 4 ),
 ( 2, 2 ),
 ( 0.000000000000000000, 1.000000000000000000 ),
 ( 0.000000000000000000, 1.000000000000000000 ),
 .UNSPECIFIED. ) 
 GEOMETRIC_REPRESENTATION_ITEM ( )  RATIONAL_B_SPLINE_SURFACE ( (
 ( 1.000000000000000000, 1.000000000000000000),
 ( 0.9953390228620291325, 0.8624445117760984880),
 ( 0.9953390228620291325, 0.8624445117760984880),
 ( 1.000000000000000000, 1.000000000000000000) ) ) 
 REPRESENTATION_ITEM ( '' )  SURFACE ( )  );
#8070=CARTESIAN_POINT ( 'NONE',  ( 5.959828726073459926, -18.96492317065689193, -7.850628836606788674 ) ) ;
#8072=FACE_OUTER_BOUND ( 'NONE', #57018, .T. ) ;
#8077=LINE ( 'NONE', #35687, #23721 ) ;
#8081=ADVANCED_FACE ( 'NONE', ( #22065 ), #58155, .F. ) ;
#8089=CIRCLE ( 'NONE', #45101, 48.09070567114147110 ) ;
#8091=CARTESIAN_POINT ( 'NONE',  ( 0.8551540677456834771, -44.61036085020937492, -17.49081417858834087 ) ) ;
#8094=CARTESIAN_POINT ( 'NONE',  ( 4.963659409799330291, -3.403493583737629002, 44.62477100936214214 ) ) ;
#8096=CARTESIAN_POINT ( 'NONE',  ( 4.963659409799332067, -44.68724496494575504, 2.450325214228241233 ) ) ;
#8098=ORIENTED_EDGE ( 'NONE', *, *, #60955, .F. ) ;
#8100=DIRECTION ( 'NONE',  ( 0.000000000000000000, 0.000000000000000000, 1.000000000000000000 ) ) ;
#8103=CARTESIAN_POINT ( 'NONE',  ( 4.956653778116996811, 40.28700667097716348, -26.26162724282331951 ) ) ;
#8110=B_SPLINE_CURVE_WITH_KNOTS ( 'NONE', 3,
 ( #40701, #20639, #15951, #58515 ),
 .UNSPECIFIED., .F., .F.,
 ( 4, 4 ),
 ( 0.000000000000000000, 0.004048833967417087357 ),
 .UNSPECIFIED. ) ;
#8111=ORIENTED_EDGE ( 'NONE', *, *, #2312, .F. ) ;
#8113=ORIENTED_EDGE ( 'NONE', *, *, #19810, .F. ) ;
#8115=VERTEX_POINT ( 'NONE', #45573 ) ;
#8118=LINE ( 'NONE', #7482, #3379 ) ;
#8139=CARTESIAN_POINT ( 'NONE',  ( 0.8557997880470599172, 34.51495345639595058, -33.22501220301865033 ) ) ;
#8149=CARTESIAN_POINT ( 'NONE',  ( 5.960721111146673579, -16.28018152803701213, 12.50019045452710742 ) ) ;
#8150=CARTESIAN_POINT ( 'NONE',  ( 5.981074661064941900, -16.28853686865607386, 12.48781255314261607 ) ) ;
#8156=CARTESIAN_POINT ( 'NONE',  ( 0.5786265663353153954, -11.69877690266688219, 46.45062944555890994 ) ) ;
#8164=VERTEX_POINT ( 'NONE', #19844 ) ;
#8170=ADVANCED_FACE ( 'NONE', ( #19229 ), #551, .T. ) ;
#8182=CARTESIAN_POINT ( 'NONE',  ( 0.9754402186311947887, 16.59348191374138537, 39.57010335554335256 ) ) ;
#8184=DIRECTION ( 'NONE',  ( -0.07439287786467649322, -0.2453289374370202780, 0.9665813013808169929 ) ) ;
#8188=VERTEX_POINT ( 'NONE', #57094 ) ;
#8191=CARTESIAN_POINT ( 'NONE',  ( 0.9730545539215883499, -42.90536227157002003, -0.5054011016617259155 ) ) ;
#8196=CARTESIAN_POINT ( 'NONE',  ( 1.227938101723756947, -42.65467462194914816, -4.762198645644879491 ) ) ;
#8200=ADVANCED_FACE ( 'NONE', ( #9810 ), #13120, .F. ) ;
#8214=CARTESIAN_POINT ( 'NONE',  ( 0.6067099128993228563, 0.7089426894590579176, 47.89177823194876282 ) ) ;
#8220=CARTESIAN_POINT ( 'NONE',  ( 0.9749527285493316819, 37.01618455594573476, 21.70110358462052957 ) ) ;
#8222=CARTESIAN_POINT ( 'NONE',  ( 0.9752132459055862235, -37.27572867006947632, -21.25214916889629890 ) ) ;
#8225=CARTESIAN_POINT ( 'NONE',  ( 0.9730545539215892381, 39.44597740938061037, 16.88610103448572630 ) ) ;
#8227=VERTEX_POINT ( 'NONE', #4771 ) ;
#8230=CARTESIAN_POINT ( 'NONE',  ( 4.956653778116987041, -48.02038484091099235, -2.599733001514835884 ) ) ;
#8239=CARTESIAN_POINT ( 'NONE',  ( 0.9749527285493317930, -41.51939261707890694, 10.82939760924488581 ) ) ;
#8243=VECTOR ( 'NONE', #36010, 1000.000000000000227 ) ;
#8251=CARTESIAN_POINT ( 'NONE',  ( 0.6846871229502932144, -41.05093867799167384, -24.69859318104532164 ) ) ;
#8255=CARTESIAN_POINT ( 'NONE',  ( 3.660087539127319989, 30.71416465583057231, 36.93668088065460609 ) ) ;
#8265=DIRECTION ( 'NONE',  ( 0.000000000000000000, 0.000000000000000000, 1.000000000000000000 ) ) ;
#8270=ORIENTED_EDGE ( 'NONE', *, *, #18755, .F. ) ;
#8277=CARTESIAN_POINT ( 'NONE',  ( 0.7762783648524376190, -7.133808749409126904, -47.37038525648367937 ) ) ;
#8278=CARTESIAN_POINT ( 'NONE',  ( 0.9730545539215892381, -21.89037132892461912, 36.90443313492323085 ) ) ;
#8283=CARTESIAN_POINT ( 'NONE',  ( 0.6067099128993238555, 11.71051825714768135, -46.44339333106602652 ) ) ;
#8292=FACE_OUTER_BOUND ( 'NONE', #12144, .T. ) ;
#8293=CARTESIAN_POINT ( 'NONE',  ( 0.5839879882012665169, 12.39641777360522390, 46.26394433311391907 ) ) ;
#8295=CARTESIAN_POINT ( 'NONE',  ( 4.956653778116966613, 48.02038484091100656, 2.599733001514495712 ) ) ;
#8297=ORIENTED_EDGE ( 'NONE', *, *, #26239, .F. ) ;
#8299=DIRECTION ( 'NONE',  ( 0.07439287786467665975, 0.9903339163990680927, -0.1170659376278801317 ) ) ;
#8300=CARTESIAN_POINT ( 'NONE',  ( 0.5809828226811617480, 47.55412398569215071, -5.711058609464832792 ) ) ;
#8301=ORIENTED_EDGE ( 'NONE', *, *, #34172, .F. ) ;
#8305=DIRECTION ( 'NONE',  ( -1.000000000000000000, -0.000000000000000000, -0.000000000000000000 ) ) ;
#8309=CARTESIAN_POINT ( 'NONE',  ( 0.9741495583595169983, 41.34222751889826242, 11.48707840139599767 ) ) ;
#8323=ORIENTED_EDGE ( 'NONE', *, *, #56024, .F. ) ;
#8331=ORIENTED_EDGE ( 'NONE', *, *, #1677, .F. ) ;
#8335=ORIENTED_EDGE ( 'NONE', *, *, #31336, .T. ) ;
#8337=ORIENTED_EDGE ( 'NONE', *, *, #57983, .F. ) ;
#8341=CARTESIAN_POINT ( 'NONE',  ( 0.8551540677456739292, -43.91216198251525782, -19.17641535420899146 ) ) ;
#8343=CARTESIAN_POINT ( 'NONE',  ( 0.8557997880470599172, -7.156447707086029730, 47.37054680076704472 ) ) ;
#8351=CARTESIAN_POINT ( 'NONE',  ( -19.02632894112265305, -12.36669073209966641, -1.822342842981515831 ) ) ;
#8355=CARTESIAN_POINT ( 'NONE',  ( 0.7056555295713307085, 23.21854706865639173, -41.89804573586712166 ) ) ;
#8360=CARTESIAN_POINT ( 'NONE',  ( 5.960221823109900008, -7.849768660536680542, 18.96526051813967229 ) ) ;
#8362=CARTESIAN_POINT ( 'NONE',  ( 4.303969348037246512, 4.133486515473304479, 47.93217632892349656 ) ) ;
#8368=CARTESIAN_POINT ( 'NONE',  ( 4.303969348037258058, -10.35452842635876003, 46.98258166031687466 ) ) ;
#8371=DIRECTION ( 'NONE',  ( 0.07836865515943411409, -0.1223011693452849408, -0.9893941468723562727 ) ) ;
#8388=EDGE_CURVE ( 'NONE', #42119, #23449, #36112, .T. ) ;
#8393=ORIENTED_EDGE ( 'NONE', *, *, #10526, .T. ) ;
#8395=ORIENTED_EDGE ( 'NONE', *, *, #5351, .F. ) ;
#8398=DIRECTION ( 'NONE',  ( -0.07439287786467650709, 0.5100024374914878811, 0.8569499480575001327 ) ) ;
#8403=CARTESIAN_POINT ( 'NONE',  ( 0.5809828226811544205, -28.72298383114515374, 38.32755012159135077 ) ) ;
#8404=ORIENTED_EDGE ( 'NONE', *, *, #3043, .T. ) ;
#8414=DIRECTION ( 'NONE',  ( 0.000000000000000000, 0.000000000000000000, 1.000000000000000000 ) ) ;
#8415=CARTESIAN_POINT ( 'NONE',  ( 0.5832366564991506852, 29.37287047358880443, 37.83193087518319686 ) ) ;
#8418=ORIENTED_EDGE ( 'NONE', *, *, #25437, .T. ) ;
#8419=CARTESIAN_POINT ( 'NONE',  ( 0.9740398440564311811, 11.50548031350441924, 41.33716823241935856 ) ) ;
#8421=FACE_OUTER_BOUND ( 'NONE', #40563, .T. ) ;
#8422=EDGE_LOOP ( 'NONE', ( #3738, #47487, #20761, #27364 ) ) ;
#8423=VECTOR ( 'NONE', #28732, 1000.000000000000114 ) ;
#8425=CARTESIAN_POINT ( 'NONE',  ( 0.9741495583595166652, 34.28086552274328369, -25.80610403442874556 ) ) ;
#8437=CARTESIAN_POINT ( 'NONE',  ( 1.154321485836934835, 22.16897757994474460, 36.74718014677574018 ) ) ;
#8440=EDGE_CURVE ( 'NONE', #57079, #2634, #6437, .T. ) ;
#8442=CARTESIAN_POINT ( 'NONE',  ( 0.9756354156337442296, 21.56699035436992418, -37.09450626018190889 ) ) ;
#8443=CARTESIAN_POINT ( 'NONE',  ( 5.959547316686252039, -16.28190225198627061, 12.49803383497722642 ) ) ;
#8447=CARTESIAN_POINT ( 'NONE',  ( 0.5809828226811544205, 5.711058609466008740, -47.55412398569200150 ) ) ;
#8450=VECTOR ( 'NONE', #46629, 1000.000000000000000 ) ;
#8453=CARTESIAN_POINT ( 'NONE',  ( 4.956653778116992370, 14.93973939759951541, -45.71126949320233734 ) ) ;
#8456=CARTESIAN_POINT ( 'NONE',  ( 0.5263152470540364281, 0.000000000000000000, -42.88844316795388778 ) ) ;
#8462=FILL_AREA_STYLE ('',( #55772 ) ) ;
#8471=ORIENTED_EDGE ( 'NONE', *, *, #1913, .F. ) ;
#8481=CARTESIAN_POINT ( 'NONE',  ( 0.9756950546413933889, 16.50968749804439994, 39.60512406639350758 ) ) ;
#8490=EDGE_CURVE ( 'NONE', #20568, #23600, #15343, .T. ) ;
#8495=ORIENTED_EDGE ( 'NONE', *, *, #55429, .F. ) ;
#8498=B_SPLINE_CURVE_WITH_KNOTS ( 'NONE', 3,
 ( #18742, #41947, #42258, #37243, #23740, #42868, #23128, #61316, #37871, #56311, #13425, #56622, #13742, #32851, #9018, #28125, #47244, #848, #29354, #9632, #25277, #53155, #19357, #53754, #14664, #43486, #48461, #10570, #57529, #24662 ),
 .UNSPECIFIED., .F., .F.,
 ( 4, 2, 2, 2, 2, 2, 2, 2, 2, 2, 2, 2, 2, 2, 4 ),
 ( 0.006594498439790126912, 0.007418584928504671355, 0.007830628172861942710, 0.008242671417219215799, 0.008654714661576487153, 0.009066757905933758507, 0.009478801150291031596, 0.009890844394648302951, 0.01030288763900557431, 0.01071493088336284566, 0.01153901737207739184, 0.01195106061643467013, 0.01236310386079194669, 0.01277514710514922498, 0.01318719034950650328 ),
 .UNSPECIFIED. ) ;
#8505=DIRECTION ( 'NONE',  ( -0.07439287786467650709, -0.1432402660415156848, -0.9868880006907405633 ) ) ;
#8509=B_SPLINE_CURVE_WITH_KNOTS ( 'NONE', 3,
 ( #57113, #33353, #52421, #28936 ),
 .UNSPECIFIED., .F., .F.,
 ( 4, 4 ),
 ( 2.168404344971008868E-19, 0.004444878191957699932 ),
 .UNSPECIFIED. ) ;
#8521=LINE ( 'NONE', #53284, #31 ) ;
#8525=AXIS2_PLACEMENT_3D ( 'NONE', #28981, #32771, #52465 ) ;
#8526=CARTESIAN_POINT ( 'NONE',  ( 0.9730545539215883499, 36.90443313492330901, 21.89037132892449478 ) ) ;
#8528=CARTESIAN_POINT ( 'NONE',  ( 0.9745511491811765792, -36.98831798234360235, -21.74846188963815052 ) ) ;
#8537=VERTEX_POINT ( 'NONE', #44519 ) ;
#8538=ORIENTED_EDGE ( 'NONE', *, *, #50205, .T. ) ;
#8541=UNCERTAINTY_MEASURE_WITH_UNIT (LENGTH_MEASURE( 1.000000000000000082E-05 ), #57006, 'distance_accuracy_value', 'NONE');
#8543=VERTEX_POINT ( 'NONE', #15996 ) ;
#8545=CARTESIAN_POINT ( 'NONE',  ( 0.9752570700956795235, -10.88256294660683032, -41.50550328400880318 ) ) ;
#8546=EDGE_CURVE ( 'NONE', #2381, #23031, #37776, .T. ) ;
#8553=ORIENTED_EDGE ( 'NONE', *, *, #8769, .T. ) ;
#8561=CARTESIAN_POINT ( 'NONE',  ( 5.959828726073459926, 17.77796293532158955, 10.25888482581865802 ) ) ;
#8562=CONICAL_SURFACE ( 'NONE', #59585, 43.08621763946400307, 1.568696531533066763 ) ;
#8566=DIRECTION ( 'NONE',  ( 0.000000000000000000, 0.000000000000000000, 1.000000000000000000 ) ) ;
#8570=VERTEX_POINT ( 'NONE', #25687 ) ;
#8579=( BOUNDED_SURFACE ( )  B_SPLINE_SURFACE ( 3, 1, ( 
 ( #36100, #25742 ),
 ( #30429, #26056 ),
 ( #12287, #55164 ),
 ( #6921, #2545 ) ),
 .UNSPECIFIED., .F., .F., .F. ) 
 B_SPLINE_SURFACE_WITH_KNOTS ( ( 4, 4 ),
 ( 2, 2 ),
 ( 0.000000000000000000, 1.000000000000000000 ),
 ( 0.000000000000000000, 1.000000000000000000 ),
 .UNSPECIFIED. ) 
 GEOMETRIC_REPRESENTATION_ITEM ( )  RATIONAL_B_SPLINE_SURFACE ( (
 ( 1.000000000000000000, 1.000000000000000000),
 ( 0.9953390228620291325, 0.8624445117760984880),
 ( 0.9953390228620291325, 0.8624445117760984880),
 ( 1.000000000000000000, 1.000000000000000000) ) ) 
 REPRESENTATION_ITEM ( '' )  SURFACE ( )  );
#8580=ORIENTED_EDGE ( 'NONE', *, *, #12902, .T. ) ;
#8581=CARTESIAN_POINT ( 'NONE',  ( 0.8551540677456715978, -43.91216198251525782, -19.17641535420899856 ) ) ;
#8583=CARTESIAN_POINT ( 'NONE',  ( 0.7762777257811898091, -0.8897018348889329520, 47.89627391089018715 ) ) ;
#8585=CARTESIAN_POINT ( 'NONE',  ( 0.9757787079277444597, -42.54650880470565966, 5.561523338227001290 ) ) ;
#8586=B_SPLINE_CURVE_WITH_KNOTS ( 'NONE', 3,
 ( #47657, #4705, #42362, #58889, #48889, #43920 ),
 .UNSPECIFIED., .F., .F.,
 ( 4, 2, 4 ),
 ( 1.506204625983992411E-16, 0.0002445252820015214666, 0.0004890505640028923375 ),
 .UNSPECIFIED. ) ;
#8588=CARTESIAN_POINT ( 'NONE',  ( 0.9741495583595178864, 42.90659993968954922, 0.3955098476633079896 ) ) ;
#8590=CARTESIAN_POINT ( 'NONE',  ( 2.281448460670569833, -37.24544744441600130, 30.23587867650742211 ) ) ;
#8592=CARTESIAN_POINT ( 'NONE',  ( 5.959547316686252039, 10.25972575517505270, 17.77749189599220969 ) ) ;
#8596=CARTESIAN_POINT ( 'NONE',  ( 4.960156602257181468, 41.85906677498984862, -20.07163247083100188 ) ) ;
#8599=FACE_OUTER_BOUND ( 'NONE', #39049, .T. ) ;
#8600=EDGE_CURVE ( 'NONE', #7019, #36997, #52703, .T. ) ;
#8606=CARTESIAN_POINT ( 'NONE',  ( 1.088908134280554441, -36.76788378223844944, 22.12904883058541472 ) ) ;
#8620=EDGE_LOOP ( 'NONE', ( #6426, #42259, #57995, #60415 ) ) ;
#8622=LINE ( 'NONE', #13053, #40351 ) ;
#8632=CARTESIAN_POINT ( 'NONE',  ( 4.956653778116975495, 26.26162724282373517, 40.28700667097690769 ) ) ;
#8635=CARTESIAN_POINT ( 'NONE',  ( 0.8551540677456715978, -47.37911285756614888, -7.157691013574858374 ) ) ;
#8636=ORIENTED_EDGE ( 'NONE', *, *, #22285, .T. ) ;
#8643=ORIENTED_EDGE ( 'NONE', *, *, #60921, .F. ) ;
#8649=AXIS2_PLACEMENT_3D ( 'NONE', #10230, #54038, #59052 ) ;
#8650=VERTEX_POINT ( 'NONE', #16608 ) ;
#8652=CARTESIAN_POINT ( 'NONE',  ( 4.960156602257179692, 38.31207700265985494, -26.21519897043388525 ) ) ;
#8660=B_SPLINE_CURVE_WITH_KNOTS ( 'NONE', 3,
 ( #56121, #42671, #61734, #47070 ),
 .UNSPECIFIED., .F., .F.,
 ( 4, 4 ),
 ( 0.000000000000000000, 0.004446090762761357312 ),
 .UNSPECIFIED. ) ;
#8667=VECTOR ( 'NONE', #6506, 999.9999999999998863 ) ;
#8672=EDGE_CURVE ( 'NONE', #31407, #817, #45315, .T. ) ;
#8674=CARTESIAN_POINT ( 'NONE',  ( 4.960156602257181468, 20.07163247083145663, 41.85906677498964257 ) ) ;
#8679=VECTOR ( 'NONE', #46616, 1000.000000000000114 ) ;
#8689=ORIENTED_EDGE ( 'NONE', *, *, #44321, .T. ) ;
#8693=CARTESIAN_POINT ( 'NONE',  ( 4.967162193818130511, -8.839793687085512275, 42.16965968614191240 ) ) ;
#8700=ADVANCED_FACE ( 'NONE', ( #26931, #2485 ), #41357, .F. ) ;
#8705=CIRCLE ( 'NONE', #45716, 43.08621763946400307 ) ;
#8707=ORIENTED_EDGE ( 'NONE', *, *, #11426, .T. ) ;
#8708=CARTESIAN_POINT ( 'NONE',  ( 1.088313998177385944, -25.50107284445290645, -34.51470853099742442 ) ) ;
#8710=CARTESIAN_POINT ( 'NONE',  ( 4.967162193818130511, 24.30453456948160351, -35.57684288741949530 ) ) ;
#8713=B_SPLINE_CURVE_WITH_KNOTS ( 'NONE', 3,
 ( #59046, #15241, #54332, #34648, #44081, #39366 ),
 .UNSPECIFIED., .F., .F.,
 ( 4, 2, 4 ),
 ( 6.149443329761889321E-18, 0.0002445244328975385408, 0.0004890488657950710100 ),
 .UNSPECIFIED. ) ;
#8714=CARTESIAN_POINT ( 'NONE',  ( 4.967162193818130511, 0.000000000000000000, 0.000000000000000000 ) ) ;
#8728=CARTESIAN_POINT ( 'NONE',  ( 5.958863334805807099, -20.34989385289159713, 2.680345151634269563 ) ) ;
#8731=AXIS2_PLACEMENT_3D ( 'NONE', #33371, #56221, #47768 ) ;
#8734=CARTESIAN_POINT ( 'NONE',  ( 4.956653778116971054, 47.05699031914949160, 9.917440902361329691 ) ) ;
#8738=ORIENTED_EDGE ( 'NONE', *, *, #31114, .F. ) ;
#8742=EDGE_LOOP ( 'NONE', ( #29205, #37448, #8707, #12677 ) ) ;
#8745=CARTESIAN_POINT ( 'NONE',  ( 0.8557997880470599172, -0.9121262075949487791, 47.89938907511593413 ) ) ;
#8746=CARTESIAN_POINT ( 'NONE',  ( 4.303969348037246512, 14.52400616872432870, -45.86537346639043022 ) ) ;
#8749=CONICAL_SURFACE ( 'NONE', #19766, 43.08621763946400307, 1.568696531533066763 ) ;
#8750=ORIENTED_EDGE ( 'NONE', *, *, #36136, .F. ) ;
#8755=CARTESIAN_POINT ( 'NONE',  ( 4.967162193818130511, 0.000000000000000000, 0.000000000000000000 ) ) ;
#8757=B_SPLINE_CURVE_WITH_KNOTS ( 'NONE', 3,
 ( #22902, #37316, #42631, #60779 ),
 .UNSPECIFIED., .F., .F.,
 ( 4, 4 ),
 ( 8.335815620909995262E-17, 0.005004741218457509078 ),
 .UNSPECIFIED. ) ;
#8765=EDGE_CURVE ( 'NONE', #61767, #13813, #42317, .T. ) ;
#8768=CARTESIAN_POINT ( 'NONE',  ( 5.959547316686252039, 17.77392908783934189, -10.26589671991344588 ) ) ;
#8769=EDGE_CURVE ( 'NONE', #45625, #51992, #27539, .T. ) ;
#8770=CARTESIAN_POINT ( 'NONE',  ( 0.5807400328401574052, 18.83234461715242247, -44.04145271122545324 ) ) ;
#8774=CARTESIAN_POINT ( 'NONE',  ( 5.959828726073459926, 5.316791119501089291, -19.82504517499707575 ) ) ;
#8775=ADVANCED_FACE ( 'NONE', ( #19620 ), #30648, .F. ) ;
#8780=CARTESIAN_POINT ( 'NONE',  ( 0.5837374860065639437, 46.31070423340730713, 12.22086613152778689 ) ) ;
#8787=B_SPLINE_CURVE_WITH_KNOTS ( 'NONE', 3,
 ( #25654, #59154, #35387, #54763, #49772, #6832, #25973, #45106, #2133, #11897, #30979, #50089, #36620, #3074, #24277, #38712, #27205, #22201, #60695 ),
 .UNSPECIFIED., .F., .F.,
 ( 4, 3, 3, 3, 3, 3, 4 ),
 ( 6.938893903907228378E-18, 0.0002724573126191740208, 0.0004086839781548500493, 0.0005449106435901848473, 0.0006811373090491499400, 0.0008459866663933689407, 0.001010840725717213149 ),
 .UNSPECIFIED. ) ;
#8796=CARTESIAN_POINT ( 'NONE',  ( 0.5827357941260203900, -6.611647889510890330, -47.43746130990125209 ) ) ;
#8805=CARTESIAN_POINT ( 'NONE',  ( 0.9730545539215883499, 0.5054011016618756846, -42.90536227157002003 ) ) ;
#8807=ORIENTED_EDGE ( 'NONE', *, *, #6062, .F. ) ;
#8809=AXIS2_PLACEMENT_3D ( 'NONE', #40609, #59673, #51199 ) ;
#8816=CARTESIAN_POINT ( 'NONE',  ( 0.5832366564991503521, -34.05963937630778560, -33.67434452455949412 ) ) ;
#8817=CARTESIAN_POINT ( 'NONE',  ( 4.967162193818130511, -28.74031574030035685, 32.10009971360062764 ) ) ;
#8830=FACE_OUTER_BOUND ( 'NONE', #27064, .T. ) ;
#8831=CARTESIAN_POINT ( 'NONE',  ( 0.6846871229502899947, 29.84551600520632419, 37.47592888575258741 ) ) ;
#8843=EDGE_CURVE ( 'NONE', #18602, #6564, #61679, .T. ) ;
#8846=CARTESIAN_POINT ( 'NONE',  ( 5.960721111146673579, 5.318514366754659939, 19.82454228767747750 ) ) ;
#8849=CARTESIAN_POINT ( 'NONE',  ( 1.154321485836933503, -41.66001465002020154, -10.30834589251754885 ) ) ;
#8868=CARTESIAN_POINT ( 'NONE',  ( 0.9730545539215883499, -10.61654491617534291, -41.57420493492396929 ) ) ;
#8889=CARTESIAN_POINT ( 'NONE',  ( 4.956653778116971942, 35.79382859084115864, 32.11725092155054995 ) ) ;
#8891=DIRECTION ( 'NONE',  ( 0.07439287786467665975, -0.4871392060438023974, -0.8701500408883660054 ) ) ;
#8895=CARTESIAN_POINT ( 'NONE',  ( 0.9741495583595178864, -30.05988007970374198, -30.61921547032183355 ) ) ;
#8906=CARTESIAN_POINT ( 'NONE',  ( 0.5809828226811556418, 44.45562576850601744, 17.82437196699697424 ) ) ;
#8907=DIRECTION ( 'NONE',  ( 0.07836865515943411409, 0.8672783706145194005, -0.4916162952473462910 ) ) ;
#8911=CARTESIAN_POINT ( 'NONE',  ( 5.960721111146673579, -14.50930005615006912, -14.51823969584094698 ) ) ;
#8912=CARTESIAN_POINT ( 'NONE',  ( 5.959547316686252039, -19.82715097195166010, 5.308980600728112620 ) ) ;
#8919=CARTESIAN_POINT ( 'NONE',  ( 0.5850706913938534814, -24.10530971368259401, -41.38834827854233112 ) ) ;
#8926=B_SPLINE_CURVE_WITH_KNOTS ( 'NONE', 3,
 ( #49851, #21658, #40799, #36089 ),
 .UNSPECIFIED., .F., .F.,
 ( 4, 4 ),
 ( 5.057544569639794935E-18, 0.004050076154992999014 ),
 .UNSPECIFIED. ) ;
#8932=CARTESIAN_POINT ( 'NONE',  ( 4.956653778116827169, 32.11725092155053574, 35.79382859084104496 ) ) ;
#8935=CIRCLE ( 'NONE', #37990, 48.09070567114147110 ) ;
#8938=CARTESIAN_POINT ( 'NONE',  ( 0.5800708057587388167, 17.74761804745402571, 44.48635630048006107 ) ) ;
#8944=VERTEX_POINT ( 'NONE', #16147 ) ;
#8954=EDGE_CURVE ( 'NONE', #19678, #28808, #7438, .T. ) ;
#8959=CARTESIAN_POINT ( 'NONE',  ( 0.5800708119828335008, -11.78915056783740489, 46.42229822050692434 ) ) ;
#8960=VERTEX_POINT ( 'NONE', #10832 ) ;
#8962=CARTESIAN_POINT ( 'NONE',  ( 5.981074661064941900, 20.52466374824937034, -0.008585178657404223673 ) ) ;
#8967=EDGE_CURVE ( 'NONE', #22241, #56714, #44545, .T. ) ;
#8968=CARTESIAN_POINT ( 'NONE',  ( 0.6846871229502899947, -17.53234844287773697, 44.58493949243999310 ) ) ;
#8971=ORIENTED_EDGE ( 'NONE', *, *, #44937, .T. ) ;
#8979=ORIENTED_EDGE ( 'NONE', *, *, #57457, .T. ) ;
#8983=CARTESIAN_POINT ( 'NONE',  ( 0.5832366564991509073, -18.58038995918320779, -44.14509737861668981 ) ) ;
#8988=ORIENTED_EDGE ( 'NONE', *, *, #52156, .T. ) ;
#8991=VERTEX_POINT ( 'NONE', #17376 ) ;
#8996=CARTESIAN_POINT ( 'NONE',  ( 0.9722240741986377666, 41.59310805473383255, -10.54237114526840102 ) ) ;
#8998=CARTESIAN_POINT ( 'NONE',  ( 5.959828726073459926, 18.96492317065693811, -7.850628836606658112 ) ) ;
#9003=CARTESIAN_POINT ( 'NONE',  ( 4.967162193818130511, 0.000000000000000000, 0.000000000000000000 ) ) ;
#9007=CARTESIAN_POINT ( 'NONE',  ( 0.8551540677456834771, 23.16399837394605044, -41.94570365541178347 ) ) ;
#9008=CARTESIAN_POINT ( 'NONE',  ( 5.960721111146673579, -2.672857320903454514, 20.35079619394241135 ) ) ;
#9013=CARTESIAN_POINT ( 'NONE',  ( 3.783278058412225864, -24.80906179324464844, 35.16831859152123485 ) ) ;
#9015=ORIENTED_EDGE ( 'NONE', *, *, #12328, .F. ) ;
#9016=CARTESIAN_POINT ( 'NONE',  ( 0.9756950546413942771, 11.01205619898776611, -41.47131842451888417 ) ) ;
#9017=DIRECTION ( 'NONE',  ( 0.000000000000000000, 0.000000000000000000, 1.000000000000000000 ) ) ;
#9018=CARTESIAN_POINT ( 'NONE',  ( -20.07366590805694173, -7.999991050865260966, -0.1389904710012628553 ) ) ;
#9020=CARTESIAN_POINT ( 'NONE',  ( 4.960156602257182357, 25.36362146861383948, 38.88108289790868355 ) ) ;
#9021=CARTESIAN_POINT ( 'NONE',  ( 2.281351352603293581, -42.18750813859374205, 22.83955855331502249 ) ) ;
#9022=ORIENTED_EDGE ( 'NONE', *, *, #27947, .F. ) ;
#9030=CARTESIAN_POINT ( 'NONE',  ( 1.227938101723756947, -22.18841447410693846, -36.73927144310534487 ) ) ;
#9032=CARTESIAN_POINT ( 'NONE',  ( 0.9730545539215883499, 21.01499094264548972, 37.40983423658480689 ) ) ;
#9042=VERTEX_POINT ( 'NONE', #19239 ) ;
#9048=ORIENTED_EDGE ( 'NONE', *, *, #31687, .F. ) ;
#9051=B_SPLINE_CURVE_WITH_KNOTS ( 'NONE', 3,
 ( #47774, #19271, #4820, #51212, #18350, #37462 ),
 .UNSPECIFIED., .F., .F.,
 ( 4, 2, 4 ),
 ( 8.673617379884035472E-19, 0.0002291966416970791869, 0.0004583932833941575065 ),
 .UNSPECIFIED. ) ;
#9054=( BOUNDED_SURFACE ( )  B_SPLINE_SURFACE ( 3, 1, ( 
 ( #37297, #42009 ),
 ( #61070, #42313 ),
 ( #18184, #47012 ),
 ( #51674, #8770 ) ),
 .UNSPECIFIED., .F., .F., .F. ) 
 B_SPLINE_SURFACE_WITH_KNOTS ( ( 4, 4 ),
 ( 2, 2 ),
 ( 0.000000000000000000, 1.000000000000000000 ),
 ( 0.000000000000000000, 1.000000000000000000 ),
 .UNSPECIFIED. ) 
 GEOMETRIC_REPRESENTATION_ITEM ( )  RATIONAL_B_SPLINE_SURFACE ( (
 ( 1.000000000000000000, 1.000000000000000000),
 ( 0.9732289882329797637, 0.9999525324661233672),
 ( 0.9732289882329797637, 0.9999525324661233672),
 ( 1.000000000000000000, 1.000000000000000000) ) ) 
 REPRESENTATION_ITEM ( '' )  SURFACE ( )  );
#9058=CARTESIAN_POINT ( 'NONE',  ( 4.963659409799328515, -33.96111158240268679, 29.14784479683099860 ) ) ;
#9059=CARTESIAN_POINT ( 'NONE',  ( 1.154321485836934391, -26.77578840293013940, -33.53917069757678604 ) ) ;
#9067=CARTESIAN_POINT ( 'NONE',  ( 4.963659409799330291, 44.68724496494573373, -2.450325214228551651 ) ) ;
#9069=CARTESIAN_POINT ( 'NONE',  ( 4.963659409799332067, 33.33129552235085669, 29.86601237216419236 ) ) ;
#9073=CARTESIAN_POINT ( 'NONE',  ( 0.5809828226811553087, 47.89273459658653564, -0.5448590168534052092 ) ) ;
#9074=B_SPLINE_CURVE_WITH_KNOTS ( 'NONE', 3,
 ( #53053, #49280, #10155, #57739, #24562, #48365 ),
 .UNSPECIFIED., .F., .F.,
 ( 4, 2, 4 ),
 ( 9.341771812940338307E-18, 0.0002291978881530158348, 0.0004583957763060222913 ),
 .UNSPECIFIED. ) ;
#9075=CARTESIAN_POINT ( 'NONE',  ( 2.624215991343608501, 47.39206852872457887, 7.662883702704825772 ) ) ;
#9077=CARTESIAN_POINT ( 'NONE',  ( 4.960156602257182357, -45.62767441207056862, 8.553784487772720269 ) ) ;
#9081=CARTESIAN_POINT ( 'NONE',  ( 0.5786265663353196143, -46.07681357296475255, -13.09387673186383516 ) ) ;
#9086=CARTESIAN_POINT ( 'NONE',  ( 5.959547316686252039, 17.77392908783919978, 10.26589671991369457 ) ) ;
#9090=CARTESIAN_POINT ( 'NONE',  ( 0.5800708119828336118, -46.09746484493488339, 13.00144522946642489 ) ) ;
#9092=B_SPLINE_CURVE_WITH_KNOTS ( 'NONE', 3,
 ( #46469, #32673, #37079, #56147, #46785, #56451 ),
 .UNSPECIFIED., .F., .F.,
 ( 4, 2, 4 ),
 ( 9.543442895606953578E-18, 0.0002291978881530148048, 0.0004583957763060200687 ),
 .UNSPECIFIED. ) ;
#9098=VERTEX_POINT ( 'NONE', #33343 ) ;
#9101=VERTEX_POINT ( 'NONE', #392 ) ;
#9102=CARTESIAN_POINT ( 'NONE',  ( 0.5837374860065638327, -6.431731162805466084, -47.46223477511620104 ) ) ;
#9107=ORIENTED_EDGE ( 'NONE', *, *, #12328, .T. ) ;
#9110=CARTESIAN_POINT ( 'NONE',  ( 1.154321713695928286, 0.8253077511132634880, -42.90848032340444007 ) ) ;
#9117=CARTESIAN_POINT ( 'NONE',  ( 5.981074661064941900, 2.670494474391997386, -20.35019299530686254 ) ) ;
#9121=CARTESIAN_POINT ( 'NONE',  ( 0.5809828226811544205, -34.25055090842130312, -33.48000389720652947 ) ) ;
#9131=CARTESIAN_POINT ( 'NONE',  ( 1.227938101723748288, 4.762198645644436290, 42.65467462194920500 ) ) ;
#9136=LINE ( 'NONE', #37992, #43980 ) ;
#9138=FACE_OUTER_BOUND ( 'NONE', #14138, .T. ) ;
#9142=CARTESIAN_POINT ( 'NONE',  ( 0.5807400328401574052, 37.66660715020906736, -29.58941477092977124 ) ) ;
#9146=CARTESIAN_POINT ( 'NONE',  ( 0.9730545539215892381, 25.71816799638828499, -34.34678117142529175 ) ) ;
#9147=CARTESIAN_POINT ( 'NONE',  ( 0.9757892942422822236, 30.30456399643835042, -30.37715353261962647 ) ) ;
#9151=CIRCLE ( 'NONE', #25157, 43.08621763946400307 ) ;
#9153=CARTESIAN_POINT ( 'NONE',  ( 0.5809828226811617480, -29.58751527316205809, 37.66417181417541826 ) ) ;
#9155=CARTESIAN_POINT ( 'NONE',  ( 0.9754402186311948997, -37.25324696807214764, -21.29160191075036224 ) ) ;
#9162=LINE ( 'NONE', #3833, #4660 ) ;
#9163=VERTEX_POINT ( 'NONE', #30450 ) ;
#9164=CARTESIAN_POINT ( 'NONE',  ( 0.5827357941260207230, -33.60975216782508568, 34.12346967353447269 ) ) ;
#9169=CARTESIAN_POINT ( 'NONE',  ( 0.9752132459055850022, -11.33038172416123679, -41.38545930839059395 ) ) ;
#9172=CARTESIAN_POINT ( 'NONE',  ( 0.9745511491811756910, -41.53317535253980708, 10.77620558745922352 ) ) ;
#9174=VERTEX_POINT ( 'NONE', #35494 ) ;
#9176=CARTESIAN_POINT ( 'NONE',  ( 0.5837374860065638327, -12.57177159055130389, -46.21667939904229172 ) ) ;
#9178=CARTESIAN_POINT ( 'NONE',  ( 4.967162193818130511, 32.10009971360111791, -28.74031574029977776 ) ) ;
#9188=B_SPLINE_CURVE_WITH_KNOTS ( 'NONE', 3,
 ( #10758, #29848, #44596, #20770 ),
 .UNSPECIFIED., .F., .F.,
 ( 4, 4 ),
 ( 9.697399036122160616E-19, 0.004050076154992999014 ),
 .UNSPECIFIED. ) ;
#9190=CARTESIAN_POINT ( 'NONE',  ( 0.5850706913938534814, -44.18063951072233664, 18.49682194437948723 ) ) ;
#9198=EDGE_LOOP ( 'NONE', ( #61449, #54592, #49997, #27287 ) ) ;
#9216=CARTESIAN_POINT ( 'NONE',  ( 0.9722240750034599754, -21.95618656573978456, -36.86535092060696428 ) ) ;
#9219=CARTESIAN_POINT ( 'NONE',  ( 4.960156602257182357, -9.558288641082077319, 45.42786611289310628 ) ) ;
#9221=CARTESIAN_POINT ( 'NONE',  ( 0.5807400328401574052, 12.92266817606014762, 46.12278621143501312 ) ) ;
#9235=ORIENTED_EDGE ( 'NONE', *, *, #29359, .F. ) ;
#9237=CARTESIAN_POINT ( 'NONE',  ( 0.8557997880470697982, -37.44587306708118035, 29.88293891557457371 ) ) ;
#9239=CARTESIAN_POINT ( 'NONE',  ( 0.8551540677456739292, 33.23105123575900421, 34.52115452272940388 ) ) ;
#9257=EDGE_CURVE ( 'NONE', #14998, #26349, #10499, .T. ) ;
#9258=VERTEX_POINT ( 'NONE', #12619 ) ;
#9263=CARTESIAN_POINT ( 'NONE',  ( 0.8557997880470599172, -47.89938907511592703, -0.9121262075951160897 ) ) ;
#9269=FACE_OUTER_BOUND ( 'NONE', #14500, .T. ) ;
#9280=CARTESIAN_POINT ( 'NONE',  ( 0.5839254010752159552, -0.09079837481654944031, 47.89590033178485129 ) ) ;
#9282=EDGE_CURVE ( 'NONE', #45511, #17579, #59398, .T. ) ;
#9290=B_SPLINE_CURVE_WITH_KNOTS ( 'NONE', 3,
 ( #37553, #27509, #8094, #27206 ),
 .UNSPECIFIED., .F., .F.,
 ( 4, 4 ),
 ( 6.961759998889881502E-17, 0.005004741218457482189 ),
 .UNSPECIFIED. ) ;
#9299=CARTESIAN_POINT ( 'NONE',  ( 0.9754402186311948997, 5.414674803234379219, -42.56545569314703670 ) ) ;
#9313=CARTESIAN_POINT ( 'NONE',  ( 4.956653778116966613, 0.000000000000000000, 0.000000000000000000 ) ) ;
#9316=CARTESIAN_POINT ( 'NONE',  ( 0.9756950546413942771, 42.52863374229713855, -5.696573146291551204 ) ) ;
#9318=ORIENTED_EDGE ( 'NONE', *, *, #14753, .T. ) ;
#9328=CARTESIAN_POINT ( 'NONE',  ( 0.9972139404380306882, -20.88226186415256791, 37.48536715150219578 ) ) ;
#9334=CARTESIAN_POINT ( 'NONE',  ( 0.5809828226811553087, -29.58751527316153940, -37.66417181417581617 ) ) ;
#9335=CARTESIAN_POINT ( 'NONE',  ( 1.154321485836934169, 42.90848031452335931, -0.8253076867720463561 ) ) ;
#9336=EDGE_LOOP ( 'NONE', ( #57439, #15063, #12618, #803, #4401, #57375 ) ) ;
#9348=CARTESIAN_POINT ( 'NONE',  ( 0.5809828226811617480, -5.711058609464997105, -47.55412398569212939 ) ) ;
#9356=CARTESIAN_POINT ( 'NONE',  ( 0.9754642270333693244, 0.1757168848625156043, -42.90808635884410194 ) ) ;
#9360=VERTEX_POINT ( 'NONE', #38586 ) ;
#9363=CARTESIAN_POINT ( 'NONE',  ( 5.981074661064941900, -19.82752479807523827, -5.303881226583607500 ) ) ;
#9372=CARTESIAN_POINT ( 'NONE',  ( 0.9752570700956783023, -21.65368877244782553, 37.04395688491842975 ) ) ;
#9374=CARTESIAN_POINT ( 'NONE',  ( 0.7056555295713335951, -34.46100226633713959, -33.27140645154231180 ) ) ;
#9378=CARTESIAN_POINT ( 'NONE',  ( 0.5800708119828333897, -46.42229822050688171, -11.78915056783756832 ) ) ;
#9379=FACE_OUTER_BOUND ( 'NONE', #20756, .T. ) ;
#9383=AXIS2_PLACEMENT_3D ( 'NONE', #33100, #23073, #22447 ) ;
#9388=VERTEX_POINT ( 'NONE', #52031 ) ;
#9390=CARTESIAN_POINT ( 'NONE',  ( 0.5809828226811553087, 46.40184912890838831, 11.86925843957183879 ) ) ;
#9392=ORIENTED_EDGE ( 'NONE', *, *, #21746, .F. ) ;
#9393=CARTESIAN_POINT ( 'NONE',  ( 0.8557997880470697982, -46.03118133706034598, 13.27832040216623355 ) ) ;
#9397=CARTESIAN_POINT ( 'NONE',  ( 2.624215991343620935, 45.98641578154050791, -13.78323291683735796 ) ) ;
#9398=CARTESIAN_POINT ( 'NONE',  ( 4.963659409799330291, 2.450325214229022830, -44.68724496494571952 ) ) ;
#9404=CARTESIAN_POINT ( 'NONE',  ( 0.5809828226811617480, -17.82437196699647686, -44.45562576850621639 ) ) ;
#9407=CARTESIAN_POINT ( 'NONE',  ( 0.5827359174754822568, -5.891371786504645769, -47.53228759166454864 ) ) ;
#9413=CARTESIAN_POINT ( 'NONE',  ( 5.974727161628367256, 16.27409205901376055, -12.50710176109990890 ) ) ;
#9414=EDGE_CURVE ( 'NONE', #6735, #47955, #11545, .T. ) ;
#9417=CARTESIAN_POINT ( 'NONE',  ( 2.624215991343608501, -37.21129343241584309, -30.33228621715073459 ) ) ;
#9419=CARTESIAN_POINT ( 'NONE',  ( 0.9730545539215883499, -15.95224156741799426, -39.83279466599056917 ) ) ;
#9421=FACE_OUTER_BOUND ( 'NONE', #44600, .T. ) ;
#9424=CARTESIAN_POINT ( 'NONE',  ( 5.959547316686252039, -5.308980600728319565, -19.82715097195160325 ) ) ;
#9425=EDGE_CURVE ( 'NONE', #33472, #11600, #8586, .T. ) ;
#9428=ORIENTED_EDGE ( 'NONE', *, *, #8843, .T. ) ;
#9441=CARTESIAN_POINT ( 'NONE',  ( 0.8551540677456715978, 24.74404575822775598, 41.03346287276436755 ) ) ;
#9444=CARTESIAN_POINT ( 'NONE',  ( 5.959547316686252039, -16.28624005235107930, 12.49238070347948870 ) ) ;
#9447=CARTESIAN_POINT ( 'NONE',  ( 0.5809828226811553087, -46.11980934799348830, 12.92184523170186594 ) ) ;
#9455=CARTESIAN_POINT ( 'NONE',  ( 0.9722240750034573109, -41.59310803641454868, -10.54237121715129177 ) ) ;
#9468=ORIENTED_EDGE ( 'NONE', *, *, #21369, .F. ) ;
#9469=CARTESIAN_POINT ( 'NONE',  ( 0.5837374860065641657, -33.73893264285572968, 33.99581326751421528 ) ) ;
#9472=VERTEX_POINT ( 'NONE', #25698 ) ;
#9476=EDGE_CURVE ( 'NONE', #4600, #50690, #44476, .T. ) ;
#9477=VERTEX_POINT ( 'NONE', #39209 ) ;
#9484=DIRECTION ( 'NONE',  ( 0.000000000000000000, 0.000000000000000000, 1.000000000000000000 ) ) ;
#9487=ORIENTED_EDGE ( 'NONE', *, *, #45842, .T. ) ;
#9489=AXIS2_PLACEMENT_3D ( 'NONE', #27123, #26814, #21811 ) ;
#9491=LINE ( 'NONE', #57698, #49981 ) ;
#9494=CARTESIAN_POINT ( 'NONE',  ( 5.958863334805807099, 18.96369761673819809, -7.853699934219702250 ) ) ;
#9498=CARTESIAN_POINT ( 'NONE',  ( 5.860006189529246790, -9.393028332204430342, -47.30964106197868091 ) ) ;
#9509=CARTESIAN_POINT ( 'NONE',  ( 4.967162193818130511, -8.839793687084915419, -42.16965968614202609 ) ) ;
#9511=ORIENTED_EDGE ( 'NONE', *, *, #7147, .T. ) ;
#9520=CARTESIAN_POINT ( 'NONE',  ( 4.956653778116997699, 42.88673967249161478, -21.75875759808661059 ) ) ;
#9533=EDGE_CURVE ( 'NONE', #7813, #39205, #37037, .T. ) ;
#9537=CARTESIAN_POINT ( 'NONE',  ( 0.5837374860065657201, 12.57177159055162008, 46.21667939904217093 ) ) ;
#9542=ORIENTED_EDGE ( 'NONE', *, *, #50112, .T. ) ;
#9545=CARTESIAN_POINT ( 'NONE',  ( 3.783198216974387851, -31.62918462580860535, 29.18723368117353090 ) ) ;
#9547=EDGE_CURVE ( 'NONE', #33579, #48168, #28023, .T. ) ;
#9548=FACE_OUTER_BOUND ( 'NONE', #58302, .T. ) ;
#9554=VERTEX_POINT ( 'NONE', #46070 ) ;
#9564=CARTESIAN_POINT ( 'NONE',  ( 0.5834872094924161701, 38.13619618345251183, -28.97678700412145858 ) ) ;
#9572=CARTESIAN_POINT ( 'NONE',  ( 1.154321713695929397, 15.65787958845416661, 39.95809834491002732 ) ) ;
#9581=VERTEX_POINT ( 'NONE', #32261 ) ;
#9593=CARTESIAN_POINT ( 'NONE',  ( 0.9968887458511656030, 26.64009929991552994, -33.63815526548957280 ) ) ;
#9596=VERTEX_POINT ( 'NONE', #60422 ) ;
#9602=CARTESIAN_POINT ( 'NONE',  ( 3.270143674763207553, 11.71453292426889270, -7.080034332678136089 ) ) ;
#9611=CARTESIAN_POINT ( 'NONE',  ( 1.227938101723748288, -41.66816631169199070, 10.28900963485366127 ) ) ;
#9617=CIRCLE ( 'NONE', #23618, 43.08621763946400307 ) ;
#9618=CARTESIAN_POINT ( 'NONE',  ( 0.5807400328401574052, -46.40483864045153695, 11.87003418057227044 ) ) ;
#9619=EDGE_CURVE ( 'NONE', #54223, #24092, #42541, .T. ) ;
#9622=EDGE_LOOP ( 'NONE', ( #28453, #33189 ) ) ;
#9627=CARTESIAN_POINT ( 'NONE',  ( 0.9756008150404608115, 42.52260101821271121, -5.741579752919210300 ) ) ;
#9628=CARTESIAN_POINT ( 'NONE',  ( 0.6067375320500724145, -11.71046088714719424, -46.44340905096873939 ) ) ;
#9629=ORIENTED_EDGE ( 'NONE', *, *, #19274, .F. ) ;
#9632=CARTESIAN_POINT ( 'NONE',  ( -19.80804008900104307, -7.933751071888869077, 1.058477306457110689 ) ) ;
#9633=CARTESIAN_POINT ( 'NONE',  ( 0.9730545539215883499, -37.40983423658487794, 21.01499094264535472 ) ) ;
#9634=EDGE_LOOP ( 'NONE', ( #20675, #36236, #53453, #58942 ) ) ;
#9635=EDGE_CURVE ( 'NONE', #38949, #9360, #22738, .T. ) ;
#9642=ORIENTED_EDGE ( 'NONE', *, *, #9425, .F. ) ;
#9643=CARTESIAN_POINT ( 'NONE',  ( 0.7762783648524368418, -29.86325223096987358, -37.45705264446610272 ) ) ;
#9646=VERTEX_POINT ( 'NONE', #46991 ) ;
#9650=CARTESIAN_POINT ( 'NONE',  ( 4.963659409799330291, 40.34793212403968710, 19.36487359954713483 ) ) ;
#9651=CARTESIAN_POINT ( 'NONE',  ( 4.967162193818130511, 38.44485641567072776, 19.45289607368836116 ) ) ;
#9658=ORIENTED_EDGE ( 'NONE', *, *, #32338, .F. ) ;
#9661=AXIS2_PLACEMENT_3D ( 'NONE', #16892, #36007, #30645 ) ;
#9663=CARTESIAN_POINT ( 'NONE',  ( 5.960221823109900008, 16.28736530777573321, 12.49086489703233482 ) ) ;
#9666=CARTESIAN_POINT ( 'NONE',  ( 2.624215991343620935, -4.864192649745717745, 47.76052319582214523 ) ) ;
#9667=FACE_OUTER_BOUND ( 'NONE', #49800, .T. ) ;
#9668=EDGE_LOOP ( 'NONE', ( #56954, #26057, #40425, #47945 ) ) ;
#9669=VECTOR ( 'NONE', #15946, 1000.000000000000114 ) ;
#9676=CARTESIAN_POINT ( 'NONE',  ( 5.959828726073459926, 12.49160845136034936, -16.28681682518051588 ) ) ;
#9678=ORIENTED_EDGE ( 'NONE', *, *, #11192, .T. ) ;
#9682=CARTESIAN_POINT ( 'NONE',  ( 4.960156602257181468, -43.79161740034464856, -15.40604254112689731 ) ) ;
#9684=FACE_OUTER_BOUND ( 'NONE', #947, .T. ) ;
#9685=ORIENTED_EDGE ( 'NONE', *, *, #45229, .T. ) ;
#9698=FACE_OUTER_BOUND ( 'NONE', #25135, .T. ) ;
#9705=ORIENTED_EDGE ( 'NONE', *, *, #22576, .T. ) ;
#9707=MANIFOLD_SOLID_BREP ( 'M5 Tapped Hole1', #5024 ) ;
#9708=B_SPLINE_CURVE_WITH_KNOTS ( 'NONE', 3,
 ( #15296, #20905, #39420, #39115 ),
 .UNSPECIFIED., .F., .F.,
 ( 4, 4 ),
 ( 2.602085213965211027E-18, 0.004050076154993003351 ),
 .UNSPECIFIED. ) ;
#9710=CARTESIAN_POINT ( 'NONE',  ( 0.9740398440564311811, -36.95080095316289714, 21.81228698783128905 ) ) ;
#9713=CARTESIAN_POINT ( 'NONE',  ( 0.8557997880470697982, -5.347802024197571669, 47.60865952216997243 ) ) ;
#9718=CARTESIAN_POINT ( 'NONE',  ( 4.956653778116995035, 36.51451553856460919, -31.29546495791814209 ) ) ;
#9722=CARTESIAN_POINT ( 'NONE',  ( 1.227938101723756947, 0.8460948827225182045, 42.91134962331487657 ) ) ;
#9725=CARTESIAN_POINT ( 'NONE',  ( 5.960221823109900008, 20.52559243573973546, 0.005450390361793623108 ) ) ;
#9727=CARTESIAN_POINT ( 'NONE',  ( 0.5809828226811553087, 0.5448590168532381206, 47.89273459658653564 ) ) ;
#9730=B_SPLINE_CURVE_WITH_KNOTS ( 'NONE', 3,
 ( #49212, #57656, #47995, #29178, #10082, #43619 ),
 .UNSPECIFIED., .F., .F.,
 ( 4, 2, 4 ),
 ( 1.525179609227833153E-16, 0.0002445252820015225508, 0.0004890505640028926628 ),
 .UNSPECIFIED. ) ;
#9746=ORIENTED_EDGE ( 'NONE', *, *, #9619, .T. ) ;
#9755=CARTESIAN_POINT ( 'NONE',  ( 0.6846871229502899947, 24.69859318104488821, 41.05093867799194385 ) ) ;
#9762=CARTESIAN_POINT ( 'NONE',  ( 0.8557997880470697982, 38.55640757422439435, 28.43566216844983074 ) ) ;
#9772=EDGE_CURVE ( 'NONE', #38048, #30064, #42909, .T. ) ;
#9782=CARTESIAN_POINT ( 'NONE',  ( 0.5807400328401574052, -46.12278621143487811, -12.92266817606063256 ) ) ;
#9784=EDGE_CURVE ( 'NONE', #3346, #38797, #7013, .T. ) ;
#9785=CARTESIAN_POINT ( 'NONE',  ( 0.9754642270333678811, 5.426415525315814392, 42.56393738774954016 ) ) ;
#9786=CARTESIAN_POINT ( 'NONE',  ( 5.960221823109900008, -16.28736530777599611, 12.49086489703200442 ) ) ;
#9791=CARTESIAN_POINT ( 'NONE',  ( 0.9754402186311935674, -11.28658745892489890, -41.39745964575707404 ) ) ;
#9800=CONICAL_SURFACE ( 'NONE', #44852, 43.08621763946400307, 1.568696531533066763 ) ;
#9801=CARTESIAN_POINT ( 'NONE',  ( 3.660087539127323097, -45.87884541725755838, 14.24113226412033661 ) ) ;
#9802=VERTEX_POINT ( 'NONE', #15319 ) ;
#9807=AXIS2_PLACEMENT_3D ( 'NONE', #19182, #42679, #10392 ) ;
#9810=FACE_OUTER_BOUND ( 'NONE', #24653, .T. ) ;
#9811=VERTEX_POINT ( 'NONE', #8055 ) ;
#9814=CARTESIAN_POINT ( 'NONE',  ( 0.9757402383260949108, -0.08489923450668514227, 42.90839848328079853 ) ) ;
#9815=CARTESIAN_POINT ( 'NONE',  ( 0.9730545539215883499, -0.5054011016609686324, -42.90536227157002713 ) ) ;
#9822=ORIENTED_EDGE ( 'NONE', *, *, #19455, .T. ) ;
#9824=EDGE_CURVE ( 'NONE', #8650, #9811, #36923, .T. ) ;
#9831=CARTESIAN_POINT ( 'NONE',  ( 1.088908134280555773, 39.34174992079780253, -17.14055988408877340 ) ) ;
#9841=CARTESIAN_POINT ( 'NONE',  ( 0.8557997880470599172, 46.03118133706026072, 13.27832040216655507 ) ) ;
#9842=CARTESIAN_POINT ( 'NONE',  ( 5.974727161628367256, 20.35137732084672635, 2.663664384318852996 ) ) ;
#9861=CARTESIAN_POINT ( 'NONE',  ( 4.956653778116488773, 2.599733001513538255, 48.02038484091099235 ) ) ;
#9862=DIRECTION ( 'NONE',  ( 0.07439287786467664587, 0.1170659376278770925, 0.9903339163990684257 ) ) ;
#9877=ORIENTED_EDGE ( 'NONE', *, *, #26281, .F. ) ;
#9880=CARTESIAN_POINT ( 'NONE',  ( 4.967162193818130511, -42.16965968614187688, -8.839793687085657936 ) ) ;
#9891=ORIENTED_EDGE ( 'NONE', *, *, #52458, .T. ) ;
#9899=DIRECTION ( 'NONE',  ( -1.000000000000000000, -0.000000000000000000, -0.000000000000000000 ) ) ;
#9900=CARTESIAN_POINT ( 'NONE',  ( 0.9756008150404585910, -42.55970871350807982, -5.459718823765970619 ) ) ;
#9912=ORIENTED_EDGE ( 'NONE', *, *, #16853, .F. ) ;
#9921=CARTESIAN_POINT ( 'NONE',  ( 0.9722240741986386547, 26.58024228478344853, -33.68410525900254271 ) ) ;
#9927=CARTESIAN_POINT ( 'NONE',  ( 0.5838002273316450497, -24.06583301632231908, 41.41085122398241936 ) ) ;
#9930=VERTEX_POINT ( 'NONE', #50349 ) ;
#9932=CARTESIAN_POINT ( 'NONE',  ( 0.9741495583595173313, -30.61921547032174828, 30.05988007970385212 ) ) ;
#9933=CARTESIAN_POINT ( 'NONE',  ( 0.5839254010752165103, 0.09079837481677424660, -47.89590033178483708 ) ) ;
#9936=CARTESIAN_POINT ( 'NONE',  ( 0.5809828226811617480, 46.11980934799338883, 12.92184523170220345 ) ) ;
#9937=CARTESIAN_POINT ( 'NONE',  ( 0.6067099128993264090, -28.59222530349251556, 38.42667919752394567 ) ) ;
#9938=B_SPLINE_CURVE_WITH_KNOTS ( 'NONE', 3,
 ( #15456, #58331, #33959, #24853 ),
 .UNSPECIFIED., .F., .F.,
 ( 4, 4 ),
 ( 4.336808689942017255E-19, 0.004048833967417088224 ),
 .UNSPECIFIED. ) ;
#9941=DIRECTION ( 'NONE',  ( 0.000000000000000000, 0.000000000000000000, 1.000000000000000000 ) ) ;
#9942=DIRECTION ( 'NONE',  ( -1.000000000000000000, -0.000000000000000000, -0.000000000000000000 ) ) ;
#9948=CARTESIAN_POINT ( 'NONE',  ( 5.959547316686252039, -20.52562247508876681, -0.003562808152834123603 ) ) ;
#9949=ADVANCED_FACE ( 'NONE', ( #38141 ), #57455, .T. ) ;
#9950=CARTESIAN_POINT ( 'NONE',  ( 0.9972139404380306882, 30.80335716430317206, 29.87264297738535745 ) ) ;
#9953=CARTESIAN_POINT ( 'NONE',  ( 4.960156602257184133, 9.558288641081755799, 45.42786611289316312 ) ) ;
#9961=CARTESIAN_POINT ( 'NONE',  ( 0.5836750258453364815, 47.50958153310759258, -6.071582023533789396 ) ) ;
#9963=VECTOR ( 'NONE', #10105, 1000.000000000000000 ) ;
#9965=EDGE_LOOP ( 'NONE', ( #44143, #39711, #36937, #41503 ) ) ;
#9969=B_SPLINE_CURVE_WITH_KNOTS ( 'NONE', 3,
 ( #23478, #4041, #43232, #27878 ),
 .UNSPECIFIED., .F., .F.,
 ( 4, 4 ),
 ( 0.000000000000000000, 0.004446090762760573217 ),
 .UNSPECIFIED. ) ;
#9972=CARTESIAN_POINT ( 'NONE',  ( 3.407937589446178528, -12.08659953757604377, -6.447869442558291198 ) ) ;
#9975=VERTEX_POINT ( 'NONE', #24011 ) ;
#9979=ORIENTED_EDGE ( 'NONE', *, *, #46543, .T. ) ;
#9983=EDGE_LOOP ( 'NONE', ( #17589, #8113, #18768, #28651 ) ) ;
#9987=EDGE_CURVE ( 'NONE', #40550, #46800, #48100, .T. ) ;
#9994=CARTESIAN_POINT ( 'NONE',  ( 5.959547316686252039, 16.28190225198601127, 12.49803383497755682 ) ) ;
#10009=CARTESIAN_POINT ( 'NONE',  ( 0.9752132459055863345, -21.25214916889619232, 37.27572867006956159 ) ) ;
#10010=CARTESIAN_POINT ( 'NONE',  ( -48.95476116535499500, 0.000000000000000000, -12.50000000000000000 ) ) ;
#10012=ORIENTED_EDGE ( 'NONE', *, *, #20922, .F. ) ;
#10015=CARTESIAN_POINT ( 'NONE',  ( 1.227938101723748288, 0.8460948827231143943, -42.91134962331486236 ) ) ;
#10020=CONICAL_SURFACE ( 'NONE', #26028, 43.08621763946400307, 1.568696531533066763 ) ;
#10021=EDGE_CURVE ( 'NONE', #24833, #19678, #19702, .T. ) ;
#10022=ORIENTED_EDGE ( 'NONE', *, *, #26746, .F. ) ;
#10023=CARTESIAN_POINT ( 'NONE',  ( 3.783198216974394956, -7.325057189010705905, 42.41041696600774458 ) ) ;
#10025=CARTESIAN_POINT ( 'NONE',  ( 5.958863334805807099, -12.49619391867170926, -16.28335246510363277 ) ) ;
#10028=CARTESIAN_POINT ( 'NONE',  ( 2.526464513654344657, -36.59988118252419298, 22.53107770806409960 ) ) ;
#10035=CARTESIAN_POINT ( 'NONE',  ( 5.959828726073459926, -2.674641840416033478, -20.35060134307033763 ) ) ;
#10038=VERTEX_POINT ( 'NONE', #37516 ) ;
#10046=B_SPLINE_CURVE_WITH_KNOTS ( 'NONE', 3,
 ( #32877, #18151, #56956, #33180, #28149, #56338 ),
 .UNSPECIFIED., .F., .F.,
 ( 4, 2, 4 ),
 ( 8.673617379884035472E-19, 0.0002291966416970792140, 0.0004583932833941575607 ),
 .UNSPECIFIED. ) ;
#10047=CARTESIAN_POINT ( 'NONE',  ( 5.981074661064941900, 16.27808421740026290, -12.50143471347264246 ) ) ;
#10048=CARTESIAN_POINT ( 'NONE',  ( 1.227938101723747621, 22.18841447410770940, -36.73927144310489012 ) ) ;
#10053=CARTESIAN_POINT ( 'NONE',  ( 0.9756354156337448957, -16.29989858042598527, -39.69194847698947370 ) ) ;
#10054=CARTESIAN_POINT ( 'NONE',  ( 0.5807400328401637335, 18.83234461715183272, 44.04145271122570904 ) ) ;
#10056=EDGE_LOOP ( 'NONE', ( #21421, #31430, #51764, #32614 ) ) ;
#10059=CARTESIAN_POINT ( 'NONE',  ( 0.9730545539215892381, -10.61654491617593266, 41.57420493492382008 ) ) ;
#10069=DIRECTION ( 'NONE',  ( 0.000000000000000000, 0.000000000000000000, 1.000000000000000000 ) ) ;
#10076=CARTESIAN_POINT ( 'NONE',  ( 0.5839254288179540620, -44.21529885210816957, -18.41284501069725721 ) ) ;
#10077=CARTESIAN_POINT ( 'NONE',  ( 0.8551540677456715978, 17.49081417858847232, -44.61036085020933228 ) ) ;
#10081=B_SPLINE_CURVE_WITH_KNOTS ( 'NONE', 3,
 ( #18951, #14252, #61210, #9841 ),
 .UNSPECIFIED., .F., .F.,
 ( 4, 4 ),
 ( 0.000000000000000000, 0.004446090762761318281 ),
 .UNSPECIFIED. ) ;
#10082=CARTESIAN_POINT ( 'NONE',  ( 0.5800708057587405930, 38.37709891224502456, -28.65679888493019334 ) ) ;
#10085=CARTESIAN_POINT ( 'NONE',  ( 0.9754642270333683252, 30.46484943293199521, -30.21634823122134605 ) ) ;
#10086=LINE ( 'NONE', #345, #16146 ) ;
#10093=ORIENTED_EDGE ( 'NONE', *, *, #9282, .F. ) ;
#10097=VERTEX_POINT ( 'NONE', #44080 ) ;
#10099=CARTESIAN_POINT ( 'NONE',  ( 0.5807400328401637335, 37.66660715020906025, -29.58941477092977834 ) ) ;
#10105=DIRECTION ( 'NONE',  ( 0.07836865515943412797, 0.7104869166657089563, -0.6993330359244840366 ) ) ;
#10123=CARTESIAN_POINT ( 'NONE',  ( 1.088313998177378839, -30.89087247895950838, 29.78798111128817538 ) ) ;
#10124=CARTESIAN_POINT ( 'NONE',  ( 0.5263152470540294336, 9.797174393178825657E-16, -8.000000000000000000 ) ) ;
#10126=EDGE_CURVE ( 'NONE', #37598, #40820, #30817, .T. ) ;
#10129=DIRECTION ( 'NONE',  ( 0.000000000000000000, 0.000000000000000000, 1.000000000000000000 ) ) ;
#10146=CARTESIAN_POINT ( 'NONE',  ( 1.227938101723748288, 34.55893248994541267, -25.45152231597022308 ) ) ;
#10149=CARTESIAN_POINT ( 'NONE',  ( 0.5800708057587371513, 47.56394202401747151, -5.628966369368563427 ) ) ;
#10155=CARTESIAN_POINT ( 'NONE',  ( 1.088908134280555329, -42.43751564162686662, 6.374115321932934286 ) ) ;
#10156=DIRECTION ( 'NONE',  ( -0.07439287786467650709, -0.9971416435352943308, 0.01320009283085898759 ) ) ;
#10166=CARTESIAN_POINT ( 'NONE',  ( 0.5786265663353196143, 37.55861529268553056, 29.72999788434305302 ) ) ;
#10172=ORIENTED_EDGE ( 'NONE', *, *, #6394, .F. ) ;
#10182=ORIENTED_EDGE ( 'NONE', *, *, #9414, .F. ) ;
#10188=LINE ( 'NONE', #19598, #54924 ) ;
#10189=CARTESIAN_POINT ( 'NONE',  ( 0.9968887458511664912, -10.46947792236065489, -41.61262323391479612 ) ) ;
#10193=CARTESIAN_POINT ( 'NONE',  ( 0.5839254288179548391, 38.05364096126358220, -29.08514953649782342 ) ) ;
#10195=EDGE_CURVE ( 'NONE', #42917, #722, #45302, .T. ) ;
#10197=CARTESIAN_POINT ( 'NONE',  ( 0.9730545539215883499, 15.95224156741883270, -39.83279466599022811 ) ) ;
#10202=DIRECTION ( 'NONE',  ( -1.000000000000000000, -0.000000000000000000, -0.000000000000000000 ) ) ;
#10210=CARTESIAN_POINT ( 'NONE',  ( 5.974727161628369032, -17.78288073588509732, 10.24903993264978119 ) ) ;
#10213=CARTESIAN_POINT ( 'NONE',  ( 1.227938101723748288, 37.58536632582807613, -20.72293514920711033 ) ) ;
#10214=VERTEX_POINT ( 'NONE', #30861 ) ;
#10221=B_SPLINE_CURVE_WITH_KNOTS ( 'NONE', 3,
 ( #27888, #61376, #56994, #18492 ),
 .UNSPECIFIED., .F., .F.,
 ( 4, 4 ),
 ( 4.470280076681872512E-19, 0.004444878191957686055 ),
 .UNSPECIFIED. ) ;
#10225=CARTESIAN_POINT ( 'NONE',  ( 0.9730545539215892381, 26.52009130076819687, -33.73144377768529978 ) ) ;
#10227=CARTESIAN_POINT ( 'NONE',  ( 0.5800708057587381505, 47.89175345272234097, 0.6275304576132049172 ) ) ;
#10228=VERTEX_POINT ( 'NONE', #42079 ) ;
#10230=CARTESIAN_POINT ( 'NONE',  ( 100.0000507999999968, 0.000000000000000000, 0.000000000000000000 ) ) ;
#10237=CARTESIAN_POINT ( 'NONE',  ( 5.960721111146673579, 19.82454228767738158, 5.318514366755001888 ) ) ;
#10246=FACE_OUTER_BOUND ( 'NONE', #7174, .T. ) ;
#10250=CARTESIAN_POINT ( 'NONE',  ( 0.5809828226811626362, -12.92184523170236510, 46.11980934799335330 ) ) ;
#10253=EDGE_CURVE ( 'NONE', #6126, #12149, #26165, .T. ) ;
#10254=CARTESIAN_POINT ( 'NONE',  ( 0.9972139404380289118, 0.6581143129160298422, 42.90441115546389028 ) ) ;
#10255=CARTESIAN_POINT ( 'NONE',  ( 0.9757402383260934675, 42.55239275983119285, -5.516496958496648340 ) ) ;
#10266=ORIENTED_EDGE ( 'NONE', *, *, #56859, .T. ) ;
#10267=CARTESIAN_POINT ( 'NONE',  ( 0.9730545539215883499, -30.69604515769629316, -29.98130006528894498 ) ) ;
#10268=CARTESIAN_POINT ( 'NONE',  ( 0.5809828226811617480, 47.55412398569215071, -5.711058609464832792 ) ) ;
#10272=ORIENTED_EDGE ( 'NONE', *, *, #41824, .F. ) ;
#10274=CARTESIAN_POINT ( 'NONE',  ( 0.7056555295713328180, -29.82339362082569778, -37.48482836297259979 ) ) ;
#10276=CARTESIAN_POINT ( 'NONE',  ( 0.6067099128993249657, -24.55985149487293029, -41.12102523654879604 ) ) ;
#10283=CARTESIAN_POINT ( 'NONE',  ( 1.227938101723748288, -42.91134962331486946, -0.8460948827229646252 ) ) ;
#10285=DIRECTION ( 'NONE',  ( 0.000000000000000000, 0.000000000000000000, 1.000000000000000000 ) ) ;
#10287=VERTEX_POINT ( 'NONE', #35897 ) ;
#10293=CARTESIAN_POINT ( 'NONE',  ( 2.281351352603290472, 22.83955855331517526, 42.18750813859367099 ) ) ;
#10298=EDGE_LOOP ( 'NONE', ( #60407, #35619, #7608, #4103 ) ) ;
#10306=VERTEX_POINT ( 'NONE', #15095 ) ;
#10310=CARTESIAN_POINT ( 'NONE',  ( 0.5800708057587377064, -38.37709891224484693, 28.65679888493045269 ) ) ;
#10317=CARTESIAN_POINT ( 'NONE',  ( 0.7762783648524387292, 43.90991295203446754, -19.15108798908265442 ) ) ;
#10325=EDGE_CURVE ( 'NONE', #61052, #10228, #6781, .T. ) ;
#10328=EDGE_CURVE ( 'NONE', #28284, #6126, #28549, .T. ) ;
#10331=CARTESIAN_POINT ( 'NONE',  ( 3.783278058412226752, -31.62921638229648025, -29.18720354295077968 ) ) ;
#10334=CARTESIAN_POINT ( 'NONE',  ( 4.967162193818130511, 38.44485641567099776, -19.45289607368781759 ) ) ;
#10337=CARTESIAN_POINT ( 'NONE',  ( 0.9754642270333693244, -37.24735125696668092, 21.30186789325742325 ) ) ;
#10340=( BOUNDED_SURFACE ( )  B_SPLINE_SURFACE ( 3, 1, ( 
 ( #30615, #17159 ),
 ( #46290, #59426 ),
 ( #60343, #21851 ),
 ( #16858, #26226 ) ),
 .UNSPECIFIED., .F., .F., .F. ) 
 B_SPLINE_SURFACE_WITH_KNOTS ( ( 4, 4 ),
 ( 2, 2 ),
 ( 0.000000000000000000, 1.000000000000000000 ),
 ( 0.000000000000000000, 1.000000000000000000 ),
 .UNSPECIFIED. ) 
 GEOMETRIC_REPRESENTATION_ITEM ( )  RATIONAL_B_SPLINE_SURFACE ( (
 ( 1.000000000000000000, 1.000000000000000000),
 ( 0.9953390228620291325, 0.8624445117760984880),
 ( 0.9953390228620291325, 0.8624445117760984880),
 ( 1.000000000000000000, 1.000000000000000000) ) ) 
 REPRESENTATION_ITEM ( '' )  SURFACE ( )  );
#10342=B_SPLINE_CURVE_WITH_KNOTS ( 'NONE', 3,
 ( #38393, #23047, #32137, #27418, #28046, #9237 ),
 .UNSPECIFIED., .F., .F.,
 ( 4, 2, 4 ),
 ( 3.511543213478341086E-18, 0.0002445244328975378903, 0.0004890488657950722027 ),
 .UNSPECIFIED. ) ;
#10347=CARTESIAN_POINT ( 'NONE',  ( 2.526464513654345545, -27.11556434133527205, -33.34586834545800826 ) ) ;
#10359=B_SPLINE_CURVE_WITH_KNOTS ( 'NONE', 3,
 ( #31923, #13757, #60393, #32862 ),
 .UNSPECIFIED., .F., .F.,
 ( 4, 4 ),
 ( 5.421010862427521207E-19, 0.004444878191957687789 ),
 .UNSPECIFIED. ) ;
#10360=CARTESIAN_POINT ( 'NONE',  ( 0.5807400328401574052, -11.87003418057276072, 46.40483864045141615 ) ) ;
#10364=VERTEX_POINT ( 'NONE', #52353 ) ;
#10378=EDGE_CURVE ( 'NONE', #23031, #29746, #48590, .T. ) ;
#10382=CARTESIAN_POINT ( 'NONE',  ( 4.967162193818130511, 0.000000000000000000, 0.000000000000000000 ) ) ;
#10389=CARTESIAN_POINT ( 'NONE',  ( 0.7057020205115037692, -5.417413437617267569, -47.59410670607645955 ) ) ;
#10390=VECTOR ( 'NONE', #21757, 1000.000000000000114 ) ;
#10391=CARTESIAN_POINT ( 'NONE',  ( 0.5809828226811553087, -44.03860873105708151, 18.83114015454682999 ) ) ;
#10392=DIRECTION ( 'NONE',  ( 0.000000000000000000, 0.000000000000000000, 1.000000000000000000 ) ) ;
#10395=CARTESIAN_POINT ( 'NONE',  ( 5.960721111146673579, 20.35079619394246109, -2.672857320903093914 ) ) ;
#10397=CARTESIAN_POINT ( 'NONE',  ( 0.9754402186311922351, 30.20795797590442433, -30.47320128434230924 ) ) ;
#10401=ADVANCED_FACE ( 'NONE', ( #47363 ), #641, .F. ) ;
#10411=CARTESIAN_POINT ( 'NONE',  ( 5.959828726073459926, -20.35060134307036250, 2.674641840415830085 ) ) ;
#10414=VERTEX_POINT ( 'NONE', #48289 ) ;
#10431=CARTESIAN_POINT ( 'NONE',  ( 0.9745511491811756910, -33.83313387735770306, -26.39034508612568075 ) ) ;
#10452=CARTESIAN_POINT ( 'NONE',  ( 5.965394784446460541, 16.27505370423064335, 12.50653125159012902 ) ) ;
#10453=CARTESIAN_POINT ( 'NONE',  ( 0.9968887458511658251, -20.88287852258416777, -37.48500720268749120 ) ) ;
#10456=B_SPLINE_CURVE_WITH_KNOTS ( 'NONE', 3,
 ( #14634, #818, #52822, #58426, #44086, #11160, #9927, #24324, #38758, #58734, #19639, #34054, #43454, #30241, #48742, #498 ),
 .UNSPECIFIED., .F., .F.,
 ( 4, 3, 3, 3, 3, 4 ),
 ( 1.250973872328959318E-17, 0.0002724568934985488250, 0.0004086836638483747801, 0.0005449104342063555619, 0.0008173270854453591923, 0.001089761613562688792 ),
 .UNSPECIFIED. ) ;
#10459=CARTESIAN_POINT ( 'NONE',  ( 0.6067375320500718594, 47.57460111700607541, -5.548194933739688750 ) ) ;
#10460=( BOUNDED_SURFACE ( )  B_SPLINE_SURFACE ( 3, 1, ( 
 ( #13775, #42584 ),
 ( #45588, #40593 ),
 ( #25226, #44668 ),
 ( #26152, #21455 ) ),
 .UNSPECIFIED., .F., .F., .F. ) 
 B_SPLINE_SURFACE_WITH_KNOTS ( ( 4, 4 ),
 ( 2, 2 ),
 ( 0.000000000000000000, 1.000000000000000000 ),
 ( 0.000000000000000000, 1.000000000000000000 ),
 .UNSPECIFIED. ) 
 GEOMETRIC_REPRESENTATION_ITEM ( )  RATIONAL_B_SPLINE_SURFACE ( (
 ( 1.000000000000000000, 1.000000000000000000),
 ( 0.9953390228620291325, 0.8624445117761032620),
 ( 0.9953390228620291325, 0.8624445117761032620),
 ( 1.000000000000000000, 1.000000000000000000) ) ) 
 REPRESENTATION_ITEM ( '' )  SURFACE ( )  );
#10461=CARTESIAN_POINT ( 'NONE',  ( 0.9722240741986374335, 37.44729083276452997, -20.94823706911160954 ) ) ;
#10463=CARTESIAN_POINT ( 'NONE',  ( 0.5807400328401574052, 33.48217046439112465, 34.25275203086247444 ) ) ;
#10466=CARTESIAN_POINT ( 'NONE',  ( 0.8557997880470697982, -41.02602466100796619, 24.73961900479237386 ) ) ;
#10473=CARTESIAN_POINT ( 'NONE',  ( 0.9752132459055861124, -25.93579301218381161, 34.18286753639630859 ) ) ;
#10474=B_SPLINE_CURVE_WITH_KNOTS ( 'NONE', 3,
 ( #52311, #43890, #933, #4996, #24125, #43264 ),
 .UNSPECIFIED., .F., .F.,
 ( 4, 2, 4 ),
 ( 9.341771812940338307E-18, 0.0002291978881530153469, 0.0004583957763060213155 ),
 .UNSPECIFIED. ) ;
#10475=CARTESIAN_POINT ( 'NONE',  ( 5.959828726073459926, -16.28681682518055851, -12.49160845136029252 ) ) ;
#10480=ORIENTED_EDGE ( 'NONE', *, *, #36378, .F. ) ;
#10483=CARTESIAN_POINT ( 'NONE',  ( 0.5809828226811560858, -11.86925843957200222, 46.40184912890835278 ) ) ;
#10485=ADVANCED_FACE ( 'NONE', ( #49515 ), #266, .F. ) ;
#10488=CARTESIAN_POINT ( 'NONE',  ( 4.967162193818130511, 0.000000000000000000, 0.000000000000000000 ) ) ;
#10490=VERTEX_POINT ( 'NONE', #49208 ) ;
#10499=CIRCLE ( 'NONE', #18509, 43.08621763946400307 ) ;
#10500=CARTESIAN_POINT ( 'NONE',  ( 0.5807400328401637335, -6.791881299635273095, -47.41494605191449807 ) ) ;
#10501=ORIENTED_EDGE ( 'NONE', *, *, #32217, .T. ) ;
#10507=CARTESIAN_POINT ( 'NONE',  ( 0.8557997880470599172, 41.93815086860288943, -23.15977007032279289 ) ) ;
#10513=CARTESIAN_POINT ( 'NONE',  ( 1.227938101723748288, 25.45152231597057124, 34.55893248994515687 ) ) ;
#10514=DIRECTION ( 'NONE',  ( -1.000000000000000000, -0.000000000000000000, -0.000000000000000000 ) ) ;
#10516=CARTESIAN_POINT ( 'NONE',  ( 5.960721111146673579, -17.77882586010674260, 10.25731071096551794 ) ) ;
#10517=ORIENTED_EDGE ( 'NONE', *, *, #53159, .F. ) ;
#10519=ORIENTED_EDGE ( 'NONE', *, *, #44360, .F. ) ;
#10525=CARTESIAN_POINT ( 'NONE',  ( 1.227938101723748288, -39.96870412324346944, 15.63977281655828300 ) ) ;
#10526=EDGE_CURVE ( 'NONE', #5033, #19687, #45785, .T. ) ;
#10528=( BOUNDED_SURFACE ( )  B_SPLINE_SURFACE ( 3, 1, ( 
 ( #50304, #17729 ),
 ( #40633, #54990 ),
 ( #36231, #45329 ),
 ( #50003, #21188 ) ),
 .UNSPECIFIED., .F., .F., .F. ) 
 B_SPLINE_SURFACE_WITH_KNOTS ( ( 4, 4 ),
 ( 2, 2 ),
 ( 0.000000000000000000, 1.000000000000000000 ),
 ( 0.000000000000000000, 1.000000000000000000 ),
 .UNSPECIFIED. ) 
 GEOMETRIC_REPRESENTATION_ITEM ( )  RATIONAL_B_SPLINE_SURFACE ( (
 ( 1.000000000000000000, 1.000000000000000000),
 ( 0.9732289882329797637, 0.9999525324661233672),
 ( 0.9732289882329797637, 0.9999525324661233672),
 ( 1.000000000000000000, 1.000000000000000000) ) ) 
 REPRESENTATION_ITEM ( '' )  SURFACE ( )  );
#10531=CARTESIAN_POINT ( 'NONE',  ( 0.8557997880470599172, 47.60865952217007191, -5.347802024196765203 ) ) ;
#10535=CARTESIAN_POINT ( 'NONE',  ( 0.9741495583595158880, 39.79188455996743556, -16.05424148287283614 ) ) ;
#10537=CARTESIAN_POINT ( 'NONE',  ( 0.6067375320500736358, -24.55990317723886562, 41.12099578548244239 ) ) ;
#10543=CARTESIAN_POINT ( 'NONE',  ( 2.624215991343608501, -4.864192649745077368, -47.76052319582220917 ) ) ;
#10549=CONICAL_SURFACE ( 'NONE', #53536, 43.08621763946400307, 1.568696531533066763 ) ;
#10552=DIRECTION ( 'NONE',  ( -1.000000000000000000, -0.000000000000000000, -0.000000000000000000 ) ) ;
#10555=CARTESIAN_POINT ( 'NONE',  ( 4.956653778116975495, -27.17045123668499684, 39.67974989265029961 ) ) ;
#10561=CARTESIAN_POINT ( 'NONE',  ( 1.154321485836933503, 0.8253076867718968090, 42.90848031452335221 ) ) ;
#10562=CARTESIAN_POINT ( 'NONE',  ( 0.5809828226811617480, -47.55412398569210808, 5.711058609465143654 ) ) ;
#10569=B_SPLINE_CURVE_WITH_KNOTS ( 'NONE', 3,
 ( #7015, #42057, #32325, #21450 ),
 .UNSPECIFIED., .F., .F.,
 ( 4, 4 ),
 ( 0.000000000000000000, 0.005004741218457419739 ),
 .UNSPECIFIED. ) ;
#10570=CARTESIAN_POINT ( 'NONE',  ( -18.25036807083938228, -7.723231599531199976, 2.086259205976699338 ) ) ;
#10574=CARTESIAN_POINT ( 'NONE',  ( 5.981074661064941900, -12.48781255314277772, -16.28853686865594952 ) ) ;
#10578=CARTESIAN_POINT ( 'NONE',  ( 0.5800708057587408151, 28.65679888493058058, 38.37709891224474035 ) ) ;
#10582=ORIENTED_EDGE ( 'NONE', *, *, #43161, .T. ) ;
#10588=B_SPLINE_CURVE_WITH_KNOTS ( 'NONE', 3,
 ( #24207, #38641, #57695, #19224 ),
 .UNSPECIFIED., .F., .F.,
 ( 4, 4 ),
 ( 2.860979249076398407E-17, 0.005004741218457448362 ),
 .UNSPECIFIED. ) ;
#10590=B_SPLINE_CURVE_WITH_KNOTS ( 'NONE', 3,
 ( #15508, #9020, #56933, #14055 ),
 .UNSPECIFIED., .F., .F.,
 ( 4, 4 ),
 ( 3.469446951953613804E-18, 0.005004741218457419739 ),
 .UNSPECIFIED. ) ;
#10592=LINE ( 'NONE', #34713, #40229 ) ;
#10594=VERTEX_POINT ( 'NONE', #17558 ) ;
#10595=CARTESIAN_POINT ( 'NONE',  ( 4.967162193818130511, 40.93989340068628024, -13.42934394584121094 ) ) ;
#10602=VERTEX_POINT ( 'NONE', #26635 ) ;
#10604=EDGE_CURVE ( 'NONE', #49888, #50007, #21634, .T. ) ;
#10605=CARTESIAN_POINT ( 'NONE',  ( 0.7762777257811892540, 11.53708189756940783, 46.49451973287607132 ) ) ;
#10607=VECTOR ( 'NONE', #30253, 1000.000000000000114 ) ;
#10611=CARTESIAN_POINT ( 'NONE',  ( 0.5839880159502333079, 18.28706857028372212, 44.26747004398423257 ) ) ;
#10617=EDGE_CURVE ( 'NONE', #31908, #28601, #12253, .T. ) ;
#10619=CARTESIAN_POINT ( 'NONE',  ( 4.967162193818130511, -28.07411493385273715, -32.68434214048198072 ) ) ;
#10629=CARTESIAN_POINT ( 'NONE',  ( 0.7056555295713284881, 43.92642606846705178, -19.10539864320352521 ) ) ;
#10635=CARTESIAN_POINT ( 'NONE',  ( 4.967162193818129623, -40.65506779172174845, 14.26841313271267886 ) ) ;
#10637=B_SPLINE_CURVE_WITH_KNOTS ( 'NONE', 3,
 ( #35237, #44343, #25817, #39634 ),
 .UNSPECIFIED., .F., .F.,
 ( 4, 4 ),
 ( 4.336808689942017736E-19, 0.004444878191957686922 ),
 .UNSPECIFIED. ) ;
#10640=CARTESIAN_POINT ( 'NONE',  ( 4.967162193818130511, -7.970725651240091025, 42.34252806656591162 ) ) ;
#10648=CARTESIAN_POINT ( 'NONE',  ( 4.960156602257182357, -2.524999074837890323, 46.35381625054453281 ) ) ;
#10649=CARTESIAN_POINT ( 'NONE',  ( 0.9754642270333692133, 16.58255499746128692, -39.57465882553911740 ) ) ;
#10662=CARTESIAN_POINT ( 'NONE',  ( 3.783278058412224976, 1.726763838446180976, 43.00370293663099375 ) ) ;
#10673=FACE_OUTER_BOUND ( 'NONE', #9965, .T. ) ;
#10674=ORIENTED_EDGE ( 'NONE', *, *, #3967, .F. ) ;
#10678=ORIENTED_EDGE ( 'NONE', *, *, #6470, .F. ) ;
#10680=EDGE_CURVE ( 'NONE', #51719, #5333, #32347, .T. ) ;
#10682=CARTESIAN_POINT ( 'NONE',  ( 0.9730545539215883499, 33.73144377768594637, -26.52009130076736554 ) ) ;
#10683=CARTESIAN_POINT ( 'NONE',  ( 2.281448460670576939, 40.87338159040670860, -25.11570011049327533 ) ) ;
#10684=ORIENTED_EDGE ( 'NONE', *, *, #47986, .F. ) ;
#10693=ORIENTED_EDGE ( 'NONE', *, *, #49345, .F. ) ;
#10696=EDGE_CURVE ( 'NONE', #50538, #29464, #33827, .T. ) ;
#10697=CARTESIAN_POINT ( 'NONE',  ( 0.6846871229502899947, 41.91507847151797250, 23.20185915381571462 ) ) ;
#10700=ADVANCED_FACE ( 'NONE', ( #9684 ), #34334, .F. ) ;
#10710=CARTESIAN_POINT ( 'NONE',  ( 5.959547316686252039, 12.49803383497728326, 16.28190225198622443 ) ) ;
#10711=B_SPLINE_CURVE_WITH_KNOTS ( 'NONE', 3,
 ( #25534, #1708, #39985, #7022, #31472, #26774 ),
 .UNSPECIFIED., .F., .F.,
 ( 4, 2, 4 ),
 ( 1.537985780943912493E-16, 0.0002445252820015181598, 0.0004890505640028825797 ),
 .UNSPECIFIED. ) ;
#10714=CARTESIAN_POINT ( 'NONE',  ( 0.5839880159502339740, 33.83547574026627558, 33.89965136132159529 ) ) ;
#10716=ORIENTED_EDGE ( 'NONE', *, *, #56353, .F. ) ;
#10724=ORIENTED_EDGE ( 'NONE', *, *, #44713, .T. ) ;
#10727=DIRECTION ( 'NONE',  ( 0.9990097760809872884, 5.448601141172737927E-18, 0.04449120468829269315 ) ) ;
#10731=CARTESIAN_POINT ( 'NONE',  ( 1.154321485836934391, 25.46626718279358315, -34.54400167111872832 ) ) ;
#10750=ORIENTED_EDGE ( 'NONE', *, *, #58268, .F. ) ;
#10751=CARTESIAN_POINT ( 'NONE',  ( 0.9730545539215883499, -25.71816799638755668, -34.34678117142582465 ) ) ;
#10753=EDGE_CURVE ( 'NONE', #10364, #42072, #15928, .T. ) ;
#10755=B_SPLINE_CURVE_WITH_KNOTS ( 'NONE', 3,
 ( #48409, #14608, #42811, #58095 ),
 .UNSPECIFIED., .F., .F.,
 ( 4, 4 ),
 ( 0.000000000000000000, 0.005004741218457407596 ),
 .UNSPECIFIED. ) ;
#10757=ORIENTED_EDGE ( 'NONE', *, *, #13296, .F. ) ;
#10758=CARTESIAN_POINT ( 'NONE',  ( 4.967162193818130511, 42.96271701169385437, 3.259922920617894793 ) ) ;
#10759=CARTESIAN_POINT ( 'NONE',  ( 4.963659409799330291, -33.96111158240226757, -29.14784479683147467 ) ) ;
#10774=CARTESIAN_POINT ( 'NONE',  ( 100.0000507999999968, 0.000000000000000000, 0.000000000000000000 ) ) ;
#10784=ADVANCED_FACE ( 'NONE', ( #5884 ), #5023, .F. ) ;
#10790=CARTESIAN_POINT ( 'NONE',  ( 0.9754642270333685472, -11.27515941577604153, 41.40054989430078081 ) ) ;
#10792=CARTESIAN_POINT ( 'NONE',  ( 0.8551540677456715978, -24.74404575822747177, -41.03346287276453097 ) ) ;
#10803=CARTESIAN_POINT ( 'NONE',  ( 0.5839254288179566155, -41.43367229384567452, -24.02657516616548605 ) ) ;
#10812=CARTESIAN_POINT ( 'NONE',  ( 1.088908134280555551, -11.85879120571477863, -41.24246781061831513 ) ) ;
#10822=ORIENTED_EDGE ( 'NONE', *, *, #50360, .F. ) ;
#10823=CARTESIAN_POINT ( 'NONE',  ( 0.5809828226811617480, 44.45562576850627323, -17.82437196699632054 ) ) ;
#10828=CARTESIAN_POINT ( 'NONE',  ( 0.9756354156337441186, -42.52418499698895005, -5.729847988735796704 ) ) ;
#10832=CARTESIAN_POINT ( 'NONE',  ( 0.5809828226811553087, -44.45562576850588243, -17.82437196699728332 ) ) ;
#10841=VERTEX_POINT ( 'NONE', #54429 ) ;
#10853=CARTESIAN_POINT ( 'NONE',  ( 0.9756354156337460060, 39.69194847698950923, -16.29989858042583961 ) ) ;
#10858=CARTESIAN_POINT ( 'NONE',  ( 4.967162193818130511, 42.34252806656594004, 7.970725651239941811 ) ) ;
#10868=CARTESIAN_POINT ( 'NONE',  ( 1.088313998177380615, 29.78798111128829262, 30.89087247895941601 ) ) ;
#10869=CIRCLE ( 'NONE', #833, 48.09070567114147110 ) ;
#10873=ORIENTED_EDGE ( 'NONE', *, *, #29769, .F. ) ;
#10876=CARTESIAN_POINT ( 'NONE',  ( 2.624215991343620935, -47.76052319582213812, -4.864192649745882946 ) ) ;
#10896=ORIENTED_EDGE ( 'NONE', *, *, #44239, .T. ) ;
#10898=CARTESIAN_POINT ( 'NONE',  ( 4.303969348037258058, -45.86537346639067891, 14.52400616872353289 ) ) ;
#10900=CARTESIAN_POINT ( 'NONE',  ( 0.7056555295713264897, -41.89804573586717140, -23.21854706865624962 ) ) ;
#10905=ORIENTED_EDGE ( 'NONE', *, *, #2477, .F. ) ;
#10911=ORIENTED_EDGE ( 'NONE', *, *, #58973, .F. ) ;
#10913=ADVANCED_FACE ( 'NONE', ( #31579 ), #4646, .F. ) ;
#10919=CARTESIAN_POINT ( 'NONE',  ( 0.8557997880470599172, 41.02602466100778145, 24.73961900479265807 ) ) ;
#10923=CARTESIAN_POINT ( 'NONE',  ( 0.5839879327111947571, -6.161619650335635079, 47.49806740880203648 ) ) ;
#10926=EDGE_CURVE ( 'NONE', #55315, #45625, #42788, .T. ) ;
#10927=ORIENTED_EDGE ( 'NONE', *, *, #1687, .T. ) ;
#10939=CARTESIAN_POINT ( 'NONE',  ( 4.960156602257182357, -46.28683144126597426, 3.546989772329730339 ) ) ;
#10943=CARTESIAN_POINT ( 'NONE',  ( 5.958863334805807099, -18.96369761673824783, 7.853699934219561918 ) ) ;
#10946=CARTESIAN_POINT ( 'NONE',  ( 0.9740398440564311811, -39.48175649279244226, 16.80263250099874028 ) ) ;
#10953=CARTESIAN_POINT ( 'NONE',  ( 0.8557997880470697982, 47.60865952216998664, 5.347802024197403803 ) ) ;
#10960=CARTESIAN_POINT ( 'NONE',  ( 0.8557997880470697982, 11.51622788066522851, -46.50333260518546297 ) ) ;
#10977=ORIENTED_EDGE ( 'NONE', *, *, #29906, .T. ) ;
#10980=VERTEX_POINT ( 'NONE', #33755 ) ;
#10985=EDGE_CURVE ( 'NONE', #9646, #33299, #33138, .T. ) ;
#10989=CARTESIAN_POINT ( 'NONE',  ( 0.5839880159502343071, 33.89965136132193635, -33.83547574026591320 ) ) ;
#10996=ORIENTED_EDGE ( 'NONE', *, *, #45461, .T. ) ;
#11011=CARTESIAN_POINT ( 'NONE',  ( 0.9730545539215883499, 33.73144377768558400, 26.52009130076782739 ) ) ;
#11017=CARTESIAN_POINT ( 'NONE',  ( 5.959828726073459926, -17.77343634131849015, 10.26672511661725018 ) ) ;
#11019=CARTESIAN_POINT ( 'NONE',  ( -16.29569048063198267, -7.897460783358359215, 1.291753785943115407 ) ) ;
#11022=CARTESIAN_POINT ( 'NONE',  ( 0.8551540677456834771, 41.94570365541202506, 23.16399837394560990 ) ) ;
#11025=CARTESIAN_POINT ( 'NONE',  ( 0.5827359174754823679, 33.60976280407646755, 34.12345922495620698 ) ) ;
#11027=ORIENTED_EDGE ( 'NONE', *, *, #34529, .F. ) ;
#11038=ORIENTED_EDGE ( 'NONE', *, *, #11476, .T. ) ;
#11045=EDGE_CURVE ( 'NONE', #7463, #46592, #25258, .T. ) ;
#11052=ORIENTED_EDGE ( 'NONE', *, *, #7819, .F. ) ;
#11062=CARTESIAN_POINT ( 'NONE',  ( 0.5809828226811617480, 24.41822904836982389, -41.20389530892281726 ) ) ;
#11063=CARTESIAN_POINT ( 'NONE',  ( 5.860006189529234355, 36.27483683749437660, 31.78942168514575073 ) ) ;
#11074=ORIENTED_EDGE ( 'NONE', *, *, #12320, .T. ) ;
#11076=CARTESIAN_POINT ( 'NONE',  ( 0.5800708057587393718, -13.00144577271073132, 46.09746469244092282 ) ) ;
#11082=( BOUNDED_SURFACE ( )  B_SPLINE_SURFACE ( 3, 1, ( 
 ( #42867, #3370 ),
 ( #61615, #38173 ),
 ( #61920, #14352 ),
 ( #50994, #8091 ) ),
 .UNSPECIFIED., .F., .F., .F. ) 
 B_SPLINE_SURFACE_WITH_KNOTS ( ( 4, 4 ),
 ( 2, 2 ),
 ( 0.000000000000000000, 1.000000000000000000 ),
 ( 0.000000000000000000, 1.000000000000000000 ),
 .UNSPECIFIED. ) 
 GEOMETRIC_REPRESENTATION_ITEM ( )  RATIONAL_B_SPLINE_SURFACE ( (
 ( 1.000000000000000000, 1.000000000000000000),
 ( 0.7269869731126817891, 0.9931720237060910339),
 ( 0.7269869731126817891, 0.9931720237060910339),
 ( 1.000000000000000000, 1.000000000000000000) ) ) 
 REPRESENTATION_ITEM ( '' )  SURFACE ( )  );
#11084=EDGE_CURVE ( 'NONE', #6983, #46350, #21234, .T. ) ;
#11085=DIRECTION ( 'NONE',  ( 0.07836865515943411409, -0.9873352307081171286, -0.1379401902675598812 ) ) ;
#11088=LINE ( 'NONE', #44926, #17862 ) ;
#11093=CARTESIAN_POINT ( 'NONE',  ( 5.959828726073459926, 20.34941966491235732, 2.683617577144452593 ) ) ;
#11098=( BOUNDED_SURFACE ( )  B_SPLINE_SURFACE ( 3, 1, ( 
 ( #37088, #18897 ),
 ( #61155, #27968 ),
 ( #57067, #13572 ),
 ( #13891, #9782 ) ),
 .UNSPECIFIED., .F., .F., .F. ) 
 B_SPLINE_SURFACE_WITH_KNOTS ( ( 4, 4 ),
 ( 2, 2 ),
 ( 0.000000000000000000, 1.000000000000000000 ),
 ( 0.000000000000000000, 1.000000000000000000 ),
 .UNSPECIFIED. ) 
 GEOMETRIC_REPRESENTATION_ITEM ( )  RATIONAL_B_SPLINE_SURFACE ( (
 ( 1.000000000000000000, 1.000000000000000000),
 ( 0.9732289882329797637, 0.9999525324661233672),
 ( 0.9732289882329797637, 0.9999525324661233672),
 ( 1.000000000000000000, 1.000000000000000000) ) ) 
 REPRESENTATION_ITEM ( '' )  SURFACE ( )  );
#11100=CARTESIAN_POINT ( 'NONE',  ( 0.9747592971366240144, -10.79247637456148645, 41.52905920980982302 ) ) ;
#11102=CARTESIAN_POINT ( 'NONE',  ( 5.960721111146673579, 10.25731071096558011, 17.77882586010670707 ) ) ;
#11103=CARTESIAN_POINT ( 'NONE',  ( 0.7762783648524412827, 41.03453896757974917, -24.71864151483671890 ) ) ;
#11108=CARTESIAN_POINT ( 'NONE',  ( 4.967162193818129623, 40.65506779172164897, 14.26841313271295952 ) ) ;
#11123=EDGE_CURVE ( 'NONE', #51919, #55413, #39385, .T. ) ;
#11124=CARTESIAN_POINT ( 'NONE',  ( 4.956653778116992370, 3.690426056930664611, -47.94889704119048446 ) ) ;
#11139=CARTESIAN_POINT ( 'NONE',  ( 0.5819845901640494645, 44.07435474487846250, 18.74765780149844474 ) ) ;
#11160=CARTESIAN_POINT ( 'NONE',  ( 0.5836750258453375917, -24.10509086647779853, 41.38803015411996711 ) ) ;
#11161=CYLINDRICAL_SURFACE ( 'NONE', #8649, 8.000000000000000000 ) ;
#11164=CARTESIAN_POINT ( 'NONE',  ( 5.981074661064941900, -14.50705827991455976, 14.51919955600710566 ) ) ;
#11177=CARTESIAN_POINT ( 'NONE',  ( 1.227938101723756947, 42.43379953535195170, -6.439911493064139236 ) ) ;
#11180=CARTESIAN_POINT ( 'NONE',  ( 0.5839254288179555052, -47.49799454719521208, 6.161657890844768559 ) ) ;
#11192=EDGE_CURVE ( 'NONE', #18069, #9258, #4777, .T. ) ;
#11193=CARTESIAN_POINT ( 'NONE',  ( 0.8551540677456715978, -0.9122407826479158599, 47.90804413217340851 ) ) ;
#11195=ORIENTED_EDGE ( 'NONE', *, *, #51799, .F. ) ;
#11197=CARTESIAN_POINT ( 'NONE',  ( 0.9730545539215883499, 41.31259007387247095, -11.59290486963463351 ) ) ;
#11199=DIRECTION ( 'NONE',  ( 0.000000000000000000, 0.000000000000000000, 1.000000000000000000 ) ) ;
#11201=CARTESIAN_POINT ( 'NONE',  ( 5.960721111146673579, 19.82781442290498219, -5.306302591836375981 ) ) ;
#11204=DIRECTION ( 'NONE',  ( 0.000000000000000000, 0.000000000000000000, 1.000000000000000000 ) ) ;
#11205=CARTESIAN_POINT ( 'NONE',  ( 0.5839880159502347512, 41.50181427378134913, -23.90868446765435351 ) ) ;
#11214=CARTESIAN_POINT ( 'NONE',  ( 0.5819845901640507968, -18.74765780149859395, 44.07435474487839144 ) ) ;
#11218=CARTESIAN_POINT ( 'NONE',  ( 3.783198216974390515, -41.98529422752523033, 9.462293521184724554 ) ) ;
#11220=CARTESIAN_POINT ( 'NONE',  ( 4.967162193818130511, -7.970725651240091025, 42.34252806656591162 ) ) ;
#11226=CIRCLE ( 'NONE', #56235, 48.09070567114147110 ) ;
#11227=CARTESIAN_POINT ( 'NONE',  ( 0.5839879882012675161, 18.32902119196566559, 44.25009266679212061 ) ) ;
#11243=CARTESIAN_POINT ( 'NONE',  ( 0.6067099128993241886, -5.548253864790723355, 47.57459301987700684 ) ) ;
#11255=CARTESIAN_POINT ( 'NONE',  ( 0.9749527285493314599, -25.89384247702547981, -34.21468599366735930 ) ) ;
#11256=CARTESIAN_POINT ( 'NONE',  ( 0.7056555295713307085, 28.48870155114964220, -38.50897360867654839 ) ) ;
#11270=CARTESIAN_POINT ( 'NONE',  ( 4.967162193818130511, -40.65506779172153529, -14.26841313271325795 ) ) ;
#11274=ORIENTED_EDGE ( 'NONE', *, *, #38482, .F. ) ;
#11275=CARTESIAN_POINT ( 'NONE',  ( 4.303969348037246512, -35.51084504003219422, 32.45857549159289590 ) ) ;
#11279=EDGE_CURVE ( 'NONE', #51719, #18847, #19902, .T. ) ;
#11284=EDGE_LOOP ( 'NONE', ( #50019, #41346, #21219, #36060 ) ) ;
#11290=CARTESIAN_POINT ( 'NONE',  ( 1.227938101723756947, 25.45152231597106507, -34.55893248994479450 ) ) ;
#11302=CARTESIAN_POINT ( 'NONE',  ( -18.24799997550736919, -12.32233744059949565, -2.099999999999997424 ) ) ;
#11303=B_SPLINE_CURVE_WITH_KNOTS ( 'NONE', 3,
 ( #38982, #23625, #15163, #34271 ),
 .UNSPECIFIED., .F., .F.,
 ( 4, 4 ),
 ( 0.000000000000000000, 0.004050076154993000749 ),
 .UNSPECIFIED. ) ;
#11305=CARTESIAN_POINT ( 'NONE',  ( 4.967162193818130511, 0.000000000000000000, 0.000000000000000000 ) ) ;
#11311=ADVANCED_FACE ( 'NONE', ( #8292 ), #56746, .T. ) ;
#11314=EDGE_CURVE ( 'NONE', #37400, #59114, #5843, .T. ) ;
#11316=CARTESIAN_POINT ( 'NONE',  ( 1.227938101723756947, 15.63977281655895979, -39.96870412324319943 ) ) ;
#11338=CARTESIAN_POINT ( 'NONE',  ( 4.303969348037246512, -27.54579249306183542, -39.44373910178637743 ) ) ;
#11345=CARTESIAN_POINT ( 'NONE',  ( 1.227938101723748288, 25.45152231597057124, 34.55893248994515687 ) ) ;
#11346=ORIENTED_EDGE ( 'NONE', *, *, #46344, .F. ) ;
#11355=( BOUNDED_SURFACE ( )  B_SPLINE_SURFACE ( 3, 1, ( 
 ( #17800, #32211 ),
 ( #26257, #36001 ),
 ( #3668, #16886 ),
 ( #60683, #26885 ) ),
 .UNSPECIFIED., .F., .F., .F. ) 
 B_SPLINE_SURFACE_WITH_KNOTS ( ( 4, 4 ),
 ( 2, 2 ),
 ( 0.000000000000000000, 1.000000000000000000 ),
 ( 0.000000000000000000, 1.000000000000000000 ),
 .UNSPECIFIED. ) 
 GEOMETRIC_REPRESENTATION_ITEM ( )  RATIONAL_B_SPLINE_SURFACE ( (
 ( 1.000000000000000000, 1.000000000000000000),
 ( 0.7269869731126817891, 0.9931720237060910339),
 ( 0.7269869731126817891, 0.9931720237060910339),
 ( 1.000000000000000000, 1.000000000000000000) ) ) 
 REPRESENTATION_ITEM ( '' )  SURFACE ( )  );
#11364=CARTESIAN_POINT ( 'NONE',  ( 1.227938101723748288, -0.8460948827228147451, 42.91134962331487657 ) ) ;
#11365=B_SPLINE_CURVE_WITH_KNOTS ( 'NONE', 3,
 ( #10268, #61928, #854, #52233, #19362, #9961, #48177, #19068, #5231, #53161, #29360, #24669, #24362, #24985, #39102, #33781 ),
 .UNSPECIFIED., .F., .F.,
 ( 4, 3, 3, 3, 3, 4 ),
 ( 1.214354834101861570E-17, 0.0002724568934985572275, 0.0004086836638483815022, 0.0005449104342063627177, 0.0008173270854453656975, 0.001089761613562685756 ),
 .UNSPECIFIED. ) ;
#11368=CARTESIAN_POINT ( 'NONE',  ( 0.6846871229502932144, 41.05093867799185858, 24.69859318104503032 ) ) ;
#11375=CARTESIAN_POINT ( 'NONE',  ( 4.956653778116992370, 26.26162724282429650, -40.28700667097652399 ) ) ;
#11377=EDGE_CURVE ( 'NONE', #30700, #21629, #18345, .T. ) ;
#11382=CARTESIAN_POINT ( 'NONE',  ( 3.270143674763207553, 13.53222904135354199, 2.058141141425647191 ) ) ;
#11387=EDGE_CURVE ( 'NONE', #15844, #1609, #1018, .T. ) ;
#11393=CARTESIAN_POINT ( 'NONE',  ( 0.8551540677456715978, -47.61725548905986471, -5.348818140991393300 ) ) ;
#11395=CARTESIAN_POINT ( 'NONE',  ( 5.959547316686252039, -20.35048796920735015, -2.675599016784462769 ) ) ;
#11400=CARTESIAN_POINT ( 'NONE',  ( 3.407937589446178528, 13.34359005742689241, 3.099921468255050439 ) ) ;
#11401=CARTESIAN_POINT ( 'NONE',  ( 0.5786265663353153954, -24.57327059187369400, -41.11783955080264974 ) ) ;
#11402=DIRECTION ( 'NONE',  ( -1.000000000000000000, -0.000000000000000000, -0.000000000000000000 ) ) ;
#11413=DIRECTION ( 'NONE',  ( 0.000000000000000000, 0.000000000000000000, 1.000000000000000000 ) ) ;
#11419=B_SPLINE_CURVE_WITH_KNOTS ( 'NONE', 3,
 ( #47428, #28312, #14543, #53032, #716, #47131 ),
 .UNSPECIFIED., .F., .F.,
 ( 4, 2, 4 ),
 ( 1.084202172485504434E-19, 0.0002445244328975358303, 0.0004890488657950715521 ),
 .UNSPECIFIED. ) ;
#11422=EDGE_LOOP ( 'NONE', ( #12867, #2761, #46049, #39710 ) ) ;
#11426=EDGE_CURVE ( 'NONE', #28284, #884, #39614, .T. ) ;
#11429=ORIENTED_EDGE ( 'NONE', *, *, #44450, .F. ) ;
#11431=CARTESIAN_POINT ( 'NONE',  ( 4.956653778116975495, 20.77844580450561551, 43.37017594958062006 ) ) ;
#11433=CARTESIAN_POINT ( 'NONE',  ( 0.5839880159502333079, 44.26747004398443863, -18.28706857028324961 ) ) ;
#11439=CARTESIAN_POINT ( 'NONE',  ( 0.9756008150404608115, -30.44122083654196587, -30.24019526051575468 ) ) ;
#11446=ORIENTED_EDGE ( 'NONE', *, *, #51680, .F. ) ;
#11452=EDGE_CURVE ( 'NONE', #52461, #48862, #22021, .T. ) ;
#11455=EDGE_CURVE ( 'NONE', #34186, #39947, #26432, .T. ) ;
#11464=LINE ( 'NONE', #24325, #24673 ) ;
#11466=CARTESIAN_POINT ( 'NONE',  ( 0.8557997880470690211, 47.89938907511594124, -0.9121262075947851322 ) ) ;
#11468=B_SPLINE_CURVE_WITH_KNOTS ( 'NONE', 3,
 ( #30364, #1854, #49477, #51318, #27526, #4611, #27838, #52243, #41965, #13140, #36636, #3696, #56327, #32552, #46347, #51630, #37566, #56641, #9032 ),
 .UNSPECIFIED., .F., .F.,
 ( 4, 3, 3, 3, 3, 3, 4 ),
 ( 9.813676791237319219E-18, 0.0002724573126191794418, 0.0004086839781548490193, 0.0005449106435901815947, 0.0006811373090491476632, 0.0008459866663933731691, 0.001010840725717210764 ),
 .UNSPECIFIED. ) ;
#11469=ADVANCED_FACE ( 'NONE', ( #751 ), #21891, .F. ) ;
#11472=CARTESIAN_POINT ( 'NONE',  ( 4.967162193818130511, -3.259922920617460029, -42.96271701169388280 ) ) ;
#11476=EDGE_CURVE ( 'NONE', #10038, #51030, #48090, .T. ) ;
#11482=CARTESIAN_POINT ( 'NONE',  ( 4.956653778116991482, -9.917440902360828758, -47.05699031914960528 ) ) ;
#11485=ORIENTED_EDGE ( 'NONE', *, *, #16894, .T. ) ;
#11494=VECTOR ( 'NONE', #28571, 1000.000000000000114 ) ;
#11496=CARTESIAN_POINT ( 'NONE',  ( 5.965394784446460541, 7.868087674480955584, -18.95742317323937343 ) ) ;
#11501=CARTESIAN_POINT ( 'NONE',  ( 5.860006189529246790, 48.13093674595585014, -3.137522369585688864 ) ) ;
#11505=VERTEX_POINT ( 'NONE', #26408 ) ;
#11506=CARTESIAN_POINT ( 'NONE',  ( 5.965394784446460541, -5.298374383010499677, -19.82972329408683976 ) ) ;
#11515=CARTESIAN_POINT ( 'NONE',  ( 2.526552050251863246, -42.96196914573630465, -1.212569781798380486 ) ) ;
#11517=VERTEX_POINT ( 'NONE', #54272 ) ;
#11521=CARTESIAN_POINT ( 'NONE',  ( 1.088313998177382391, -36.76812638579213655, -22.12859469727376904 ) ) ;
#11525=B_SPLINE_CURVE_WITH_KNOTS ( 'NONE', 3,
 ( #32899, #51975, #9067, #28174 ),
 .UNSPECIFIED., .F., .F.,
 ( 4, 4 ),
 ( 0.000000000000000000, 0.005004741218457413668 ),
 .UNSPECIFIED. ) ;
#11529=CARTESIAN_POINT ( 'NONE',  ( 5.965394784446458765, -20.52536205633085231, 0.01447339372446240606 ) ) ;
#11545=B_SPLINE_CURVE_WITH_KNOTS ( 'NONE', 3,
 ( #28233, #61417, #18534, #18861 ),
 .UNSPECIFIED., .F., .F.,
 ( 4, 4 ),
 ( 2.168404344971008868E-19, 0.004048833967417088224 ),
 .UNSPECIFIED. ) ;
#11546=CARTESIAN_POINT ( 'NONE',  ( 0.6067099128993235224, 6.954009037736147647, 47.38952184036235593 ) ) ;
#11547=EDGE_CURVE ( 'NONE', #31462, #3804, #57720, .T. ) ;
#11554=VECTOR ( 'NONE', #38590, 1000.000000000000000 ) ;
#11556=CARTESIAN_POINT ( 'NONE',  ( 5.981074661064941900, -18.96560215432011631, -7.846517100474756035 ) ) ;
#11565=CARTESIAN_POINT ( 'NONE',  ( 0.8557997880470697982, -13.27832040216607190, -46.03118133706039572 ) ) ;
#11569=CARTESIAN_POINT ( 'NONE',  ( 3.270143674763207553, -2.058141141425505527, -13.53222904135356330 ) ) ;
#11572=CARTESIAN_POINT ( 'NONE',  ( 1.227938101723756947, 37.58536632582779191, 20.72293514920763258 ) ) ;
#11583=EDGE_CURVE ( 'NONE', #29154, #12616, #4123, .T. ) ;
#11584=CARTESIAN_POINT ( 'NONE',  ( 0.9730545539215883499, 41.31259007387230753, 11.59290486963521971 ) ) ;
#11588=B_SPLINE_CURVE_WITH_KNOTS ( 'NONE', 3,
 ( #16922, #17523, #45431, #50709, #46055, #31309, #60719, #40744, #3096, #30681, #31003, #7476, #12844, #7799, #50111, #25995 ),
 .UNSPECIFIED., .F., .F.,
 ( 4, 3, 3, 3, 3, 4 ),
 ( 1.551621725782133590E-17, 0.0002724568934985473071, 0.0004086836638483666486, 0.0005449104342063532851, 0.0008173270854453651554, 0.001089761613562688575 ),
 .UNSPECIFIED. ) ;
#11590=CARTESIAN_POINT ( 'NONE',  ( 2.624215991343608501, -30.33228621715059603, 37.21129343241594256 ) ) ;
#11593=CARTESIAN_POINT ( 'NONE',  ( 5.959547316686252039, -17.77392908783926728, -10.26589671991357022 ) ) ;
#11596=ORIENTED_EDGE ( 'NONE', *, *, #58050, .F. ) ;
#11600=VERTEX_POINT ( 'NONE', #57060 ) ;
#11603=CARTESIAN_POINT ( 'NONE',  ( 0.5809828226811544205, 33.48000389720665027, -34.25055090842118233 ) ) ;
#11622=CARTESIAN_POINT ( 'NONE',  ( 2.526464513654345989, -41.18424249084326760, 12.29060355381837155 ) ) ;
#11631=CARTESIAN_POINT ( 'NONE',  ( 0.9722240741986371004, -42.61332881199390954, 5.023189681690606534 ) ) ;
#11632=VECTOR ( 'NONE', #25139, 1000.000000000000000 ) ;
#11633=CARTESIAN_POINT ( 'NONE',  ( 0.5807400328401574052, 12.92266817606079421, -46.12278621143483548 ) ) ;
#11638=CARTESIAN_POINT ( 'NONE',  ( 4.967162193818130511, 28.07411493385340862, -32.68434214048137676 ) ) ;
#11644=EDGE_LOOP ( 'NONE', ( #51259, #14923, #46278, #49922 ) ) ;
#11646=DIRECTION ( 'NONE',  ( 0.07836865515943411409, 0.1223011693452784876, 0.9893941468723570498 ) ) ;
#11647=CARTESIAN_POINT ( 'NONE',  ( 0.7057020205114987732, 44.57024707370739236, -17.55108080125399184 ) ) ;
#11655=CARTESIAN_POINT ( 'NONE',  ( 0.9756950546413944991, -41.47131842451891970, -11.01205619898762933 ) ) ;
#11659=ORIENTED_EDGE ( 'NONE', *, *, #36136, .T. ) ;
#11660=ORIENTED_EDGE ( 'NONE', *, *, #40548, .F. ) ;
#11663=CARTESIAN_POINT ( 'NONE',  ( 0.6846871229502932144, 5.395516691087188121, 47.60345020167353880 ) ) ;
#11666=ORIENTED_EDGE ( 'NONE', *, *, #48568, .T. ) ;
#11674=CARTESIAN_POINT ( 'NONE',  ( 0.6846871229502932144, 46.04462816497486699, 13.23224427737845232 ) ) ;
#11677=CARTESIAN_POINT ( 'NONE',  ( 0.5850706913938533704, -37.88789093229785010, -29.30134895053094013 ) ) ;
#11680=VERTEX_POINT ( 'NONE', #9153 ) ;
#11681=CARTESIAN_POINT ( 'NONE',  ( 0.5850706913938533704, -24.10530971368318021, 41.38834827854200427 ) ) ;
#11686=CARTESIAN_POINT ( 'NONE',  ( 5.959547316686252039, 14.51128755440521267, 14.51632612601533801 ) ) ;
#11689=CARTESIAN_POINT ( 'NONE',  ( 0.9730545539215883499, -25.71816799638802920, 34.34678117142546938 ) ) ;
#11693=ORIENTED_EDGE ( 'NONE', *, *, #22923, .F. ) ;
#11704=CARTESIAN_POINT ( 'NONE',  ( 0.5850706913938534814, -37.88789093229826932, 29.30134895053040722 ) ) ;
#11708=CARTESIAN_POINT ( 'NONE',  ( 1.227938101723756947, 20.72293514920803048, -37.58536632582757875 ) ) ;
#11715=CARTESIAN_POINT ( 'NONE',  ( 4.303969348037258058, 45.22910199346975446, 16.39840148505108886 ) ) ;
#11718=( BOUNDED_SURFACE ( )  B_SPLINE_SURFACE ( 3, 1, ( 
 ( #10237, #22101 ),
 ( #26176, #41228 ),
 ( #40007, #12107 ),
 ( #2355, #55281 ) ),
 .UNSPECIFIED., .F., .F., .F. ) 
 B_SPLINE_SURFACE_WITH_KNOTS ( ( 4, 4 ),
 ( 2, 2 ),
 ( 0.000000000000000000, 1.000000000000000000 ),
 ( 0.000000000000000000, 1.000000000000000000 ),
 .UNSPECIFIED. ) 
 GEOMETRIC_REPRESENTATION_ITEM ( )  RATIONAL_B_SPLINE_SURFACE ( (
 ( 1.000000000000000000, 1.000000000000000000),
 ( 0.9953390228620291325, 0.8624445117760984880),
 ( 0.9953390228620291325, 0.8624445117760984880),
 ( 1.000000000000000000, 1.000000000000000000) ) ) 
 REPRESENTATION_ITEM ( '' )  SURFACE ( )  );
#11725=CARTESIAN_POINT ( 'NONE',  ( 4.956653778116990594, -20.77844580450529577, -43.37017594958076927 ) ) ;
#11735=CARTESIAN_POINT ( 'NONE',  ( 0.8557997880470599172, 47.60865952217007191, -5.347802024196765203 ) ) ;
#11743=EDGE_CURVE ( 'NONE', #9098, #8039, #15956, .T. ) ;
#11745=CARTESIAN_POINT ( 'NONE',  ( 0.9730545539215883499, -42.60426903087349615, -5.099196237955331057 ) ) ;
#11746=EDGE_LOOP ( 'NONE', ( #54409, #42973, #41859, #26636 ) ) ;
#11750=CARTESIAN_POINT ( 'NONE',  ( 0.7056555295713301534, 13.20840017675017819, 46.04438433984157086 ) ) ;
#11768=AXIS2_PLACEMENT_3D ( 'NONE', #5092, #57102, #10129 ) ;
#11783=CARTESIAN_POINT ( 'NONE',  ( 0.5809828226811553087, 38.32755012159145025, 28.72298383114502229 ) ) ;
#11786=CARTESIAN_POINT ( 'NONE',  ( -17.29657906255854982, -12.34027659683576772, -1.992589851484418917 ) ) ;
#11790=EDGE_CURVE ( 'NONE', #22861, #13203, #57692, .T. ) ;
#11791=CARTESIAN_POINT ( 'NONE',  ( 5.958863334805807099, -17.77634700750936148, 10.26176968287914093 ) ) ;
#11803=CARTESIAN_POINT ( 'NONE',  ( 5.860006189529246790, -40.11385274514700683, 26.78264244998084820 ) ) ;
#11813=EDGE_LOOP ( 'NONE', ( #34237, #6478, #11027, #61008 ) ) ;
#11818=CARTESIAN_POINT ( 'NONE',  ( 0.6067375320500725255, 41.82999795871641169, -23.33187539052085668 ) ) ;
#11825=( BOUNDED_SURFACE ( )  B_SPLINE_SURFACE ( 3, 1, ( 
 ( #16884, #17184 ),
 ( #55062, #50372 ),
 ( #21882, #21260 ),
 ( #36303, #12491 ) ),
 .UNSPECIFIED., .F., .F., .F. ) 
 B_SPLINE_SURFACE_WITH_KNOTS ( ( 4, 4 ),
 ( 2, 2 ),
 ( 0.000000000000000000, 1.000000000000000000 ),
 ( 0.000000000000000000, 1.000000000000000000 ),
 .UNSPECIFIED. ) 
 GEOMETRIC_REPRESENTATION_ITEM ( )  RATIONAL_B_SPLINE_SURFACE ( (
 ( 1.000000000000000000, 1.000000000000000000),
 ( 0.9732289882329797637, 0.9999525324661233672),
 ( 0.9732289882329797637, 0.9999525324661233672),
 ( 1.000000000000000000, 1.000000000000000000) ) ) 
 REPRESENTATION_ITEM ( '' )  SURFACE ( )  );
#11828=CARTESIAN_POINT ( 'NONE',  ( 0.9754642270333696574, 41.49150764699772509, -10.93570046136864882 ) ) ;
#11851=VECTOR ( 'NONE', #42378, 1000.000000000000000 ) ;
#11852=ORIENTED_EDGE ( 'NONE', *, *, #24431, .F. ) ;
#11861=ORIENTED_EDGE ( 'NONE', *, *, #14553, .T. ) ;
#11867=CARTESIAN_POINT ( 'NONE',  ( 0.5809828226811553087, 23.47450554821769231, -41.74875432577623258 ) ) ;
#11871=CARTESIAN_POINT ( 'NONE',  ( 3.783278058412225864, 39.06943705276857060, -18.05212641201930168 ) ) ;
#11885=CARTESIAN_POINT ( 'NONE',  ( 0.9730545539215883499, -39.83279466599050522, 15.95224156741815236 ) ) ;
#11888=VECTOR ( 'NONE', #52666, 1000.000000000000000 ) ;
#11892=CARTESIAN_POINT ( 'NONE',  ( 0.6846871229502932144, -24.69859318104518309, 41.05093867799178042 ) ) ;
#11897=CARTESIAN_POINT ( 'NONE',  ( 0.9757787079277437936, -39.62711913632688265, -16.45683390770826549 ) ) ;
#11898=CARTESIAN_POINT ( 'NONE',  ( 0.5800708119828337228, 28.65679933661850498, -38.37709857409239333 ) ) ;
#11899=CARTESIAN_POINT ( 'NONE',  ( 3.660087539127333311, 16.63102164621095014, -45.06758728829451854 ) ) ;
#11901=VERTEX_POINT ( 'NONE', #19347 ) ;
#11902=CARTESIAN_POINT ( 'NONE',  ( 4.303969348037258058, -36.81598326424571610, 30.97035057417647508 ) ) ;
#11903=CARTESIAN_POINT ( 'NONE',  ( 0.5809828226811553087, -29.58751527316153940, -37.66417181417581617 ) ) ;
#11904=ADVANCED_FACE ( 'NONE', ( #28415 ), #43125, .F. ) ;
#11908=LINE ( 'NONE', #50395, #12982 ) ;
#11909=ORIENTED_EDGE ( 'NONE', *, *, #10378, .T. ) ;
#11912=CARTESIAN_POINT ( 'NONE',  ( 5.960721111146673579, -0.006321279846963646747, 20.52557019979492026 ) ) ;
#11916=ADVANCED_FACE ( 'NONE', ( #38464 ), #24255, .F. ) ;
#11928=CARTESIAN_POINT ( 'NONE',  ( 0.9747592971366235703, -0.3237797888851980943, -42.90728926179870228 ) ) ;
#11942=CARTESIAN_POINT ( 'NONE',  ( 4.967162193818130511, 0.000000000000000000, 0.000000000000000000 ) ) ;
#11960=CARTESIAN_POINT ( 'NONE',  ( 0.9752570700956787464, 21.65368877244807067, -37.04395688491826633 ) ) ;
#11967=CARTESIAN_POINT ( 'NONE',  ( 0.8557997880470599172, 37.44587306708097429, 29.88293891557482951 ) ) ;
#11973=CARTESIAN_POINT ( 'NONE',  ( 0.5836750258453351492, 46.21662382526654511, 12.57171936981178995 ) ) ;
#11974=CARTESIAN_POINT ( 'NONE',  ( 0.5800708057587394828, 44.48635630048023870, -17.74761804745354254 ) ) ;
#11989=ADVANCED_FACE ( 'NONE', ( #45022 ), #34697, .F. ) ;
#11992=ORIENTED_EDGE ( 'NONE', *, *, #15032, .T. ) ;
#11993=LINE ( 'NONE', #21055, #7033 ) ;
#11997=CARTESIAN_POINT ( 'NONE',  ( 1.088908134280552664, 39.93902428011489292, 15.69861202536767131 ) ) ;
#12000=ADVANCED_FACE ( 'NONE', ( #40324 ), #38816, .T. ) ;
#12007=VERTEX_POINT ( 'NONE', #15883 ) ;
#12008=CARTESIAN_POINT ( 'NONE',  ( 0.9730545539215883499, -42.90536227157002003, 0.5054011016611185125 ) ) ;
#12021=CARTESIAN_POINT ( 'NONE',  ( 0.5809828226811617480, 12.92184523170268839, -46.11980934799325382 ) ) ;
#12024=B_SPLINE_CURVE_WITH_KNOTS ( 'NONE', 3,
 ( #40846, #44309, #12322, #40233 ),
 .UNSPECIFIED., .F., .F.,
 ( 4, 4 ),
 ( 2.168404344971008868E-19, 0.004048833967417081285 ),
 .UNSPECIFIED. ) ;
#12027=CARTESIAN_POINT ( 'NONE',  ( 3.270143674763207553, -5.490410281242683155, -12.53844339339240754 ) ) ;
#12031=DIRECTION ( 'NONE',  ( -0.07439287786467650709, -0.7830499462674556099, 0.6174937095821675381 ) ) ;
#12032=CARTESIAN_POINT ( 'NONE',  ( 3.783198216974391404, 7.325057189011020320, -42.41041696600769484 ) ) ;
#12033=CARTESIAN_POINT ( 'NONE',  ( 0.6067099128993204138, 29.71710940500729592, 37.56352526808316838 ) ) ;
#12038=CARTESIAN_POINT ( 'NONE',  ( 1.227938101723756947, 10.28900963485438425, -41.66816631169181306 ) ) ;
#12043=CARTESIAN_POINT ( 'NONE',  ( -17.97369999999976642, 0.000000000000000000, 2.099999999999994760 ) ) ;
#12045=ORIENTED_EDGE ( 'NONE', *, *, #14501, .T. ) ;
#12047=CARTESIAN_POINT ( 'NONE',  ( 3.660176727303401822, -14.24118031989626232, 45.87883389004763757 ) ) ;
#12050=ORIENTED_EDGE ( 'NONE', *, *, #5352, .T. ) ;
#12052=CARTESIAN_POINT ( 'NONE',  ( 0.6846871229502899947, -13.23224427737796915, -46.04462816497500910 ) ) ;
#12058=CARTESIAN_POINT ( 'NONE',  ( 3.783278058412225864, -3.901118461247123470, 42.86118820526429829 ) ) ;
#12062=CARTESIAN_POINT ( 'NONE',  ( 5.965394784446460541, -20.34787558161485066, -2.693446924985554602 ) ) ;
#12074=CARTESIAN_POINT ( 'NONE',  ( 0.5839879882012687373, 12.39635945869026834, -46.26395995854822729 ) ) ;
#12081=CARTESIAN_POINT ( 'NONE',  ( 4.956653778116975495, 14.93973939759886704, 45.71126949320255761 ) ) ;
#12085=CARTESIAN_POINT ( 'NONE',  ( 4.967162193818130511, -42.96271701169384016, -3.259922920618186115 ) ) ;
#12086=CARTESIAN_POINT ( 'NONE',  ( 0.9730545539215883499, 36.90443313492330901, 21.89037132892449478 ) ) ;
#12087=B_SPLINE_CURVE_WITH_KNOTS ( 'NONE', 3,
 ( #39007, #43707, #11100, #57435, #48991, #15488, #43394, #48373, #33991, #38387, #28961, #49289, #10790, #1352, #34913, #24574, #14573, #5436, #755 ),
 .UNSPECIFIED., .F., .F.,
 ( 4, 3, 3, 3, 3, 3, 4 ),
 ( 6.938893903907227607E-18, 0.0002724573126191799839, 0.0004086839781548505914, 0.0005449106435901909188, 0.0006811373090491549273, 0.0008459866663933714344, 0.001010840725717212282 ),
 .UNSPECIFIED. ) ;
#12095=CARTESIAN_POINT ( 'NONE',  ( 0.5819845079324661441, 46.14435090135493311, -12.83441846783082418 ) ) ;
#12098=CARTESIAN_POINT ( 'NONE',  ( 0.5809828226811617480, 37.66417181417551774, 29.58751527316192664 ) ) ;
#12102=EDGE_CURVE ( 'NONE', #44660, #4479, #16682, .T. ) ;
#12103=DIRECTION ( 'NONE',  ( 0.07836865515943411409, -0.8672783706145228422, 0.4916162952473402958 ) ) ;
#12107=CARTESIAN_POINT ( 'NONE',  ( 0.5786265663353153954, -46.45062944555884599, -11.69877690266703851 ) ) ;
#12115=VERTEX_POINT ( 'NONE', #13046 ) ;
#12118=CARTESIAN_POINT ( 'NONE',  ( 1.227938101723748288, 41.23019537246709376, 11.92353943227963597 ) ) ;
#12119=( BOUNDED_SURFACE ( )  B_SPLINE_SURFACE ( 3, 1, ( 
 ( #14291, #783 ),
 ( #460, #53392 ),
 ( #24600, #53089 ),
 ( #61854, #10500 ) ),
 .UNSPECIFIED., .F., .F., .F. ) 
 B_SPLINE_SURFACE_WITH_KNOTS ( ( 4, 4 ),
 ( 2, 2 ),
 ( 0.000000000000000000, 1.000000000000000000 ),
 ( 0.000000000000000000, 1.000000000000000000 ),
 .UNSPECIFIED. ) 
 GEOMETRIC_REPRESENTATION_ITEM ( )  RATIONAL_B_SPLINE_SURFACE ( (
 ( 1.000000000000000000, 1.000000000000000000),
 ( 0.9953390228620291325, 0.8624445117760984880),
 ( 0.9953390228620291325, 0.8624445117760984880),
 ( 1.000000000000000000, 1.000000000000000000) ) ) 
 REPRESENTATION_ITEM ( '' )  SURFACE ( )  );
#12121=DIRECTION ( 'NONE',  ( 0.000000000000000000, 0.000000000000000000, -1.000000000000000000 ) ) ;
#12122=CARTESIAN_POINT ( 'NONE',  ( 5.959828726073459926, -18.96145866559666615, -7.858992891710077089 ) ) ;
#12124=EDGE_LOOP ( 'NONE', ( #19912, #19211, #22237, #55809 ) ) ;
#12128=CARTESIAN_POINT ( 'NONE',  ( 3.660087539126826606, -22.37124151181825127, 42.51124390328611469 ) ) ;
#12130=ORIENTED_EDGE ( 'NONE', *, *, #1264, .F. ) ;
#12132=ORIENTED_EDGE ( 'NONE', *, *, #10753, .F. ) ;
#12133=FACE_OUTER_BOUND ( 'NONE', #11422, .T. ) ;
#12140=VERTEX_POINT ( 'NONE', #8300 ) ;
#12142=CARTESIAN_POINT ( 'NONE',  ( 5.958863334805807099, 0.001220270595885530451, 20.52565293643016275 ) ) ;
#12144=EDGE_LOOP ( 'NONE', ( #49020, #49610, #43695, #37166 ) ) ;
#12145=CARTESIAN_POINT ( 'NONE',  ( 2.526552050251863690, -27.11558601691289638, 33.34585601411856715 ) ) ;
#12148=EDGE_CURVE ( 'NONE', #46817, #1532, #47302, .T. ) ;
#12149=VERTEX_POINT ( 'NONE', #27420 ) ;
#12150=CARTESIAN_POINT ( 'NONE',  ( 2.624215991343608501, 19.66774719433037788, -43.79392271049049867 ) ) ;
#12155=ORIENTED_EDGE ( 'NONE', *, *, #8954, .F. ) ;
#12161=CARTESIAN_POINT ( 'NONE',  ( 3.270143674763207553, 8.548517033725252290, 10.69018354892890876 ) ) ;
#12164=ORIENTED_EDGE ( 'NONE', *, *, #9425, .T. ) ;
#12167=DIRECTION ( 'NONE',  ( 0.07439287786467665975, -0.8701500408883711124, 0.4871392060437932936 ) ) ;
#12186=AXIS2_PLACEMENT_3D ( 'NONE', #10488, #29583, #5748 ) ;
#12187=CARTESIAN_POINT ( 'NONE',  ( 0.5850706913938533704, -33.73916126769427848, -33.99603398296626011 ) ) ;
#12190=CARTESIAN_POINT ( 'NONE',  ( 4.967162193818130511, -8.839793687085512275, 42.16965968614191240 ) ) ;
#12203=CARTESIAN_POINT ( 'NONE',  ( 0.9740398440564312921, -26.44872719679347739, -33.78760696452732049 ) ) ;
#12218=ORIENTED_EDGE ( 'NONE', *, *, #36955, .F. ) ;
#12226=ADVANCED_FACE ( 'NONE', ( #43093 ), #37093, .F. ) ;
#12228=ORIENTED_EDGE ( 'NONE', *, *, #27751, .T. ) ;
#12229=CARTESIAN_POINT ( 'NONE',  ( 0.9754402186311946776, -0.1875553420608594424, -42.90805920318128130 ) ) ;
#12233=CARTESIAN_POINT ( 'NONE',  ( 0.8551540677456715978, 33.23105123575899711, 34.52115452272941098 ) ) ;
#12236=CARTESIAN_POINT ( 'NONE',  ( 5.974727161628367256, 19.82156119440445607, -5.327229920347220649 ) ) ;
#12240=DIRECTION ( 'NONE',  ( -1.000000000000000000, -0.000000000000000000, -0.000000000000000000 ) ) ;
#12250=CARTESIAN_POINT ( 'NONE',  ( 0.9730545539215883499, -34.34678117142574649, 25.71816799638765971 ) ) ;
#12251=DIRECTION ( 'NONE',  ( -1.000000000000000000, 0.000000000000000000, 0.000000000000000000 ) ) ;
#12253=LINE ( 'NONE', #55746, #31822 ) ;
#12254=ORIENTED_EDGE ( 'NONE', *, *, #9533, .T. ) ;
#12258=CARTESIAN_POINT ( 'NONE',  ( 2.624215991343620935, 37.21129343241644705, -30.33228621714997431 ) ) ;
#12259=ADVANCED_FACE ( 'NONE', ( #9548 ), #49500, .F. ) ;
#12264=CARTESIAN_POINT ( 'NONE',  ( 0.9730545539215883499, 41.57420493492384850, 10.61654491617579055 ) ) ;
#12265=CARTESIAN_POINT ( 'NONE',  ( 0.5786265663353196143, -44.52624106864154641, 17.66171603226064590 ) ) ;
#12266=CARTESIAN_POINT ( 'NONE',  ( 5.965394784446460541, -17.76824826579347416, -10.27521535480980219 ) ) ;
#12278=CARTESIAN_POINT ( 'NONE',  ( 0.5809828226811553087, -46.11980934799348830, 12.92184523170186594 ) ) ;
#12282=CARTESIAN_POINT ( 'NONE',  ( 0.9730545539215883499, 10.61654491617563423, 41.57420493492389113 ) ) ;
#12283=B_SPLINE_CURVE_WITH_KNOTS ( 'NONE', 3,
 ( #30956, #50064, #22176, #4268, #31571, #46612 ),
 .UNSPECIFIED., .F., .F.,
 ( 4, 2, 4 ),
 ( 0.000000000000000000, 0.0002291966416970788345, 0.0004583932833941576691 ),
 .UNSPECIFIED. ) ;
#12286=ORIENTED_EDGE ( 'NONE', *, *, #35859, .F. ) ;
#12287=CARTESIAN_POINT ( 'NONE',  ( 5.959828726073459926, 12.49160845136013265, 16.28681682518067930 ) ) ;
#12292=CARTESIAN_POINT ( 'NONE',  ( 5.958863334805807099, 0.001220270596169137139, -20.52565293643016275 ) ) ;
#12299=CARTESIAN_POINT ( 'NONE',  ( 0.8551540677456715978, 46.03951182599426772, 13.28067116677218529 ) ) ;
#12306=CARTESIAN_POINT ( 'NONE',  ( 5.981074661064941900, 12.48781255314267113, 16.28853686865603123 ) ) ;
#12307=CARTESIAN_POINT ( 'NONE',  ( 0.9758171775293912331, 26.12572690811914455, 34.03798695362321070 ) ) ;
#12311=CARTESIAN_POINT ( 'NONE',  ( 3.783278058412224976, -29.18720354295066599, 31.62921638229657262 ) ) ;
#12314=ORIENTED_EDGE ( 'NONE', *, *, #27036, .T. ) ;
#12318=CARTESIAN_POINT ( 'NONE',  ( 0.9756008150404607004, -16.28894658522360217, 39.69644259322203084 ) ) ;
#12320=EDGE_CURVE ( 'NONE', #9811, #3346, #47968, .T. ) ;
#12322=CARTESIAN_POINT ( 'NONE',  ( 3.783198216974386963, -12.79806054635163370, 41.09147814699338852 ) ) ;
#12328=EDGE_CURVE ( 'NONE', #31835, #8537, #39788, .T. ) ;
#12332=CARTESIAN_POINT ( 'NONE',  ( 0.5786265663353196143, -11.69877690266622317, -46.45062944555905204 ) ) ;
#12335=CARTESIAN_POINT ( 'NONE',  ( 5.960721111146673579, 20.34914600876575363, -2.685391721745826299 ) ) ;
#12337=CARTESIAN_POINT ( 'NONE',  ( 5.960721111146673579, -18.96073515164543011, -7.860635756377828187 ) ) ;
#12357=CARTESIAN_POINT ( 'NONE',  ( 4.967162193818130511, 0.000000000000000000, 0.000000000000000000 ) ) ;
#12358=CARTESIAN_POINT ( 'NONE',  ( 0.5850706913938534814, 44.31965802246106279, 18.16120156791897244 ) ) ;
#12369=CARTESIAN_POINT ( 'NONE',  ( 1.154321485836935723, -29.75729673892721650, 30.92445806269068242 ) ) ;
#12371=ORIENTED_EDGE ( 'NONE', *, *, #15288, .T. ) ;
#12377=CARTESIAN_POINT ( 'NONE',  ( 0.9730545539215883499, -30.69604515769629316, -29.98130006528894498 ) ) ;
#12384=CARTESIAN_POINT ( 'NONE',  ( 4.960156602257181468, -46.28683144126593874, -3.546989772330372492 ) ) ;
#12391=CARTESIAN_POINT ( 'NONE',  ( 5.959828726073459926, -19.82738831247216993, 5.308046411394905739 ) ) ;
#12395=CARTESIAN_POINT ( 'NONE',  ( 0.9736507210033057413, -5.153758453069271717, -42.59776535855984747 ) ) ;
#12397=CARTESIAN_POINT ( 'NONE',  ( 0.5839879882012686263, 37.99844431214167884, 29.15719377327458872 ) ) ;
#12409=CARTESIAN_POINT ( 'NONE',  ( 4.967162193818130511, 3.259922920617742914, 42.96271701169386859 ) ) ;
#12420=DIRECTION ( 'NONE',  ( -1.000000000000000000, -0.000000000000000000, -0.000000000000000000 ) ) ;
#12427=VERTEX_POINT ( 'NONE', #43718 ) ;
#12437=CARTESIAN_POINT ( 'NONE',  ( 3.407937589446174087, 7.970324840161956637, 11.14158115674376148 ) ) ;
#12440=CARTESIAN_POINT ( 'NONE',  ( 5.965394784446458765, 20.52536205633085231, -0.01447339372431907453 ) ) ;
#12441=CARTESIAN_POINT ( 'NONE',  ( 0.5819845901640494645, 41.70428411658559043, -23.55368560422299140 ) ) ;
#12450=ORIENTED_EDGE ( 'NONE', *, *, #29300, .F. ) ;
#12456=CARTESIAN_POINT ( 'NONE',  ( 4.967162193818130511, -40.93989340068600313, -13.42934394584206359 ) ) ;
#12472=ORIENTED_EDGE ( 'NONE', *, *, #21522, .T. ) ;
#12478=CARTESIAN_POINT ( 'NONE',  ( 0.9730545539215883499, -29.98130006528883129, 30.69604515769640329 ) ) ;
#12482=CARTESIAN_POINT ( 'NONE',  ( 0.7056555295713289322, -47.37451042924659106, 7.085402321211620169 ) ) ;
#12487=( BOUNDED_SURFACE ( )  B_SPLINE_SURFACE ( 3, 1, ( 
 ( #4320, #37583 ),
 ( #38202, #13454 ),
 ( #9663, #18155 ),
 ( #32566, #51643 ) ),
 .UNSPECIFIED., .F., .F., .F. ) 
 B_SPLINE_SURFACE_WITH_KNOTS ( ( 4, 4 ),
 ( 2, 2 ),
 ( 0.000000000000000000, 1.000000000000000000 ),
 ( 0.000000000000000000, 1.000000000000000000 ),
 .UNSPECIFIED. ) 
 GEOMETRIC_REPRESENTATION_ITEM ( )  RATIONAL_B_SPLINE_SURFACE ( (
 ( 1.000000000000000000, 1.000000000000000000),
 ( 0.9953390228620291325, 0.8624445117761032620),
 ( 0.9953390228620291325, 0.8624445117761032620),
 ( 1.000000000000000000, 1.000000000000000000) ) ) 
 REPRESENTATION_ITEM ( '' )  SURFACE ( )  );
#12488=CARTESIAN_POINT ( 'NONE',  ( 0.9756008150404598123, -39.58764833544687889, 16.55159915785265667 ) ) ;
#12491=CARTESIAN_POINT ( 'NONE',  ( 0.5807400328401574052, -18.83234461715214181, 44.04145271122558825 ) ) ;
#12496=CARTESIAN_POINT ( 'NONE',  ( 0.5837374860065631665, -24.10515569139019831, -41.38807031854337737 ) ) ;
#12497=EDGE_CURVE ( 'NONE', #26349, #44905, #61359, .T. ) ;
#12499=CARTESIAN_POINT ( 'NONE',  ( -48.95476116535499500, 1.530808498934191127E-15, 12.50000000000000000 ) ) ;
#12526=EDGE_CURVE ( 'NONE', #46592, #22531, #7551, .T. ) ;
#12535=CARTESIAN_POINT ( 'NONE',  ( 0.7762777257811902532, 43.90991299786900015, 19.15108781300947172 ) ) ;
#12537=FACE_OUTER_BOUND ( 'NONE', #56777, .T. ) ;
#12540=CARTESIAN_POINT ( 'NONE',  ( 0.9730545539215883499, 10.61654491617563423, 41.57420493492389113 ) ) ;
#12544=ORIENTED_EDGE ( 'NONE', *, *, #11476, .F. ) ;
#12545=VERTEX_POINT ( 'NONE', #36156 ) ;
#12556=ADVANCED_FACE ( 'NONE', ( #51144 ), #47720, .T. ) ;
#12557=CARTESIAN_POINT ( 'NONE',  ( 5.958863334805807099, 14.51296551801802970, -14.51469124124464827 ) ) ;
#12559=CARTESIAN_POINT ( 'NONE',  ( 0.8551540677456834771, 47.37911285756630519, -7.157691013573882266 ) ) ;
#12562=( BOUNDED_SURFACE ( )  B_SPLINE_SURFACE ( 3, 1, ( 
 ( #46761, #56740 ),
 ( #61127, #8831 ),
 ( #47669, #14174 ),
 ( #22947, #33278 ) ),
 .UNSPECIFIED., .F., .F., .F. ) 
 B_SPLINE_SURFACE_WITH_KNOTS ( ( 4, 4 ),
 ( 2, 2 ),
 ( 0.000000000000000000, 1.000000000000000000 ),
 ( 0.000000000000000000, 1.000000000000000000 ),
 .UNSPECIFIED. ) 
 GEOMETRIC_REPRESENTATION_ITEM ( )  RATIONAL_B_SPLINE_SURFACE ( (
 ( 1.000000000000000000, 1.000000000000000000),
 ( 0.9953390228620291325, 0.8624445117760984880),
 ( 0.9953390228620291325, 0.8624445117760984880),
 ( 1.000000000000000000, 1.000000000000000000) ) ) 
 REPRESENTATION_ITEM ( '' )  SURFACE ( )  );
#12565=CARTESIAN_POINT ( 'NONE',  ( 0.5807400328401637335, 38.33001520688989672, -28.72484455891601840 ) ) ;
#12566=LINE ( 'NONE', #3134, #36874 ) ;
#12571=ADVANCED_FACE ( 'NONE', ( #56764 ), #11098, .F. ) ;
#12578=CARTESIAN_POINT ( 'NONE',  ( 0.5827357941260215002, -29.44458568814485488, -37.77622264066042135 ) ) ;
#12579=ORIENTED_EDGE ( 'NONE', *, *, #25585, .T. ) ;
#12581=VECTOR ( 'NONE', #40261, 1000.000000000000000 ) ;
#12590=ORIENTED_EDGE ( 'NONE', *, *, #51270, .T. ) ;
#12594=ORIENTED_EDGE ( 'NONE', *, *, #28006, .F. ) ;
#12597=VERTEX_POINT ( 'NONE', #46793 ) ;
#12599=VERTEX_POINT ( 'NONE', #32369 ) ;
#12600=CARTESIAN_POINT ( 'NONE',  ( 0.8551540677456715978, 5.348818140990894143, 47.61725548905992866 ) ) ;
#12601=B_SPLINE_CURVE_WITH_KNOTS ( 'NONE', 3,
 ( #41499, #55875, #23301, #12998, #32091, #7960 ),
 .UNSPECIFIED., .F., .F.,
 ( 4, 2, 4 ),
 ( 8.148123767742043513E-18, 0.0002291978881530167022, 0.0004583957763060252186 ),
 .UNSPECIFIED. ) ;
#12606=EDGE_CURVE ( 'NONE', #58891, #21001, #9162, .T. ) ;
#12616=VERTEX_POINT ( 'NONE', #23272 ) ;
#12617=CARTESIAN_POINT ( 'NONE',  ( 0.9754642270333672149, -42.90808635884414457, -0.1757168848623658075 ) ) ;
#12618=ORIENTED_EDGE ( 'NONE', *, *, #43178, .F. ) ;
#12619=CARTESIAN_POINT ( 'NONE',  ( 4.967162193818130511, 3.259922920617742914, 42.96271701169386859 ) ) ;
#12621=CARTESIAN_POINT ( 'NONE',  ( 2.281351352603241622, -17.13758816714718591, -44.80774876812576935 ) ) ;
#12624=CARTESIAN_POINT ( 'NONE',  ( 4.967162193818130511, 7.970725651240403664, -42.34252806656584056 ) ) ;
#12630=DIRECTION ( 'NONE',  ( -1.000000000000000000, -0.000000000000000000, -0.000000000000000000 ) ) ;
#12635=B_SPLINE_CURVE_WITH_KNOTS ( 'NONE', 3,
 ( #48739, #24632, #57492, #10531 ),
 .UNSPECIFIED., .F., .F.,
 ( 4, 4 ),
 ( 0.000000000000000000, 0.004446090762761387670 ),
 .UNSPECIFIED. ) ;
#12637=CARTESIAN_POINT ( 'NONE',  ( 4.956653778116488773, 2.599733001513538255, 48.02038484091099235 ) ) ;
#12646=CARTESIAN_POINT ( 'NONE',  ( 5.958863334805807099, -2.680345151634763834, 20.34989385289152963 ) ) ;
#12647=EDGE_CURVE ( 'NONE', #42943, #10214, #57576, .T. ) ;
#12651=CARTESIAN_POINT ( 'NONE',  ( 5.960721111146673579, -16.28018152803684515, -12.50019045452732591 ) ) ;
#12662=EDGE_LOOP ( 'NONE', ( #58487, #60313, #44710, #37752 ) ) ;
#12667=VECTOR ( 'NONE', #8891, 1000.000000000000114 ) ;
#12669=CIRCLE ( 'NONE', #1623, 48.09070567114147110 ) ;
#12677=ORIENTED_EDGE ( 'NONE', *, *, #24352, .F. ) ;
#12680=EDGE_CURVE ( 'NONE', #10980, #57884, #28572, .T. ) ;
#12688=CARTESIAN_POINT ( 'NONE',  ( 3.660087539127315992, 47.83637163185232311, 4.399983418616303155 ) ) ;
#12689=VERTEX_POINT ( 'NONE', #48308 ) ;
#12690=CARTESIAN_POINT ( 'NONE',  ( 4.967162193818130511, 0.000000000000000000, 0.000000000000000000 ) ) ;
#12693=CARTESIAN_POINT ( 'NONE',  ( 0.6846871229502899947, -19.12907057981172088, -43.92355552798057516 ) ) ;
#12695=CARTESIAN_POINT ( 'NONE',  ( 0.9752570700956790795, 30.17732761204941738, 30.50353876750642357 ) ) ;
#12706=CARTESIAN_POINT ( 'NONE',  ( 0.6846871229502899947, 11.56285438919697306, -46.49193983736579128 ) ) ;
#12708=CARTESIAN_POINT ( 'NONE',  ( 0.9968887458511662691, -22.02152923727777178, 36.82760690604620635 ) ) ;
#12713=VECTOR ( 'NONE', #7971, 1000.000000000000114 ) ;
#12716=CARTESIAN_POINT ( 'NONE',  ( 3.407937589446174087, 10.00592723328973932, -9.356405769958946905 ) ) ;
#12717=CARTESIAN_POINT ( 'NONE',  ( 0.5809828226811553087, -12.92184523170170607, -46.11980934799353093 ) ) ;
#12718=CARTESIAN_POINT ( 'NONE',  ( 3.407937589446178528, 11.62731850632894215, -7.243367523630903193 ) ) ;
#12719=B_SPLINE_CURVE_WITH_KNOTS ( 'NONE', 3,
 ( #53146, #10561, #48764, #10254, #35001, #24658 ),
 .UNSPECIFIED., .F., .F.,
 ( 4, 2, 4 ),
 ( 9.875171458978167205E-18, 0.0002291978881530160788, 0.0004583957763060222913 ),
 .UNSPECIFIED. ) ;
#12721=CARTESIAN_POINT ( 'NONE',  ( 0.5809828226811553087, -41.20389530892325070, 24.41822904836909203 ) ) ;
#12724=EDGE_CURVE ( 'NONE', #11600, #10306, #43953, .T. ) ;
#12728=CARTESIAN_POINT ( 'NONE',  ( 4.956653778116990594, -39.67974989265022145, -27.17045123668512474 ) ) ;
#12737=CARTESIAN_POINT ( 'NONE',  ( 4.956653778116966613, 0.000000000000000000, 0.000000000000000000 ) ) ;
#12738=FACE_OUTER_BOUND ( 'NONE', #55249, .T. ) ;
#12753=VECTOR ( 'NONE', #44513, 1000.000000000000114 ) ;
#12757=FACE_OUTER_BOUND ( 'NONE', #1772, .T. ) ;
#12771=ORIENTED_EDGE ( 'NONE', *, *, #46076, .F. ) ;
#12776=EDGE_CURVE ( 'NONE', #9477, #24263, #49389, .T. ) ;
#12777=CARTESIAN_POINT ( 'NONE',  ( 2.281351352603289584, -7.562287671717538906, 47.37344280316143852 ) ) ;
#12780=CARTESIAN_POINT ( 'NONE',  ( 2.624215991343608501, 47.98682984381861161, 1.411420423865641149 ) ) ;
#12791=AXIS2_PLACEMENT_3D ( 'NONE', #2054, #16488, #21186 ) ;
#12795=CARTESIAN_POINT ( 'NONE',  ( 0.5807400328401637335, 18.83234461715243313, -44.04145271122544614 ) ) ;
#12797=FACE_OUTER_BOUND ( 'NONE', #61203, .T. ) ;
#12804=CARTESIAN_POINT ( 'NONE',  ( 0.9752132459055852243, -39.55248938404429992, 16.63533515462565404 ) ) ;
#12807=FACE_OUTER_BOUND ( 'NONE', #61834, .T. ) ;
#12823=CARTESIAN_POINT ( 'NONE',  ( 0.5807400328401637335, -34.25275203086259523, 33.48217046439098965 ) ) ;
#12826=B_SPLINE_CURVE_WITH_KNOTS ( 'NONE', 3,
 ( #43162, #19969, #58138, #34367 ),
 .UNSPECIFIED., .F., .F.,
 ( 4, 4 ),
 ( 0.000000000000000000, 0.004048833967417087357 ),
 .UNSPECIFIED. ) ;
#12828=EDGE_CURVE ( 'NONE', #25918, #2384, #58689, .T. ) ;
#12830=EDGE_LOOP ( 'NONE', ( #47025, #9048, #56256, #21291 ) ) ;
#12836=EDGE_CURVE ( 'NONE', #55315, #20695, #46103, .T. ) ;
#12844=CARTESIAN_POINT ( 'NONE',  ( 0.5832366564991507962, -38.16363840618235770, -28.94058080282821166 ) ) ;
#12861=( BOUNDED_SURFACE ( )  B_SPLINE_SURFACE ( 3, 1, ( 
 ( #57394, #4464 ),
 ( #23603, #28918 ),
 ( #35802, #11677 ),
 ( #44586, #30760 ) ),
 .UNSPECIFIED., .F., .F., .F. ) 
 B_SPLINE_SURFACE_WITH_KNOTS ( ( 4, 4 ),
 ( 2, 2 ),
 ( 0.000000000000000000, 1.000000000000000000 ),
 ( 0.000000000000000000, 1.000000000000000000 ),
 .UNSPECIFIED. ) 
 GEOMETRIC_REPRESENTATION_ITEM ( )  RATIONAL_B_SPLINE_SURFACE ( (
 ( 1.000000000000000000, 1.000000000000000000),
 ( 0.9732289882329797637, 0.9999525324661233672),
 ( 0.9732289882329797637, 0.9999525324661233672),
 ( 1.000000000000000000, 1.000000000000000000) ) ) 
 REPRESENTATION_ITEM ( '' )  SURFACE ( )  );
#12866=VECTOR ( 'NONE', #5042, 1000.000000000000114 ) ;
#12867=ORIENTED_EDGE ( 'NONE', *, *, #49712, .T. ) ;
#12868=CARTESIAN_POINT ( 'NONE',  ( 4.963659409799330291, 42.53037318520993182, 13.93274247732036031 ) ) ;
#12872=CARTESIAN_POINT ( 'NONE',  ( 0.9722240750034573109, 21.95618656574004746, 36.86535092060686480 ) ) ;
#12876=CARTESIAN_POINT ( 'NONE',  ( 5.960221823109900008, -2.673723662181486826, 20.35070456576729825 ) ) ;
#12883=EDGE_CURVE ( 'NONE', #817, #42473, #36782, .T. ) ;
#12887=AXIS2_PLACEMENT_3D ( 'NONE', #36774, #13264, #55844 ) ;
#12890=CARTESIAN_POINT ( 'NONE',  ( 0.5800708119828333897, 47.89175345941821149, -0.6275298934116645411 ) ) ;
#12893=CARTESIAN_POINT ( 'NONE',  ( 5.974727161628367256, -17.76736931401867281, 10.27590650342006384 ) ) ;
#12902=EDGE_CURVE ( 'NONE', #46350, #46904, #39745, .T. ) ;
#12907=ORIENTED_EDGE ( 'NONE', *, *, #32191, .T. ) ;
#12937=ORIENTED_EDGE ( 'NONE', *, *, #25020, .T. ) ;
#12944=CARTESIAN_POINT ( 'NONE',  ( 0.6067375320500691949, -29.71715680108759727, 37.56348932307251687 ) ) ;
#12957=CARTESIAN_POINT ( 'NONE',  ( 5.965394784446458765, 20.34787558161486842, -2.693446924985416491 ) ) ;
#12961=ADVANCED_FACE ( 'NONE', ( #51688 ), #44778, .F. ) ;
#12964=EDGE_CURVE ( 'NONE', #58751, #33696, #61686, .T. ) ;
#12982=VECTOR ( 'NONE', #2464, 999.9999999999998863 ) ;
#12983=CARTESIAN_POINT ( 'NONE',  ( 0.8557997880470690211, -34.51495345639526136, -33.22501220301936797 ) ) ;
#12994=CARTESIAN_POINT ( 'NONE',  ( 5.860006189529234355, -21.31760477694612987, 43.26650951066862660 ) ) ;
#12997=CARTESIAN_POINT ( 'NONE',  ( 5.959547316686252039, 14.51632612601528827, -14.51128755440526241 ) ) ;
#12998=CARTESIAN_POINT ( 'NONE',  ( 0.9972139404380309102, 17.02682566833184552, 39.38665787682671038 ) ) ;
#13004=CARTESIAN_POINT ( 'NONE',  ( 4.956653778116966613, 0.000000000000000000, 0.000000000000000000 ) ) ;
#13016=CARTESIAN_POINT ( 'NONE',  ( 3.270143674763207553, -11.98875605389984500, 6.605065939546772569 ) ) ;
#13020=FACE_OUTER_BOUND ( 'NONE', #52106, .T. ) ;
#13021=CARTESIAN_POINT ( 'NONE',  ( 0.6067099128993225232, -6.954009037735842114, -47.38952184036241277 ) ) ;
#13022=CARTESIAN_POINT ( 'NONE',  ( 1.227938101723748288, -22.18841447410744649, 36.73927144310504644 ) ) ;
#13025=ORIENTED_EDGE ( 'NONE', *, *, #15942, .T. ) ;
#13026=VECTOR ( 'NONE', #58623, 1000.000000000000114 ) ;
#13027=CARTESIAN_POINT ( 'NONE',  ( 5.960221823109900008, 17.77295928189541740, 10.26751639438374397 ) ) ;
#13028=CARTESIAN_POINT ( 'NONE',  ( 0.8557997880470697982, -17.48760788519248521, 44.60232077416680596 ) ) ;
#13042=CONICAL_SURFACE ( 'NONE', #19073, 43.08621763946400307, 1.568696531533066763 ) ;
#13044=CARTESIAN_POINT ( 'NONE',  ( 3.407937589446178528, 12.82481284928203813, 4.815089211105102684 ) ) ;
#13046=CARTESIAN_POINT ( 'NONE',  ( 0.8557997880470599172, -41.93815086860273311, 23.15977007032308421 ) ) ;
#13049=CARTESIAN_POINT ( 'NONE',  ( 0.5809828226811565299, -23.47450554821739743, 41.74875432577639600 ) ) ;
#13053=CARTESIAN_POINT ( 'NONE',  ( 3.407937589446174087, -12.47329436636624678, -5.663729899985203708 ) ) ;
#13056=CARTESIAN_POINT ( 'NONE',  ( 5.960721111146673579, -20.34914600876573587, -2.685391721745965299 ) ) ;
#13059=AXIS2_PLACEMENT_3D ( 'NONE', #35850, #15812, #11413 ) ;
#13065=CARTESIAN_POINT ( 'NONE',  ( 4.956653778116975495, -14.93973939759918323, 45.71126949320244393 ) ) ;
#13075=CARTESIAN_POINT ( 'NONE',  ( 4.303969348037246512, 30.97035057417713588, -36.81598326424517609 ) ) ;
#13079=CIRCLE ( 'NONE', #40107, 48.09070567114147110 ) ;
#13081=ORIENTED_EDGE ( 'NONE', *, *, #12828, .F. ) ;
#13093=CARTESIAN_POINT ( 'NONE',  ( 5.965394784446460541, -2.664747781315973896, -20.35165389555757187 ) ) ;
#13096=CARTESIAN_POINT ( 'NONE',  ( 4.303969348037258058, -46.98258166031682492, -10.35452842635891990 ) ) ;
#13100=CARTESIAN_POINT ( 'NONE',  ( 5.958863334805807099, 2.680345151634340617, 20.34989385289158648 ) ) ;
#13105=CARTESIAN_POINT ( 'NONE',  ( 0.9722240750034576440, -42.61332880321396033, -5.023189755349382501 ) ) ;
#13106=EDGE_CURVE ( 'NONE', #49884, #23849, #13460, .T. ) ;
#13114=CARTESIAN_POINT ( 'NONE',  ( 0.5786265663353153954, -44.52624106864131193, -17.66171603226127829 ) ) ;
#13120=( BOUNDED_SURFACE ( )  B_SPLINE_SURFACE ( 3, 1, ( 
 ( #14222, #13599 ),
 ( #9494, #9190 ),
 ( #52713, #28297 ),
 ( #5081, #28599 ) ),
 .UNSPECIFIED., .F., .F., .F. ) 
 B_SPLINE_SURFACE_WITH_KNOTS ( ( 4, 4 ),
 ( 2, 2 ),
 ( 0.000000000000000000, 1.000000000000000000 ),
 ( 0.000000000000000000, 1.000000000000000000 ),
 .UNSPECIFIED. ) 
 GEOMETRIC_REPRESENTATION_ITEM ( )  RATIONAL_B_SPLINE_SURFACE ( (
 ( 1.000000000000000000, 1.000000000000000000),
 ( 0.9732289882329797637, 0.9999525324661233672),
 ( 0.9732289882329797637, 0.9999525324661233672),
 ( 1.000000000000000000, 1.000000000000000000) ) ) 
 REPRESENTATION_ITEM ( '' )  SURFACE ( )  );
#13122=CARTESIAN_POINT ( 'NONE',  ( 0.8557997880470697982, 47.37054680076715840, -7.156447707085226817 ) ) ;
#13123=EDGE_CURVE ( 'NONE', #23728, #24678, #45639, .T. ) ;
#13134=CARTESIAN_POINT ( 'NONE',  ( 3.407937589446178528, 7.243367523631024874, 11.62731850632886754 ) ) ;
#13137=FACE_OUTER_BOUND ( 'NONE', #56021, .T. ) ;
#13139=VERTEX_POINT ( 'NONE', #48847 ) ;
#13140=CARTESIAN_POINT ( 'NONE',  ( 0.9757787079277449038, 21.42002160630820384, 37.17954582422744636 ) ) ;
#13146=CARTESIAN_POINT ( 'NONE',  ( 5.958863334805807099, -20.35021240744037030, 2.677925489610294196 ) ) ;
#13157=DIRECTION ( 'NONE',  ( -1.000000000000000000, -0.000000000000000000, -0.000000000000000000 ) ) ;
#13166=CARTESIAN_POINT ( 'NONE',  ( 3.270143674763207553, -6.605065939546730824, -11.98875605389986454 ) ) ;
#13175=DIRECTION ( 'NONE',  ( 0.07836865515943411409, 0.9608836331491523719, 0.2656332009267416416 ) ) ;
#13177=CARTESIAN_POINT ( 'NONE',  ( 0.9756950546413931669, 21.37039651692549924, -37.20808764646317002 ) ) ;
#13180=CARTESIAN_POINT ( 'NONE',  ( 0.9730545539215883499, -6.101350888304943432, 42.47233286818615028 ) ) ;
#13184=CARTESIAN_POINT ( 'NONE',  ( 0.5827359174754822568, 6.611633125157481139, -47.43746338751526537 ) ) ;
#13185=CARTESIAN_POINT ( 'NONE',  ( 0.5807400328401637335, -46.12278621143487811, -12.92266817606064322 ) ) ;
#13193=EDGE_CURVE ( 'NONE', #47724, #58012, #3004, .T. ) ;
#13194=CARTESIAN_POINT ( 'NONE',  ( 0.7056555295713289322, 46.04438433984174139, -13.20840017674969857 ) ) ;
#13197=( NAMED_UNIT ( * ) PLANE_ANGLE_UNIT ( ) SI_UNIT ( $, .RADIAN. ) );
#13199=EDGE_LOOP ( 'NONE', ( #26353, #34243, #7054, #22416 ) ) ;
#13203=VERTEX_POINT ( 'NONE', #25353 ) ;
#13212=CARTESIAN_POINT ( 'NONE',  ( 0.6067099128993235224, 13.08009036336202513, 46.07641759122967784 ) ) ;
#13213=CARTESIAN_POINT ( 'NONE',  ( 0.9745511491811748028, 16.10518088436905870, 39.77127619790144308 ) ) ;
#13216=CARTESIAN_POINT ( 'NONE',  ( 0.9730545539215883499, 30.69604515769692554, -29.98130006528829483 ) ) ;
#13223=ORIENTED_EDGE ( 'NONE', *, *, #58886, .T. ) ;
#13224=CARTESIAN_POINT ( 'NONE',  ( 0.9757402383260949108, -42.90839848328079853, -0.08489923450683498074 ) ) ;
#13227=CARTESIAN_POINT ( 'NONE',  ( 4.967162193818130511, 0.000000000000000000, 0.000000000000000000 ) ) ;
#13233=CARTESIAN_POINT ( 'NONE',  ( 0.5800708119828335008, 24.48933355903764308, 41.16171018093167788 ) ) ;
#13238=CARTESIAN_POINT ( 'NONE',  ( 4.956653778116991482, -14.93973939759855263, -45.71126949320266419 ) ) ;
#13243=VECTOR ( 'NONE', #30784, 1000.000000000000114 ) ;
#13253=CARTESIAN_POINT ( 'NONE',  ( 4.956653778116975495, -2.599733001514665798, 48.02038484091099235 ) ) ;
#13255=CARTESIAN_POINT ( 'NONE',  ( 0.5807400328401574052, 17.82553128098408735, 44.45848844984448789 ) ) ;
#13257=EDGE_CURVE ( 'NONE', #22938, #53786, #37436, .T. ) ;
#13259=CARTESIAN_POINT ( 'NONE',  ( 4.967162193818130511, 8.839793687085215623, 42.16965968614196925 ) ) ;
#13264=DIRECTION ( 'NONE',  ( -1.000000000000000000, -0.000000000000000000, -0.000000000000000000 ) ) ;
#13267=ORIENTED_EDGE ( 'NONE', *, *, #54076, .T. ) ;
#13268=EDGE_CURVE ( 'NONE', #4433, #22519, #17234, .T. ) ;
#13270=CARTESIAN_POINT ( 'NONE',  ( 0.5832366564991505742, -33.67434452455936622, 34.05963937630789928 ) ) ;
#13271=CARTESIAN_POINT ( 'NONE',  ( 4.963659409799332067, -20.22157859941758318, 39.92545197189544837 ) ) ;
#13275=CARTESIAN_POINT ( 'NONE',  ( 0.5807400328401574052, -17.82553128098376050, -44.45848844984462289 ) ) ;
#13282=CARTESIAN_POINT ( 'NONE',  ( 4.956653778116975495, 9.917440902361160937, 47.05699031914952712 ) ) ;
#13291=CARTESIAN_POINT ( 'NONE',  ( 0.5827357941260210561, 44.10984861950480962, -18.66407988912442306 ) ) ;
#13293=FACE_OUTER_BOUND ( 'NONE', #37322, .T. ) ;
#13296=EDGE_CURVE ( 'NONE', #11901, #51356, #10456, .T. ) ;
#13301=CARTESIAN_POINT ( 'NONE',  ( 0.9730545539215883499, -21.01499094264522682, -37.40983423658496321 ) ) ;
#13313=CARTESIAN_POINT ( 'NONE',  ( 0.5807400328401574052, 24.41979442053169080, 41.20655774452978193 ) ) ;
#13314=PRODUCT ( 'straight bevel gear(static)_iso_ISO - Straight bevel gear 2M 48GT 49PT 20PA 5FW ---48O25H100MD16.0N', 'straight bevel gear(static)_iso_ISO - Straight bevel gear 2M 48GT 49PT 20PA 5FW ---48O25H100MD16.0N', '', ( #17104 ) ) ;
#13316=CARTESIAN_POINT ( 'NONE',  ( 0.9741495583595186636, -42.59115242362810250, 5.208308905147964296 ) ) ;
#13319=CARTESIAN_POINT ( 'NONE',  ( 1.154321713695928286, 20.73950268329824809, 37.57248787340945739 ) ) ;
#13327=CARTESIAN_POINT ( 'NONE',  ( 5.965394784446458765, 5.298374383010636457, -19.82972329408680778 ) ) ;
#13331=AXIS2_PLACEMENT_3D ( 'NONE', #25969, #19060, #17810 ) ;
#13336=CARTESIAN_POINT ( 'NONE',  ( 0.5839879327111903162, 12.48412918464437915, 46.24044206955228731 ) ) ;
#13341=ORIENTED_EDGE ( 'NONE', *, *, #44909, .T. ) ;
#13343=CARTESIAN_POINT ( 'NONE',  ( 4.303969348037258058, 10.35452842635908510, -46.98258166031678940 ) ) ;
#13351=EDGE_CURVE ( 'NONE', #59557, #37326, #50610, .T. ) ;
#13356=CARTESIAN_POINT ( 'NONE',  ( 5.959828726073459926, -20.34941966491237508, -2.683617577144310484 ) ) ;
#13357=B_SPLINE_CURVE_WITH_KNOTS ( 'NONE', 3,
 ( #31222, #36251, #53093, #61252, #47187, #10197 ),
 .UNSPECIFIED., .F., .F.,
 ( 4, 2, 4 ),
 ( 7.564592850777163085E-18, 0.0002291978881530175695, 0.0004583957763060276039 ),
 .UNSPECIFIED. ) ;
#13362=CARTESIAN_POINT ( 'NONE',  ( 0.8557997880470697982, 46.50333260518559086, 11.51622788066474534 ) ) ;
#13363=FACE_OUTER_BOUND ( 'NONE', #49862, .T. ) ;
#13373=CARTESIAN_POINT ( 'NONE',  ( 0.9756008150404595902, 0.1421465480002861714, 42.90824081423206593 ) ) ;
#13377=ORIENTED_EDGE ( 'NONE', *, *, #22018, .F. ) ;
#13384=CARTESIAN_POINT ( 'NONE',  ( 4.967162193818130511, -23.56777426397153974, -36.06913038482822742 ) ) ;
#13385=ORIENTED_EDGE ( 'NONE', *, *, #42997, .T. ) ;
#13396=CARTESIAN_POINT ( 'NONE',  ( 4.956653778117001252, 47.05699031914963371, -9.917440902360649346 ) ) ;
#13404=CARTESIAN_POINT ( 'NONE',  ( 0.8557997880470690211, 19.17299735372009550, 43.90420959842187187 ) ) ;
#13405=CARTESIAN_POINT ( 'NONE',  ( 0.9741495583595178864, 5.992561317325774795, -42.48790363482595467 ) ) ;
#13410=CARTESIAN_POINT ( 'NONE',  ( 5.960221823109900008, -17.77840967225727553, 10.25807604135590978 ) ) ;
#13417=CARTESIAN_POINT ( 'NONE',  ( 0.9730545539215883499, 30.69604515769650632, 29.98130006528872826 ) ) ;
#13422=CARTESIAN_POINT ( 'NONE',  ( 0.9752570700956808558, 11.32817567195968955, -41.38610171411344396 ) ) ;
#13425=CARTESIAN_POINT ( 'NONE',  ( -19.85946183287803635, -7.946284510655257094, -0.9343843706440355668 ) ) ;
#13431=CARTESIAN_POINT ( 'NONE',  ( 1.154321713695928953, 41.23280394713393093, 11.90271797554028232 ) ) ;
#13434=CARTESIAN_POINT ( 'NONE',  ( 5.960221823109900008, 14.51763960716758106, 14.50993159119815701 ) ) ;
#13451=CARTESIAN_POINT ( 'NONE',  ( 2.624215991343620935, 40.85210347989567481, -25.21574086439663276 ) ) ;
#13454=CARTESIAN_POINT ( 'NONE',  ( 0.5786265663353196143, -37.55861529268533161, -29.72999788434331592 ) ) ;
#13455=ORIENTED_EDGE ( 'NONE', *, *, #24282, .F. ) ;
#13456=CARTESIAN_POINT ( 'NONE',  ( 0.9752132459055854463, 11.33038172416152634, 41.38545930839050868 ) ) ;
#13460=B_SPLINE_CURVE_WITH_KNOTS ( 'NONE', 3,
 ( #10334, #29427, #44189, #38547 ),
 .UNSPECIFIED., .F., .F.,
 ( 4, 4 ),
 ( 0.000000000000000000, 0.005004741218457418872 ),
 .UNSPECIFIED. ) ;
#13464=ORIENTED_EDGE ( 'NONE', *, *, #55742, .T. ) ;
#13473=CARTESIAN_POINT ( 'NONE',  ( 0.5839254288179566155, 47.47429404163007405, 6.341681103464710922 ) ) ;
#13482=ORIENTED_EDGE ( 'NONE', *, *, #41406, .T. ) ;
#13484=CARTESIAN_POINT ( 'NONE',  ( 0.6846871229502932144, 38.52803883689338704, -28.47437962186088001 ) ) ;
#13487=CARTESIAN_POINT ( 'NONE',  ( 5.974727161628369032, -7.840226266082411577, -18.96851388233655200 ) ) ;
#13488=CARTESIAN_POINT ( 'NONE',  ( 0.5839879327111905383, 6.161619650335993903, -47.49806740880204359 ) ) ;
#13497=CARTESIAN_POINT ( 'NONE',  ( 0.5839880159502339740, 46.25220722086348957, 12.44022138820703205 ) ) ;
#13503=ORIENTED_EDGE ( 'NONE', *, *, #16715, .F. ) ;
#13519=CARTESIAN_POINT ( 'NONE',  ( 0.5839879882012672940, 3.018602137292904642E-05, 47.89596766821092189 ) ) ;
#13525=CARTESIAN_POINT ( 'NONE',  ( 0.9736507210033056303, -16.00326134587889015, -39.81239086052233489 ) ) ;
#13531=FACE_OUTER_BOUND ( 'NONE', #55019, .T. ) ;
#13532=CARTESIAN_POINT ( 'NONE',  ( 4.967162193818130511, 0.000000000000000000, 0.000000000000000000 ) ) ;
#13533=ORIENTED_EDGE ( 'NONE', *, *, #29555, .T. ) ;
#13536=CARTESIAN_POINT ( 'NONE',  ( 0.9740398440564304039, 26.44872719679369411, 33.78760696452714996 ) ) ;
#13539=CARTESIAN_POINT ( 'NONE',  ( 0.8551540677456715978, -7.157691013574694061, 47.37911285756618440 ) ) ;
#13543=EDGE_LOOP ( 'NONE', ( #39491, #31858, #35306, #156 ) ) ;
#13548=CARTESIAN_POINT ( 'NONE',  ( 0.5839879327111913154, -44.28486549479612933, -18.24507200299090925 ) ) ;
#13560=CARTESIAN_POINT ( 'NONE',  ( 0.9752570700956810779, 37.04395688491844396, 21.65368877244764789 ) ) ;
#13562=CARTESIAN_POINT ( 'NONE',  ( 5.960221823109900008, -14.50993159119800957, -14.51763960716773383 ) ) ;
#13565=LINE ( 'NONE', #45546, #49439 ) ;
#13571=DIRECTION ( 'NONE',  ( -0.07836865515943411409, 0.1223011693452993043, -0.9893941468723544963 ) ) ;
#13572=CARTESIAN_POINT ( 'NONE',  ( 0.5850706913938533704, -46.21698775168636075, -12.57184842332066133 ) ) ;
#13578=EDGE_CURVE ( 'NONE', #31835, #4479, #9617, .T. ) ;
#13581=( BOUNDED_SURFACE ( )  B_SPLINE_SURFACE ( 3, 1, ( 
 ( #9086, #4663 ),
 ( #37944, #56686 ),
 ( #41709, #36698 ),
 ( #60771, #23812 ) ),
 .UNSPECIFIED., .F., .F., .F. ) 
 B_SPLINE_SURFACE_WITH_KNOTS ( ( 4, 4 ),
 ( 2, 2 ),
 ( 0.000000000000000000, 1.000000000000000000 ),
 ( 0.000000000000000000, 1.000000000000000000 ),
 .UNSPECIFIED. ) 
 GEOMETRIC_REPRESENTATION_ITEM ( )  RATIONAL_B_SPLINE_SURFACE ( (
 ( 1.000000000000000000, 1.000000000000000000),
 ( 0.9732289882329797637, 0.9999525324661233672),
 ( 0.9732289882329797637, 0.9999525324661233672),
 ( 1.000000000000000000, 1.000000000000000000) ) ) 
 REPRESENTATION_ITEM ( '' )  SURFACE ( )  );
#13587=ORIENTED_EDGE ( 'NONE', *, *, #42616, .F. ) ;
#13596=ORIENTED_EDGE ( 'NONE', *, *, #33958, .F. ) ;
#13599=CARTESIAN_POINT ( 'NONE',  ( 0.5807400328401574052, -44.04145271122577299, 18.83234461715166930 ) ) ;
#13601=ORIENTED_EDGE ( 'NONE', *, *, #32477, .F. ) ;
#13603=CARTESIAN_POINT ( 'NONE',  ( 4.956653778116973719, 31.29546495791849736, 36.51451553856430365 ) ) ;
#13608=ORIENTED_EDGE ( 'NONE', *, *, #53091, .T. ) ;
#13609=DIRECTION ( 'NONE',  ( -1.000000000000000000, -0.000000000000000000, -0.000000000000000000 ) ) ;
#13611=CARTESIAN_POINT ( 'NONE',  ( 0.9749527285493295725, -21.20640438431165364, -37.30179927241198357 ) ) ;
#13614=CARTESIAN_POINT ( 'NONE',  ( 0.9722240741986377666, -26.58024228478319628, 33.68410525900274166 ) ) ;
#13615=CARTESIAN_POINT ( 'NONE',  ( 3.270143674763207553, -13.53222904135355620, 2.058141141425546827 ) ) ;
#13620=CARTESIAN_POINT ( 'NONE',  ( 4.956653778117001252, 47.94889704119056972, -3.690426056929486887 ) ) ;
#13621=LINE ( 'NONE', #13016, #23689 ) ;
#13627=CARTESIAN_POINT ( 'NONE',  ( 4.960156602257182357, 8.553784487772873035, 45.62767441207052599 ) ) ;
#13628=CARTESIAN_POINT ( 'NONE',  ( 0.9757892942422816684, 42.90845395884348079, -0.05132855327749175772 ) ) ;
#13630=CARTESIAN_POINT ( 'NONE',  ( 4.956653778116975495, -9.917440902361487787, 47.05699031914946318 ) ) ;
#13634=B_SPLINE_CURVE_WITH_KNOTS ( 'NONE', 3,
 ( #27412, #52140, #23647, #42775, #61829, #56223, #56528, #43084, #38087, #8293, #13336, #9537, #3587, #51826, #56834, #17719 ),
 .UNSPECIFIED., .F., .F.,
 ( 4, 3, 3, 3, 3, 4 ),
 ( 1.214354834101861570E-17, 0.0002724568934985521318, 0.0004086836638483778159, 0.0005449104342063536104, 0.0008173270854453650470, 0.001089761613562688792 ),
 .UNSPECIFIED. ) ;
#13635=CARTESIAN_POINT ( 'NONE',  ( 0.6846871229502899947, 23.20185915381614805, -41.91507847151773802 ) ) ;
#13643=DIRECTION ( 'NONE',  ( 0.9990097760809872884, 5.448601141172755645E-18, 0.04449120468829285274 ) ) ;
#13650=CIRCLE ( 'NONE', #596, 48.09070567114147110 ) ;
#13652=CARTESIAN_POINT ( 'NONE',  ( 4.956653778116970166, 43.37017594958054900, 20.77844580450576117 ) ) ;
#13655=EDGE_CURVE ( 'NONE', #2006, #41630, #7835, .T. ) ;
#13662=EDGE_LOOP ( 'NONE', ( #43997, #4639, #43630, #51651 ) ) ;
#13664=CARTESIAN_POINT ( 'NONE',  ( 0.9740398440564311811, 41.55177796653848077, 10.70454588197301149 ) ) ;
#13678=ADVANCED_FACE ( 'NONE', ( #51358 ), #53149, .F. ) ;
#13682=VERTEX_POINT ( 'NONE', #9073 ) ;
#13687=LINE ( 'NONE', #51871, #27184 ) ;
#13689=CARTESIAN_POINT ( 'NONE',  ( 0.5809828226811553087, 47.41188724015889022, -6.791453954329836229 ) ) ;
#13698=AXIS2_PLACEMENT_3D ( 'NONE', #43491, #29060, #38179 ) ;
#13708=VERTEX_POINT ( 'NONE', #42611 ) ;
#13709=VECTOR ( 'NONE', #36395, 1000.000000000000114 ) ;
#13711=CARTESIAN_POINT ( 'NONE',  ( 4.956653778116987930, -47.05699031914942054, -9.917440902361647659 ) ) ;
#13727=ORIENTED_EDGE ( 'NONE', *, *, #6143, .F. ) ;
#13729=CARTESIAN_POINT ( 'NONE',  ( 5.959828726073459926, -20.52560994243598813, -0.004526594003305732528 ) ) ;
#13732=DIRECTION ( 'NONE',  ( -1.000000000000000000, -0.000000000000000000, -0.000000000000000000 ) ) ;
#13734=EDGE_CURVE ( 'NONE', #28932, #56419, #24602, .T. ) ;
#13737=CARTESIAN_POINT ( 'NONE',  ( 0.9730545539215883499, 11.59290486963565137, -41.31259007387218674 ) ) ;
#13741=CARTESIAN_POINT ( 'NONE',  ( 4.956653778116966613, 0.000000000000000000, 0.000000000000000000 ) ) ;
#13742=CARTESIAN_POINT ( 'NONE',  ( -20.00591024382368488, -7.982430833260542258, -0.5467354857925370570 ) ) ;
#13756=CARTESIAN_POINT ( 'NONE',  ( 0.6067099128993245216, -29.71710940500705433, -37.56352526808334602 ) ) ;
#13757=CARTESIAN_POINT ( 'NONE',  ( 2.281448460670572054, -44.80776276180760220, -17.13756432392885287 ) ) ;
#13761=CARTESIAN_POINT ( 'NONE',  ( 0.5837374860065633886, -29.01294733976387263, 38.10878877974134582 ) ) ;
#13763=CARTESIAN_POINT ( 'NONE',  ( 0.5819845901640493535, -38.27312528999452468, 28.79568196372255429 ) ) ;
#13768=CARTESIAN_POINT ( 'NONE',  ( 0.9730545539215883499, -39.44597740938048958, -16.88610103448599986 ) ) ;
#13774=CARTESIAN_POINT ( 'NONE',  ( 0.7762783648524366198, 46.49451980369979509, 11.53708172997836456 ) ) ;
#13775=CARTESIAN_POINT ( 'NONE',  ( 5.959547316686252039, 2.682663672454640658, 20.34955788964377632 ) ) ;
#13783=( NAMED_UNIT ( * ) SI_UNIT ( $, .STERADIAN. ) SOLID_ANGLE_UNIT ( ) );
#13784=EDGE_CURVE ( 'NONE', #51079, #55702, #60465, .T. ) ;
#13790=CIRCLE ( 'NONE', #4694, 43.08621763946400307 ) ;
#13795=CARTESIAN_POINT ( 'NONE',  ( 5.959547316686252039, -2.682663672455063431, 20.34955788964371948 ) ) ;
#13799=FACE_OUTER_BOUND ( 'NONE', #51577, .T. ) ;
#13802=CARTESIAN_POINT ( 'NONE',  ( 0.5807400328401574052, -41.75144119563902478, 23.47602859900699812 ) ) ;
#13813=VERTEX_POINT ( 'NONE', #48520 ) ;
#13816=CARTESIAN_POINT ( 'NONE',  ( 1.227938101723756947, 6.439911493064564674, 42.43379953535188065 ) ) ;
#13820=CARTESIAN_POINT ( 'NONE',  ( 0.6067099128993237445, -46.07641759122972047, 13.08009036336186526 ) ) ;
#13822=DIRECTION ( 'NONE',  ( 1.000000000000000000, 0.000000000000000000, 0.000000000000000000 ) ) ;
#13833=ORIENTED_EDGE ( 'NONE', *, *, #58541, .T. ) ;
#13834=CARTESIAN_POINT ( 'NONE',  ( 0.5850706913938533704, -0.1816364388703713695, 47.89601588673689037 ) ) ;
#13839=CARTESIAN_POINT ( 'NONE',  ( 3.783198216974390071, 14.86152287314682852, 40.39102707215861443 ) ) ;
#13843=CARTESIAN_POINT ( 'NONE',  ( 4.967162193818130511, 0.000000000000000000, 0.000000000000000000 ) ) ;
#13849=CARTESIAN_POINT ( 'NONE',  ( 0.5827359174754811466, -33.60976280407625438, -34.12345922495646278 ) ) ;
#13862=VECTOR ( 'NONE', #27952, 1000.000000000000114 ) ;
#13867=CARTESIAN_POINT ( 'NONE',  ( 4.963659409799330291, 29.14784479683158480, -33.96111158240212546 ) ) ;
#13868=CARTESIAN_POINT ( 'NONE',  ( 0.5800708057587368183, 46.42229836006555388, -11.78915002112674415 ) ) ;
#13869=CARTESIAN_POINT ( 'NONE',  ( 0.5837374860065636106, -46.21667939904224198, 12.57177159055146554 ) ) ;
#13871=LINE ( 'NONE', #33901, #11888 ) ;
#13874=FACE_OUTER_BOUND ( 'NONE', #23852, .T. ) ;
#13875=CARTESIAN_POINT ( 'NONE',  ( 0.9736507210033054083, 30.65767007549955636, -30.02062799605167953 ) ) ;
#13877=CARTESIAN_POINT ( 'NONE',  ( 1.154321713695929619, -34.54400171733321656, 25.46626713715447110 ) ) ;
#13881=CARTESIAN_POINT ( 'NONE',  ( 0.9756354156337477823, -37.09450626018194441, -21.56699035436975365 ) ) ;
#13884=CARTESIAN_POINT ( 'NONE',  ( 1.227938101723756947, 34.55893248994507161, 25.45152231597068848 ) ) ;
#13885=CARTESIAN_POINT ( 'NONE',  ( 0.9757787079277444597, 39.62711913632698923, 16.45683390770799193 ) ) ;
#13887=B_SPLINE_CURVE_WITH_KNOTS ( 'NONE', 3,
 ( #19929, #39340, #6076, #16138 ),
 .UNSPECIFIED., .F., .F.,
 ( 4, 4 ),
 ( 1.734723475976807094E-18, 0.004050076154993002484 ),
 .UNSPECIFIED. ) ;
#13889=CARTESIAN_POINT ( 'NONE',  ( 4.967162193818132288, 19.45289607368876617, -38.44485641567052880 ) ) ;
#13890=CARTESIAN_POINT ( 'NONE',  ( 0.5839880159502351953, 23.90868446765477273, 41.50181427378110754 ) ) ;
#13891=CARTESIAN_POINT ( 'NONE',  ( 5.959547316686252039, 19.82715097195154996, 5.308980600728524735 ) ) ;
#13892=EDGE_CURVE ( 'NONE', #4050, #47638, #8110, .T. ) ;
#13897=ORIENTED_EDGE ( 'NONE', *, *, #54468, .F. ) ;
#13898=EDGE_LOOP ( 'NONE', ( #61945, #41165, #7059, #40662 ) ) ;
#13901=EDGE_CURVE ( 'NONE', #61276, #59093, #3660, .T. ) ;
#13910=CARTESIAN_POINT ( 'NONE',  ( 0.9968887458511651589, 11.73947777183279051, -41.27232779986108113 ) ) ;
#13912=B_SPLINE_CURVE_WITH_KNOTS ( 'NONE', 3,
 ( #59712, #16829, #55007, #2695 ),
 .UNSPECIFIED., .F., .F.,
 ( 4, 4 ),
 ( 6.505213034913026604E-19, 0.004048833967417086489 ),
 .UNSPECIFIED. ) ;
#13915=ORIENTED_EDGE ( 'NONE', *, *, #52235, .F. ) ;
#13917=CARTESIAN_POINT ( 'NONE',  ( 0.9752570700956796346, -33.90066715551953536, -26.30364510018343438 ) ) ;
#13925=CARTESIAN_POINT ( 'NONE',  ( 0.9741495583595179975, -0.3955098476634577032, 42.90659993968954922 ) ) ;
#13935=CARTESIAN_POINT ( 'NONE',  ( 0.9730545539215892381, 29.98130006528861813, 30.69604515769660935 ) ) ;
#13949=CARTESIAN_POINT ( 'NONE',  ( 0.9730545539215883499, 21.01499094264548972, 37.40983423658480689 ) ) ;
#13952=FACE_OUTER_BOUND ( 'NONE', #10298, .T. ) ;
#13953=ORIENTED_EDGE ( 'NONE', *, *, #58107, .F. ) ;
#13959=CARTESIAN_POINT ( 'NONE',  ( 4.956653778116975495, -35.79382859084138602, 32.11725092155030836 ) ) ;
#13963=( BOUNDED_SURFACE ( )  B_SPLINE_SURFACE ( 3, 1, ( 
 ( #43079, #14265 ),
 ( #22719, #61524 ),
 ( #27728, #18031 ),
 ( #33064, #18344 ) ),
 .UNSPECIFIED., .F., .F., .F. ) 
 B_SPLINE_SURFACE_WITH_KNOTS ( ( 4, 4 ),
 ( 2, 2 ),
 ( 0.000000000000000000, 1.000000000000000000 ),
 ( 0.000000000000000000, 1.000000000000000000 ),
 .UNSPECIFIED. ) 
 GEOMETRIC_REPRESENTATION_ITEM ( )  RATIONAL_B_SPLINE_SURFACE ( (
 ( 1.000000000000000000, 1.000000000000000000),
 ( 0.9953390228620291325, 0.8624445117761032620),
 ( 0.9953390228620291325, 0.8624445117761032620),
 ( 1.000000000000000000, 1.000000000000000000) ) ) 
 REPRESENTATION_ITEM ( '' )  SURFACE ( )  );
#13965=B_SPLINE_CURVE_WITH_KNOTS ( 'NONE', 3,
 ( #55822, #42377, #17945, #12944, #27328, #18550 ),
 .UNSPECIFIED., .F., .F.,
 ( 4, 2, 4 ),
 ( 1.540307523853160897E-16, 0.0002445252820015214666, 0.0004890505640028889765 ),
 .UNSPECIFIED. ) ;
#13966=ADVANCED_FACE ( 'NONE', ( #16882 ), #21142, .F. ) ;
#13967=CARTESIAN_POINT ( 'NONE',  ( 5.860006189529234355, 3.137522369586185800, -48.13093674595581462 ) ) ;
#13993=VERTEX_POINT ( 'NONE', #41312 ) ;
#13997=CARTESIAN_POINT ( 'NONE',  ( 1.227938101723756947, 26.79402671879326547, 33.52879263017872091 ) ) ;
#14004=CARTESIAN_POINT ( 'NONE',  ( -17.97369999999976642, 0.000000000000000000, -1.381000053334577907E-15 ) ) ;
#14011=EDGE_CURVE ( 'NONE', #59309, #30886, #28957, .T. ) ;
#14015=EDGE_LOOP ( 'NONE', ( #2717, #61959, #13464, #48922 ) ) ;
#14019=CARTESIAN_POINT ( 'NONE',  ( 4.956653778116980824, -40.28700667097698584, 26.26162724282358951 ) ) ;
#14027=EDGE_LOOP ( 'NONE', ( #1515, #32100, #6145, #10022 ) ) ;
#14028=CARTESIAN_POINT ( 'NONE',  ( 4.967162193818131399, -38.83676580803778933, 18.65818244221244981 ) ) ;
#14030=CARTESIAN_POINT ( 'NONE',  ( 5.860006189529246790, -15.48781697582016115, -45.67886430272047704 ) ) ;
#14031=B_SPLINE_CURVE_WITH_KNOTS ( 'NONE', 3,
 ( #11220, #25616, #35347, #29388 ),
 .UNSPECIFIED., .F., .F.,
 ( 4, 4 ),
 ( 0.000000000000000000, 0.005004741218457411933 ),
 .UNSPECIFIED. ) ;
#14037=( BOUNDED_SURFACE ( )  B_SPLINE_SURFACE ( 3, 1, ( 
 ( #6505, #25647 ),
 ( #44790, #47689 ),
 ( #1831, #4732 ),
 ( #43009, #48 ) ),
 .UNSPECIFIED., .F., .F., .F. ) 
 B_SPLINE_SURFACE_WITH_KNOTS ( ( 4, 4 ),
 ( 2, 2 ),
 ( 0.000000000000000000, 1.000000000000000000 ),
 ( 0.000000000000000000, 1.000000000000000000 ),
 .UNSPECIFIED. ) 
 GEOMETRIC_REPRESENTATION_ITEM ( )  RATIONAL_B_SPLINE_SURFACE ( (
 ( 1.000000000000000000, 1.000000000000000000),
 ( 0.9732289882329797637, 0.9999525324661233672),
 ( 0.9732289882329797637, 0.9999525324661233672),
 ( 1.000000000000000000, 1.000000000000000000) ) ) 
 REPRESENTATION_ITEM ( '' )  SURFACE ( )  );
#14038=DIRECTION ( 'NONE',  ( 0.000000000000000000, 0.000000000000000000, 1.000000000000000000 ) ) ;
#14045=EDGE_CURVE ( 'NONE', #44739, #50327, #50670, .T. ) ;
#14047=CARTESIAN_POINT ( 'NONE',  ( 0.7056555295713301534, -47.89404551051140402, 0.8411712675126342686 ) ) ;
#14050=EDGE_LOOP ( 'NONE', ( #6686, #45911, #37661, #9015 ) ) ;
#14054=EDGE_LOOP ( 'NONE', ( #21273, #47960, #29457, #4567 ) ) ;
#14055=CARTESIAN_POINT ( 'NONE',  ( 4.967162193818130511, 23.56777426397178132, 36.06913038482807821 ) ) ;
#14069=CARTESIAN_POINT ( 'NONE',  ( 4.960156602257180580, 41.40608197274633540, 20.99019478193063648 ) ) ;
#14070=B_SPLINE_CURVE_WITH_KNOTS ( 'NONE', 3,
 ( #14557, #53047, #61511, #10459, #10149, #29243 ),
 .UNSPECIFIED., .F., .F.,
 ( 4, 2, 4 ),
 ( 1.516708938535782939E-16, 0.0002445252820015207619, 0.0004890505640028898439 ),
 .UNSPECIFIED. ) ;
#14074=CARTESIAN_POINT ( 'NONE',  ( 0.5786265663353153954, -28.58414684753512702, 38.43785771743193891 ) ) ;
#14075=ORIENTED_EDGE ( 'NONE', *, *, #18760, .T. ) ;
#14084=EDGE_CURVE ( 'NONE', #37022, #4220, #57610, .T. ) ;
#14090=CARTESIAN_POINT ( 'NONE',  ( 1.227938101723748288, -42.43379953535180960, -6.439911493065006987 ) ) ;
#14094=ORIENTED_EDGE ( 'NONE', *, *, #3532, .F. ) ;
#14112=ADVANCED_FACE ( 'NONE', ( #15795 ), #27551, .F. ) ;
#14115=FACE_OUTER_BOUND ( 'NONE', #5331, .T. ) ;
#14119=ORIENTED_EDGE ( 'NONE', *, *, #24978, .F. ) ;
#14120=( BOUNDED_SURFACE ( )  B_SPLINE_SURFACE ( 3, 1, ( 
 ( #49114, #48806 ),
 ( #29690, #30609 ),
 ( #5556, #6166 ),
 ( #24693, #54403 ) ),
 .UNSPECIFIED., .F., .F., .F. ) 
 B_SPLINE_SURFACE_WITH_KNOTS ( ( 4, 4 ),
 ( 2, 2 ),
 ( 0.000000000000000000, 1.000000000000000000 ),
 ( 0.000000000000000000, 1.000000000000000000 ),
 .UNSPECIFIED. ) 
 GEOMETRIC_REPRESENTATION_ITEM ( )  RATIONAL_B_SPLINE_SURFACE ( (
 ( 1.000000000000000000, 1.000000000000000000),
 ( 0.7269869731126821222, 0.9931720237060910339),
 ( 0.7269869731126821222, 0.9931720237060910339),
 ( 1.000000000000000000, 1.000000000000000000) ) ) 
 REPRESENTATION_ITEM ( '' )  SURFACE ( )  );
#14138=EDGE_LOOP ( 'NONE', ( #49789, #36959, #47888, #25601 ) ) ;
#14159=CARTESIAN_POINT ( 'NONE',  ( 0.8551540677456739292, 38.56334384152469852, -28.44084013485079865 ) ) ;
#14167=CARTESIAN_POINT ( 'NONE',  ( 4.956653778117001252, 47.05699031914963371, -9.917440902360649346 ) ) ;
#14168=FACE_OUTER_BOUND ( 'NONE', #55494, .T. ) ;
#14174=CARTESIAN_POINT ( 'NONE',  ( 0.5786265663353153954, 29.72999788434292512, 37.55861529268563714 ) ) ;
#14180=CARTESIAN_POINT ( 'NONE',  ( 0.5809828226811544205, 33.48000389720665027, -34.25055090842118233 ) ) ;
#14181=CARTESIAN_POINT ( 'NONE',  ( 2.624215991343608501, -1.411420423865808571, 47.98682984381860450 ) ) ;
#14187=DIRECTION ( 'NONE',  ( 0.000000000000000000, 0.000000000000000000, 1.000000000000000000 ) ) ;
#14189=AXIS2_PLACEMENT_3D ( 'NONE', #15271, #28739, #34376 ) ;
#14190=CARTESIAN_POINT ( 'NONE',  ( 0.9741495583595187746, -36.96045061395516740, -21.79582154536840832 ) ) ;
#14199=CARTESIAN_POINT ( 'NONE',  ( 0.5836750258453343720, -33.99574025613934225, 33.73891062492391768 ) ) ;
#14201=( BOUNDED_SURFACE ( )  B_SPLINE_SURFACE ( 3, 1, ( 
 ( #42761, #9221 ),
 ( #28330, #4497 ),
 ( #18955, #38075 ),
 ( #109, #52431 ) ),
 .UNSPECIFIED., .F., .F., .F. ) 
 B_SPLINE_SURFACE_WITH_KNOTS ( ( 4, 4 ),
 ( 2, 2 ),
 ( 0.000000000000000000, 1.000000000000000000 ),
 ( 0.000000000000000000, 1.000000000000000000 ),
 .UNSPECIFIED. ) 
 GEOMETRIC_REPRESENTATION_ITEM ( )  RATIONAL_B_SPLINE_SURFACE ( (
 ( 1.000000000000000000, 1.000000000000000000),
 ( 0.9732289882329797637, 0.9999525324661233672),
 ( 0.9732289882329797637, 0.9999525324661233672),
 ( 1.000000000000000000, 1.000000000000000000) ) ) 
 REPRESENTATION_ITEM ( '' )  SURFACE ( )  );
#14208=CARTESIAN_POINT ( 'NONE',  ( 0.5850706913938533704, -18.16120156791848217, -44.31965802246125463 ) ) ;
#14212=CARTESIAN_POINT ( 'NONE',  ( 4.967162193818130511, 0.000000000000000000, 0.000000000000000000 ) ) ;
#14217=EDGE_LOOP ( 'NONE', ( #47564, #47976, #5902, #8030 ) ) ;
#14222=CARTESIAN_POINT ( 'NONE',  ( 5.959547316686252039, 18.96456592444100053, -7.851524054666214170 ) ) ;
#14229=ORIENTED_EDGE ( 'NONE', *, *, #29356, .F. ) ;
#14241=VERTEX_POINT ( 'NONE', #25795 ) ;
#14244=EDGE_CURVE ( 'NONE', #25918, #14380, #40212, .T. ) ;
#14246=CARTESIAN_POINT ( 'NONE',  ( 4.956653778116966613, 0.000000000000000000, 0.000000000000000000 ) ) ;
#14247=CARTESIAN_POINT ( 'NONE',  ( 4.967162193818130511, 23.56777426397178132, 36.06913038482807821 ) ) ;
#14249=CARTESIAN_POINT ( 'NONE',  ( 0.9747592971366239034, -42.49794971112896036, 5.921534893733981342 ) ) ;
#14252=CARTESIAN_POINT ( 'NONE',  ( 3.660176727303384503, 45.87883389004768020, 14.24118031989607225 ) ) ;
#14253=CARTESIAN_POINT ( 'NONE',  ( 4.967162193818130511, -2.375726030842872927, 43.02067033766017801 ) ) ;
#14255=CARTESIAN_POINT ( 'NONE',  ( 1.227938101723756947, -0.8460948827222184443, -42.91134962331487657 ) ) ;
#14256=ADVANCED_FACE ( 'NONE', ( #1972 ), #33599, .F. ) ;
#14258=CARTESIAN_POINT ( 'NONE',  ( 0.8551540677456715978, 23.16399837394604688, -41.94570365541178347 ) ) ;
#14259=LINE ( 'NONE', #53054, #46422 ) ;
#14264=B_SPLINE_CURVE_WITH_KNOTS ( 'NONE', 3,
 ( #37329, #17917, #56403, #13519, #50180, #33869, #47333, #23517, #623, #9727 ),
 .UNSPECIFIED., .F., .F.,
 ( 4, 3, 3, 4 ),
 ( 0.0005448802484326158158, 0.0005449104342063607661, 0.0008173270854453680827, 0.001089761613562689226 ),
 .UNSPECIFIED. ) ;
#14265=CARTESIAN_POINT ( 'NONE',  ( 0.5807400328401637335, 0.5448834511096761757, -47.89582301953902999 ) ) ;
#14275=CARTESIAN_POINT ( 'NONE',  ( 5.981074661064941900, -14.51919955600725842, -14.50705827991440877 ) ) ;
#14284=EDGE_CURVE ( 'NONE', #53979, #31908, #35765, .T. ) ;
#14291=CARTESIAN_POINT ( 'NONE',  ( 5.960721111146673579, 2.672857320903031741, 20.35079619394246819 ) ) ;
#14298=DIRECTION ( 'NONE',  ( 0.000000000000000000, 0.000000000000000000, 1.000000000000000000 ) ) ;
#14303=CARTESIAN_POINT ( 'NONE',  ( 5.959828726073459926, 7.858992891710142814, -18.96145866559664483 ) ) ;
#14304=CARTESIAN_POINT ( 'NONE',  ( 0.9740398440564310700, -42.59352035928883140, -5.189371650077303499 ) ) ;
#14307=CARTESIAN_POINT ( 'NONE',  ( 0.7056555295713317077, 41.89804573586738456, 23.21854706865595830 ) ) ;
#14313=CARTESIAN_POINT ( 'NONE',  ( 0.5839879882104920261, 5.827794150371782279E-15, 47.89596766822081264 ) ) ;
#14319=CARTESIAN_POINT ( 'NONE',  ( 0.5809828226811617480, -17.82437196699647686, -44.45562576850621639 ) ) ;
#14331=CARTESIAN_POINT ( 'NONE',  ( 2.624215991343608501, 4.864192649745388231, 47.76052319582218075 ) ) ;
#14333=CARTESIAN_POINT ( 'NONE',  ( 3.783278058412225864, 35.16831859152132722, 24.80906179324452054 ) ) ;
#14339=CARTESIAN_POINT ( 'NONE',  ( 1.154321713695927620, -41.66001467525148172, 10.30834583266716287 ) ) ;
#14341=CARTESIAN_POINT ( 'NONE',  ( 0.5807400328401574052, -46.12278621143506996, 12.92266817605998419 ) ) ;
#14345=CARTESIAN_POINT ( 'NONE',  ( 5.981074661064941900, -10.26976685693835556, 17.77058762078859999 ) ) ;
#14352=CARTESIAN_POINT ( 'NONE',  ( 2.624215991343620935, -44.87417713512076745, -17.05978231157451219 ) ) ;
#14355=VERTEX_POINT ( 'NONE', #2276 ) ;
#14359=CARTESIAN_POINT ( 'NONE',  ( 2.624215991343620935, 30.33228621715034734, 37.21129343241614151 ) ) ;
#14361=ORIENTED_EDGE ( 'NONE', *, *, #8954, .T. ) ;
#14371=CARTESIAN_POINT ( 'NONE',  ( 4.963659409799330291, 39.92545197189549100, 20.22157859941743752 ) ) ;
#14380=VERTEX_POINT ( 'NONE', #51131 ) ;
#14386=CARTESIAN_POINT ( 'NONE',  ( 0.9730545539215883499, 0.5054011016618756846, -42.90536227157002003 ) ) ;
#14389=CARTESIAN_POINT ( 'NONE',  ( 0.5807400328401637335, -38.33001520688930697, -28.72484455891680710 ) ) ;
#14391=EDGE_CURVE ( 'NONE', #2006, #16817, #27528, .T. ) ;
#14392=VERTEX_POINT ( 'NONE', #22960 ) ;
#14394=CARTESIAN_POINT ( 'NONE',  ( 1.154321713695929619, 17.18284946700681104, -39.32643513900308108 ) ) ;
#14400=VERTEX_POINT ( 'NONE', #18563 ) ;
#14405=AXIS2_PLACEMENT_3D ( 'NONE', #57657, #42685, #43003 ) ;
#14407=CARTESIAN_POINT ( 'NONE',  ( 0.8557997880470599172, 11.51622788066458369, 46.50333260518563350 ) ) ;
#14417=AXIS2_PLACEMENT_3D ( 'NONE', #36880, #27765, #18066 ) ;
#14418=CARTESIAN_POINT ( 'NONE',  ( 5.958863334805807099, 20.34989385289154029, 2.680345151634683454 ) ) ;
#14422=ADVANCED_FACE ( 'NONE', ( #46465 ), #26654, .T. ) ;
#14423=CARTESIAN_POINT ( 'NONE',  ( 1.227938101723748288, -10.28900963485351205, -41.66816631169202623 ) ) ;
#14424=CARTESIAN_POINT ( 'NONE',  ( 0.8557997880470606944, 47.37054680076706603, 7.156447707085862753 ) ) ;
#14428=EDGE_CURVE ( 'NONE', #61565, #44407, #31979, .T. ) ;
#14431=ADVANCED_FACE ( 'NONE', ( #3510 ), #29551, .F. ) ;
#14433=VERTEX_POINT ( 'NONE', #37373 ) ;
#14439=ORIENTED_EDGE ( 'NONE', *, *, #39008, .T. ) ;
#14441=VERTEX_POINT ( 'NONE', #4122 ) ;
#14447=EDGE_LOOP ( 'NONE', ( #34858, #46504, #3858, #5587 ) ) ;
#14449=B_SPLINE_CURVE_WITH_KNOTS ( 'NONE', 3,
 ( #61485, #23302, #42427, #57705, #9814, #57098, #33636, #18608, #56795, #28604, #13925, #33028, #48037 ),
 .UNSPECIFIED., .F., .F.,
 ( 4, 3, 3, 3, 4 ),
 ( 0.0005054209210073039738, 0.0005449106435901839799, 0.0006811373090491489642, 0.0008459866663933692660, 0.001010840725717212932 ),
 .UNSPECIFIED. ) ;
#14454=CARTESIAN_POINT ( 'NONE',  ( 5.959547316686252039, -7.851524054666280783, -18.96456592444097922 ) ) ;
#14459=LINE ( 'NONE', #47967, #41933 ) ;
#14461=ORIENTED_EDGE ( 'NONE', *, *, #9784, .F. ) ;
#14462=CARTESIAN_POINT ( 'NONE',  ( 5.860006189529234355, 40.09484204000635543, -26.81109398084667106 ) ) ;
#14470=DIRECTION ( 'NONE',  ( -1.000000000000000000, -0.000000000000000000, -0.000000000000000000 ) ) ;
#14475=CARTESIAN_POINT ( 'NONE',  ( 5.974727161628367256, -10.24903993265021285, 17.78288073588484863 ) ) ;
#14476=EDGE_CURVE ( 'NONE', #43532, #18131, #31182, .T. ) ;
#14478=CARTESIAN_POINT ( 'NONE',  ( 0.5807400328401574052, 38.33001520688988961, -28.72484455891602906 ) ) ;
#14485=( BOUNDED_SURFACE ( )  B_SPLINE_SURFACE ( 3, 1, ( 
 ( #61402, #19153 ),
 ( #42347, #12 ),
 ( #9413, #5316 ),
 ( #10047, #33250 ) ),
 .UNSPECIFIED., .F., .F., .F. ) 
 B_SPLINE_SURFACE_WITH_KNOTS ( ( 4, 4 ),
 ( 2, 2 ),
 ( 0.000000000000000000, 1.000000000000000000 ),
 ( 0.000000000000000000, 1.000000000000000000 ),
 .UNSPECIFIED. ) 
 GEOMETRIC_REPRESENTATION_ITEM ( )  RATIONAL_B_SPLINE_SURFACE ( (
 ( 1.000000000000000000, 1.000000000000000000),
 ( 0.7269869731126821222, 0.9931720237060910339),
 ( 0.7269869731126821222, 0.9931720237060910339),
 ( 1.000000000000000000, 1.000000000000000000) ) ) 
 REPRESENTATION_ITEM ( '' )  SURFACE ( )  );
#14490=CARTESIAN_POINT ( 'NONE',  ( 0.5836750258453353712, -23.79054009282519289, -41.56963612796212004 ) ) ;
#14494=CARTESIAN_POINT ( 'NONE',  ( 0.9722240750034564227, 34.39263040572789265, 25.65687433776909643 ) ) ;
#14500=EDGE_LOOP ( 'NONE', ( #6849, #59080, #32087, #39544 ) ) ;
#14501=EDGE_CURVE ( 'NONE', #1609, #59890, #34518, .T. ) ;
#14502=CARTESIAN_POINT ( 'NONE',  ( 0.9756950546413931669, 5.696573146291977530, 42.52863374229711013 ) ) ;
#14507=ORIENTED_EDGE ( 'NONE', *, *, #27677, .T. ) ;
#14509=ADVANCED_FACE ( 'NONE', ( #53588 ), #38369, .F. ) ;
#14522=CARTESIAN_POINT ( 'NONE',  ( 5.960721111146673579, -10.25731071096570268, -17.77882586010663246 ) ) ;
#14523=CIRCLE ( 'NONE', #36529, 47.67072199303260049 ) ;
#14526=CARTESIAN_POINT ( 'NONE',  ( 0.9756950546413944991, -34.10037081504538037, -26.04419981250922689 ) ) ;
#14535=VERTEX_POINT ( 'NONE', #21647 ) ;
#14543=CARTESIAN_POINT ( 'NONE',  ( 0.6067099128993197477, -38.42667919752384620, -28.59222530349265412 ) ) ;
#14550=CARTESIAN_POINT ( 'NONE',  ( 0.5809828226811553087, -46.11980934799348830, 12.92184523170186594 ) ) ;
#14553=EDGE_CURVE ( 'NONE', #8991, #7406, #20004, .T. ) ;
#14557=CARTESIAN_POINT ( 'NONE',  ( 0.8557997880470599172, 47.60865952217007191, -5.347802024196765203 ) ) ;
#14560=CARTESIAN_POINT ( 'NONE',  ( 4.303969348037246512, -47.36875205922767407, -8.413118729224548176 ) ) ;
#14562=CARTESIAN_POINT ( 'NONE',  ( 2.526552050251863246, -22.53110080776681556, 36.59987178591175194 ) ) ;
#14573=CARTESIAN_POINT ( 'NONE',  ( 0.9741495583595165542, -11.48707840139614866, 41.34222751889824821 ) ) ;
#14581=CARTESIAN_POINT ( 'NONE',  ( 5.960721111146673579, -5.318514366755071165, 19.82454228767736382 ) ) ;
#14585=EDGE_CURVE ( 'NONE', #41729, #26419, #38767, .T. ) ;
#14588=CIRCLE ( 'NONE', #57512, 8.000000000000000000 ) ;
#14591=EDGE_CURVE ( 'NONE', #49122, #5485, #17775, .T. ) ;
#14596=VECTOR ( 'NONE', #32893, 1000.000000000000000 ) ;
#14599=CARTESIAN_POINT ( 'NONE',  ( 0.9747592971366223491, 42.58247319705107259, 5.279515277919533567 ) ) ;
#14600=EDGE_LOOP ( 'NONE', ( #40062, #38176, #60007, #30485 ) ) ;
#14608=CARTESIAN_POINT ( 'NONE',  ( 4.963659409799330291, -37.47512675766677859, -24.46566636552866214 ) ) ;
#14611=ORIENTED_EDGE ( 'NONE', *, *, #55791, .F. ) ;
#14613=CARTESIAN_POINT ( 'NONE',  ( 0.9754402186311929013, 0.1875553420611592303, 42.90805920318130262 ) ) ;
#14617=B_SPLINE_CURVE_WITH_KNOTS ( 'NONE', 3,
 ( #56512, #13627, #28626, #30091 ),
 .UNSPECIFIED., .F., .F.,
 ( 4, 4 ),
 ( 5.647850449853784215E-17, 0.005004741218457476985 ),
 .UNSPECIFIED. ) ;
#14618=ORIENTED_EDGE ( 'NONE', *, *, #60955, .T. ) ;
#14626=CARTESIAN_POINT ( 'NONE',  ( 0.9756354156337460060, 26.22428641656300741, -33.96210048825346917 ) ) ;
#14627=ORIENTED_EDGE ( 'NONE', *, *, #41368, .F. ) ;
#14634=CARTESIAN_POINT ( 'NONE',  ( 0.5809828226811617480, -24.41822904836953612, 41.20389530892298779 ) ) ;
#14637=ORIENTED_EDGE ( 'NONE', *, *, #38088, .F. ) ;
#14642=CONICAL_SURFACE ( 'NONE', #28606, 43.08621763946400307, 1.568696531533066763 ) ;
#14643=LINE ( 'NONE', #58433, #6951 ) ;
#14645=CARTESIAN_POINT ( 'NONE',  ( 3.783278058412225420, 36.37891728069903508, -22.99727281874588058 ) ) ;
#14651=CARTESIAN_POINT ( 'NONE',  ( 5.958863334805807099, 19.82594244347352586, -5.313608583996313861 ) ) ;
#14655=DIRECTION ( 'NONE',  ( 0.000000000000000000, 0.000000000000000000, 1.000000000000000000 ) ) ;
#14658=CARTESIAN_POINT ( 'NONE',  ( 0.5807400328401574052, 47.41494605191442702, 6.791881299635745606 ) ) ;
#14659=CARTESIAN_POINT ( 'NONE',  ( 0.9730545539215883499, 30.69604515769692554, -29.98130006528829483 ) ) ;
#14661=EDGE_CURVE ( 'NONE', #59261, #58751, #33700, .T. ) ;
#14664=CARTESIAN_POINT ( 'NONE',  ( -18.90751475399365589, -7.774715922560747394, 1.885931201481398922 ) ) ;
#14666=EDGE_LOOP ( 'NONE', ( #31618, #49110, #51377, #8297 ) ) ;
#14672=CARTESIAN_POINT ( 'NONE',  ( 0.8557997880470599172, 28.43566216844970640, 38.55640757422448672 ) ) ;
#14675=EDGE_CURVE ( 'NONE', #18847, #51998, #5745, .T. ) ;
#14677=AXIS2_PLACEMENT_3D ( 'NONE', #3759, #61387, #13822 ) ;
#14682=CARTESIAN_POINT ( 'NONE',  ( 0.5819845079324652559, -37.72030202710095637, 29.51613512130369799 ) ) ;
#14690=VERTEX_POINT ( 'NONE', #1904 ) ;
#14694=FACE_OUTER_BOUND ( 'NONE', #34409, .T. ) ;
#14696=CARTESIAN_POINT ( 'NONE',  ( 0.8557997880470606944, -34.51495345639572321, 33.22501220301889191 ) ) ;
#14701=EDGE_LOOP ( 'NONE', ( #15216, #49875, #40953, #40460 ) ) ;
#14705=CARTESIAN_POINT ( 'NONE',  ( 4.967162193818130511, 0.000000000000000000, 0.000000000000000000 ) ) ;
#14713=CARTESIAN_POINT ( 'NONE',  ( 4.956653778116966613, 0.000000000000000000, 0.000000000000000000 ) ) ;
#14719=CARTESIAN_POINT ( 'NONE',  ( 0.8557997880470690211, -46.50333260518550560, -11.51622788066506686 ) ) ;
#14735=CARTESIAN_POINT ( 'NONE',  ( 0.9752570700956806338, -37.27462300504088688, 21.25416333281084746 ) ) ;
#14738=ADVANCED_FACE ( 'NONE', ( #23486 ), #3557, .F. ) ;
#14743=CARTESIAN_POINT ( 'NONE',  ( 0.5809828226811617480, 23.47450554821709900, 41.74875432577658074 ) ) ;
#14744=ORIENTED_EDGE ( 'NONE', *, *, #6197, .T. ) ;
#14751=ORIENTED_EDGE ( 'NONE', *, *, #33058, .F. ) ;
#14753=EDGE_CURVE ( 'NONE', #25935, #15210, #10221, .T. ) ;
#14754=B_SPLINE_CURVE_WITH_KNOTS ( 'NONE', 3,
 ( #24547, #44300, #10453, #405, #19247, #5103 ),
 .UNSPECIFIED., .F., .F.,
 ( 4, 2, 4 ),
 ( 3.476216610979977084E-18, 0.0002291966416970801898, 0.0004583932833941569101 ),
 .UNSPECIFIED. ) ;
#14757=( BOUNDED_SURFACE ( )  B_SPLINE_SURFACE ( 3, 1, ( 
 ( #31281, #35382 ),
 ( #49766, #17191 ),
 ( #35696, #11892 ),
 ( #55377, #55070 ) ),
 .UNSPECIFIED., .F., .F., .F. ) 
 B_SPLINE_SURFACE_WITH_KNOTS ( ( 4, 4 ),
 ( 2, 2 ),
 ( 0.000000000000000000, 1.000000000000000000 ),
 ( 0.000000000000000000, 1.000000000000000000 ),
 .UNSPECIFIED. ) 
 GEOMETRIC_REPRESENTATION_ITEM ( )  RATIONAL_B_SPLINE_SURFACE ( (
 ( 1.000000000000000000, 1.000000000000000000),
 ( 0.9953390228620291325, 0.8624445117761032620),
 ( 0.9953390228620291325, 0.8624445117761032620),
 ( 1.000000000000000000, 1.000000000000000000) ) ) 
 REPRESENTATION_ITEM ( '' )  SURFACE ( )  );
#14760=ORIENTED_EDGE ( 'NONE', *, *, #43745, .F. ) ;
#14761=CARTESIAN_POINT ( 'NONE',  ( 0.9747592971366236814, -16.71904224817876639, -39.51726118357609607 ) ) ;
#14768=ORIENTED_EDGE ( 'NONE', *, *, #41755, .F. ) ;
#14769=CARTESIAN_POINT ( 'NONE',  ( 5.960221823109900008, 7.849768660536558862, -18.96526051813972913 ) ) ;
#14772=CARTESIAN_POINT ( 'NONE',  ( 0.8557997880470690211, 41.02602466100812961, -24.73961900479208609 ) ) ;
#14779=ORIENTED_EDGE ( 'NONE', *, *, #19968, .F. ) ;
#14790=CARTESIAN_POINT ( 'NONE',  ( -17.69685288772385690, -7.723236801699937537, -2.086240377089799480 ) ) ;
#14798=B_SPLINE_CURVE_WITH_KNOTS ( 'NONE', 3,
 ( #30731, #6908, #45182, #2211, #40476, #11973, #31054, #50162, #13497, #22584, #32601, #8780, #31988, #42021, #18193, #9390 ),
 .UNSPECIFIED., .F., .F.,
 ( 4, 3, 3, 3, 3, 4 ),
 ( 1.040890552917501732E-17, 0.0002724568934985527823, 0.0004086836638483798759, 0.0005449104342063559956, 0.0008173270854453659143, 0.001089761613562691394 ),
 .UNSPECIFIED. ) ;
#14800=CARTESIAN_POINT ( 'NONE',  ( 0.5836750258453341500, 33.73891062492405979, 33.99574025613924988 ) ) ;
#14801=CARTESIAN_POINT ( 'NONE',  ( 0.9730545539215883499, -10.61654491617534291, -41.57420493492396929 ) ) ;
#14806=CARTESIAN_POINT ( 'NONE',  ( 3.270143674763207553, -13.60381564321235359, 1.514386915940542311 ) ) ;
#14808=CARTESIAN_POINT ( 'NONE',  ( 0.9730545539215883499, -21.01499094264575618, 37.40983423658466478 ) ) ;
#14809=FACE_OUTER_BOUND ( 'NONE', #29944, .T. ) ;
#14815=CARTESIAN_POINT ( 'NONE',  ( 0.5786265663353196143, 28.58414684753485346, 38.43785771743214497 ) ) ;
#14816=CIRCLE ( 'NONE', #3782, 12.50000000000000000 ) ;
#14820=ORIENTED_EDGE ( 'NONE', *, *, #27421, .F. ) ;
#14827=CARTESIAN_POINT ( 'NONE',  ( 2.624215991343620935, 25.21574086439706619, 40.85210347989540480 ) ) ;
#14828=CARTESIAN_POINT ( 'NONE',  ( 0.9754402186311944556, -34.15542855230918917, -25.97197377940591068 ) ) ;
#14835=CARTESIAN_POINT ( 'NONE',  ( 0.9722240741986377666, -30.74950262511622512, 29.92651525529365131 ) ) ;
#14843=DIRECTION ( 'NONE',  ( 0.000000000000000000, 0.000000000000000000, 1.000000000000000000 ) ) ;
#14846=CARTESIAN_POINT ( 'NONE',  ( 4.963659409799333844, -24.46566636552799068, -37.47512675766720491 ) ) ;
#14851=VERTEX_POINT ( 'NONE', #10953 ) ;
#14853=FACE_OUTER_BOUND ( 'NONE', #35099, .T. ) ;
#14859=EDGE_CURVE ( 'NONE', #20273, #30001, #39163, .T. ) ;
#14865=ADVANCED_FACE ( 'NONE', ( #24108 ), #22797, .F. ) ;
#14872=DIRECTION ( 'NONE',  ( -1.000000000000000000, -0.000000000000000000, -0.000000000000000000 ) ) ;
#14874=CARTESIAN_POINT ( 'NONE',  ( 5.958863334805807099, -12.49619391867194373, 16.28335246510346224 ) ) ;
#14877=CARTESIAN_POINT ( 'NONE',  ( 0.5809828226811553087, -41.20389530892325070, 24.41822904836909203 ) ) ;
#14883=ADVANCED_FACE ( 'NONE', ( #52917 ), #40028, .F. ) ;
#14884=CARTESIAN_POINT ( 'NONE',  ( 5.959547316686252039, -16.28624005235090877, -12.49238070347970364 ) ) ;
#14887=CARTESIAN_POINT ( 'NONE',  ( 4.303969348037246512, 2.158280495710879876, -48.06163817123223936 ) ) ;
#14897=CARTESIAN_POINT ( 'NONE',  ( 5.960221823109900008, 5.307149561567809926, 19.82761049839343670 ) ) ;
#14898=B_SPLINE_CURVE_WITH_KNOTS ( 'NONE', 3,
 ( #40696, #26249, #7434, #41609 ),
 .UNSPECIFIED., .F., .F.,
 ( 4, 4 ),
 ( 0.000000000000000000, 0.004446090762761359047 ),
 .UNSPECIFIED. ) ;
#14902=CARTESIAN_POINT ( 'NONE',  ( 4.956653778116982600, -45.71126949320260735, 14.93973939759871072 ) ) ;
#14903=AXIS2_PLACEMENT_3D ( 'NONE', #19583, #761, #439 ) ;
#14910=ADVANCED_FACE ( 'NONE', ( #9698 ), #14757, .F. ) ;
#14911=CARTESIAN_POINT ( 'NONE',  ( 0.5832366564991497970, 37.83193087518350950, -29.37287047358843139 ) ) ;
#14912=ORIENTED_EDGE ( 'NONE', *, *, #23555, .F. ) ;
#14916=CONICAL_SURFACE ( 'NONE', #34943, 43.08621763946400307, 1.568696531533066763 ) ;
#14923=ORIENTED_EDGE ( 'NONE', *, *, #20881, .F. ) ;
#14925=CARTESIAN_POINT ( 'NONE',  ( 1.154321485836933725, 10.30834589251769451, -41.66001465002018023 ) ) ;
#14934=ORIENTED_EDGE ( 'NONE', *, *, #31089, .F. ) ;
#14937=DIRECTION ( 'NONE',  ( -1.000000000000000000, -0.000000000000000000, -0.000000000000000000 ) ) ;
#14938=EDGE_CURVE ( 'NONE', #10414, #49122, #46708, .T. ) ;
#14940=( BOUNDED_SURFACE ( )  B_SPLINE_SURFACE ( 3, 1, ( 
 ( #1679, #15201 ),
 ( #29898, #44046 ),
 ( #49013, #30202 ),
 ( #53994, #44640 ) ),
 .UNSPECIFIED., .F., .F., .F. ) 
 B_SPLINE_SURFACE_WITH_KNOTS ( ( 4, 4 ),
 ( 2, 2 ),
 ( 0.000000000000000000, 1.000000000000000000 ),
 ( 0.000000000000000000, 1.000000000000000000 ),
 .UNSPECIFIED. ) 
 GEOMETRIC_REPRESENTATION_ITEM ( )  RATIONAL_B_SPLINE_SURFACE ( (
 ( 1.000000000000000000, 1.000000000000000000),
 ( 0.9953390228620291325, 0.8624445117761032620),
 ( 0.9953390228620291325, 0.8624445117761032620),
 ( 1.000000000000000000, 1.000000000000000000) ) ) 
 REPRESENTATION_ITEM ( '' )  SURFACE ( )  );
#14944=CARTESIAN_POINT ( 'NONE',  ( 4.956653778116970166, 36.51451553856417576, 31.29546495791861460 ) ) ;
#14966=CONICAL_SURFACE ( 'NONE', #49951, 43.08621763946400307, 1.568696531533066763 ) ;
#14970=CARTESIAN_POINT ( 'NONE',  ( 0.9749527285493299056, 42.57770849153634174, -5.317382389862751246 ) ) ;
#14972=CARTESIAN_POINT ( 'NONE',  ( 0.5800708119828325016, 17.74761857127127840, -44.48635609075538611 ) ) ;
#14979=CARTESIAN_POINT ( 'NONE',  ( 4.303969348037258058, 30.97035057417660298, 36.81598326424561662 ) ) ;
#14984=CARTESIAN_POINT ( 'NONE',  ( 0.5800708057587384836, -44.48635630048008238, 17.74761804745386584 ) ) ;
#14986=CARTESIAN_POINT ( 'NONE',  ( 0.5800708119828336118, -29.65250521075920886, -37.61306658477503362 ) ) ;
#14998=VERTEX_POINT ( 'NONE', #40102 ) ;
#15005=CARTESIAN_POINT ( 'NONE',  ( 0.9730545539215883499, -34.34678117142538412, -25.71816799638815354 ) ) ;
#15018=EDGE_CURVE ( 'NONE', #10097, #5228, #2448, .T. ) ;
#15020=CARTESIAN_POINT ( 'NONE',  ( 0.7762783648524371749, 7.133808749409432437, 47.37038525648361542 ) ) ;
#15026=CARTESIAN_POINT ( 'NONE',  ( 0.9749527285493325701, -21.70110358462066458, 37.01618455594564949 ) ) ;
#15031=DIRECTION ( 'NONE',  ( -1.000000000000000000, -0.000000000000000000, -0.000000000000000000 ) ) ;
#15032=EDGE_CURVE ( 'NONE', #33451, #56839, #1514, .T. ) ;
#15036=CARTESIAN_POINT ( 'NONE',  ( 0.8551540677456715978, -47.90804413217340141, -0.9122407826480831705 ) ) ;
#15041=LINE ( 'NONE', #30974, #8243 ) ;
#15044=CARTESIAN_POINT ( 'NONE',  ( 0.5832367798473374609, 18.58036934788136563, -44.14510605973664781 ) ) ;
#15048=CARTESIAN_POINT ( 'NONE',  ( 3.783278058412224976, 18.05212641201972446, 39.06943705276837164 ) ) ;
#15050=ORIENTED_EDGE ( 'NONE', *, *, #25341, .T. ) ;
#15052=EDGE_CURVE ( 'NONE', #9163, #39811, #33424, .T. ) ;
#15053=CARTESIAN_POINT ( 'NONE',  ( 0.9722240741986373225, -41.29187377038493878, -11.66659279944019545 ) ) ;
#15057=CARTESIAN_POINT ( 'NONE',  ( 0.6067375320500700830, -17.67235760802231681, -44.51755737952373693 ) ) ;
#15063=ORIENTED_EDGE ( 'NONE', *, *, #41623, .F. ) ;
#15081=CARTESIAN_POINT ( 'NONE',  ( 5.959547316686252039, 0.003562808152905788499, -20.52562247508876681 ) ) ;
#15084=B_SPLINE_CURVE_WITH_KNOTS ( 'NONE', 3,
 ( #5804, #45004, #40308, #10858 ),
 .UNSPECIFIED., .F., .F.,
 ( 4, 4 ),
 ( 0.000000000000000000, 0.004048833967417086489 ),
 .UNSPECIFIED. ) ;
#15089=ORIENTED_EDGE ( 'NONE', *, *, #17540, .T. ) ;
#15093=CARTESIAN_POINT ( 'NONE',  ( 1.154321713695929841, 33.53917066545422898, 26.77578845938192487 ) ) ;
#15095=CARTESIAN_POINT ( 'NONE',  ( 0.9730545539215883499, -42.60426903087357431, 5.099196237954729760 ) ) ;
#15101=ADVANCED_FACE ( 'NONE', ( #39790, #61005 ), #61611, .T. ) ;
#15106=CARTESIAN_POINT ( 'NONE',  ( 0.5819845079324657000, 34.18710788661951483, 33.54497088780092895 ) ) ;
#15109=CARTESIAN_POINT ( 'NONE',  ( 0.5839880159502345292, 29.19321933421549531, -37.97080096460551601 ) ) ;
#15120=ORIENTED_EDGE ( 'NONE', *, *, #3223, .T. ) ;
#15133=FACE_OUTER_BOUND ( 'NONE', #34451, .T. ) ;
#15136=EDGE_CURVE ( 'NONE', #10287, #48653, #661, .T. ) ;
#15140=CARTESIAN_POINT ( 'NONE',  ( 0.9730545539215883499, -41.31259007387239279, 11.59290486963492128 ) ) ;
#15148=B_SPLINE_CURVE_WITH_KNOTS ( 'NONE', 3,
 ( #35830, #54899, #31108, #26402, #26712, #2588 ),
 .UNSPECIFIED., .F., .F.,
 ( 4, 2, 4 ),
 ( 1.519728548185745998E-16, 0.0002445252820015200571, 0.0004890505640028882176 ),
 .UNSPECIFIED. ) ;
#15150=ORIENTED_EDGE ( 'NONE', *, *, #46686, .T. ) ;
#15151=CARTESIAN_POINT ( 'NONE',  ( 0.8551540677456715978, -34.52115452272906282, -33.23105123575935949 ) ) ;
#15153=CARTESIAN_POINT ( 'NONE',  ( 1.227938101723748288, 0.8460948827231143943, -42.91134962331486236 ) ) ;
#15159=CARTESIAN_POINT ( 'NONE',  ( 3.270143674763207553, 3.277085381513114015, 13.28976595685394635 ) ) ;
#15163=CARTESIAN_POINT ( 'NONE',  ( 2.526464513654346433, 6.809833384819025781, 42.43615126908559176 ) ) ;
#15173=B_SPLINE_CURVE_WITH_KNOTS ( 'NONE', 3,
 ( #48028, #77, #18919, #52709, #14828, #5390, #14526, #24514, #19841, #28596, #5078, #28294, #56787, #13917, #58011, #10431, #47411, #38959, #23908 ),
 .UNSPECIFIED., .F., .F.,
 ( 4, 3, 3, 3, 3, 3, 4 ),
 ( 0.000000000000000000, 0.0002724573126191766771, 0.0004086839781548628429, 0.0005449106435901976409, 0.0006811373090491553610, 0.0008459866663933662302, 0.001010840725717216402 ),
 .UNSPECIFIED. ) ;
#15188=ORIENTED_EDGE ( 'NONE', *, *, #45876, .T. ) ;
#15189=ORIENTED_EDGE ( 'NONE', *, *, #37727, .T. ) ;
#15193=ORIENTED_EDGE ( 'NONE', *, *, #52467, .T. ) ;
#15201=CARTESIAN_POINT ( 'NONE',  ( 0.5807400328401637335, 29.58941477093070915, -37.66660715020834260 ) ) ;
#15202=CARTESIAN_POINT ( 'NONE',  ( 4.963659409799329403, -19.36487359954728049, 40.34793212403964446 ) ) ;
#15207=EDGE_CURVE ( 'NONE', #18160, #28471, #61777, .T. ) ;
#15210=VERTEX_POINT ( 'NONE', #26892 ) ;
#15212=ADVANCED_FACE ( 'NONE', ( #29049 ), #51179, .T. ) ;
#15213=ORIENTED_EDGE ( 'NONE', *, *, #54194, .T. ) ;
#15216=ORIENTED_EDGE ( 'NONE', *, *, #14045, .T. ) ;
#15224=CARTESIAN_POINT ( 'NONE',  ( 0.9730545539215883499, -42.90536227157002003, -0.5054011016617259155 ) ) ;
#15225=( BOUNDED_SURFACE ( )  B_SPLINE_SURFACE ( 3, 1, ( 
 ( #4238, #55945 ),
 ( #12440, #8032 ),
 ( #41887, #27763 ),
 ( #8962, #46272 ) ),
 .UNSPECIFIED., .F., .F., .F. ) 
 B_SPLINE_SURFACE_WITH_KNOTS ( ( 4, 4 ),
 ( 2, 2 ),
 ( 0.000000000000000000, 1.000000000000000000 ),
 ( 0.000000000000000000, 1.000000000000000000 ),
 .UNSPECIFIED. ) 
 GEOMETRIC_REPRESENTATION_ITEM ( )  RATIONAL_B_SPLINE_SURFACE ( (
 ( 1.000000000000000000, 1.000000000000000000),
 ( 0.7269869731126821222, 0.9931720237060910339),
 ( 0.7269869731126821222, 0.9931720237060910339),
 ( 1.000000000000000000, 1.000000000000000000) ) ) 
 REPRESENTATION_ITEM ( '' )  SURFACE ( )  );
#15226=CARTESIAN_POINT ( 'NONE',  ( 3.270143674763207553, -13.60381564321233228, -1.514386915940737710 ) ) ;
#15231=CARTESIAN_POINT ( 'NONE',  ( 0.5819845079324652559, 23.55367910461055558, -41.70428776698872753 ) ) ;
#15234=CARTESIAN_POINT ( 'NONE',  ( 2.526552050251862358, -40.15571433620797137, 15.32056541070828537 ) ) ;
#15235=EDGE_CURVE ( 'NONE', #56168, #2858, #4197, .T. ) ;
#15241=CARTESIAN_POINT ( 'NONE',  ( 0.5800708119828327236, 5.628966929618427706, -47.56394195701280836 ) ) ;
#15243=B_SPLINE_CURVE_WITH_KNOTS ( 'NONE', 3,
 ( #22240, #46067, #3715, #41665 ),
 .UNSPECIFIED., .F., .F.,
 ( 4, 4 ),
 ( 8.359247967715799972E-17, 0.005004741218457506476 ),
 .UNSPECIFIED. ) ;
#15244=CARTESIAN_POINT ( 'NONE',  ( 0.5809828226811617480, 47.89273459658653564, 0.5448590168534191980 ) ) ;
#15250=CARTESIAN_POINT ( 'NONE',  ( -15.87364823402127811, -12.50000869668378556, -0.1364485216735404627 ) ) ;
#15256=CARTESIAN_POINT ( 'NONE',  ( 0.7056555295713337062, -28.48870155114937219, 38.50897360867676156 ) ) ;
#15259=DIRECTION ( 'NONE',  ( 0.07836865515943411409, -0.1379401902675706781, 0.9873352307081156853 ) ) ;
#15261=ADVANCED_FACE ( 'NONE', ( #57214 ), #3923, .F. ) ;
#15263=CARTESIAN_POINT ( 'NONE',  ( 3.270143674763207553, 10.69018354892887324, 8.548517033725294922 ) ) ;
#15267=CARTESIAN_POINT ( 'NONE',  ( 0.5836750258453370366, -12.57171936981193916, 46.21662382526648116 ) ) ;
#15271=CARTESIAN_POINT ( 'NONE',  ( 4.967162193818130511, 0.000000000000000000, 0.000000000000000000 ) ) ;
#15273=B_SPLINE_CURVE_WITH_KNOTS ( 'NONE', 3,
 ( #30930, #44747, #36267, #50041, #21531, #46284 ),
 .UNSPECIFIED., .F., .F.,
 ( 4, 2, 4 ),
 ( 1.035625919765556564E-17, 0.0002291978881530155638, 0.0004583957763060207734 ),
 .UNSPECIFIED. ) ;
#15276=CARTESIAN_POINT ( 'NONE',  ( 4.960156602257184133, 34.56254177294310637, -30.99165383632728421 ) ) ;
#15278=CARTESIAN_POINT ( 'NONE',  ( 4.967162193818130511, 7.970725651239789045, 42.34252806656596846 ) ) ;
#15282=CARTESIAN_POINT ( 'NONE',  ( 0.9730545539215883499, 21.01499094264601908, -37.40983423658450846 ) ) ;
#15287=EDGE_CURVE ( 'NONE', #11600, #23542, #58783, .T. ) ;
#15288=EDGE_CURVE ( 'NONE', #13993, #31436, #41632, .T. ) ;
#15289=CARTESIAN_POINT ( 'NONE',  ( 0.9968887458511656030, -33.63815526548964385, -26.64009929991538783 ) ) ;
#15296=CARTESIAN_POINT ( 'NONE',  ( 4.967162193818130511, 32.68434214048205888, -28.07411493385260925 ) ) ;
#15300=CARTESIAN_POINT ( 'NONE',  ( 4.303969348037246512, -36.81598326424528977, -30.97035057417698312 ) ) ;
#15302=DIRECTION ( 'NONE',  ( 0.07439287786467665975, -0.01320009283087630186, 0.9971416435352941088 ) ) ;
#15303=( BOUNDED_SURFACE ( )  B_SPLINE_SURFACE ( 3, 1, ( 
 ( #29033, #24645 ),
 ( #34664, #10543 ),
 ( #24024, #44093 ),
 ( #826, #29638 ) ),
 .UNSPECIFIED., .F., .F., .F. ) 
 B_SPLINE_SURFACE_WITH_KNOTS ( ( 4, 4 ),
 ( 2, 2 ),
 ( 0.000000000000000000, 1.000000000000000000 ),
 ( 0.000000000000000000, 1.000000000000000000 ),
 .UNSPECIFIED. ) 
 GEOMETRIC_REPRESENTATION_ITEM ( )  RATIONAL_B_SPLINE_SURFACE ( (
 ( 1.000000000000000000, 1.000000000000000000),
 ( 0.7269869731126821222, 0.9931720237060910339),
 ( 0.7269869731126821222, 0.9931720237060910339),
 ( 1.000000000000000000, 1.000000000000000000) ) ) 
 REPRESENTATION_ITEM ( '' )  SURFACE ( )  );
#15315=CARTESIAN_POINT ( 'NONE',  ( 0.5836750258453360374, -6.431686642655086494, 47.46217286060750951 ) ) ;
#15317=EDGE_LOOP ( 'NONE', ( #27371, #51181, #44891, #44715 ) ) ;
#15318=VERTEX_POINT ( 'NONE', #39708 ) ;
#15319=CARTESIAN_POINT ( 'NONE',  ( 1.227938101723756947, 22.18841447410719780, 36.73927144310519566 ) ) ;
#15327=ORIENTED_EDGE ( 'NONE', *, *, #36554, .F. ) ;
#15328=LINE ( 'NONE', #52586, #58356 ) ;
#15334=CARTESIAN_POINT ( 'NONE',  ( 0.8551540677456739292, 46.51172240253136891, -11.51835730326431850 ) ) ;
#15338=CARTESIAN_POINT ( 'NONE',  ( 0.8551540677456715978, 47.90804413217340851, 0.9122407826477486603 ) ) ;
#15343=B_SPLINE_CURVE_WITH_KNOTS ( 'NONE', 3,
 ( #310, #37651, #14761, #15, #52948, #33257, #38269, #4693, #23521, #47338, #52327, #10053, #29150, #48268, #32629, #61105, #56409, #13525, #9419 ),
 .UNSPECIFIED., .F., .F.,
 ( 4, 3, 3, 3, 3, 3, 4 ),
 ( 0.000000000000000000, 0.0002724573126191739665, 0.0004086839781548579098, 0.0005449106435901954724, 0.0006811373090491585052, 0.0008459866663933821680, 0.001010840725717218353 ),
 .UNSPECIFIED. ) ;
#15344=B_SPLINE_CURVE_WITH_KNOTS ( 'NONE', 3,
 ( #42798, #53088, #43733, #47796 ),
 .UNSPECIFIED., .F., .F.,
 ( 4, 4 ),
 ( 0.000000000000000000, 0.005004741218457414535 ),
 .UNSPECIFIED. ) ;
#15349=CARTESIAN_POINT ( 'NONE',  ( 2.281448460670573386, 11.14236343022437659, -46.66132715497951011 ) ) ;
#15352=ADVANCED_FACE ( 'NONE', ( #25576 ), #59181, .F. ) ;
#15353=CARTESIAN_POINT ( 'NONE',  ( 0.9757892942422835558, -37.13414688883477766, 21.49867881049932095 ) ) ;
#15354=CARTESIAN_POINT ( 'NONE',  ( 0.9754402186311943446, 16.24692483025473067, -39.71365199966000148 ) ) ;
#15361=CARTESIAN_POINT ( 'NONE',  ( 4.956653778116990594, -3.690426056929668075, -47.94889704119055551 ) ) ;
#15374=DIRECTION ( 'NONE',  ( -0.07836865515943412797, -0.4916162952473555614, 0.8672783706145142935 ) ) ;
#15375=CARTESIAN_POINT ( 'NONE',  ( 0.9730545539215883499, -5.099196237954599198, -42.60426903087358852 ) ) ;
#15384=ORIENTED_EDGE ( 'NONE', *, *, #42801, .F. ) ;
#15407=CARTESIAN_POINT ( 'NONE',  ( 0.7056555295713251574, 33.27140645154245391, -34.46100226633700458 ) ) ;
#15408=CARTESIAN_POINT ( 'NONE',  ( -15.98202953935055959, -7.972086415228249123, 0.6796618530310959416 ) ) ;
#15409=CARTESIAN_POINT ( 'NONE',  ( 0.8557997880470690211, 23.15977007032381607, -41.93815086860232810 ) ) ;
#15414=CARTESIAN_POINT ( 'NONE',  ( 0.5836750258453368145, 29.30109045202441820, -37.88760409476664393 ) ) ;
#15419=DIRECTION ( 'NONE',  ( 0.07439287786467665975, 0.7991213610169868309, -0.5965490341031238763 ) ) ;
#15420=VECTOR ( 'NONE', #25720, 1000.000000000000227 ) ;
#15422=EDGE_LOOP ( 'NONE', ( #42505, #59941, #57835, #30617 ) ) ;
#15424=B_SPLINE_CURVE_WITH_KNOTS ( 'NONE', 3,
 ( #51985, #9077, #43544, #43237 ),
 .UNSPECIFIED., .F., .F.,
 ( 4, 4 ),
 ( 7.757919228897728493E-17, 0.005004741218457496067 ),
 .UNSPECIFIED. ) ;
#15425=CARTESIAN_POINT ( 'NONE',  ( 0.5786265663353196143, -38.43785771743223023, 28.58414684753472201 ) ) ;
#15426=EDGE_CURVE ( 'NONE', #25300, #38104, #42192, .T. ) ;
#15430=EDGE_CURVE ( 'NONE', #10841, #8991, #58151, .T. ) ;
#15431=ORIENTED_EDGE ( 'NONE', *, *, #48538, .T. ) ;
#15433=VERTEX_POINT ( 'NONE', #56541 ) ;
#15435=CARTESIAN_POINT ( 'NONE',  ( 0.9730545539215892381, 39.44597740938061037, 16.88610103448572630 ) ) ;
#15436=AXIS2_PLACEMENT_3D ( 'NONE', #27318, #23242, #7898 ) ;
#15441=ORIENTED_EDGE ( 'NONE', *, *, #23685, .T. ) ;
#15445=CARTESIAN_POINT ( 'NONE',  ( 0.8557997880470599172, 24.73961900479308440, -41.02602466100753276 ) ) ;
#15448=ORIENTED_EDGE ( 'NONE', *, *, #6139, .T. ) ;
#15456=CARTESIAN_POINT ( 'NONE',  ( 1.227938101723747621, -20.72293514920724533, -37.58536632582800507 ) ) ;
#15467=( BOUNDED_SURFACE ( )  B_SPLINE_SURFACE ( 3, 1, ( 
 ( #54970, #17709 ),
 ( #13027, #2350 ),
 ( #59678, #32122 ),
 ( #26476, #16792 ) ),
 .UNSPECIFIED., .F., .F., .F. ) 
 B_SPLINE_SURFACE_WITH_KNOTS ( ( 4, 4 ),
 ( 2, 2 ),
 ( 0.000000000000000000, 1.000000000000000000 ),
 ( 0.000000000000000000, 1.000000000000000000 ),
 .UNSPECIFIED. ) 
 GEOMETRIC_REPRESENTATION_ITEM ( )  RATIONAL_B_SPLINE_SURFACE ( (
 ( 1.000000000000000000, 1.000000000000000000),
 ( 0.9953390228620291325, 0.8624445117760984880),
 ( 0.9953390228620291325, 0.8624445117760984880),
 ( 1.000000000000000000, 1.000000000000000000) ) ) 
 REPRESENTATION_ITEM ( '' )  SURFACE ( )  );
#15470=EDGE_CURVE ( 'NONE', #51356, #29746, #53439, .T. ) ;
#15474=FACE_OUTER_BOUND ( 'NONE', #51098, .T. ) ;
#15477=CARTESIAN_POINT ( 'NONE',  ( 4.967162193818130511, 0.000000000000000000, 0.000000000000000000 ) ) ;
#15481=CIRCLE ( 'NONE', #29461, 43.08621763946400307 ) ;
#15486=CARTESIAN_POINT ( 'NONE',  ( 2.281351352603294913, 19.56575819747284584, -43.80196780981699334 ) ) ;
#15488=CARTESIAN_POINT ( 'NONE',  ( 0.9756008150404597012, -10.96816689273726908, 41.48296819691550752 ) ) ;
#15507=CARTESIAN_POINT ( 'NONE',  ( 4.967162193818130511, 0.000000000000000000, 0.000000000000000000 ) ) ;
#15508=CARTESIAN_POINT ( 'NONE',  ( 4.956653778116975495, 26.26162724282373517, 40.28700667097690769 ) ) ;
#15509=LINE ( 'NONE', #49015, #31922 ) ;
#15521=CARTESIAN_POINT ( 'NONE',  ( 4.303969348037258058, -32.45857549159325828, 35.51084504003185316 ) ) ;
#15533=CARTESIAN_POINT ( 'NONE',  ( 5.959547316686252039, 20.52562247508876681, -0.003562808152693846490 ) ) ;
#15535=ORIENTED_EDGE ( 'NONE', *, *, #22063, .F. ) ;
#15537=CARTESIAN_POINT ( 'NONE',  ( 0.5809828226811617480, 24.41822904836982389, -41.20389530892281726 ) ) ;
#15551=B_SPLINE_CURVE_WITH_KNOTS ( 'NONE', 3,
 ( #16378, #35501, #30773, #49892 ),
 .UNSPECIFIED., .F., .F.,
 ( 4, 4 ),
 ( 1.192622389734054877E-18, 0.004444878191957666105 ),
 .UNSPECIFIED. ) ;
#15554=CARTESIAN_POINT ( 'NONE',  ( 0.5807400328401637335, -5.711437504336293713, 47.55718917606841956 ) ) ;
#15560=EDGE_CURVE ( 'NONE', #46829, #12599, #7846, .T. ) ;
#15569=ORIENTED_EDGE ( 'NONE', *, *, #48733, .T. ) ;
#15570=CARTESIAN_POINT ( 'NONE',  ( 0.6846871229502899947, -37.47592888575268688, 29.84551600520619274 ) ) ;
#15572=CARTESIAN_POINT ( 'NONE',  ( 4.303969348037258058, -47.93217632892346103, -4.133486515473800083 ) ) ;
#15574=VECTOR ( 'NONE', #5106, 1000.000000000000114 ) ;
#15579=ORIENTED_EDGE ( 'NONE', *, *, #10378, .F. ) ;
#15580=EDGE_LOOP ( 'NONE', ( #7630, #10757, #42908, #46118 ) ) ;
#15584=CARTESIAN_POINT ( 'NONE',  ( 0.5809828226811617480, 41.74875432577682233, -23.47450554821666202 ) ) ;
#15597=B_SPLINE_CURVE_WITH_KNOTS ( 'NONE', 3,
 ( #42374, #18547, #28863, #37676, #38597, #5341, #23546, #10076, #24475, #37360, #13548, #32654, #42676, #61738, #51737, #20102 ),
 .UNSPECIFIED., .F., .F.,
 ( 4, 3, 3, 3, 3, 4 ),
 ( 1.250973872328959318E-17, 0.0002724568934985534328, 0.0004086836638483776533, 0.0005449104342063536104, 0.0008173270854453626617, 0.001089761613562690310 ),
 .UNSPECIFIED. ) ;
#15604=ADVANCED_FACE ( 'NONE', ( #43721 ), #33192, .T. ) ;
#15609=CARTESIAN_POINT ( 'NONE',  ( 4.967162193818130511, 0.000000000000000000, 0.000000000000000000 ) ) ;
#15610=ORIENTED_EDGE ( 'NONE', *, *, #5112, .F. ) ;
#15617=ORIENTED_EDGE ( 'NONE', *, *, #13901, .F. ) ;
#15619=CARTESIAN_POINT ( 'NONE',  ( 0.5839254288179557273, -6.341681103464875235, 47.47429404163006694 ) ) ;
#15622=VERTEX_POINT ( 'NONE', #56846 ) ;
#15624=ORIENTED_EDGE ( 'NONE', *, *, #15989, .F. ) ;
#15631=ORIENTED_EDGE ( 'NONE', *, *, #8440, .T. ) ;
#15632=VECTOR ( 'NONE', #8371, 1000.000000000000114 ) ;
#15650=EDGE_CURVE ( 'NONE', #48653, #9174, #58637, .T. ) ;
#15653=CARTESIAN_POINT ( 'NONE',  ( 3.660176727303410260, -45.87883389004760915, -14.24118031989642574 ) ) ;
#15661=CARTESIAN_POINT ( 'NONE',  ( 0.5839879327111922036, 18.24507200299104426, -44.28486549479607959 ) ) ;
#15669=( BOUNDED_SURFACE ( )  B_SPLINE_SURFACE ( 3, 1, ( 
 ( #899, #18797 ),
 ( #20037, #24097 ),
 ( #39151, #23475 ),
 ( #13795, #42920 ) ),
 .UNSPECIFIED., .F., .F., .F. ) 
 B_SPLINE_SURFACE_WITH_KNOTS ( ( 4, 4 ),
 ( 2, 2 ),
 ( 0.000000000000000000, 1.000000000000000000 ),
 ( 0.000000000000000000, 1.000000000000000000 ),
 .UNSPECIFIED. ) 
 GEOMETRIC_REPRESENTATION_ITEM ( )  RATIONAL_B_SPLINE_SURFACE ( (
 ( 1.000000000000000000, 1.000000000000000000),
 ( 0.9953390228620291325, 0.8624445117760984880),
 ( 0.9953390228620291325, 0.8624445117760984880),
 ( 1.000000000000000000, 1.000000000000000000) ) ) 
 REPRESENTATION_ITEM ( '' )  SURFACE ( )  );
#15672=CARTESIAN_POINT ( 'NONE',  ( 0.6067375320500723035, 23.33187539052128301, 41.82999795871614879 ) ) ;
#15675=CARTESIAN_POINT ( 'NONE',  ( 3.270143674763207553, 0.2742231296311491984, -13.68510027222512981 ) ) ;
#15677=CARTESIAN_POINT ( 'NONE',  ( 5.960721111146673579, -12.50019045452726907, -16.28018152803688778 ) ) ;
#15695=CARTESIAN_POINT ( 'NONE',  ( 0.5839254288179548391, -44.28478521851634753, 18.24509008251461850 ) ) ;
#15697=CARTESIAN_POINT ( 'NONE',  ( 0.5800708119828333897, 47.40012378203040555, -6.873289505980164193 ) ) ;
#15701=ORIENTED_EDGE ( 'NONE', *, *, #27446, .T. ) ;
#15720=EDGE_CURVE ( 'NONE', #44327, #3716, #16074, .T. ) ;
#15722=CARTESIAN_POINT ( 'NONE',  ( -15.94137352497273419, -7.982459924543421792, 0.5466233485435718631 ) ) ;
#15725=CARTESIAN_POINT ( 'NONE',  ( 5.960721111146673579, -19.82454228767742066, -5.318514366754864220 ) ) ;
#15728=CARTESIAN_POINT ( 'NONE',  ( 0.5809828226811617480, 33.48000389720616710, 34.25055090842165839 ) ) ;
#15735=CARTESIAN_POINT ( 'NONE',  ( 1.227938101723748288, 10.28900963485380693, 41.66816631169195517 ) ) ;
#15741=ORIENTED_EDGE ( 'NONE', *, *, #47307, .F. ) ;
#15744=AXIS2_PLACEMENT_3D ( 'NONE', #34633, #9899, #48114 ) ;
#15747=CARTESIAN_POINT ( 'NONE',  ( 1.154321713695931839, 25.46626713715458834, 34.54400171733310998 ) ) ;
#15749=CARTESIAN_POINT ( 'NONE',  ( 0.8557997880470599172, -37.44587306708076824, -29.88293891557508530 ) ) ;
#15760=( BOUNDED_SURFACE ( )  B_SPLINE_SURFACE ( 3, 1, ( 
 ( #43285, #29463 ),
 ( #52956, #38583 ),
 ( #14769, #19780 ),
 ( #19167, #638 ) ),
 .UNSPECIFIED., .F., .F., .F. ) 
 B_SPLINE_SURFACE_WITH_KNOTS ( ( 4, 4 ),
 ( 2, 2 ),
 ( 0.000000000000000000, 1.000000000000000000 ),
 ( 0.000000000000000000, 1.000000000000000000 ),
 .UNSPECIFIED. ) 
 GEOMETRIC_REPRESENTATION_ITEM ( )  RATIONAL_B_SPLINE_SURFACE ( (
 ( 1.000000000000000000, 1.000000000000000000),
 ( 0.9953390228620291325, 0.8624445117761032620),
 ( 0.9953390228620291325, 0.8624445117761032620),
 ( 1.000000000000000000, 1.000000000000000000) ) ) 
 REPRESENTATION_ITEM ( '' )  SURFACE ( )  );
#15762=ORIENTED_EDGE ( 'NONE', *, *, #51680, .T. ) ;
#15763=CARTESIAN_POINT ( 'NONE',  ( 1.227938101723756947, 41.66816631169191965, 10.28900963485394904 ) ) ;
#15783=CARTESIAN_POINT ( 'NONE',  ( 0.8557997880470599172, 7.156447707086380561, -47.37054680076698077 ) ) ;
#15787=VECTOR ( 'NONE', #2888, 1000.000000000000114 ) ;
#15795=FACE_OUTER_BOUND ( 'NONE', #37142, .T. ) ;
#15796=CARTESIAN_POINT ( 'NONE',  ( 0.9722240750034573109, 6.177112354445118747, 42.46141201102046381 ) ) ;
#15797=FACE_OUTER_BOUND ( 'NONE', #11644, .T. ) ;
#15799=CARTESIAN_POINT ( 'NONE',  ( 0.6067099128993247437, 41.12102523654892394, -24.55985149487281305 ) ) ;
#15807=ORIENTED_EDGE ( 'NONE', *, *, #36514, .T. ) ;
#15812=DIRECTION ( 'NONE',  ( -1.000000000000000000, -0.000000000000000000, -0.000000000000000000 ) ) ;
#15829=B_SPLINE_CURVE_WITH_KNOTS ( 'NONE', 3,
 ( #5778, #14925, #43123, #19305, #23993, #38124 ),
 .UNSPECIFIED., .F., .F.,
 ( 4, 2, 4 ),
 ( 9.140795285775094282E-18, 0.0002291978881530172714, 0.0004583957763060254355 ),
 .UNSPECIFIED. ) ;
#15844=VERTEX_POINT ( 'NONE', #13816 ) ;
#15845=CARTESIAN_POINT ( 'NONE',  ( 2.281351352603296245, 30.23585463601430590, -37.24546109640787250 ) ) ;
#15846=CARTESIAN_POINT ( 'NONE',  ( 5.981074661064941900, 18.96560215432005947, 7.846517100474887485 ) ) ;
#15847=VECTOR ( 'NONE', #3815, 1000.000000000000114 ) ;
#15851=CARTESIAN_POINT ( 'NONE',  ( 4.967162193818130511, -43.02067033766017801, -2.375726030843023029 ) ) ;
#15856=FACE_OUTER_BOUND ( 'NONE', #24117, .T. ) ;
#15861=B_SPLINE_CURVE_WITH_KNOTS ( 'NONE', 3,
 ( #7257, #12311, #3187, #55810 ),
 .UNSPECIFIED., .F., .F.,
 ( 4, 4 ),
 ( 0.000000000000000000, 0.004050076154993000749 ),
 .UNSPECIFIED. ) ;
#15865=CARTESIAN_POINT ( 'NONE',  ( -17.69803791752843836, -12.32468874903235267, 2.086332406704181519 ) ) ;
#15873=DIRECTION ( 'NONE',  ( -0.07439287786467653485, 0.6957517427943171739, -0.7144194931002945115 ) ) ;
#15875=VECTOR ( 'NONE', #46867, 1000.000000000000114 ) ;
#15880=CARTESIAN_POINT ( 'NONE',  ( 0.5807400328401637335, -37.66660715020886840, 29.58941477093002348 ) ) ;
#15882=CARTESIAN_POINT ( 'NONE',  ( 5.860006189529246790, 31.81514841426808005, -36.25227510158430277 ) ) ;
#15883=CARTESIAN_POINT ( 'NONE',  ( 0.9730545539215883499, 42.90536227157002003, 0.5054011016614263774 ) ) ;
#15887=CARTESIAN_POINT ( 'NONE',  ( 0.9730545539215883499, 37.40983423658502716, -21.01499094264509893 ) ) ;
#15897=CARTESIAN_POINT ( 'NONE',  ( 4.967162193818130511, -32.68434214048189546, 28.07411493385282242 ) ) ;
#15899=DIRECTION ( 'NONE',  ( 0.07836865515943412797, 0.6131273243286281538, -0.7860872967108163412 ) ) ;
#15901=CARTESIAN_POINT ( 'NONE',  ( -48.95476116535499500, 0.000000000000000000, 0.000000000000000000 ) ) ;
#15902=CARTESIAN_POINT ( 'NONE',  ( 2.624215991343620935, -45.98641578154040843, 13.78323291683767415 ) ) ;
#15907=CARTESIAN_POINT ( 'NONE',  ( 0.5809828226811553087, -37.66417181417572380, 29.58751527316164953 ) ) ;
#15913=ORIENTED_EDGE ( 'NONE', *, *, #13296, .T. ) ;
#15919=CARTESIAN_POINT ( 'NONE',  ( 3.407937589446174087, 12.47329436636629119, 5.663729899985116667 ) ) ;
#15923=VERTEX_POINT ( 'NONE', #1519 ) ;
#15928=B_SPLINE_CURVE_WITH_KNOTS ( 'NONE', 3,
 ( #47005, #4038, #33209, #9374, #37605, #52280 ),
 .UNSPECIFIED., .F., .F.,
 ( 4, 2, 4 ),
 ( 9.965227682168975268E-18, 0.0002445244328975359929, 0.0004890488657950620112 ),
 .UNSPECIFIED. ) ;
#15932=CARTESIAN_POINT ( 'NONE',  ( 4.967162193818130511, 28.74031574030056646, -32.10009971360042158 ) ) ;
#15933=CARTESIAN_POINT ( 'NONE',  ( 0.9730545539215883499, -0.5054011016609686324, -42.90536227157002713 ) ) ;
#15938=EDGE_CURVE ( 'NONE', #54002, #44253, #18203, .T. ) ;
#15942=EDGE_CURVE ( 'NONE', #39564, #10841, #24276, .T. ) ;
#15946=DIRECTION ( 'NONE',  ( -0.07439287786467650709, 0.6174937095821703137, 0.7830499462674533895 ) ) ;
#15951=CARTESIAN_POINT ( 'NONE',  ( 3.783198216974390959, -9.462293521184577116, -41.98529422752524454 ) ) ;
#15956=LINE ( 'NONE', #49763, #21749 ) ;
#15959=LINE ( 'NONE', #44484, #60453 ) ;
#15961=AXIS2_PLACEMENT_3D ( 'NONE', #40181, #34844, #16040 ) ;
#15963=ORIENTED_EDGE ( 'NONE', *, *, #24386, .T. ) ;
#15967=CARTESIAN_POINT ( 'NONE',  ( 5.960721111146673579, 20.35079619394246109, -2.672857320903093914 ) ) ;
#15969=CARTESIAN_POINT ( 'NONE',  ( 0.9756008150404587020, 39.58764833544701389, -16.55159915785236890 ) ) ;
#15971=CARTESIAN_POINT ( 'NONE',  ( 3.407937589446174087, -9.356405769958984209, -10.00592723328970912 ) ) ;
#15972=FACE_OUTER_BOUND ( 'NONE', #9983, .T. ) ;
#15979=CARTESIAN_POINT ( 'NONE',  ( 5.981074661064941900, -0.008585178657759484633, 20.52466374824937034 ) ) ;
#15982=CARTESIAN_POINT ( 'NONE',  ( 5.981074661064941900, -12.50143471347269930, -16.27808421740022027 ) ) ;
#15989=EDGE_CURVE ( 'NONE', #21198, #52461, #21283, .T. ) ;
#15996=CARTESIAN_POINT ( 'NONE',  ( 1.227938101723748288, -22.18841447410744649, 36.73927144310504644 ) ) ;
#16006=CARTESIAN_POINT ( 'NONE',  ( 1.227938101723748288, -36.73927144310496828, -22.18841447410757795 ) ) ;
#16014=EDGE_CURVE ( 'NONE', #32792, #30530, #43725, .T. ) ;
#16019=CARTESIAN_POINT ( 'NONE',  ( 0.9968887458511670463, 33.63815526548984991, 26.64009929991515691 ) ) ;
#16020=( BOUNDED_SURFACE ( )  B_SPLINE_SURFACE ( 3, 1, ( 
 ( #3934, #28687 ),
 ( #52177, #8968 ),
 ( #14303, #28378 ),
 ( #18070, #47813 ) ),
 .UNSPECIFIED., .F., .F., .F. ) 
 B_SPLINE_SURFACE_WITH_KNOTS ( ( 4, 4 ),
 ( 2, 2 ),
 ( 0.000000000000000000, 1.000000000000000000 ),
 ( 0.000000000000000000, 1.000000000000000000 ),
 .UNSPECIFIED. ) 
 GEOMETRIC_REPRESENTATION_ITEM ( )  RATIONAL_B_SPLINE_SURFACE ( (
 ( 1.000000000000000000, 1.000000000000000000),
 ( 0.9953390228620291325, 0.8624445117760984880),
 ( 0.9953390228620291325, 0.8624445117760984880),
 ( 1.000000000000000000, 1.000000000000000000) ) ) 
 REPRESENTATION_ITEM ( '' )  SURFACE ( )  );
#16025=CARTESIAN_POINT ( 'NONE',  ( -17.42622638222554698, -7.737665651455587046, -2.032071817730983554 ) ) ;
#16030=CARTESIAN_POINT ( 'NONE',  ( 0.8557997880470599172, -43.90420959842167292, -19.17299735372055736 ) ) ;
#16038=ORIENTED_EDGE ( 'NONE', *, *, #9547, .F. ) ;
#16039=CARTESIAN_POINT ( 'NONE',  ( 5.960721111146673579, 5.318514366754659939, 19.82454228767747750 ) ) ;
#16040=DIRECTION ( 'NONE',  ( 0.000000000000000000, 0.000000000000000000, 1.000000000000000000 ) ) ;
#16049=ORIENTED_EDGE ( 'NONE', *, *, #34883, .T. ) ;
#16067=CARTESIAN_POINT ( 'NONE',  ( 0.8551540677456739292, 37.45266983663496063, 29.88829867897826631 ) ) ;
#16071=CARTESIAN_POINT ( 'NONE',  ( 0.5809828226811553087, 37.66417181417592275, -29.58751527316140795 ) ) ;
#16074=B_SPLINE_CURVE_WITH_KNOTS ( 'NONE', 3,
 ( #53675, #29891, #47621, #37624, #23891, #32291 ),
 .UNSPECIFIED., .F., .F.,
 ( 4, 2, 4 ),
 ( 1.084202172485504434E-19, 0.0002445244328975357219, 0.0004890488657950713353 ),
 .UNSPECIFIED. ) ;
#16076=ORIENTED_EDGE ( 'NONE', *, *, #46382, .F. ) ;
#16077=CARTESIAN_POINT ( 'NONE',  ( 0.5786265663353153954, -34.37803667029788812, -33.35675271369575512 ) ) ;
#16080=CARTESIAN_POINT ( 'NONE',  ( 0.7762777257811928067, 29.86325207275931959, -37.45705273430974103 ) ) ;
#16086=CARTESIAN_POINT ( 'NONE',  ( 1.227938101723756947, -33.52879263017882039, 26.79402671879314823 ) ) ;
#16092=CARTESIAN_POINT ( 'NONE',  ( 5.860006189529246790, 3.171667470663204647, -48.12869875779304607 ) ) ;
#16101=CARTESIAN_POINT ( 'NONE',  ( 0.9752570700956788574, -26.30364510018335267, 33.90066715551964194 ) ) ;
#16102=EDGE_CURVE ( 'NONE', #29930, #28235, #9290, .T. ) ;
#16130=CARTESIAN_POINT ( 'NONE',  ( 0.9752570700956806338, 42.51066151201240473, 5.829291291128810393 ) ) ;
#16132=VERTEX_POINT ( 'NONE', #46637 ) ;
#16138=CARTESIAN_POINT ( 'NONE',  ( 1.227938101723756947, 20.72293514920803048, -37.58536632582757875 ) ) ;
#16140=EDGE_CURVE ( 'NONE', #56839, #43658, #8498, .T. ) ;
#16143=ORIENTED_EDGE ( 'NONE', *, *, #22204, .F. ) ;
#16146=VECTOR ( 'NONE', #58281, 1000.000000000000114 ) ;
#16147=CARTESIAN_POINT ( 'NONE',  ( 4.956653778116982600, -45.35992544608539845, 15.97476558431867844 ) ) ;
#16149=CARTESIAN_POINT ( 'NONE',  ( 5.959828726073459926, -19.82504517499716812, 5.316791119500744678 ) ) ;
#16157=CARTESIAN_POINT ( 'NONE',  ( 0.9730545539215883499, -37.40983423658458662, -21.01499094264588763 ) ) ;
#16159=CARTESIAN_POINT ( 'NONE',  ( 4.967162193818130511, 28.07411493385340862, -32.68434214048137676 ) ) ;
#16164=B_SPLINE_CURVE_WITH_KNOTS ( 'NONE', 3,
 ( #23249, #13867, #46766, #4719 ),
 .UNSPECIFIED., .F., .F.,
 ( 4, 4 ),
 ( 0.000000000000000000, 0.005004741218457429280 ),
 .UNSPECIFIED. ) ;
#16165=CARTESIAN_POINT ( 'NONE',  ( 0.7762777257811898091, 47.89627391089018715, 0.8897018348887656414 ) ) ;
#16170=ORIENTED_EDGE ( 'NONE', *, *, #19412, .F. ) ;
#16171=CARTESIAN_POINT ( 'NONE',  ( -17.83468216677388796, -12.32233744059949565, 2.099999999999995648 ) ) ;
#16174=CARTESIAN_POINT ( 'NONE',  ( 0.5807400328401574052, 41.20655774453003772, -24.41979442053125737 ) ) ;
#16175=CARTESIAN_POINT ( 'NONE',  ( 1.154321485836934391, 41.23280395520824726, -11.90271791109269550 ) ) ;
#16177=CARTESIAN_POINT ( 'NONE',  ( 3.660087539127329759, -8.130906407639741929, -47.34518630204118494 ) ) ;
#16185=CARTESIAN_POINT ( 'NONE',  ( 5.974727161628369032, -14.52429704002373789, 14.50236057684819535 ) ) ;
#16203=CARTESIAN_POINT ( 'NONE',  ( 0.9757787079277445708, 41.45659305953935814, -11.06737752163053834 ) ) ;
#16207=CARTESIAN_POINT ( 'NONE',  ( 0.9722240750034577550, 42.90442369954359947, -0.5819398758581642017 ) ) ;
#16216=ORIENTED_EDGE ( 'NONE', *, *, #27805, .F. ) ;
#16229=B_SPLINE_CURVE_WITH_KNOTS ( 'NONE', 3,
 ( #41142, #21390, #50199, #11375 ),
 .UNSPECIFIED., .F., .F.,
 ( 4, 4 ),
 ( 0.000000000000000000, 0.005004741218457415403 ),
 .UNSPECIFIED. ) ;
#16230=VECTOR ( 'NONE', #12031, 1000.000000000000114 ) ;
#16232=VECTOR ( 'NONE', #36441, 1000.000000000000114 ) ;
#16245=CARTESIAN_POINT ( 'NONE',  ( 5.959828726073459926, -10.25888482581871841, 17.77796293532155048 ) ) ;
#16246=CARTESIAN_POINT ( 'NONE',  ( 4.967162193818130511, -40.65506779172153529, -14.26841313271325795 ) ) ;
#16248=CARTESIAN_POINT ( 'NONE',  ( 5.974727161628367256, -19.82156119440448805, 5.327229920347082093 ) ) ;
#16256=CARTESIAN_POINT ( 'NONE',  ( 0.5807400328401637335, 34.25275203086236075, 33.48217046439123834 ) ) ;
#16273=B_SPLINE_CURVE_WITH_KNOTS ( 'NONE', 3,
 ( #48915, #39237, #48602, #58286 ),
 .UNSPECIFIED., .F., .F.,
 ( 4, 4 ),
 ( 8.673617379884035472E-19, 0.004050076154993002484 ),
 .UNSPECIFIED. ) ;
#16279=CARTESIAN_POINT ( 'NONE',  ( 0.8551540677456739292, -29.88829867897839421, 37.45266983663486826 ) ) ;
#16281=ORIENTED_EDGE ( 'NONE', *, *, #19061, .F. ) ;
#16284=ORIENTED_EDGE ( 'NONE', *, *, #25020, .F. ) ;
#16286=EDGE_CURVE ( 'NONE', #18521, #35798, #7068, .T. ) ;
#16293=CARTESIAN_POINT ( 'NONE',  ( 3.783278058412224976, -20.00643011788481829, 38.10568111914496825 ) ) ;
#16295=CARTESIAN_POINT ( 'NONE',  ( 0.5786265663353196143, 17.66171603226080222, 44.52624106864148246 ) ) ;
#16300=CARTESIAN_POINT ( 'NONE',  ( 4.956653778116966613, 0.000000000000000000, 0.000000000000000000 ) ) ;
#16309=ORIENTED_EDGE ( 'NONE', *, *, #42453, .T. ) ;
#16316=( BOUNDED_SURFACE ( )  B_SPLINE_SURFACE ( 3, 1, ( 
 ( #49565, #54249 ),
 ( #25450, #58329 ),
 ( #29537, #11368 ),
 ( #16375, #48645 ) ),
 .UNSPECIFIED., .F., .F., .F. ) 
 B_SPLINE_SURFACE_WITH_KNOTS ( ( 4, 4 ),
 ( 2, 2 ),
 ( 0.000000000000000000, 1.000000000000000000 ),
 ( 0.000000000000000000, 1.000000000000000000 ),
 .UNSPECIFIED. ) 
 GEOMETRIC_REPRESENTATION_ITEM ( )  RATIONAL_B_SPLINE_SURFACE ( (
 ( 1.000000000000000000, 1.000000000000000000),
 ( 0.9953390228620291325, 0.8624445117761032620),
 ( 0.9953390228620291325, 0.8624445117761032620),
 ( 1.000000000000000000, 1.000000000000000000) ) ) 
 REPRESENTATION_ITEM ( '' )  SURFACE ( )  );
#16319=EDGE_CURVE ( 'NONE', #29746, #18686, #51103, .T. ) ;
#16323=FACE_OUTER_BOUND ( 'NONE', #7075, .T. ) ;
#16325=CARTESIAN_POINT ( 'NONE',  ( 2.526552050251864134, 27.11558601691313797, -33.34585601411836109 ) ) ;
#16332=LINE ( 'NONE', #50161, #51898 ) ;
#16343=CARTESIAN_POINT ( 'NONE',  ( 5.960721111146673579, 12.50019045452716426, 16.28018152803696950 ) ) ;
#16344=CARTESIAN_POINT ( 'NONE',  ( 0.9740398440564304039, -41.55177796653840261, -10.70454588197330814 ) ) ;
#16347=CARTESIAN_POINT ( 'NONE',  ( 0.5807400328401574052, -47.41494605191447675, 6.791881299635412539 ) ) ;
#16353=DIRECTION ( 'NONE',  ( 0.07836865515943411409, 0.5052769534812749930, -0.8593913859058531779 ) ) ;
#16360=ORIENTED_EDGE ( 'NONE', *, *, #30598, .F. ) ;
#16362=DIRECTION ( 'NONE',  ( 0.000000000000000000, 0.000000000000000000, 1.000000000000000000 ) ) ;
#16368=ORIENTED_EDGE ( 'NONE', *, *, #29906, .F. ) ;
#16374=ORIENTED_EDGE ( 'NONE', *, *, #40172, .F. ) ;
#16375=CARTESIAN_POINT ( 'NONE',  ( 5.960721111146673579, -17.77882586010660049, -10.25731071096576486 ) ) ;
#16378=CARTESIAN_POINT ( 'NONE',  ( 0.8557997880470690211, 41.93815086860257679, 23.15977007032337553 ) ) ;
#16397=CIRCLE ( 'NONE', #29405, 48.09070567114147110 ) ;
#16402=EDGE_CURVE ( 'NONE', #21513, #437, #25786, .T. ) ;
#16407=EDGE_CURVE ( 'NONE', #15433, #35962, #42935, .T. ) ;
#16413=EDGE_CURVE ( 'NONE', #21601, #35431, #11226, .T. ) ;
#16424=CARTESIAN_POINT ( 'NONE',  ( 1.227938101723756947, -4.762198645644731165, 42.65467462194916948 ) ) ;
#16429=CARTESIAN_POINT ( 'NONE',  ( 0.9730545539215883499, 42.47233286818616449, 6.101350888304794218 ) ) ;
#16438=CARTESIAN_POINT ( 'NONE',  ( 0.5827357941260201679, 12.04516435546866937, -46.35666768646123614 ) ) ;
#16440=ORIENTED_EDGE ( 'NONE', *, *, #37798, .F. ) ;
#16441=DIRECTION ( 'NONE',  ( 0.000000000000000000, 0.000000000000000000, 1.000000000000000000 ) ) ;
#16443=EDGE_CURVE ( 'NONE', #47692, #44331, #35514, .T. ) ;
#16449=VERTEX_POINT ( 'NONE', #26093 ) ;
#16454=PRODUCT_DEFINITION ( 'UNKNOWN', '', #55895, #34227 ) ;
#16460=CARTESIAN_POINT ( 'NONE',  ( 0.5827357941260221663, 46.16863402900295910, -12.74691551863582717 ) ) ;
#16461=CARTESIAN_POINT ( 'NONE',  ( 0.5809828226811553087, -47.55412398569202281, -5.711058609465819558 ) ) ;
#16468=CARTESIAN_POINT ( 'NONE',  ( -15.88737024819575439, -12.49768255930560024, -0.2758842803416746703 ) ) ;
#16488=DIRECTION ( 'NONE',  ( -1.000000000000000000, -0.000000000000000000, -0.000000000000000000 ) ) ;
#16492=CARTESIAN_POINT ( 'NONE',  ( 0.5838002273316433843, -47.50378804015149115, 6.116619957188576429 ) ) ;
#16495=ORIENTED_EDGE ( 'NONE', *, *, #17908, .F. ) ;
#16508=CARTESIAN_POINT ( 'NONE',  ( 0.5809828226811617480, 34.25055090842200656, -33.48000389720580472 ) ) ;
#16519=CARTESIAN_POINT ( 'NONE',  ( 0.7056555295713285991, -33.27140645154220522, 34.46100226633724617 ) ) ;
#16523=CIRCLE ( 'NONE', #9489, 48.09070567114147110 ) ;
#16526=CARTESIAN_POINT ( 'NONE',  ( 0.5809828226811565299, -17.82437196699712700, 44.45562576850595349 ) ) ;
#16527=ORIENTED_EDGE ( 'NONE', *, *, #7992, .T. ) ;
#16528=FACE_OUTER_BOUND ( 'NONE', #13199, .T. ) ;
#16529=CARTESIAN_POINT ( 'NONE',  ( 0.5809828226811553087, -47.55412398569202281, -5.711058609465819558 ) ) ;
#16533=FACE_OUTER_BOUND ( 'NONE', #38889, .T. ) ;
#16541=CARTESIAN_POINT ( 'NONE',  ( 3.270143674763207553, 10.69018354892899403, -8.548517033725143932 ) ) ;
#16546=CARTESIAN_POINT ( 'NONE',  ( 0.5800708057587363742, -23.40241940841928781, -41.78924035064549969 ) ) ;
#16548=ORIENTED_EDGE ( 'NONE', *, *, #16402, .T. ) ;
#16549=VECTOR ( 'NONE', #39804, 1000.000000000000114 ) ;
#16554=CARTESIAN_POINT ( 'NONE',  ( 5.959547316686252039, -10.25972575517542396, 17.77749189599199653 ) ) ;
#16560=EDGE_CURVE ( 'NONE', #694, #2809, #21238, .T. ) ;
#16561=LINE ( 'NONE', #55368, #30849 ) ;
#16569=( BOUNDED_SURFACE ( )  B_SPLINE_SURFACE ( 3, 1, ( 
 ( #3796, #51408 ),
 ( #47062, #23851 ),
 ( #25, #4098 ),
 ( #46751, #22937 ) ),
 .UNSPECIFIED., .F., .F., .F. ) 
 B_SPLINE_SURFACE_WITH_KNOTS ( ( 4, 4 ),
 ( 2, 2 ),
 ( 0.000000000000000000, 1.000000000000000000 ),
 ( 0.000000000000000000, 1.000000000000000000 ),
 .UNSPECIFIED. ) 
 GEOMETRIC_REPRESENTATION_ITEM ( )  RATIONAL_B_SPLINE_SURFACE ( (
 ( 1.000000000000000000, 1.000000000000000000),
 ( 0.9953390228620291325, 0.8624445117761032620),
 ( 0.9953390228620291325, 0.8624445117761032620),
 ( 1.000000000000000000, 1.000000000000000000) ) ) 
 REPRESENTATION_ITEM ( '' )  SURFACE ( )  );
#16572=EDGE_CURVE ( 'NONE', #19565, #26674, #28710, .T. ) ;
#16574=CARTESIAN_POINT ( 'NONE',  ( 0.9757892942422820015, -26.16173342773518584, -34.01031843153919709 ) ) ;
#16579=CARTESIAN_POINT ( 'NONE',  ( 0.8557997880470599172, -29.88293891557496096, 37.44587306708088192 ) ) ;
#16590=VECTOR ( 'NONE', #35169, 1000.000000000000114 ) ;
#16591=VERTEX_POINT ( 'NONE', #27953 ) ;
#16596=ORIENTED_EDGE ( 'NONE', *, *, #20237, .T. ) ;
#16608=CARTESIAN_POINT ( 'NONE',  ( 4.956653778116975495, 15.97476558431885252, 45.35992544608534160 ) ) ;
#16613=FACE_OUTER_BOUND ( 'NONE', #31810, .T. ) ;
#16618=LINE ( 'NONE', #55423, #56761 ) ;
#16624=CARTESIAN_POINT ( 'NONE',  ( -20.07361639412344800, -12.49998595421523184, -0.1399944396052446860 ) ) ;
#16632=ORIENTED_EDGE ( 'NONE', *, *, #29359, .T. ) ;
#16636=CARTESIAN_POINT ( 'NONE',  ( 0.5786265663353196143, 6.967625775956395984, -47.39171391660384813 ) ) ;
#16640=CARTESIAN_POINT ( 'NONE',  ( 0.9747592971366223491, 36.99691261380240803, -21.73404615330581890 ) ) ;
#16646=EDGE_CURVE ( 'NONE', #22519, #12427, #33159, .T. ) ;
#16652=CARTESIAN_POINT ( 'NONE',  ( 0.6846871229502899947, 43.92355552798064622, -19.12907057981156811 ) ) ;
#16654=ORIENTED_EDGE ( 'NONE', *, *, #40618, .T. ) ;
#16658=LINE ( 'NONE', #30736, #45713 ) ;
#16662=CARTESIAN_POINT ( 'NONE',  ( 0.9747592971366237924, -41.52905920980975907, -10.79247637456163034 ) ) ;
#16667=CARTESIAN_POINT ( 'NONE',  ( 0.9730545539215883499, -26.52009130076748278, -33.73144377768585400 ) ) ;
#16670=VERTEX_POINT ( 'NONE', #26759 ) ;
#16672=CARTESIAN_POINT ( 'NONE',  ( 1.154321485836934169, 39.95809831208277529, 15.65787964449878444 ) ) ;
#16678=CIRCLE ( 'NONE', #28701, 48.09070567114147110 ) ;
#16682=B_SPLINE_CURVE_WITH_KNOTS ( 'NONE', 3,
 ( #12118, #40630, #36537, #3287 ),
 .UNSPECIFIED., .F., .F.,
 ( 4, 4 ),
 ( 2.168404344971008868E-19, 0.004048833967417086489 ),
 .UNSPECIFIED. ) ;
#16694=DIRECTION ( 'NONE',  ( 0.000000000000000000, 0.000000000000000000, 1.000000000000000000 ) ) ;
#16696=ORIENTED_EDGE ( 'NONE', *, *, #59404, .T. ) ;
#16700=CARTESIAN_POINT ( 'NONE',  ( 0.9757892942422827787, -16.37293303864333893, 39.66188497122489309 ) ) ;
#16706=EDGE_CURVE ( 'NONE', #21206, #46227, #12601, .T. ) ;
#16711=CARTESIAN_POINT ( 'NONE',  ( 0.5809828226811548646, 29.58751527316178809, 37.66417181417562432 ) ) ;
#16714=CARTESIAN_POINT ( 'NONE',  ( 0.9722240750034580881, 42.61332880321398164, 5.023189755349083185 ) ) ;
#16715=EDGE_CURVE ( 'NONE', #52796, #34886, #17029, .T. ) ;
#16717=VECTOR ( 'NONE', #54574, 1000.000000000000114 ) ;
#16721=ORIENTED_EDGE ( 'NONE', *, *, #37074, .T. ) ;
#16725=DIRECTION ( 'NONE',  ( 0.000000000000000000, 0.000000000000000000, 1.000000000000000000 ) ) ;
#16728=ORIENTED_EDGE ( 'NONE', *, *, #6697, .T. ) ;
#16734=ORIENTED_EDGE ( 'NONE', *, *, #40918, .F. ) ;
#16736=CARTESIAN_POINT ( 'NONE',  ( 0.5827359174754830340, 47.89462060834303259, 0.3632382226752371990 ) ) ;
#16737=VECTOR ( 'NONE', #37625, 1000.000000000000227 ) ;
#16738=CARTESIAN_POINT ( 'NONE',  ( 2.526464513654346433, -4.405490210168683696, 42.75268905308553258 ) ) ;
#16745=B_SPLINE_CURVE_WITH_KNOTS ( 'NONE', 3,
 ( #55628, #27145, #8033, #46273 ),
 .UNSPECIFIED., .F., .F.,
 ( 4, 4 ),
 ( 0.000000000000000000, 0.004446090762761381598 ),
 .UNSPECIFIED. ) ;
#16746=CARTESIAN_POINT ( 'NONE',  ( 0.9741495583595156660, 42.48790363482606125, 5.992561317325313830 ) ) ;
#16766=ORIENTED_EDGE ( 'NONE', *, *, #25585, .F. ) ;
#16767=CARTESIAN_POINT ( 'NONE',  ( 5.960721111146673579, -19.82454228767749527, 5.318514366754590661 ) ) ;
#16769=CARTESIAN_POINT ( 'NONE',  ( 4.963659409799332067, -44.62477100936216345, -3.403493583737785322 ) ) ;
#16772=CONICAL_SURFACE ( 'NONE', #11768, 43.08621763946400307, 1.568696531533066763 ) ;
#16775=VECTOR ( 'NONE', #15374, 999.9999999999998863 ) ;
#16777=CARTESIAN_POINT ( 'NONE',  ( 4.956653778116988818, -43.37017594958040689, -20.77844580450608447 ) ) ;
#16784=CARTESIAN_POINT ( 'NONE',  ( 0.5809828226811617480, 46.40184912890855884, -11.86925843957117799 ) ) ;
#16786=CARTESIAN_POINT ( 'NONE',  ( 5.960221823109900008, -5.317678907195300120, -19.82478916873573027 ) ) ;
#16791=ORIENTED_EDGE ( 'NONE', *, *, #20670, .F. ) ;
#16792=CARTESIAN_POINT ( 'NONE',  ( 0.5807400328401637335, -41.75144119563869793, -23.47602859900758432 ) ) ;
#16794=CARTESIAN_POINT ( 'NONE',  ( 0.7762783648524365088, -13.25585403815088270, -46.03397615175199320 ) ) ;
#16796=CARTESIAN_POINT ( 'NONE',  ( 5.958863334805807099, -17.77512673691326128, 10.26388325355056885 ) ) ;
#16804=CARTESIAN_POINT ( 'NONE',  ( 2.281448460670571610, -38.84544723616124884, -28.15071835136437883 ) ) ;
#16807=CARTESIAN_POINT ( 'NONE',  ( 4.967162193818130511, 0.000000000000000000, 0.000000000000000000 ) ) ;
#16813=CARTESIAN_POINT ( 'NONE',  ( 0.5834872094924171693, -47.51530820063771188, 6.026535573893953668 ) ) ;
#16815=ORIENTED_EDGE ( 'NONE', *, *, #57315, .F. ) ;
#16817=VERTEX_POINT ( 'NONE', #38050 ) ;
#16821=CARTESIAN_POINT ( 'NONE',  ( 5.960721111146673579, 7.860635756377893912, -18.96073515164540879 ) ) ;
#16826=CARTESIAN_POINT ( 'NONE',  ( 4.960156602257182357, 45.62767441207063968, -8.553784487772425393 ) ) ;
#16829=CARTESIAN_POINT ( 'NONE',  ( 2.526552050251864134, -29.52128340070579426, -31.23611603144895099 ) ) ;
#16833=CARTESIAN_POINT ( 'NONE',  ( 0.5850706913938534814, -0.1816364388696994903, -47.89601588673689037 ) ) ;
#16837=CARTESIAN_POINT ( 'NONE',  ( 0.9722240741986378776, 42.61332881199394507, -5.023189681690327646 ) ) ;
#16839=EDGE_CURVE ( 'NONE', #56316, #56726, #19846, .T. ) ;
#16847=ORIENTED_EDGE ( 'NONE', *, *, #44258, .T. ) ;
#16853=EDGE_CURVE ( 'NONE', #19785, #40624, #26008, .T. ) ;
#16858=CARTESIAN_POINT ( 'NONE',  ( 5.959547316686252039, -14.51632612601538952, 14.51128755440516116 ) ) ;
#16864=CARTESIAN_POINT ( 'NONE',  ( 3.407937589446174087, 12.08659953757617878, -6.447869442558038067 ) ) ;
#16872=CARTESIAN_POINT ( 'NONE',  ( 5.959828726073459926, -7.850628836606978744, 18.96492317065680666 ) ) ;
#16876=CARTESIAN_POINT ( 'NONE',  ( 0.7762783648524376190, -47.37038525648364384, 7.133808749409267236 ) ) ;
#16879=CARTESIAN_POINT ( 'NONE',  ( 5.860006189529246790, -9.426589201135824325, 47.30296539008822521 ) ) ;
#16880=SHAPE_REPRESENTATION ( 'straight bevel gear(static)_iso_ISO - Straight bevel gear 2M 48GT 49PT 20PA 5FW ---48O25H100MD16.0N', ( #14677 ), #24677 ) ;
#16882=FACE_OUTER_BOUND ( 'NONE', #7643, .T. ) ;
#16884=CARTESIAN_POINT ( 'NONE',  ( 5.959547316686252039, 7.858107265727752200, -18.96183906913535466 ) ) ;
#16886=CARTESIAN_POINT ( 'NONE',  ( 2.624215991343620935, -19.66774719432946483, -43.79392271049091079 ) ) ;
#16888=CARTESIAN_POINT ( 'NONE',  ( 3.783278058412224087, -35.16831859152115669, -24.80906179324477279 ) ) ;
#16891=CARTESIAN_POINT ( 'NONE',  ( 1.227938101723748288, 29.74462687941226235, 30.94118573761323177 ) ) ;
#16892=CARTESIAN_POINT ( 'NONE',  ( 4.956653778116966613, 0.000000000000000000, 0.000000000000000000 ) ) ;
#16894=EDGE_CURVE ( 'NONE', #23349, #5776, #1345, .T. ) ;
#16900=CARTESIAN_POINT ( 'NONE',  ( 0.9747592971366254577, 39.51726118357611739, -16.71904224817861362 ) ) ;
#16903=CARTESIAN_POINT ( 'NONE',  ( 0.7762783648524385072, 17.50713302551388395, -44.59086139387524383 ) ) ;
#16908=CARTESIAN_POINT ( 'NONE',  ( 1.088313998177383501, 41.24258460930637682, 11.85828975620022696 ) ) ;
#16910=CIRCLE ( 'NONE', #14903, 48.09070567114147110 ) ;
#16916=CARTESIAN_POINT ( 'NONE',  ( 5.960721111146673579, 14.50930005615016682, -14.51823969584084573 ) ) ;
#16922=CARTESIAN_POINT ( 'NONE',  ( 0.5809828226811617480, -37.66417181417530458, -29.58751527316218954 ) ) ;
#16930=CARTESIAN_POINT ( 'NONE',  ( 1.227938101723748288, -11.92353943227977986, 41.23019537246705823 ) ) ;
#16932=ORIENTED_EDGE ( 'NONE', *, *, #40798, .T. ) ;
#16937=EDGE_LOOP ( 'NONE', ( #2481, #43040, #23045, #37926 ) ) ;
#16950=EDGE_CURVE ( 'NONE', #9174, #15318, #49190, .T. ) ;
#16953=FACE_OUTER_BOUND ( 'NONE', #54800, .T. ) ;
#16956=( BOUNDED_SURFACE ( )  B_SPLINE_SURFACE ( 3, 1, ( 
 ( #24496, #5367 ),
 ( #43636, #678 ),
 ( #10411, #19820 ),
 ( #57992, #53298 ) ),
 .UNSPECIFIED., .F., .F., .F. ) 
 B_SPLINE_SURFACE_WITH_KNOTS ( ( 4, 4 ),
 ( 2, 2 ),
 ( 0.000000000000000000, 1.000000000000000000 ),
 ( 0.000000000000000000, 1.000000000000000000 ),
 .UNSPECIFIED. ) 
 GEOMETRIC_REPRESENTATION_ITEM ( )  RATIONAL_B_SPLINE_SURFACE ( (
 ( 1.000000000000000000, 1.000000000000000000),
 ( 0.9953390228620291325, 0.8624445117760984880),
 ( 0.9953390228620291325, 0.8624445117760984880),
 ( 1.000000000000000000, 1.000000000000000000) ) ) 
 REPRESENTATION_ITEM ( '' )  SURFACE ( )  );
#16959=CARTESIAN_POINT ( 'NONE',  ( 0.9736507210033060744, 21.84312502845843085, -36.93248879681188868 ) ) ;
#16961=CARTESIAN_POINT ( 'NONE',  ( 5.965394784446460541, -16.29267539192351322, 12.48356622107649194 ) ) ;
#16964=CARTESIAN_POINT ( 'NONE',  ( 5.958863334805807099, -5.311251202228990387, 19.82657410201433734 ) ) ;
#16970=CARTESIAN_POINT ( 'NONE',  ( 5.965394784446460541, -7.868087674481078153, 18.95742317323932014 ) ) ;
#16978=ADVANCED_FACE ( 'NONE', ( #43982 ), #6285, .F. ) ;
#16983=CARTESIAN_POINT ( 'NONE',  ( 0.6067375320500740798, -41.12099578548233580, -24.55990317723900418 ) ) ;
#16988=CARTESIAN_POINT ( 'NONE',  ( 0.9745511491811739146, -5.938142320543633446, 42.49552597049456892 ) ) ;
#16993=CARTESIAN_POINT ( 'NONE',  ( 0.9736507210033069626, 16.00326134587917437, 39.81239086052219278 ) ) ;
#17001=VERTEX_POINT ( 'NONE', #48955 ) ;
#17003=CARTESIAN_POINT ( 'NONE',  ( 0.5838002273316423851, 44.19779719735699786, 18.45474575185529886 ) ) ;
#17007=DIRECTION ( 'NONE',  ( 0.000000000000000000, 0.000000000000000000, 1.000000000000000000 ) ) ;
#17013=ORIENTED_EDGE ( 'NONE', *, *, #10328, .T. ) ;
#17014=ORIENTED_EDGE ( 'NONE', *, *, #13193, .T. ) ;
#17017=CARTESIAN_POINT ( 'NONE',  ( 0.9745511491811755800, -16.73445648040599210, 39.51062171155255953 ) ) ;
#17020=B_SPLINE_CURVE_WITH_KNOTS ( 'NONE', 3,
 ( #53487, #39749, #10293, #48493 ),
 .UNSPECIFIED., .F., .F.,
 ( 4, 4 ),
 ( 0.000000000000000000, 0.004446090762761359914 ),
 .UNSPECIFIED. ) ;
#17022=B_SPLINE_CURVE_WITH_KNOTS ( 'NONE', 3,
 ( #14424, #24419, #38861, #19132, #20052, #57915 ),
 .UNSPECIFIED., .F., .F.,
 ( 4, 2, 4 ),
 ( 1.523470724839017254E-16, 0.0002445252820015216292, 0.0004890505640028909281 ),
 .UNSPECIFIED. ) ;
#17029=B_SPLINE_CURVE_WITH_KNOTS ( 'NONE', 3,
 ( #18305, #51170, #8255, #13603 ),
 .UNSPECIFIED., .F., .F.,
 ( 4, 4 ),
 ( 1.409462824231155764E-18, 0.004444878191957670442 ),
 .UNSPECIFIED. ) ;
#17033=DIRECTION ( 'NONE',  ( 0.000000000000000000, 0.000000000000000000, 1.000000000000000000 ) ) ;
#17051=VERTEX_POINT ( 'NONE', #36116 ) ;
#17052=CARTESIAN_POINT ( 'NONE',  ( 0.5832366564991502411, 47.89515933308369000, -0.2724446024279091327 ) ) ;
#17056=ORIENTED_EDGE ( 'NONE', *, *, #36675, .T. ) ;
#17066=ORIENTED_EDGE ( 'NONE', *, *, #5964, .T. ) ;
#17069=DIRECTION ( 'NONE',  ( -1.000000000000000000, -0.000000000000000000, -0.000000000000000000 ) ) ;
#17083=CARTESIAN_POINT ( 'NONE',  ( 0.9722240741986374335, 36.86535088273205929, 21.95618662952198719 ) ) ;
#17086=CARTESIAN_POINT ( 'NONE',  ( 5.960721111146673579, 10.25731071096558011, 17.77882586010670707 ) ) ;
#17090=CARTESIAN_POINT ( 'NONE',  ( 0.8551540677456715978, 46.03951182599445957, -13.28067116677154225 ) ) ;
#17097=CARTESIAN_POINT ( 'NONE',  ( 4.956653778116987041, -47.27023054223747067, -8.845409907521421644 ) ) ;
#17102=CARTESIAN_POINT ( 'NONE',  ( 1.227938101723756947, -37.58536632582764980, -20.72293514920789903 ) ) ;
#17104=PRODUCT_CONTEXT ( 'NONE', #38386, 'mechanical' ) ;
#17108=ADVANCED_FACE ( 'NONE', ( #9421 ), #19154, .F. ) ;
#17114=CARTESIAN_POINT ( 'NONE',  ( 4.967162193818130511, 0.000000000000000000, 0.000000000000000000 ) ) ;
#17122=ORIENTED_EDGE ( 'NONE', *, *, #40172, .T. ) ;
#17125=ADVANCED_FACE ( 'NONE', ( #37653 ), #51134, .F. ) ;
#17143=CARTESIAN_POINT ( 'NONE',  ( 1.154321713695927842, 42.64911660416112227, -4.782433421669653129 ) ) ;
#17147=ORIENTED_EDGE ( 'NONE', *, *, #35691, .F. ) ;
#17148=EDGE_CURVE ( 'NONE', #2619, #46035, #40240, .T. ) ;
#17151=ORIENTED_EDGE ( 'NONE', *, *, #34529, .T. ) ;
#17154=CARTESIAN_POINT ( 'NONE',  ( 0.5786265663353153954, -0.7221568112303078379, -47.89572889566446889 ) ) ;
#17159=CARTESIAN_POINT ( 'NONE',  ( 0.8551540677456715978, 33.23105123575947317, -34.52115452272894913 ) ) ;
#17167=EDGE_CURVE ( 'NONE', #2188, #22415, #33455, .T. ) ;
#17169=FACE_OUTER_BOUND ( 'NONE', #11746, .T. ) ;
#17171=FACE_OUTER_BOUND ( 'NONE', #36432, .T. ) ;
#17173=ORIENTED_EDGE ( 'NONE', *, *, #34382, .T. ) ;
#17174=CARTESIAN_POINT ( 'NONE',  ( 0.9757787079277440156, -30.36877398309923137, 30.31292661677481348 ) ) ;
#17177=CARTESIAN_POINT ( 'NONE',  ( 5.959547316686252039, 2.675599016784261597, 20.35048796920737857 ) ) ;
#17181=CARTESIAN_POINT ( 'NONE',  ( 5.974727161628369032, 5.327229920347426706, -19.82156119440440278 ) ) ;
#17184=CARTESIAN_POINT ( 'NONE',  ( 0.5807400328401574052, -17.82553128098440354, 44.45848844984437420 ) ) ;
#17191=CARTESIAN_POINT ( 'NONE',  ( 0.5786265663353196143, -24.57327059187427309, 41.11783955080230868 ) ) ;
#17198=CARTESIAN_POINT ( 'NONE',  ( 2.624215991343620935, -47.39206852872462861, 7.662883702704499811 ) ) ;
#17203=CARTESIAN_POINT ( 'NONE',  ( 5.960721111146673579, 14.50930005615016682, -14.51823969584084573 ) ) ;
#17205=ORIENTED_EDGE ( 'NONE', *, *, #43914, .F. ) ;
#17210=CARTESIAN_POINT ( 'NONE',  ( 0.5837374860065632776, -0.1816420316512093458, -47.89569815517036488 ) ) ;
#17212=ORIENTED_EDGE ( 'NONE', *, *, #52828, .F. ) ;
#17213=CARTESIAN_POINT ( 'NONE',  ( 0.5786265663353153954, 28.58414684753542900, -38.43785771743173996 ) ) ;
#17223=ORIENTED_EDGE ( 'NONE', *, *, #21014, .T. ) ;
#17229=CARTESIAN_POINT ( 'NONE',  ( 0.9730545539215892381, -16.88610103448586131, 39.44597740938055352 ) ) ;
#17231=CARTESIAN_POINT ( 'NONE',  ( 0.9745511491811755800, 10.77620558745937096, 41.53317535253976445 ) ) ;
#17234=B_SPLINE_CURVE_WITH_KNOTS ( 'NONE', 3,
 ( #54766, #7143, #16900, #36015, #55080, #15969, #39370, #48435, #33743, #5496, #34352, #10853, #1415, #6407, #29025, #24635, #10535, #5191, #29627 ),
 .UNSPECIFIED., .F., .F.,
 ( 4, 3, 3, 3, 3, 3, 4 ),
 ( 9.813676791237319219E-18, 0.0002724573126191672987, 0.0004086839781548454414, 0.0005449106435901818115, 0.0006811373090491508074, 0.0008459866663933726270, 0.001010840725717207728 ),
 .UNSPECIFIED. ) ;
#17242=ORIENTED_EDGE ( 'NONE', *, *, #17889, .T. ) ;
#17246=CARTESIAN_POINT ( 'NONE',  ( 1.227938101723756947, -41.23019537246717903, 11.92353943227934998 ) ) ;
#17249=LINE ( 'NONE', #55741, #18833 ) ;
#17253=DIRECTION ( 'NONE',  ( -0.07836865515943411409, 0.9893941468723557175, 0.1223011693452884796 ) ) ;
#17259=CARTESIAN_POINT ( 'NONE',  ( 4.956653778116988818, -45.71126949320240840, -14.93973939759935021 ) ) ;
#17261=CARTESIAN_POINT ( 'NONE',  ( 0.5834872094924171693, 6.476680342367262533, -47.45604551759230105 ) ) ;
#17270=EDGE_CURVE ( 'NONE', #31508, #29077, #52057, .T. ) ;
#17288=CARTESIAN_POINT ( 'NONE',  ( 0.9741495583595162211, -5.992561317325463044, 42.48790363482602572 ) ) ;
#17303=VERTEX_POINT ( 'NONE', #16930 ) ;
#17306=CARTESIAN_POINT ( 'NONE',  ( 0.9730545539215883499, 26.52009130076770305, 33.73144377768567637 ) ) ;
#17310=CARTESIAN_POINT ( 'NONE',  ( 5.959547316686252039, 2.675599016784533823, -20.35048796920733949 ) ) ;
#17312=CARTESIAN_POINT ( 'NONE',  ( 5.981074661064941900, 14.51919955600715539, 14.50705827991451002 ) ) ;
#17321=CARTESIAN_POINT ( 'NONE',  ( 4.956653778116975495, 9.917440902361160937, 47.05699031914952712 ) ) ;
#17333=ADVANCED_FACE ( 'NONE', ( #12537 ), #61195, .F. ) ;
#17338=ORIENTED_EDGE ( 'NONE', *, *, #33178, .F. ) ;
#17341=DIRECTION ( 'NONE',  ( -1.000000000000000000, -0.000000000000000000, -0.000000000000000000 ) ) ;
#17342=CARTESIAN_POINT ( 'NONE',  ( 4.960156602257184133, -46.35381625054454702, -2.524999074838052859 ) ) ;
#17349=B_SPLINE_CURVE_WITH_KNOTS ( 'NONE', 3,
 ( #37621, #12890, #56685, #3444, #27275, #18192 ),
 .UNSPECIFIED., .F., .F.,
 ( 4, 2, 4 ),
 ( 6.149443329761889321E-18, 0.0002445244328975371855, 0.0004890488657950682995 ),
 .UNSPECIFIED. ) ;
#17355=CARTESIAN_POINT ( 'NONE',  ( 2.281448460670570277, -34.83871297539680967, -32.98023336626270208 ) ) ;
#17372=CARTESIAN_POINT ( 'NONE',  ( 0.7056555295713273779, -17.55111680842069788, 44.57023068418421730 ) ) ;
#17376=CARTESIAN_POINT ( 'NONE',  ( 4.956653778116991482, 8.845409907521601056, -47.27023054223744225 ) ) ;
#17381=DIRECTION ( 'NONE',  ( -0.07836865515943411409, -0.9873352307081181278, 0.1379401902675529146 ) ) ;
#17396=CARTESIAN_POINT ( 'NONE',  ( 3.270143674763207553, 11.98875605389988941, -6.605065939546689080 ) ) ;
#17398=CARTESIAN_POINT ( 'NONE',  ( 0.5800708119828336118, -0.6275298934111632754, -47.89175345941821860 ) ) ;
#17413=DIRECTION ( 'NONE',  ( -0.07439287786467649322, 0.9262902123089771234, 0.3693942911085679737 ) ) ;
#17428=CARTESIAN_POINT ( 'NONE',  ( 1.227938101723748288, 42.91134962331487657, 0.8460948827226649760 ) ) ;
#17434=ORIENTED_EDGE ( 'NONE', *, *, #50075, .F. ) ;
#17443=ORIENTED_EDGE ( 'NONE', *, *, #31687, .T. ) ;
#17455=ORIENTED_EDGE ( 'NONE', *, *, #45923, .T. ) ;
#17461=ADVANCED_FACE ( 'NONE', ( #14694 ), #5247, .T. ) ;
#17466=CIRCLE ( 'NONE', #50496, 43.08621763946400307 ) ;
#17470=EDGE_CURVE ( 'NONE', #17001, #6542, #7223, .T. ) ;
#17471=CARTESIAN_POINT ( 'NONE',  ( 0.8557997880470599172, -23.15977007032294210, -41.93815086860281127 ) ) ;
#17473=ORIENTED_EDGE ( 'NONE', *, *, #18327, .T. ) ;
#17474=CARTESIAN_POINT ( 'NONE',  ( 0.9749527285493312379, -30.54214995146794465, 30.13822974582802061 ) ) ;
#17478=CARTESIAN_POINT ( 'NONE',  ( 5.974727161628369032, -12.50710176110020200, 16.27409205901354383 ) ) ;
#17492=EDGE_CURVE ( 'NONE', #47692, #25196, #457, .T. ) ;
#17496=CARTESIAN_POINT ( 'NONE',  ( 0.5809828226811617480, 37.66417181417551774, 29.58751527316192664 ) ) ;
#17508=DIRECTION ( 'NONE',  ( -0.07836865515943411409, -0.9968932487286223942, 0.007886984708653930337 ) ) ;
#17514=B_SPLINE_CURVE_WITH_KNOTS ( 'NONE', 3,
 ( #52589, #9682, #45388, #16246 ),
 .UNSPECIFIED., .F., .F.,
 ( 4, 4 ),
 ( 8.777083671441753062E-17, 0.005004741218457508210 ),
 .UNSPECIFIED. ) ;
#17519=CARTESIAN_POINT ( 'NONE',  ( 4.967162193818130511, -36.06913038482782952, -23.56777426397217567 ) ) ;
#17523=CARTESIAN_POINT ( 'NONE',  ( 0.5819845901640492425, -37.72030663501136871, -29.51612926147656069 ) ) ;
#17533=VERTEX_POINT ( 'NONE', #34723 ) ;
#17540=EDGE_CURVE ( 'NONE', #45338, #58089, #22899, .T. ) ;
#17548=EDGE_CURVE ( 'NONE', #33299, #38729, #18461, .T. ) ;
#17558=CARTESIAN_POINT ( 'NONE',  ( 0.8557997880470697982, 13.27832040216639520, 46.03118133706031045 ) ) ;
#17561=VERTEX_POINT ( 'NONE', #30611 ) ;
#17565=CARTESIAN_POINT ( 'NONE',  ( 0.5807400328401637335, 6.791881299636274072, -47.41494605191435596 ) ) ;
#17567=CARTESIAN_POINT ( 'NONE',  ( 0.9730545539215883499, 37.40983423658502716, -21.01499094264509893 ) ) ;
#17579=VERTEX_POINT ( 'NONE', #38820 ) ;
#17581=VECTOR ( 'NONE', #5943, 1000.000000000000114 ) ;
#17586=EDGE_CURVE ( 'NONE', #28808, #50125, #28106, .T. ) ;
#17589=ORIENTED_EDGE ( 'NONE', *, *, #29484, .F. ) ;
#17591=ORIENTED_EDGE ( 'NONE', *, *, #47014, .T. ) ;
#17599=( BOUNDED_SURFACE ( )  B_SPLINE_SURFACE ( 3, 1, ( 
 ( #22406, #45611 ),
 ( #36525, #55591 ),
 ( #3275, #7671 ),
 ( #21174, #26797 ) ),
 .UNSPECIFIED., .F., .F., .F. ) 
 B_SPLINE_SURFACE_WITH_KNOTS ( ( 4, 4 ),
 ( 2, 2 ),
 ( 0.000000000000000000, 1.000000000000000000 ),
 ( 0.000000000000000000, 1.000000000000000000 ),
 .UNSPECIFIED. ) 
 GEOMETRIC_REPRESENTATION_ITEM ( )  RATIONAL_B_SPLINE_SURFACE ( (
 ( 1.000000000000000000, 1.000000000000000000),
 ( 0.9953390228620291325, 0.8624445117761032620),
 ( 0.9953390228620291325, 0.8624445117761032620),
 ( 1.000000000000000000, 1.000000000000000000) ) ) 
 REPRESENTATION_ITEM ( '' )  SURFACE ( )  );
#17605=CARTESIAN_POINT ( 'NONE',  ( 0.8557997880470606944, 19.17299735372068525, -43.90420959842161608 ) ) ;
#17607=CARTESIAN_POINT ( 'NONE',  ( 0.5839879327111939800, 44.28486549479623591, 18.24507200299058951 ) ) ;
#17611=ORIENTED_EDGE ( 'NONE', *, *, #59120, .T. ) ;
#17637=DIRECTION ( 'NONE',  ( 0.000000000000000000, 0.000000000000000000, 1.000000000000000000 ) ) ;
#17640=CARTESIAN_POINT ( 'NONE',  ( 0.6846871229502899947, -23.20185915381586383, 41.91507847151790855 ) ) ;
#17643=CARTESIAN_POINT ( 'NONE',  ( 0.9749527285493317930, 39.53206838353044361, 16.68386601451053508 ) ) ;
#17648=DIRECTION ( 'NONE',  ( -1.000000000000000000, -0.000000000000000000, -0.000000000000000000 ) ) ;
#17658=CIRCLE ( 'NONE', #52652, 48.09070567114147110 ) ;
#17659=CARTESIAN_POINT ( 'NONE',  ( 5.958863334805807099, -18.96369761673814835, -7.853699934219834589 ) ) ;
#17660=CONICAL_SURFACE ( 'NONE', #56635, 43.08621763946400307, 1.568696531533066763 ) ;
#17663=ORIENTED_EDGE ( 'NONE', *, *, #54318, .T. ) ;
#17666=( BOUNDED_SURFACE ( )  B_SPLINE_SURFACE ( 3, 1, ( 
 ( #41914, #37209 ),
 ( #60981, #26553 ),
 ( #18090, #30949 ),
 ( #7111, #36282 ) ),
 .UNSPECIFIED., .F., .F., .F. ) 
 B_SPLINE_SURFACE_WITH_KNOTS ( ( 4, 4 ),
 ( 2, 2 ),
 ( 0.000000000000000000, 1.000000000000000000 ),
 ( 0.000000000000000000, 1.000000000000000000 ),
 .UNSPECIFIED. ) 
 GEOMETRIC_REPRESENTATION_ITEM ( )  RATIONAL_B_SPLINE_SURFACE ( (
 ( 1.000000000000000000, 1.000000000000000000),
 ( 0.9732289882329797637, 0.9999525324661233672),
 ( 0.9732289882329797637, 0.9999525324661233672),
 ( 1.000000000000000000, 1.000000000000000000) ) ) 
 REPRESENTATION_ITEM ( '' )  SURFACE ( )  );
#17673=CARTESIAN_POINT ( 'NONE',  ( 4.967162193818130511, -42.16965968614187688, -8.839793687085657936 ) ) ;
#17684=EDGE_CURVE ( 'NONE', #21167, #59165, #57256, .T. ) ;
#17690=CARTESIAN_POINT ( 'NONE',  ( 4.967162193818130511, 14.26841313271336809, -40.65506779172149976 ) ) ;
#17697=CARTESIAN_POINT ( 'NONE',  ( 0.7057020205115017708, -0.8412108057956128038, 47.89404687311021291 ) ) ;
#17701=CARTESIAN_POINT ( 'NONE',  ( 0.9752570700956793015, -5.371905812151864801, -42.57087745267996581 ) ) ;
#17705=DIRECTION ( 'NONE',  ( 0.000000000000000000, 0.000000000000000000, 1.000000000000000000 ) ) ;
#17709=CARTESIAN_POINT ( 'NONE',  ( 0.8551540677456715978, -41.94570365541186874, -23.16399837394590122 ) ) ;
#17719=CARTESIAN_POINT ( 'NONE',  ( 0.5809828226811553087, 12.92184523170202937, 46.11980934799343856 ) ) ;
#17729=CARTESIAN_POINT ( 'NONE',  ( 0.5807400328401574052, -12.92266817605982432, -46.12278621143511259 ) ) ;
#17734=EDGE_CURVE ( 'NONE', #30064, #57079, #35682, .T. ) ;
#17735=CARTESIAN_POINT ( 'NONE',  ( 0.9736507210033049642, 41.32746151989300643, 11.54000710819829045 ) ) ;
#17738=DIRECTION ( 'NONE',  ( -0.07439287786467652097, -0.3937848822959301165, -0.9161872986448742484 ) ) ;
#17745=CARTESIAN_POINT ( 'NONE',  ( 0.8557997880470606944, -34.51495345639572321, 33.22501220301889191 ) ) ;
#17746=CARTESIAN_POINT ( 'NONE',  ( 0.6846871229502932144, -47.37786444808388353, -7.109010606687882650 ) ) ;
#17753=CARTESIAN_POINT ( 'NONE',  ( 1.227938101723748288, -17.20315230597871903, 39.32113113558960293 ) ) ;
#17756=CARTESIAN_POINT ( 'NONE',  ( 4.303969348037246512, 20.38638383586178904, -43.57722561725938704 ) ) ;
#17775=B_SPLINE_CURVE_WITH_KNOTS ( 'NONE', 3,
 ( #26966, #45472, #55450, #16030 ),
 .UNSPECIFIED., .F., .F.,
 ( 4, 4 ),
 ( 0.000000000000000000, 0.004446090762761376394 ),
 .UNSPECIFIED. ) ;
#17778=CARTESIAN_POINT ( 'NONE',  ( 0.7762777257811890319, -7.133808567472593509, 47.37038525518532595 ) ) ;
#17780=CARTESIAN_POINT ( 'NONE',  ( 0.5800708119828326126, 23.40241990038095921, -41.78924007434301302 ) ) ;
#17786=CARTESIAN_POINT ( 'NONE',  ( 0.6846871229502899947, 17.53234844287802474, -44.58493949243987942 ) ) ;
#17790=CARTESIAN_POINT ( 'NONE',  ( 1.088313998177382391, 41.64627086748865992, -10.35171213034648119 ) ) ;
#17793=FACE_OUTER_BOUND ( 'NONE', #12830, .T. ) ;
#17795=CARTESIAN_POINT ( 'NONE',  ( 2.624215991343620935, -11.05657803851078036, 46.71702075422648903 ) ) ;
#17800=CARTESIAN_POINT ( 'NONE',  ( 5.981074661064941900, 7.846517100474549977, 18.96560215432020158 ) ) ;
#17801=AXIS2_PLACEMENT_3D ( 'NONE', #43929, #29474, #45163 ) ;
#17802=CARTESIAN_POINT ( 'NONE',  ( 5.974727161628367256, -10.27590650342025214, -17.76736931401856623 ) ) ;
#17810=DIRECTION ( 'NONE',  ( 0.000000000000000000, 0.000000000000000000, 1.000000000000000000 ) ) ;
#17813=AXIS2_PLACEMENT_3D ( 'NONE', #14246, #33653, #61809 ) ;
#17815=VERTEX_POINT ( 'NONE', #18079 ) ;
#17817=CARTESIAN_POINT ( 'NONE',  ( 4.956653778116986153, -48.02038484091102077, 2.599733001514167086 ) ) ;
#17820=ORIENTED_EDGE ( 'NONE', *, *, #38482, .T. ) ;
#17829=CARTESIAN_POINT ( 'NONE',  ( 0.5832366564991499081, -28.94058080282808376, 38.16363840618244296 ) ) ;
#17830=ORIENTED_EDGE ( 'NONE', *, *, #28775, .F. ) ;
#17833=B_SPLINE_CURVE_WITH_KNOTS ( 'NONE', 3,
 ( #31492, #54973, #45609, #17102 ),
 .UNSPECIFIED., .F., .F.,
 ( 4, 4 ),
 ( 5.553824967135426632E-18, 0.004050076154993001616 ),
 .UNSPECIFIED. ) ;
#17834=ORIENTED_EDGE ( 'NONE', *, *, #23858, .T. ) ;
#17835=LINE ( 'NONE', #60717, #6708 ) ;
#17839=EDGE_CURVE ( 'NONE', #57673, #2634, #35552, .T. ) ;
#17843=VECTOR ( 'NONE', #22906, 1000.000000000000114 ) ;
#17844=DIRECTION ( 'NONE',  ( -1.000000000000000000, 0.000000000000000000, -0.000000000000000000 ) ) ;
#17853=ORIENTED_EDGE ( 'NONE', *, *, #4488, .T. ) ;
#17857=CARTESIAN_POINT ( 'NONE',  ( 0.9757892942422822236, 34.01031843153931078, -26.16173342773506150 ) ) ;
#17859=CARTESIAN_POINT ( 'NONE',  ( 0.5809828226811553087, -12.92184523170170607, -46.11980934799353093 ) ) ;
#17862=VECTOR ( 'NONE', #29866, 1000.000000000000114 ) ;
#17864=CARTESIAN_POINT ( 'NONE',  ( 0.7057020205115032141, 34.46103118762836459, -33.27137945725683466 ) ) ;
#17877=CARTESIAN_POINT ( 'NONE',  ( 5.960721111146673579, -2.672857320903454514, 20.35079619394241135 ) ) ;
#17878=CARTESIAN_POINT ( 'NONE',  ( 0.5850706913938534814, 29.01314519953853477, -38.10903744847111341 ) ) ;
#17880=CARTESIAN_POINT ( 'NONE',  ( 2.624215991343620935, 19.66774719432979524, 43.79392271049075447 ) ) ;
#17881=CARTESIAN_POINT ( 'NONE',  ( 0.5819845901640494645, 6.701564444318373504, -47.42480841519682144 ) ) ;
#17886=CARTESIAN_POINT ( 'NONE',  ( 0.5839879327111933138, -29.22928252017487338, -37.94312859586442244 ) ) ;
#17889=EDGE_CURVE ( 'NONE', #17815, #7813, #51944, .T. ) ;
#17894=CARTESIAN_POINT ( 'NONE',  ( 5.981074661064941900, -17.77058762078884868, 10.26976685693792390 ) ) ;
#17908=EDGE_CURVE ( 'NONE', #52379, #3804, #6309, .T. ) ;
#17917=CARTESIAN_POINT ( 'NONE',  ( 0.5839879882104920261, 1.006200712814167388E-05, 47.89596766822081264 ) ) ;
#17918=CARTESIAN_POINT ( 'NONE',  ( 0.9752132459055861124, 16.63533515462578904, 39.55248938404422887 ) ) ;
#17926=DIRECTION ( 'NONE',  ( 0.07439287786467665975, -0.3937848822959491568, 0.9161872986448660328 ) ) ;
#17929=EDGE_CURVE ( 'NONE', #27219, #28691, #4107, .T. ) ;
#17930=ORIENTED_EDGE ( 'NONE', *, *, #54468, .T. ) ;
#17935=CARTESIAN_POINT ( 'NONE',  ( 4.960156602257182357, -30.99165383632791659, 34.56254177294259478 ) ) ;
#17937=PLANE ( 'NONE',  #15436 ) ;
#17942=CARTESIAN_POINT ( 'NONE',  ( 3.660087539127327538, -14.24113226412018385, -45.87884541725762233 ) ) ;
#17944=EDGE_CURVE ( 'NONE', #50798, #8991, #30312, .T. ) ;
#17945=CARTESIAN_POINT ( 'NONE',  ( 0.7057020205114974409, -29.82342581815230886, 37.48480537461322371 ) ) ;
#17949=CARTESIAN_POINT ( 'NONE',  ( 0.9730545539215883499, 39.83279466599061891, -15.95224156741785393 ) ) ;
#17957=CARTESIAN_POINT ( 'NONE',  ( 0.5850706913938533704, 18.16120156791880902, 44.31965802246111963 ) ) ;
#17958=DIRECTION ( 'NONE',  ( -0.07439287786467652097, 0.8701500408883644511, 0.4871392060438053950 ) ) ;
#17959=FACE_OUTER_BOUND ( 'NONE', #45734, .T. ) ;
#17963=ORIENTED_EDGE ( 'NONE', *, *, #31839, .T. ) ;
#17967=CARTESIAN_POINT ( 'NONE',  ( 0.5800708057587378175, -34.30831467131380208, 33.42085258735466624 ) ) ;
#17987=ORIENTED_EDGE ( 'NONE', *, *, #59393, .F. ) ;
#17997=CARTESIAN_POINT ( 'NONE',  ( 1.154321485836933281, 20.73950273457894511, -37.57248783354748412 ) ) ;
#17999=CARTESIAN_POINT ( 'NONE',  ( 4.956653778116970166, 39.67974989265038488, 27.17045123668485829 ) ) ;
#18006=CARTESIAN_POINT ( 'NONE',  ( 0.8551540677456715978, -19.17641535420820986, -43.91216198251559888 ) ) ;
#18011=CARTESIAN_POINT ( 'NONE',  ( 4.967162193818130511, 42.96271701169388990, -3.259922920617310371 ) ) ;
#18013=CARTESIAN_POINT ( 'NONE',  ( 4.967162193818130511, 0.000000000000000000, 0.000000000000000000 ) ) ;
#18015=CARTESIAN_POINT ( 'NONE',  ( 0.8551540677456834771, 34.52115452272929019, 33.23105123575912501 ) ) ;
#18018=CARTESIAN_POINT ( 'NONE',  ( 5.958863334805807099, 12.49619391867182294, -16.28335246510355105 ) ) ;
#18021=CARTESIAN_POINT ( 'NONE',  ( 3.660087539127323986, -36.93668088065471267, 30.71416465583044442 ) ) ;
#18025=CARTESIAN_POINT ( 'NONE',  ( -16.15200392031422538, -12.45603944020924381, -1.053615289124667287 ) ) ;
#18026=CARTESIAN_POINT ( 'NONE',  ( 4.956653778116966613, 0.000000000000000000, 0.000000000000000000 ) ) ;
#18029=CARTESIAN_POINT ( 'NONE',  ( 4.967162193818130511, 0.000000000000000000, 0.000000000000000000 ) ) ;
#18030=B_SPLINE_CURVE_WITH_KNOTS ( 'NONE', 3,
 ( #53463, #33468, #19990, #9328, #38480, #57854 ),
 .UNSPECIFIED., .F., .F.,
 ( 4, 2, 4 ),
 ( 7.757919228897728493E-18, 0.0002291978881530148861, 0.0004583957763060220202 ),
 .UNSPECIFIED. ) ;
#18031=CARTESIAN_POINT ( 'NONE',  ( 0.6846871229502932144, 0.8641397935266237340, -47.90045233486063125 ) ) ;
#18033=DIRECTION ( 'NONE',  ( -1.000000000000000000, -0.000000000000000000, -0.000000000000000000 ) ) ;
#18042=CARTESIAN_POINT ( 'NONE',  ( 3.660176727303398270, 43.62748706623523276, 20.10773453922302423 ) ) ;
#18055=ADVANCED_FACE ( 'NONE', ( #42664 ), #32765, .T. ) ;
#18059=ORIENTED_EDGE ( 'NONE', *, *, #31551, .T. ) ;
#18061=B_SPLINE_CURVE_WITH_KNOTS ( 'NONE', 3,
 ( #16891, #59783, #50990, #26891 ),
 .UNSPECIFIED., .F., .F.,
 ( 4, 4 ),
 ( 8.673617379884035472E-19, 0.004048833967417087357 ),
 .UNSPECIFIED. ) ;
#18062=VERTEX_POINT ( 'NONE', #29468 ) ;
#18066=DIRECTION ( 'NONE',  ( 0.000000000000000000, 0.000000000000000000, 1.000000000000000000 ) ) ;
#18069=VERTEX_POINT ( 'NONE', #9131 ) ;
#18070=CARTESIAN_POINT ( 'NONE',  ( 5.959547316686252039, 7.858107265727752200, -18.96183906913535466 ) ) ;
#18079=CARTESIAN_POINT ( 'NONE',  ( 1.227938101723748288, -37.58536632582793402, 20.72293514920737323 ) ) ;
#18085=CARTESIAN_POINT ( 'NONE',  ( 0.5834872094924169472, -18.11905305011485368, -44.33648115256919198 ) ) ;
#18086=CARTESIAN_POINT ( 'NONE',  ( 4.967162193818130511, 42.96271701169385437, 3.259922920617894793 ) ) ;
#18087=CARTESIAN_POINT ( 'NONE',  ( 4.960156602257180580, 14.43621227656587536, -44.12083041402437544 ) ) ;
#18090=CARTESIAN_POINT ( 'NONE',  ( 5.958863334805807099, -19.82594244347356494, 5.313608583996176193 ) ) ;
#18093=CARTESIAN_POINT ( 'NONE',  ( 4.956653778116974607, -32.11725092155068495, 35.79382859084104496 ) ) ;
#18095=FACE_OUTER_BOUND ( 'NONE', #27168, .T. ) ;
#18097=CARTESIAN_POINT ( 'NONE',  ( 0.7056555295713324849, 19.10539864320401549, 43.92642606846683861 ) ) ;
#18101=CARTESIAN_POINT ( 'NONE',  ( 0.5827357941260208340, -47.89462047563812064, 0.3632531319012696214 ) ) ;
#18107=ORIENTED_EDGE ( 'NONE', *, *, #46382, .T. ) ;
#18109=CARTESIAN_POINT ( 'NONE',  ( 0.8557997880470690211, 0.9121262075946178216, 47.89938907511594124 ) ) ;
#18117=CARTESIAN_POINT ( 'NONE',  ( 0.9754642270333695464, 11.27515941577631686, -41.40054989430066001 ) ) ;
#18130=DIRECTION ( 'NONE',  ( -1.000000000000000000, -0.000000000000000000, -0.000000000000000000 ) ) ;
#18131=VERTEX_POINT ( 'NONE', #54183 ) ;
#18135=ORIENTED_EDGE ( 'NONE', *, *, #54076, .F. ) ;
#18137=DIRECTION ( 'NONE',  ( -1.000000000000000000, -0.000000000000000000, -0.000000000000000000 ) ) ;
#18151=CARTESIAN_POINT ( 'NONE',  ( 0.9722240741986378776, -42.46141200043695108, -6.177112427866298994 ) ) ;
#18152=CARTESIAN_POINT ( 'NONE',  ( 0.8557997880470697982, 46.50333260518559086, 11.51622788066474534 ) ) ;
#18153=CARTESIAN_POINT ( 'NONE',  ( 0.5839254288179547281, 29.08514953649819290, 38.05364096126326956 ) ) ;
#18155=CARTESIAN_POINT ( 'NONE',  ( 0.6846871229502932144, -37.47592888575227477, -29.84551600520671855 ) ) ;
#18160=VERTEX_POINT ( 'NONE', #34812 ) ;
#18170=ORIENTED_EDGE ( 'NONE', *, *, #58271, .T. ) ;
#18184=CARTESIAN_POINT ( 'NONE',  ( 5.958863334805807099, -7.853699934220021106, 18.96369761673806664 ) ) ;
#18185=CARTESIAN_POINT ( 'NONE',  ( 0.5839254288179547281, 6.341681103465229619, -47.47429404163003142 ) ) ;
#18190=ORIENTED_EDGE ( 'NONE', *, *, #29628, .F. ) ;
#18192=CARTESIAN_POINT ( 'NONE',  ( 0.8557997880470690211, 47.89938907511594124, -0.9121262075947851322 ) ) ;
#18193=CARTESIAN_POINT ( 'NONE',  ( 0.5819845079324649229, 46.37938935563231269, 11.95724301473523710 ) ) ;
#18203=CIRCLE ( 'NONE', #52213, 48.09070567114147110 ) ;
#18215=CARTESIAN_POINT ( 'NONE',  ( 5.959828726073459926, 20.52560994243598813, 0.004526594003449061453 ) ) ;
#18218=ORIENTED_EDGE ( 'NONE', *, *, #24526, .T. ) ;
#18221=CARTESIAN_POINT ( 'NONE',  ( 2.526552050251864134, 15.32056541070842748, 40.15571433620791453 ) ) ;
#18224=( BOUNDED_SURFACE ( )  B_SPLINE_SURFACE ( 3, 1, ( 
 ( #53947, #15151 ),
 ( #1321, #54556 ),
 ( #58641, #16077 ),
 ( #11686, #39277 ) ),
 .UNSPECIFIED., .F., .F., .F. ) 
 B_SPLINE_SURFACE_WITH_KNOTS ( ( 4, 4 ),
 ( 2, 2 ),
 ( 0.000000000000000000, 1.000000000000000000 ),
 ( 0.000000000000000000, 1.000000000000000000 ),
 .UNSPECIFIED. ) 
 GEOMETRIC_REPRESENTATION_ITEM ( )  RATIONAL_B_SPLINE_SURFACE ( (
 ( 1.000000000000000000, 1.000000000000000000),
 ( 0.9953390228620291325, 0.8624445117760984880),
 ( 0.9953390228620291325, 0.8624445117760984880),
 ( 1.000000000000000000, 1.000000000000000000) ) ) 
 REPRESENTATION_ITEM ( '' )  SURFACE ( )  );
#18225=DIRECTION ( 'NONE',  ( 0.000000000000000000, 0.000000000000000000, 1.000000000000000000 ) ) ;
#18229=EDGE_LOOP ( 'NONE', ( #20084, #8323, #24370, #49611 ) ) ;
#18233=CARTESIAN_POINT ( 'NONE',  ( 4.967162193818130511, 23.56777426397178132, 36.06913038482807821 ) ) ;
#18239=CARTESIAN_POINT ( 'NONE',  ( 4.956653778116974607, -32.11725092155068495, 35.79382859084104496 ) ) ;
#18240=CARTESIAN_POINT ( 'NONE',  ( 0.7762783648524335112, 24.71864151483714167, 41.03453896757949337 ) ) ;
#18253=CARTESIAN_POINT ( 'NONE',  ( 1.088313998177379949, 39.93881167962123158, -15.69908095455111940 ) ) ;
#18257=CARTESIAN_POINT ( 'NONE',  ( 0.8551540677456715978, -46.03951182599436720, 13.28067116677186199 ) ) ;
#18258=CARTESIAN_POINT ( 'NONE',  ( 0.8551540677456715978, -11.51835730326447127, -46.51172240253133339 ) ) ;
#18259=CARTESIAN_POINT ( 'NONE',  ( 1.227938101723756947, 36.73927144310543014, -22.18841447410681411 ) ) ;
#18260=CARTESIAN_POINT ( 'NONE',  ( 4.967162193818130511, -23.56777426397153974, -36.06913038482822742 ) ) ;
#18261=CARTESIAN_POINT ( 'NONE',  ( 0.5850706913938534814, 18.49682194437964355, 44.18063951072227269 ) ) ;
#18262=B_SPLINE_CURVE_WITH_KNOTS ( 'NONE', 3,
 ( #3028, #55333, #1789, #12456 ),
 .UNSPECIFIED., .F., .F.,
 ( 4, 4 ),
 ( 2.168404344971008868E-19, 0.004048833967417083887 ),
 .UNSPECIFIED. ) ;
#18269=ORIENTED_EDGE ( 'NONE', *, *, #17470, .F. ) ;
#18285=B_SPLINE_CURVE_WITH_KNOTS ( 'NONE', 3,
 ( #14672, #19672, #23748, #53761, #10578, #33785 ),
 .UNSPECIFIED., .F., .F.,
 ( 4, 2, 4 ),
 ( 1.511413994009955268E-16, 0.0002445252820015196235, 0.0004890505640028881091 ),
 .UNSPECIFIED. ) ;
#18288=CARTESIAN_POINT ( 'NONE',  ( 0.5839879327111923146, -12.48412918464404875, -46.24044206955234415 ) ) ;
#18299=VERTEX_POINT ( 'NONE', #26945 ) ;
#18302=B_SPLINE_CURVE_WITH_KNOTS ( 'NONE', 3,
 ( #59284, #8437, #27563, #3427, #12872, #45233 ),
 .UNSPECIFIED., .F., .F.,
 ( 4, 2, 4 ),
 ( 1.056081928668503685E-17, 0.0002291978881530153469, 0.0004583957763060201229 ),
 .UNSPECIFIED. ) ;
#18303=ORIENTED_EDGE ( 'NONE', *, *, #3995, .T. ) ;
#18305=CARTESIAN_POINT ( 'NONE',  ( 0.8557997880470697982, 29.88293891557470516, 37.44587306708108088 ) ) ;
#18316=CARTESIAN_POINT ( 'NONE',  ( 0.9968887458511631605, -26.64009929991527059, 33.63815526548975043 ) ) ;
#18320=ORIENTED_EDGE ( 'NONE', *, *, #44937, .F. ) ;
#18321=CARTESIAN_POINT ( 'NONE',  ( 4.963659409799330291, 44.62477100936222030, -3.403493583736868278 ) ) ;
#18324=CARTESIAN_POINT ( 'NONE',  ( 5.959547316686252039, -10.26589671991350983, -17.77392908783930636 ) ) ;
#18325=PRODUCT_DEFINITION_SHAPE ( 'NONE', 'NONE',  #16454 ) ;
#18327=EDGE_CURVE ( 'NONE', #11505, #38319, #51160, .T. ) ;
#18329=CARTESIAN_POINT ( 'NONE',  ( 5.974727161628369032, 10.27590650342037293, -17.76736931401850228 ) ) ;
#18336=CARTESIAN_POINT ( 'NONE',  ( 5.958863334805807099, 10.26388325355063103, 17.77512673691322576 ) ) ;
#18342=CARTESIAN_POINT ( 'NONE',  ( 3.270143674763207553, -3.806843787666013945, 13.14781761974168006 ) ) ;
#18343=VECTOR ( 'NONE', #38714, 1000.000000000000114 ) ;
#18344=CARTESIAN_POINT ( 'NONE',  ( 0.8551540677456715978, 0.9122407826482503701, -47.90804413217340141 ) ) ;
#18345=LINE ( 'NONE', #56527, #59886 ) ;
#18347=( BOUNDED_SURFACE ( )  B_SPLINE_SURFACE ( 3, 1, ( 
 ( #22700, #60901 ),
 ( #26552, #40375 ),
 ( #46839, #31256 ),
 ( #8911, #18015 ) ),
 .UNSPECIFIED., .F., .F., .F. ) 
 B_SPLINE_SURFACE_WITH_KNOTS ( ( 4, 4 ),
 ( 2, 2 ),
 ( 0.000000000000000000, 1.000000000000000000 ),
 ( 0.000000000000000000, 1.000000000000000000 ),
 .UNSPECIFIED. ) 
 GEOMETRIC_REPRESENTATION_ITEM ( )  RATIONAL_B_SPLINE_SURFACE ( (
 ( 1.000000000000000000, 1.000000000000000000),
 ( 0.7269869731126817891, 0.9931720237060910339),
 ( 0.7269869731126817891, 0.9931720237060910339),
 ( 1.000000000000000000, 1.000000000000000000) ) ) 
 REPRESENTATION_ITEM ( '' )  SURFACE ( )  );
#18350=CARTESIAN_POINT ( 'NONE',  ( 1.154321713695927842, -6.418927679455929791, 42.43366804783613588 ) ) ;
#18352=VERTEX_POINT ( 'NONE', #33197 ) ;
#18356=ORIENTED_EDGE ( 'NONE', *, *, #36962, .F. ) ;
#18363=CARTESIAN_POINT ( 'NONE',  ( 0.9752132459055862235, 41.50604997043411970, 10.88033124649634686 ) ) ;
#18366=DIRECTION ( 'NONE',  ( -1.000000000000000000, -0.000000000000000000, -0.000000000000000000 ) ) ;
#18373=EDGE_LOOP ( 'NONE', ( #57095, #48313, #6237, #3454 ) ) ;
#18380=CARTESIAN_POINT ( 'NONE',  ( 0.9757954354143116849, 5.207268878499845415E-15, 42.90846090505964128 ) ) ;
#18384=FACE_OUTER_BOUND ( 'NONE', #56191, .T. ) ;
#18390=CARTESIAN_POINT ( 'NONE',  ( 0.5819845079324659221, -47.54334065046000291, -5.801222053075574259 ) ) ;
#18395=ORIENTED_EDGE ( 'NONE', *, *, #32993, .T. ) ;
#18399=CARTESIAN_POINT ( 'NONE',  ( 0.8557997880470697982, -11.51622788066490166, 46.50333260518556244 ) ) ;
#18402=ADVANCED_FACE ( 'NONE', ( #33506 ), #45674, .F. ) ;
#18410=CARTESIAN_POINT ( 'NONE',  ( 0.9747592971366236814, 5.279515277919996308, -42.58247319705097311 ) ) ;
#18421=CARTESIAN_POINT ( 'NONE',  ( 5.959547316686252039, 18.96183906913532269, 7.858107265727816149 ) ) ;
#18426=EDGE_LOOP ( 'NONE', ( #12286, #40116, #11, #45663 ) ) ;
#18427=CARTESIAN_POINT ( 'NONE',  ( 0.9730545539215883499, -29.98130006528840141, -30.69604515769682251 ) ) ;
#18432=CARTESIAN_POINT ( 'NONE',  ( 4.960156602257181468, -20.07163247083176572, 41.85906677498953599 ) ) ;
#18443=CARTESIAN_POINT ( 'NONE',  ( 4.967162193818130511, 0.000000000000000000, 0.000000000000000000 ) ) ;
#18453=ORIENTED_EDGE ( 'NONE', *, *, #29071, .T. ) ;
#18455=CARTESIAN_POINT ( 'NONE',  ( 5.960721111146673579, -18.96073515164554379, 7.860635756377555516 ) ) ;
#18456=CARTESIAN_POINT ( 'NONE',  ( 0.9757787079277447928, 34.01751575780821213, 26.15233402543277208 ) ) ;
#18461=B_SPLINE_CURVE_WITH_KNOTS ( 'NONE', 3,
 ( #6167, #29386, #11218, #20614 ),
 .UNSPECIFIED., .F., .F.,
 ( 4, 4 ),
 ( 8.673617379884035472E-19, 0.004048833967417084755 ),
 .UNSPECIFIED. ) ;
#18464=ORIENTED_EDGE ( 'NONE', *, *, #51799, .T. ) ;
#18489=EDGE_CURVE ( 'NONE', #7406, #22531, #34429, .T. ) ;
#18491=B_SPLINE_CURVE_WITH_KNOTS ( 'NONE', 3,
 ( #19805, #24170, #43621, #34209, #10397, #32983, #56750, #9147, #23873, #28872, #18883, #28255, #10085, #29180, #4417, #29488, #52056, #13875, #23557 ),
 .UNSPECIFIED., .F., .F.,
 ( 4, 3, 3, 3, 3, 3, 4 ),
 ( 0.000000000000000000, 0.0002724573126191776528, 0.0004086839781548526514, 0.0005449106435901898346, 0.0006811373090491660946, 0.0008459866663933752291, 0.001010840725717213149 ),
 .UNSPECIFIED. ) ;
#18492=CARTESIAN_POINT ( 'NONE',  ( 4.956653778116991482, -2.599733001514001440, -48.02038484091103498 ) ) ;
#18500=ORIENTED_EDGE ( 'NONE', *, *, #53581, .F. ) ;
#18504=PRESENTATION_STYLE_ASSIGNMENT (( #23201 ) ) ;
#18507=EDGE_CURVE ( 'NONE', #20977, #13708, #29704, .T. ) ;
#18509=AXIS2_PLACEMENT_3D ( 'NONE', #13227, #41747, #26693 ) ;
#18516=CARTESIAN_POINT ( 'NONE',  ( 0.5809828226811553087, -6.791453954330003207, -47.41188724015886180 ) ) ;
#18518=ORIENTED_EDGE ( 'NONE', *, *, #61136, .T. ) ;
#18519=CARTESIAN_POINT ( 'NONE',  ( 0.6846871229502899947, -47.90045233486065968, 0.8641397935257868479 ) ) ;
#18521=VERTEX_POINT ( 'NONE', #44765 ) ;
#18524=ORIENTED_EDGE ( 'NONE', *, *, #39217, .T. ) ;
#18527=CARTESIAN_POINT ( 'NONE',  ( 4.303969348037246512, -8.413118729224382975, 47.36875205922770249 ) ) ;
#18530=FACE_OUTER_BOUND ( 'NONE', #43991, .T. ) ;
#18534=CARTESIAN_POINT ( 'NONE',  ( 3.783198216974387851, 12.79806054635192147, -41.09147814699330326 ) ) ;
#18539=CARTESIAN_POINT ( 'NONE',  ( 0.5809828226811553087, 24.41822904836923058, 41.20389530892317254 ) ) ;
#18542=ORIENTED_EDGE ( 'NONE', *, *, #46403, .T. ) ;
#18547=CARTESIAN_POINT ( 'NONE',  ( 0.5819845901640494645, -44.07435474487832039, -18.74765780149875027 ) ) ;
#18550=CARTESIAN_POINT ( 'NONE',  ( 0.5809828226811617480, -29.58751527316205809, 37.66417181417541826 ) ) ;
#18553=CARTESIAN_POINT ( 'NONE',  ( 0.5819845901640494645, -46.37938751183692432, 11.95725023767341355 ) ) ;
#18554=LINE ( 'NONE', #24167, #37918 ) ;
#18559=AXIS2_PLACEMENT_3D ( 'NONE', #55189, #36742, #59581 ) ;
#18563=CARTESIAN_POINT ( 'NONE',  ( 4.956653778116982600, -47.27023054223759857, 8.845409907520762616 ) ) ;
#18566=B_SPLINE_CURVE_WITH_KNOTS ( 'NONE', 3,
 ( #5292, #29425, #47935, #15044, #25043, #44187, #34150, #57290, #38241, #1217, #15661, #39473, #20352, #43248, #34763, #33533 ),
 .UNSPECIFIED., .F., .F.,
 ( 4, 3, 3, 3, 3, 4 ),
 ( 1.250973872328959318E-17, 0.0002724568934985569023, 0.0004086836638483783580, 0.0005449104342063597903, 0.0008173270854453586502, 0.001089761613562687925 ),
 .UNSPECIFIED. ) ;
#18567=CARTESIAN_POINT ( 'NONE',  ( 5.959547316686252039, -14.51128755440531393, -14.51632612601523853 ) ) ;
#18570=CARTESIAN_POINT ( 'NONE',  ( 0.9756354156337464500, 39.59221474545864083, 16.54067710771375488 ) ) ;
#18577=CARTESIAN_POINT ( 'NONE',  ( 0.5838002273316419410, -33.96372661229960244, 33.77111476497762510 ) ) ;
#18579=B_SPLINE_CURVE_WITH_KNOTS ( 'NONE', 3,
 ( #37020, #22897, #56082, #13194, #61385, #42026 ),
 .UNSPECIFIED., .F., .F.,
 ( 4, 2, 4 ),
 ( 3.529906531158615134E-18, 0.0002445244328975369687, 0.0004890488657950704679 ),
 .UNSPECIFIED. ) ;
#18582=ORIENTED_EDGE ( 'NONE', *, *, #42881, .F. ) ;
#18587=B_SPLINE_CURVE_WITH_KNOTS ( 'NONE', 3,
 ( #11011, #24786, #16019, #57968, #15093, #35131 ),
 .UNSPECIFIED., .F., .F.,
 ( 4, 2, 4 ),
 ( 3.471140604459641645E-18, 0.0002291966416970808403, 0.0004583932833941582112 ),
 .UNSPECIFIED. ) ;
#18588=CARTESIAN_POINT ( 'NONE',  ( 0.9752570700956797456, -41.50550328400875344, 10.88256294660697243 ) ) ;
#18589=VERTEX_POINT ( 'NONE', #22170 ) ;
#18591=ORIENTED_EDGE ( 'NONE', *, *, #51336, .T. ) ;
#18592=CARTESIAN_POINT ( 'NONE',  ( 0.5819845079324665882, -12.83441846783097873, -46.14435090135489048 ) ) ;
#18597=CARTESIAN_POINT ( 'NONE',  ( 4.956653778116982600, -45.71126949320260735, 14.93973939759871072 ) ) ;
#18602=VERTEX_POINT ( 'NONE', #3045 ) ;
#18608=CARTESIAN_POINT ( 'NONE',  ( 0.9752570700956796346, -0.2306661201224228797, 42.90785210525869786 ) ) ;
#18626=EDGE_CURVE ( 'NONE', #30942, #33762, #7855, .T. ) ;
#18630=ADVANCED_FACE ( 'NONE', ( #17169 ), #17666, .F. ) ;
#18631=CARTESIAN_POINT ( 'NONE',  ( 1.227938101723748288, 15.63977281655842511, 39.96870412324341260 ) ) ;
#18650=CARTESIAN_POINT ( 'NONE',  ( 5.960721111146673579, 0.006321279846536711350, 20.52557019979492026 ) ) ;
#18653=VERTEX_POINT ( 'NONE', #38144 ) ;
#18655=CARTESIAN_POINT ( 'NONE',  ( 0.9730545539215883499, -42.90536227157002003, 0.5054011016611185125 ) ) ;
#18656=CARTESIAN_POINT ( 'NONE',  ( 2.281351352603287808, 43.80196780981719940, 19.56575819747240885 ) ) ;
#18662=DIRECTION ( 'NONE',  ( 0.000000000000000000, 0.000000000000000000, 1.000000000000000000 ) ) ;
#18671=CARTESIAN_POINT ( 'NONE',  ( 1.227938101723747621, 30.94118573761354440, -29.74462687941193551 ) ) ;
#18681=EDGE_CURVE ( 'NONE', #36654, #45591, #33741, .T. ) ;
#18684=CARTESIAN_POINT ( 'NONE',  ( 1.227938101723748288, 15.63977281655842511, 39.96870412324341260 ) ) ;
#18686=VERTEX_POINT ( 'NONE', #48136 ) ;
#18691=CARTESIAN_POINT ( 'NONE',  ( 4.960156602257177916, 35.23783291257167605, 30.22163187094397685 ) ) ;
#18697=VECTOR ( 'NONE', #58880, 1000.000000000000114 ) ;
#18705=CARTESIAN_POINT ( 'NONE',  ( 4.963659409799333844, -37.47512675766712675, 24.46566636552813634 ) ) ;
#18707=( BOUNDED_SURFACE ( )  B_SPLINE_SURFACE ( 3, 1, ( 
 ( #53703, #5782 ),
 ( #21454, #49036 ),
 ( #21147, #35879 ),
 ( #15533, #24934 ) ),
 .UNSPECIFIED., .F., .F., .F. ) 
 B_SPLINE_SURFACE_WITH_KNOTS ( ( 4, 4 ),
 ( 2, 2 ),
 ( 0.000000000000000000, 1.000000000000000000 ),
 ( 0.000000000000000000, 1.000000000000000000 ),
 .UNSPECIFIED. ) 
 GEOMETRIC_REPRESENTATION_ITEM ( )  RATIONAL_B_SPLINE_SURFACE ( (
 ( 1.000000000000000000, 1.000000000000000000),
 ( 0.9732289882329797637, 0.9999525324661233672),
 ( 0.9732289882329797637, 0.9999525324661233672),
 ( 1.000000000000000000, 1.000000000000000000) ) ) 
 REPRESENTATION_ITEM ( '' )  SURFACE ( )  );
#18713=CARTESIAN_POINT ( 'NONE',  ( 1.227938101723756947, 37.58536632582779191, 20.72293514920763258 ) ) ;
#18714=CARTESIAN_POINT ( 'NONE',  ( 0.5832367798473407916, 0.2724222379467150512, -47.89515946578894301 ) ) ;
#18716=CARTESIAN_POINT ( 'NONE',  ( 5.981074661064941900, 5.303881226583402331, 19.82752479807529156 ) ) ;
#18726=CARTESIAN_POINT ( 'NONE',  ( 0.5807400328401637335, 41.20655774453003062, -24.41979442053126448 ) ) ;
#18727=CARTESIAN_POINT ( 'NONE',  ( 4.967162193818130511, -32.10009971360091896, 28.74031574030002645 ) ) ;
#18733=CARTESIAN_POINT ( 'NONE',  ( 0.6067099128993237445, -47.89177823194876282, 0.7089426894588903849 ) ) ;
#18739=CARTESIAN_POINT ( 'NONE',  ( 4.956653778116999476, 43.37017594958085454, -20.77844580450516077 ) ) ;
#18742=CARTESIAN_POINT ( 'NONE',  ( -17.97369999999976642, -7.719455939378112141, -2.099999999999997424 ) ) ;
#18745=ORIENTED_EDGE ( 'NONE', *, *, #31403, .T. ) ;
#18755=EDGE_CURVE ( 'NONE', #48168, #55855, #30266, .T. ) ;
#18759=CARTESIAN_POINT ( 'NONE',  ( 2.526464513654347321, -22.53107770806397525, -36.59988118252427114 ) ) ;
#18760=EDGE_CURVE ( 'NONE', #14535, #41116, #41496, .T. ) ;
#18761=CARTESIAN_POINT ( 'NONE',  ( 0.5836750258453344831, -29.30109045202416596, 37.88760409476686419 ) ) ;
#18765=ORIENTED_EDGE ( 'NONE', *, *, #12724, .F. ) ;
#18768=ORIENTED_EDGE ( 'NONE', *, *, #1334, .F. ) ;
#18774=CARTESIAN_POINT ( 'NONE',  ( 0.8551540677456715978, 44.61036085020975861, -17.49081417858738519 ) ) ;
#18785=( LENGTH_UNIT ( ) NAMED_UNIT ( * ) SI_UNIT ( .MILLI., .METRE. ) );
#18786=CARTESIAN_POINT ( 'NONE',  ( 5.974727161628367256, -19.82959049719571709, -5.297264154380866508 ) ) ;
#18797=CARTESIAN_POINT ( 'NONE',  ( 0.8551540677456715978, 5.348818140991581593, -47.61725548905984340 ) ) ;
#18816=CARTESIAN_POINT ( 'NONE',  ( 1.088908134280555107, -39.93902428011476502, -15.69861202536792710 ) ) ;
#18819=CARTESIAN_POINT ( 'NONE',  ( 4.303969348037246512, 42.70173985163847874, -22.16169334783792877 ) ) ;
#18824=ORIENTED_EDGE ( 'NONE', *, *, #31047, .T. ) ;
#18825=FACE_OUTER_BOUND ( 'NONE', #56732, .T. ) ;
#18830=CONICAL_SURFACE ( 'NONE', #61803, 48.09070567114147110, 0.04450589592585947607 ) ;
#18833=VECTOR ( 'NONE', #55128, 1000.000000000000114 ) ;
#18835=ORIENTED_EDGE ( 'NONE', *, *, #59487, .T. ) ;
#18838=ORIENTED_EDGE ( 'NONE', *, *, #14244, .T. ) ;
#18841=ORIENTED_EDGE ( 'NONE', *, *, #19120, .T. ) ;
#18842=CARTESIAN_POINT ( 'NONE',  ( 0.5786265663353153954, -47.89572889566446889, 0.7221568112304753706 ) ) ;
#18844=CARTESIAN_POINT ( 'NONE',  ( 1.227938101723756947, -11.92353943227920610, -41.23019537246722876 ) ) ;
#18845=CARTESIAN_POINT ( 'NONE',  ( 1.227938101723748288, 0.8460948827231143943, -42.91134962331486236 ) ) ;
#18846=CARTESIAN_POINT ( 'NONE',  ( 5.960721111146673579, 16.28787783074210438, 12.49016043756476790 ) ) ;
#18847=VERTEX_POINT ( 'NONE', #14944 ) ;
#18849=ADVANCED_FACE ( 'NONE', ( #35276, #15856 ), #5494, .F. ) ;
#18851=CARTESIAN_POINT ( 'NONE',  ( 0.5807400328401637335, 34.25275203086282261, -33.48217046439074807 ) ) ;
#18855=CARTESIAN_POINT ( 'NONE',  ( 0.5786265663353153954, 13.09387673186335377, 46.07681357296491598 ) ) ;
#18861=CARTESIAN_POINT ( 'NONE',  ( 4.967162193818130511, 13.42934394584221280, -40.93989340068594629 ) ) ;
#18863=ORIENTED_EDGE ( 'NONE', *, *, #31089, .T. ) ;
#18883=CARTESIAN_POINT ( 'NONE',  ( 0.9757402383260941336, 30.40085236181992201, -30.28078671294493773 ) ) ;
#18890=CARTESIAN_POINT ( 'NONE',  ( 0.9757892942422827787, -37.18547544211197220, -21.40977514834421314 ) ) ;
#18896=CARTESIAN_POINT ( 'NONE',  ( 4.967162193818130511, 38.83676580803767564, 18.65818244221271627 ) ) ;
#18897=CARTESIAN_POINT ( 'NONE',  ( 0.5807400328401574052, -46.40483864045135931, -11.87003418057292237 ) ) ;
#18899=CARTESIAN_POINT ( 'NONE',  ( 0.5819845079324652559, -33.54497088780105685, 34.18710788661938693 ) ) ;
#18904=CARTESIAN_POINT ( 'NONE',  ( 0.9757892942422808913, -11.15510465568972265, -41.43309903783668346 ) ) ;
#18905=EDGE_CURVE ( 'NONE', #51992, #20695, #49605, .T. ) ;
#18909=ORIENTED_EDGE ( 'NONE', *, *, #22713, .F. ) ;
#18911=EDGE_LOOP ( 'NONE', ( #32863, #44841 ) ) ;
#18919=CARTESIAN_POINT ( 'NONE',  ( 0.9747592971366235703, -34.23774590565619746, -25.86343094887217475 ) ) ;
#18920=ORIENTED_EDGE ( 'NONE', *, *, #34026, .T. ) ;
#18924=ORIENTED_EDGE ( 'NONE', *, *, #20227, .T. ) ;
#18931=LINE ( 'NONE', #47423, #32918 ) ;
#18934=B_SPLINE_CURVE_WITH_KNOTS ( 'NONE', 3,
 ( #3819, #22955, #12032, #59602 ),
 .UNSPECIFIED., .F., .F.,
 ( 4, 4 ),
 ( 2.168404344971008868E-19, 0.004048833967417087357 ),
 .UNSPECIFIED. ) ;
#18943=CARTESIAN_POINT ( 'NONE',  ( 1.227938101723748288, 17.20315230597897482, -39.32113113558949635 ) ) ;
#18944=CARTESIAN_POINT ( 'NONE',  ( 0.5809828226811544205, 33.48000389720665027, -34.25055090842118233 ) ) ;
#18949=CARTESIAN_POINT ( 'NONE',  ( 4.303969348037258058, -22.16169334783867484, 42.70173985163810215 ) ) ;
#18951=CARTESIAN_POINT ( 'NONE',  ( 4.956653778116949738, 45.71126949320249366, 14.93973939759898606 ) ) ;
#18955=CARTESIAN_POINT ( 'NONE',  ( 5.958863334805807099, -5.313608583996383139, -19.82594244347351520 ) ) ;
#18962=CARTESIAN_POINT ( 'NONE',  ( 4.967162193818129623, -19.45289607368849616, 38.44485641567065670 ) ) ;
#18963=CARTESIAN_POINT ( 'NONE',  ( 0.9722240750034567558, -39.41582016107710018, 16.95645446544471824 ) ) ;
#18964=EDGE_CURVE ( 'NONE', #10097, #38122, #56375, .T. ) ;
#18966=DIRECTION ( 'NONE',  ( 0.000000000000000000, 0.000000000000000000, 1.000000000000000000 ) ) ;
#18967=( BOUNDED_SURFACE ( )  B_SPLINE_SURFACE ( 3, 1, ( 
 ( #20021, #29390 ),
 ( #43209, #28776 ),
 ( #5257, #23773 ),
 ( #9994, #14389 ) ),
 .UNSPECIFIED., .F., .F., .F. ) 
 B_SPLINE_SURFACE_WITH_KNOTS ( ( 4, 4 ),
 ( 2, 2 ),
 ( 0.000000000000000000, 1.000000000000000000 ),
 ( 0.000000000000000000, 1.000000000000000000 ),
 .UNSPECIFIED. ) 
 GEOMETRIC_REPRESENTATION_ITEM ( )  RATIONAL_B_SPLINE_SURFACE ( (
 ( 1.000000000000000000, 1.000000000000000000),
 ( 0.9953390228620291325, 0.8624445117760984880),
 ( 0.9953390228620291325, 0.8624445117760984880),
 ( 1.000000000000000000, 1.000000000000000000) ) ) 
 REPRESENTATION_ITEM ( '' )  SURFACE ( )  );
#18972=ADVANCED_FACE ( 'NONE', ( #41219 ), #9800, .T. ) ;
#18973=CARTESIAN_POINT ( 'NONE',  ( 4.956653778116986153, -48.02038484091102077, 2.599733001514167086 ) ) ;
#18974=CARTESIAN_POINT ( 'NONE',  ( 0.9730545539215883499, -36.90443313492345823, 21.89037132892422832 ) ) ;
#18977=AXIS2_PLACEMENT_3D ( 'NONE', #11305, #44848, #27559 ) ;
#18981=ORIENTED_EDGE ( 'NONE', *, *, #20951, .F. ) ;
#18984=CARTESIAN_POINT ( 'NONE',  ( 0.8557997880470697982, 28.43566216845025352, -38.55640757422408882 ) ) ;
#18990=CARTESIAN_POINT ( 'NONE',  ( 5.959547316686252039, 7.858107265727477753, 18.96183906913546480 ) ) ;
#18992=EDGE_CURVE ( 'NONE', #5228, #6983, #38436, .T. ) ;
#18996=CARTESIAN_POINT ( 'NONE',  ( 0.5827357941260199459, 37.77622264066054214, -29.44458568814473054 ) ) ;
#19004=CARTESIAN_POINT ( 'NONE',  ( 1.088313998177379283, 15.69908095455155639, 39.93881167962107526 ) ) ;
#19007=ORIENTED_EDGE ( 'NONE', *, *, #40907, .F. ) ;
#19011=ORIENTED_EDGE ( 'NONE', *, *, #44249, .T. ) ;
#19012=DIRECTION ( 'NONE',  ( 0.000000000000000000, 0.000000000000000000, 1.000000000000000000 ) ) ;
#19016=VECTOR ( 'NONE', #49094, 999.9999999999998863 ) ;
#19018=CARTESIAN_POINT ( 'NONE',  ( 0.5839879882012681822, -47.48621496524027208, -6.251648354650674477 ) ) ;
#19028=DIRECTION ( 'NONE',  ( -0.07836865515943411409, 0.007886984708657411927, 0.9968932487286223942 ) ) ;
#19043=CARTESIAN_POINT ( 'NONE',  ( 0.5839254288179533958, -47.89590036163259157, -0.09078831291274436222 ) ) ;
#19044=ADVANCED_FACE ( 'NONE', ( #41839 ), #37762, .T. ) ;
#19052=CARTESIAN_POINT ( 'NONE',  ( 4.303969348037258058, 22.16169334783896971, -42.70173985163793873 ) ) ;
#19055=CARTESIAN_POINT ( 'NONE',  ( 0.9740398440564312921, 42.48528956276145152, -6.011466167923673609 ) ) ;
#19060=DIRECTION ( 'NONE',  ( -1.000000000000000000, -0.000000000000000000, -0.000000000000000000 ) ) ;
#19061=EDGE_CURVE ( 'NONE', #50265, #10364, #37443, .T. ) ;
#19064=EDGE_CURVE ( 'NONE', #29464, #50394, #54884, .T. ) ;
#19066=CARTESIAN_POINT ( 'NONE',  ( 1.088908134280554885, -30.89124834763367744, -29.78762923589999900 ) ) ;
#19068=CARTESIAN_POINT ( 'NONE',  ( 0.5839254288179563934, 47.49799454719525471, -6.161657890844459473 ) ) ;
#19070=CARTESIAN_POINT ( 'NONE',  ( 0.5809828226811617480, -44.45562576850614533, 17.82437196699665094 ) ) ;
#19073=AXIS2_PLACEMENT_3D ( 'NONE', #24849, #20768, #43990 ) ;
#19083=ORIENTED_EDGE ( 'NONE', *, *, #19064, .T. ) ;
#19084=CARTESIAN_POINT ( 'NONE',  ( 5.959547316686252039, 12.49803383497749820, -16.28190225198605745 ) ) ;
#19085=EDGE_CURVE ( 'NONE', #44253, #5033, #10081, .T. ) ;
#19090=CARTESIAN_POINT ( 'NONE',  ( 0.6067099128993237445, 46.44339333106615442, 11.71051825714719463 ) ) ;
#19093=CARTESIAN_POINT ( 'NONE',  ( 0.9752570700956806338, 0.2306661201227225566, -42.90785210525867654 ) ) ;
#19105=B_SPLINE_CURVE_WITH_KNOTS ( 'NONE', 3,
 ( #54621, #25833, #58396, #10507 ),
 .UNSPECIFIED., .F., .F.,
 ( 4, 4 ),
 ( 0.000000000000000000, 0.004446090762761384201 ),
 .UNSPECIFIED. ) ;
#19112=CARTESIAN_POINT ( 'NONE',  ( 0.7057020205115001055, 7.085441699094293000, -47.37450661940661689 ) ) ;
#19116=VECTOR ( 'NONE', #25165, 1000.000000000000000 ) ;
#19120=EDGE_CURVE ( 'NONE', #35558, #25685, #4054, .T. ) ;
#19122=EDGE_CURVE ( 'NONE', #1997, #9596, #20472, .T. ) ;
#19123=CARTESIAN_POINT ( 'NONE',  ( 0.5807400328401574052, -41.20655774452986719, 24.41979442053154514 ) ) ;
#19131=CARTESIAN_POINT ( 'NONE',  ( 0.5807400328401574052, 28.72484455891640920, 38.33001520688959829 ) ) ;
#19132=CARTESIAN_POINT ( 'NONE',  ( 0.6067375320500714153, 47.38951440911015567, 6.954068056450886104 ) ) ;
#19134=CARTESIAN_POINT ( 'NONE',  ( 2.624215991343608501, 42.26352390376127488, -22.77108897942091659 ) ) ;
#19135=EDGE_LOOP ( 'NONE', ( #44574, #24461, #53840, #27934 ) ) ;
#19139=CARTESIAN_POINT ( 'NONE',  ( 4.956653778116961284, 40.28700667097682953, 26.26162724282386662 ) ) ;
#19142=CARTESIAN_POINT ( 'NONE',  ( 4.963659409799330291, -42.53037318520986076, -13.93274247732065696 ) ) ;
#19145=ORIENTED_EDGE ( 'NONE', *, *, #15207, .F. ) ;
#19153=CARTESIAN_POINT ( 'NONE',  ( 0.8551540677456739292, -38.56334384152450667, 28.44084013485104379 ) ) ;
#19154=( BOUNDED_SURFACE ( )  B_SPLINE_SURFACE ( 3, 1, ( 
 ( #4386, #28842 ),
 ( #43589, #57028 ),
 ( #311, #18527 ),
 ( #9117, #61407 ) ),
 .UNSPECIFIED., .F., .F., .F. ) 
 B_SPLINE_SURFACE_WITH_KNOTS ( ( 4, 4 ),
 ( 2, 2 ),
 ( 0.000000000000000000, 1.000000000000000000 ),
 ( 0.000000000000000000, 1.000000000000000000 ),
 .UNSPECIFIED. ) 
 GEOMETRIC_REPRESENTATION_ITEM ( )  RATIONAL_B_SPLINE_SURFACE ( (
 ( 1.000000000000000000, 1.000000000000000000),
 ( 0.7269869731126821222, 0.9931720237060910339),
 ( 0.7269869731126821222, 0.9931720237060910339),
 ( 1.000000000000000000, 1.000000000000000000) ) ) 
 REPRESENTATION_ITEM ( '' )  SURFACE ( )  );
#19156=EDGE_CURVE ( 'NONE', #24678, #22536, #53960, .T. ) ;
#19160=CARTESIAN_POINT ( 'NONE',  ( 1.227938101723748288, -42.65467462194921922, 4.762198645644287076 ) ) ;
#19167=CARTESIAN_POINT ( 'NONE',  ( 5.960721111146673579, 7.848955554238515653, -18.96557324978279624 ) ) ;
#19169=CARTESIAN_POINT ( 'NONE',  ( 0.9736507210033054083, 25.76216842460696199, 34.31386771842671379 ) ) ;
#19173=DIRECTION ( 'NONE',  ( -1.000000000000000000, -0.000000000000000000, -0.000000000000000000 ) ) ;
#19179=CARTESIAN_POINT ( 'NONE',  ( 5.960721111146673579, -10.25731071096570268, -17.77882586010663246 ) ) ;
#19180=EDGE_CURVE ( 'NONE', #4359, #54823, #56322, .T. ) ;
#19181=CARTESIAN_POINT ( 'NONE',  ( 3.407937589446178528, -13.10584870154469606, 3.987184287467740784 ) ) ;
#19182=CARTESIAN_POINT ( 'NONE',  ( 0.5263152470540294336, 0.000000000000000000, 0.000000000000000000 ) ) ;
#19187=ADVANCED_FACE ( 'NONE', ( #35204 ), #22818, .T. ) ;
#19188=CARTESIAN_POINT ( 'NONE',  ( 0.5809828226811617480, -44.03860873105681151, -18.83114015454746237 ) ) ;
#19194=CARTESIAN_POINT ( 'NONE',  ( 1.088908134280555995, -41.64642044161486467, -10.35121946298456486 ) ) ;
#19197=LINE ( 'NONE', #38310, #1429 ) ;
#19202=CARTESIAN_POINT ( 'NONE',  ( 0.5837374860065662752, 29.01294733976413553, -38.10878877974113266 ) ) ;
#19203=CARTESIAN_POINT ( 'NONE',  ( 0.5819845079324669213, 24.34013310064393920, 41.25022834067357280 ) ) ;
#19204=CARTESIAN_POINT ( 'NONE',  ( 3.270143674763207553, -3.277085381513213047, 13.28976595685392681 ) ) ;
#19205=ORIENTED_EDGE ( 'NONE', *, *, #51122, .F. ) ;
#19211=ORIENTED_EDGE ( 'NONE', *, *, #42273, .F. ) ;
#19215=ORIENTED_EDGE ( 'NONE', *, *, #33756, .F. ) ;
#19223=ORIENTED_EDGE ( 'NONE', *, *, #51122, .T. ) ;
#19224=CARTESIAN_POINT ( 'NONE',  ( 4.967162193818131399, 42.16965968614193372, 8.839793687085363061 ) ) ;
#19229=FACE_OUTER_BOUND ( 'NONE', #24322, .T. ) ;
#19232=CARTESIAN_POINT ( 'NONE',  ( 4.303969348037258058, -8.413118729223747039, -47.36875205922780907 ) ) ;
#19233=DIRECTION ( 'NONE',  ( -1.000000000000000000, -0.000000000000000000, -0.000000000000000000 ) ) ;
#19239=CARTESIAN_POINT ( 'NONE',  ( 4.956653778116994147, 35.79382859084161339, -32.11725092155005967 ) ) ;
#19247=CARTESIAN_POINT ( 'NONE',  ( 1.154321713695929175, -20.73950268329797453, -37.57248787340957108 ) ) ;
#19253=CARTESIAN_POINT ( 'NONE',  ( 0.5809828226811617480, 0.5448590168539207967, -47.89273459658652854 ) ) ;
#19258=CARTESIAN_POINT ( 'NONE',  ( 3.783198216974391404, -22.99723434398817545, 36.37893817280279052 ) ) ;
#19271=CARTESIAN_POINT ( 'NONE',  ( 0.9722240741986373225, -6.177112427866152444, 42.46141200043699371 ) ) ;
#19274=EDGE_CURVE ( 'NONE', #9802, #12689, #18302, .T. ) ;
#19277=CARTESIAN_POINT ( 'NONE',  ( 4.303969348037246512, 32.45857549159302380, 35.51084504003208764 ) ) ;
#19282=CARTESIAN_POINT ( 'NONE',  ( 0.5827359174754811466, -41.29633904010498924, -24.26188383263413684 ) ) ;
#19286=ORIENTED_EDGE ( 'NONE', *, *, #28188, .T. ) ;
#19297=ORIENTED_EDGE ( 'NONE', *, *, #48428, .F. ) ;
#19298=CARTESIAN_POINT ( 'NONE',  ( 0.9730545539215883499, -37.40983423658458662, -21.01499094264588763 ) ) ;
#19303=ORIENTED_EDGE ( 'NONE', *, *, #44117, .T. ) ;
#19304=CARTESIAN_POINT ( 'NONE',  ( 0.9730545539215883499, 0.5054011016612682816, 42.90536227157002003 ) ) ;
#19305=CARTESIAN_POINT ( 'NONE',  ( 0.9972139404380291339, 10.46878911444733973, -41.61281131482451201 ) ) ;
#19306=FACE_OUTER_BOUND ( 'NONE', #54320, .T. ) ;
#19308=ORIENTED_EDGE ( 'NONE', *, *, #5343, .T. ) ;
#19313=VERTEX_POINT ( 'NONE', #48517 ) ;
#19316=CARTESIAN_POINT ( 'NONE',  ( 0.8557997880470606944, -19.17299735372040459, 43.90420959842174398 ) ) ;
#19319=CARTESIAN_POINT ( 'NONE',  ( 0.5819845901640493535, -17.90867915372020391, -44.42187107932964096 ) ) ;
#19320=( BOUNDED_SURFACE ( )  B_SPLINE_SURFACE ( 3, 1, ( 
 ( #40941, #11803 ),
 ( #2677, #59070 ),
 ( #49998, #54984 ),
 ( #20877, #30881 ) ),
 .UNSPECIFIED., .F., .F., .F. ) 
 B_SPLINE_SURFACE_WITH_KNOTS ( ( 4, 4 ),
 ( 2, 2 ),
 ( 0.000000000000000000, 1.000000000000000000 ),
 ( 0.000000000000000000, 1.000000000000000000 ),
 .UNSPECIFIED. ) 
 GEOMETRIC_REPRESENTATION_ITEM ( )  RATIONAL_B_SPLINE_SURFACE ( (
 ( 1.000000000000000000, 1.000000000000000000),
 ( 0.7269869731126817891, 0.9931720237060910339),
 ( 0.7269869731126817891, 0.9931720237060910339),
 ( 1.000000000000000000, 1.000000000000000000) ) ) 
 REPRESENTATION_ITEM ( '' )  SURFACE ( )  );
#19325=EDGE_LOOP ( 'NONE', ( #30826, #23279, #48626, #24888 ) ) ;
#19341=B_SPLINE_CURVE_WITH_KNOTS ( 'NONE', 3,
 ( #3436, #56376, #26965, #51060 ),
 .UNSPECIFIED., .F., .F.,
 ( 4, 4 ),
 ( 0.000000000000000000, 0.005004741218457183817 ),
 .UNSPECIFIED. ) ;
#19347=CARTESIAN_POINT ( 'NONE',  ( 0.5809828226811617480, -24.41822904836953612, 41.20389530892298779 ) ) ;
#19348=EDGE_CURVE ( 'NONE', #21932, #16132, #6260, .T. ) ;
#19351=CARTESIAN_POINT ( 'NONE',  ( 0.9745511491811736926, 42.58443036172455720, -5.262846425219182223 ) ) ;
#19357=CARTESIAN_POINT ( 'NONE',  ( -19.25636039734503413, -7.824477911287009313, 1.668439766839475480 ) ) ;
#19360=B_SPLINE_CURVE_WITH_KNOTS ( 'NONE', 3,
 ( #15735, #20422, #38317, #58605 ),
 .UNSPECIFIED., .F., .F.,
 ( 4, 4 ),
 ( 8.673617379884035472E-19, 0.004048833967417083887 ),
 .UNSPECIFIED. ) ;
#19361=CARTESIAN_POINT ( 'NONE',  ( 5.965394784446460541, -12.48356622107665714, -16.29267539192338887 ) ) ;
#19362=CARTESIAN_POINT ( 'NONE',  ( 0.5834872094924180574, 47.51530820063773319, -6.026535573893641029 ) ) ;
#19363=ORIENTED_EDGE ( 'NONE', *, *, #12836, .T. ) ;
#19368=B_SPLINE_CURVE_WITH_KNOTS ( 'NONE', 3,
 ( #30318, #39138, #1489, #15932 ),
 .UNSPECIFIED., .F., .F.,
 ( 4, 4 ),
 ( 1.962615573354719267E-17, 0.005004741218457437087 ),
 .UNSPECIFIED. ) ;
#19377=ADVANCED_FACE ( 'NONE', ( #34134 ), #15669, .F. ) ;
#19382=EDGE_CURVE ( 'NONE', #9472, #14392, #11525, .T. ) ;
#19385=CARTESIAN_POINT ( 'NONE',  ( 5.959547316686252039, -20.34955788964378698, 2.682663672454569159 ) ) ;
#19389=CARTESIAN_POINT ( 'NONE',  ( 0.6067375320500703051, -46.07640252006471115, -13.08014790719075293 ) ) ;
#19393=B_SPLINE_CURVE_WITH_KNOTS ( 'NONE', 3,
 ( #13396, #53120, #29320, #19951 ),
 .UNSPECIFIED., .F., .F.,
 ( 4, 4 ),
 ( 0.000000000000000000, 0.004446090762761387670 ),
 .UNSPECIFIED. ) ;
#19395=PRESENTATION_STYLE_ASSIGNMENT (( #4956 ) ) ;
#19404=B_SPLINE_CURVE_WITH_KNOTS ( 'NONE', 3,
 ( #3584, #56831, #23339, #13959 ),
 .UNSPECIFIED., .F., .F.,
 ( 4, 4 ),
 ( 0.000000000000000000, 0.005004741218457404127 ),
 .UNSPECIFIED. ) ;
#19410=CARTESIAN_POINT ( 'NONE',  ( 0.9736507210033075177, -21.84312502845817150, 36.93248879681202368 ) ) ;
#19412=EDGE_CURVE ( 'NONE', #8164, #694, #17514, .T. ) ;
#19413=CARTESIAN_POINT ( 'NONE',  ( 4.956653778116971942, 35.79382859084115864, 32.11725092155054995 ) ) ;
#19420=EDGE_CURVE ( 'NONE', #56419, #28932, #42735, .T. ) ;
#19423=CARTESIAN_POINT ( 'NONE',  ( 0.5807400328401574052, -47.41494605191439149, -6.791881299636076008 ) ) ;
#19424=ORIENTED_EDGE ( 'NONE', *, *, #10617, .T. ) ;
#19432=CARTESIAN_POINT ( 'NONE',  ( 1.227938101723756947, 17.20315230597844192, 39.32113113558972373 ) ) ;
#19442=CARTESIAN_POINT ( 'NONE',  ( 4.967162193818130511, 38.83676580803792433, -18.65818244221215849 ) ) ;
#19444=ADVANCED_FACE ( 'NONE', ( #25951 ), #28450, .F. ) ;
#19446=CARTESIAN_POINT ( 'NONE',  ( 4.967162193818131399, -19.45289607368795259, -38.44485641567092671 ) ) ;
#19451=CARTESIAN_POINT ( 'NONE',  ( 0.8557997880470697982, -47.37054680076710866, 7.156447707085535903 ) ) ;
#19453=ADVANCED_FACE ( 'NONE', ( #29713 ), #26435, .F. ) ;
#19455=EDGE_CURVE ( 'NONE', #5939, #33472, #2516, .T. ) ;
#19457=CARTESIAN_POINT ( 'NONE',  ( 1.088908134280558881, 36.76788378223859155, -22.12904883058516603 ) ) ;
#19459=ORIENTED_EDGE ( 'NONE', *, *, #22530, .T. ) ;
#19461=CARTESIAN_POINT ( 'NONE',  ( 0.5832366564991509073, 44.35361744978938958, 18.07697797533105089 ) ) ;
#19465=CARTESIAN_POINT ( 'NONE',  ( 5.981074661064941900, -16.27808421740034817, 12.50143471347253765 ) ) ;
#19466=B_SPLINE_CURVE_WITH_KNOTS ( 'NONE', 3,
 ( #28520, #4380, #61705, #18844 ),
 .UNSPECIFIED., .F., .F.,
 ( 4, 4 ),
 ( 4.670885906470169154E-18, 0.004050076154993004218 ),
 .UNSPECIFIED. ) ;
#19477=EDGE_CURVE ( 'NONE', #42440, #61394, #6495, .T. ) ;
#19483=CARTESIAN_POINT ( 'NONE',  ( 4.956653778116990594, 2.599733001515011743, -48.02038484091096393 ) ) ;
#19488=CARTESIAN_POINT ( 'NONE',  ( -17.29438283698436862, -7.748258867160539687, 1.991845353126138862 ) ) ;
#19491=EDGE_CURVE ( 'NONE', #51084, #52796, #20334, .T. ) ;
#19495=CARTESIAN_POINT ( 'NONE',  ( 0.5839880159502333079, -23.90868446765450628, -41.50181427378129229 ) ) ;
#19497=EDGE_CURVE ( 'NONE', #23542, #6995, #28718, .T. ) ;
#19498=AXIS2_PLACEMENT_3D ( 'NONE', #27785, #33738, #28707 ) ;
#19499=CARTESIAN_POINT ( 'NONE',  ( -4.473699999999999122, 5.863696293535578419E-15, 47.67072199303260049 ) ) ;
#19502=CARTESIAN_POINT ( 'NONE',  ( 0.5819845079324666992, 28.79567599618816232, -38.27312975753780933 ) ) ;
#19505=DIRECTION ( 'NONE',  ( 0.07836865515943411409, 0.9893941468723566057, -0.1223011693452815268 ) ) ;
#19507=CARTESIAN_POINT ( 'NONE',  ( 0.9736507210033050752, 5.153758453069551493, 42.59776535855981194 ) ) ;
#19513=CARTESIAN_POINT ( 'NONE',  ( 0.9749527285493309048, -10.82939760924474193, -41.51939261707894957 ) ) ;
#19514=ORIENTED_EDGE ( 'NONE', *, *, #22477, .T. ) ;
#19515=CARTESIAN_POINT ( 'NONE',  ( 5.960221823109900008, -12.49951306783078131, -16.28072933292543922 ) ) ;
#19521=CARTESIAN_POINT ( 'NONE',  ( 3.783198216974390959, 31.62918462580879719, -29.18723368117329997 ) ) ;
#19525=ADVANCED_FACE ( 'NONE', ( #22791 ), #24802, .F. ) ;
#19529=VERTEX_POINT ( 'NONE', #3969 ) ;
#19531=EDGE_CURVE ( 'NONE', #9388, #18069, #3054, .T. ) ;
#19533=ORIENTED_EDGE ( 'NONE', *, *, #6397, .F. ) ;
#19544=FACE_OUTER_BOUND ( 'NONE', #29650, .T. ) ;
#19556=AXIS2_PLACEMENT_3D ( 'NONE', #50500, #7572, #27624 ) ;
#19565=VERTEX_POINT ( 'NONE', #2741 ) ;
#19566=CARTESIAN_POINT ( 'NONE',  ( 5.959828726073459926, -10.26672511661768006, 17.77343634131824146 ) ) ;
#19570=CARTESIAN_POINT ( 'NONE',  ( 5.960721111146673579, 20.34914600876571456, 2.685391721746106963 ) ) ;
#19574=CARTESIAN_POINT ( 'NONE',  ( 0.9757892942422831117, -26.08029006934560101, 34.07281211842312985 ) ) ;
#19577=CARTESIAN_POINT ( 'NONE',  ( 3.660087539127334200, 32.61167949558434742, -35.27260502801098596 ) ) ;
#19580=DIRECTION ( 'NONE',  ( -1.000000000000000000, -0.000000000000000000, -0.000000000000000000 ) ) ;
#19583=CARTESIAN_POINT ( 'NONE',  ( 4.956653778116966613, 0.000000000000000000, 0.000000000000000000 ) ) ;
#19588=CARTESIAN_POINT ( 'NONE',  ( 0.7762783648524398394, 37.45705264446620220, -29.86325223096974923 ) ) ;
#19595=CARTESIAN_POINT ( 'NONE',  ( 4.963659409799331179, -43.98510776953404644, -8.262218268420943090 ) ) ;
#19597=VECTOR ( 'NONE', #43191, 1000.000000000000114 ) ;
#19598=CARTESIAN_POINT ( 'NONE',  ( 3.407937589446178528, 10.00592723328961142, 9.356405769959087237 ) ) ;
#19599=CIRCLE ( 'NONE', #564, 43.08621763946400307 ) ;
#19601=ADVANCED_FACE ( 'NONE', ( #21873 ), #7213, .F. ) ;
#19602=CARTESIAN_POINT ( 'NONE',  ( 0.5809828226811617480, 38.32755012159184815, -28.72298383114449294 ) ) ;
#19603=ADVANCED_FACE ( 'NONE', ( #8072 ), #60826, .F. ) ;
#19606=CARTESIAN_POINT ( 'NONE',  ( 0.7762783648524405056, -11.53708172997851911, 46.49451980369975246 ) ) ;
#19607=CARTESIAN_POINT ( 'NONE',  ( 1.088313998177382613, 42.43756598879024722, 6.373602917100332554 ) ) ;
#19615=ORIENTED_EDGE ( 'NONE', *, *, #29709, .T. ) ;
#19620=FACE_OUTER_BOUND ( 'NONE', #57860, .T. ) ;
#19628=DIRECTION ( 'NONE',  ( 0.07439287786467667363, 0.7144194931003065019, -0.6957517427943048505 ) ) ;
#19639=CARTESIAN_POINT ( 'NONE',  ( 0.5839879327111919816, -23.86931774877327683, 41.52454255611500855 ) ) ;
#19642=VERTEX_POINT ( 'NONE', #43154 ) ;
#19643=CIRCLE ( 'NONE', #54608, 48.09070567114147110 ) ;
#19645=CARTESIAN_POINT ( 'NONE',  ( 0.5834872094924189456, 0.2270145249679870747, -47.89542889285417004 ) ) ;
#19646=CARTESIAN_POINT ( 'NONE',  ( 0.9730545539215883499, -26.52009130076794108, 33.73144377768549163 ) ) ;
#19648=CARTESIAN_POINT ( 'NONE',  ( 1.227938101723756947, 36.73927144310543014, -22.18841447410681411 ) ) ;
#19662=CARTESIAN_POINT ( 'NONE',  ( 0.9758171775293909000, 42.54062484958064516, -5.606549717953765111 ) ) ;
#19664=ORIENTED_EDGE ( 'NONE', *, *, #20519, .T. ) ;
#19669=DIRECTION ( 'NONE',  ( 0.000000000000000000, 0.000000000000000000, 1.000000000000000000 ) ) ;
#19672=CARTESIAN_POINT ( 'NONE',  ( 0.7762777257811890319, 28.45155622761428660, 38.54028505510729730 ) ) ;
#19678=VERTEX_POINT ( 'NONE', #37850 ) ;
#19684=CARTESIAN_POINT ( 'NONE',  ( 3.270143674763207553, -11.71453292426884296, 7.080034332678216913 ) ) ;
#19687=VERTEX_POINT ( 'NONE', #9936 ) ;
#19702=B_SPLINE_CURVE_WITH_KNOTS ( 'NONE', 3,
 ( #37838, #60978, #52193, #18086 ),
 .UNSPECIFIED., .F., .F.,
 ( 4, 4 ),
 ( 0.000000000000000000, 0.005004741218457439689 ),
 .UNSPECIFIED. ) ;
#19708=CARTESIAN_POINT ( 'NONE',  ( 0.6846871229502932144, -29.84551600520658354, 37.47592888575237424 ) ) ;
#19718=CARTESIAN_POINT ( 'NONE',  ( 4.303969348037246512, -45.22910199346984683, 16.39840148505076911 ) ) ;
#19722=VECTOR ( 'NONE', #865, 1000.000000000000114 ) ;
#19727=CARTESIAN_POINT ( 'NONE',  ( 3.270143674763207553, 13.68510027222513337, -0.2742231296309999844 ) ) ;
#19730=CARTESIAN_POINT ( 'NONE',  ( 0.5850706913938533704, -47.46255051844948980, -6.431767090163312162 ) ) ;
#19734=EDGE_CURVE ( 'NONE', #59493, #25828, #55542, .T. ) ;
#19737=CARTESIAN_POINT ( 'NONE',  ( 1.227938101723756947, -30.94118573761292623, -29.74462687941258210 ) ) ;
#19744=B_SPLINE_CURVE_WITH_KNOTS ( 'NONE', 3,
 ( #54421, #48286, #7115, #6488 ),
 .UNSPECIFIED., .F., .F.,
 ( 4, 4 ),
 ( 0.000000000000000000, 0.004446090762761341700 ),
 .UNSPECIFIED. ) ;
#19748=CARTESIAN_POINT ( 'NONE',  ( 0.9730545539215883499, -41.31259007387222226, -11.59290486963550393 ) ) ;
#19759=ORIENTED_EDGE ( 'NONE', *, *, #56632, .F. ) ;
#19760=CARTESIAN_POINT ( 'NONE',  ( 4.956653778116991482, -21.75875759808677046, -42.88673967249153662 ) ) ;
#19766=AXIS2_PLACEMENT_3D ( 'NONE', #19930, #10202, #14298 ) ;
#19770=CARTESIAN_POINT ( 'NONE',  ( 0.5837374860065644988, 33.73893264285595706, -33.99581326751397370 ) ) ;
#19774=CARTESIAN_POINT ( 'NONE',  ( 5.959547316686252039, -7.858107265727618085, -18.96183906913540795 ) ) ;
#19780=CARTESIAN_POINT ( 'NONE',  ( 0.6846871229502932144, -19.12907057981236036, 43.92355552798031937 ) ) ;
#19785=VERTEX_POINT ( 'NONE', #50745 ) ;
#19786=CARTESIAN_POINT ( 'NONE',  ( 2.281351352603291804, -44.80774876812572671, 17.13758816714735644 ) ) ;
#19795=LINE ( 'NONE', #19181, #37958 ) ;
#19803=CARTESIAN_POINT ( 'NONE',  ( 0.9757954354143122400, -4.033171854401937560E-17, -42.90846090505964128 ) ) ;
#19805=CARTESIAN_POINT ( 'NONE',  ( 0.9730545539215883499, 29.98130006528905156, -30.69604515769618658 ) ) ;
#19810=EDGE_CURVE ( 'NONE', #16670, #147, #54764, .T. ) ;
#19820=CARTESIAN_POINT ( 'NONE',  ( 0.5786265663353153954, 47.39171391660402577, -6.967625775955234246 ) ) ;
#19826=EDGE_CURVE ( 'NONE', #38104, #9098, #9969, .T. ) ;
#19828=CARTESIAN_POINT ( 'NONE',  ( 5.960721111146673579, -12.50019045452726907, -16.28018152803688778 ) ) ;
#19829=CIRCLE ( 'NONE', #24823, 43.08621763946400307 ) ;
#19833=CARTESIAN_POINT ( 'NONE',  ( 0.9722240741986377666, 25.65687427836904888, 34.39263045016065234 ) ) ;
#19834=ORIENTED_EDGE ( 'NONE', *, *, #57794, .T. ) ;
#19837=CARTESIAN_POINT ( 'NONE',  ( 3.407937589446174087, -12.08659953757613259, 6.447869442558121555 ) ) ;
#19841=CARTESIAN_POINT ( 'NONE',  ( 0.9758171775293910111, -34.04519363167618451, -26.11633498242663975 ) ) ;
#19842=ORIENTED_EDGE ( 'NONE', *, *, #19826, .F. ) ;
#19844=CARTESIAN_POINT ( 'NONE',  ( 4.956653778116988818, -45.35992544608517818, -15.97476558431931082 ) ) ;
#19846=LINE ( 'NONE', #28917, #230 ) ;
#19857=CARTESIAN_POINT ( 'NONE',  ( 4.303969348037246512, 40.54345935592778716, 25.89994482339384163 ) ) ;
#19860=VECTOR ( 'NONE', #57023, 1000.000000000000114 ) ;
#19864=CARTESIAN_POINT ( 'NONE',  ( 1.154321485836934169, 39.32643515542059731, -17.18284940416407736 ) ) ;
#19879=CARTESIAN_POINT ( 'NONE',  ( 4.967162193818130511, 0.000000000000000000, 0.000000000000000000 ) ) ;
#19880=ADVANCED_FACE ( 'NONE', ( #13799 ), #60452, .F. ) ;
#19881=CARTESIAN_POINT ( 'NONE',  ( 0.5807400328401574052, 28.72484455891697053, -38.33001520688919328 ) ) ;
#19884=CARTESIAN_POINT ( 'NONE',  ( 0.5832367798473397924, -41.61463593465321509, 23.71165515427700043 ) ) ;
#19887=CARTESIAN_POINT ( 'NONE',  ( 3.660176727303411148, 20.10773453922346832, -43.62748706623501960 ) ) ;
#19898=ORIENTED_EDGE ( 'NONE', *, *, #26446, .T. ) ;
#19902=CIRCLE ( 'NONE', #32770, 48.09070567114147110 ) ;
#19912=ORIENTED_EDGE ( 'NONE', *, *, #58107, .T. ) ;
#19916=CARTESIAN_POINT ( 'NONE',  ( 0.9722240741986376555, -39.41582013185135480, -16.95645453362505961 ) ) ;
#19922=CARTESIAN_POINT ( 'NONE',  ( 0.5839879882012675161, 37.99840755997087172, -29.15724166963611452 ) ) ;
#19923=ORIENTED_EDGE ( 'NONE', *, *, #14585, .T. ) ;
#19929=CARTESIAN_POINT ( 'NONE',  ( 4.967162193818132288, 19.45289607368876617, -38.44485641567052880 ) ) ;
#19930=CARTESIAN_POINT ( 'NONE',  ( 4.967162193818130511, 0.000000000000000000, 0.000000000000000000 ) ) ;
#19951=CARTESIAN_POINT ( 'NONE',  ( 0.8557997880470599172, 46.50333260518575429, -11.51622788066409697 ) ) ;
#19958=CARTESIAN_POINT ( 'NONE',  ( 5.960721111146673579, 2.685391721746036353, -20.34914600876572521 ) ) ;
#19961=CARTESIAN_POINT ( 'NONE',  ( 2.624215991343620935, -13.78323291683751606, -45.98641578154045817 ) ) ;
#19968=EDGE_CURVE ( 'NONE', #8227, #8570, #52550, .T. ) ;
#19969=CARTESIAN_POINT ( 'NONE',  ( 2.526552050251863246, 37.81244156771019505, -20.43086833796918356 ) ) ;
#19970=ADVANCED_FACE ( 'NONE', ( #32207 ), #39644, .F. ) ;
#19973=ORIENTED_EDGE ( 'NONE', *, *, #51257, .F. ) ;
#19974=CARTESIAN_POINT ( 'NONE',  ( 0.8557997880470690211, -28.43566216844996930, 38.55640757422429488 ) ) ;
#19975=CONICAL_SURFACE ( 'NONE', #43000, 43.08621763946400307, 1.568696531533066763 ) ;
#19976=DIRECTION ( 'NONE',  ( 0.07439287786467665975, 0.9971416435352942198, 0.01320009283087282027 ) ) ;
#19977=EDGE_CURVE ( 'NONE', #61565, #17051, #8077, .T. ) ;
#19980=CARTESIAN_POINT ( 'NONE',  ( 5.958863334805807099, -20.35021240744033122, -2.677925489610565979 ) ) ;
#19986=ORIENTED_EDGE ( 'NONE', *, *, #27947, .T. ) ;
#19990=CARTESIAN_POINT ( 'NONE',  ( 1.088908134280558437, -20.77739698351960129, 37.54826033999255230 ) ) ;
#19993=( BOUNDED_SURFACE ( )  B_SPLINE_SURFACE ( 3, 1, ( 
 ( #2765, #44799 ),
 ( #36013, #26580 ),
 ( #1518, #17198 ),
 ( #15967, #35079 ) ),
 .UNSPECIFIED., .F., .F., .F. ) 
 B_SPLINE_SURFACE_WITH_KNOTS ( ( 4, 4 ),
 ( 2, 2 ),
 ( 0.000000000000000000, 1.000000000000000000 ),
 ( 0.000000000000000000, 1.000000000000000000 ),
 .UNSPECIFIED. ) 
 GEOMETRIC_REPRESENTATION_ITEM ( )  RATIONAL_B_SPLINE_SURFACE ( (
 ( 1.000000000000000000, 1.000000000000000000),
 ( 0.7269869731126817891, 0.9931720237060910339),
 ( 0.7269869731126817891, 0.9931720237060910339),
 ( 1.000000000000000000, 1.000000000000000000) ) ) 
 REPRESENTATION_ITEM ( '' )  SURFACE ( )  );
#20004=B_SPLINE_CURVE_WITH_KNOTS ( 'NONE', 3,
 ( #31357, #54834, #21963, #59851 ),
 .UNSPECIFIED., .F., .F.,
 ( 4, 4 ),
 ( 0.000000000000000000, 0.004446090762761376394 ),
 .UNSPECIFIED. ) ;
#20007=CARTESIAN_POINT ( 'NONE',  ( 5.974727161628367256, 16.29297756969631195, 12.48248968439934536 ) ) ;
#20008=VERTEX_POINT ( 'NONE', #7127 ) ;
#20020=CARTESIAN_POINT ( 'NONE',  ( 0.5839880159502364165, -6.296669079378488298, 47.48028790449881598 ) ) ;
#20021=CARTESIAN_POINT ( 'NONE',  ( 5.960721111146673579, 16.28018152803675633, 12.50019045452743782 ) ) ;
#20023=B_SPLINE_CURVE_WITH_KNOTS ( 'NONE', 3,
 ( #23088, #168, #43444, #48128, #23390, #3948, #56268, #61879, #33114, #19018, #47509, #4555, #52187, #61272, #18390, #23696 ),
 .UNSPECIFIED., .F., .F.,
 ( 4, 3, 3, 3, 3, 4 ),
 ( 1.127622383284612036E-17, 0.0002724568934985558181, 0.0004086836638483798759, 0.0005449104342063616335, 0.0008173270854453682996, 0.001089761613562687925 ),
 .UNSPECIFIED. ) ;
#20025=CARTESIAN_POINT ( 'NONE',  ( 0.5809828226811617480, 17.82437196699680726, 44.45562576850608139 ) ) ;
#20029=CARTESIAN_POINT ( 'NONE',  ( 4.956653778116966613, 0.000000000000000000, 0.000000000000000000 ) ) ;
#20033=ORIENTED_EDGE ( 'NONE', *, *, #3223, .F. ) ;
#20037=CARTESIAN_POINT ( 'NONE',  ( 5.960221823109900008, -2.684531185214569238, 20.34928172836725935 ) ) ;
#20047=CARTESIAN_POINT ( 'NONE',  ( 0.5807400328401637335, -47.89582301953902999, -0.5448834511095090871 ) ) ;
#20052=CARTESIAN_POINT ( 'NONE',  ( 0.5800708057587374844, 47.40012370174866874, 6.873290064481538231 ) ) ;
#20063=FACE_OUTER_BOUND ( 'NONE', #61938, .T. ) ;
#20074=ORIENTED_EDGE ( 'NONE', *, *, #52156, .F. ) ;
#20077=LINE ( 'NONE', #28837, #19860 ) ;
#20080=FACE_OUTER_BOUND ( 'NONE', #30366, .T. ) ;
#20081=CARTESIAN_POINT ( 'NONE',  ( 0.5839879327111923146, 33.80333292213305896, -33.93179405280454120 ) ) ;
#20084=ORIENTED_EDGE ( 'NONE', *, *, #20858, .T. ) ;
#20095=LINE ( 'NONE', #53269, #39597 ) ;
#20097=EDGE_CURVE ( 'NONE', #47245, #30566, #24703, .T. ) ;
#20100=ORIENTED_EDGE ( 'NONE', *, *, #36442, .T. ) ;
#20102=CARTESIAN_POINT ( 'NONE',  ( 0.5809828226811553087, -44.45562576850588243, -17.82437196699728332 ) ) ;
#20103=FACE_OUTER_BOUND ( 'NONE', #26777, .T. ) ;
#20107=DIRECTION ( 'NONE',  ( -1.000000000000000000, -0.000000000000000000, -0.000000000000000000 ) ) ;
#20108=CARTESIAN_POINT ( 'NONE',  ( -15.87375730239583937, -7.999984958122236200, 0.1385333841346340356 ) ) ;
#20110=DIRECTION ( 'NONE',  ( 0.000000000000000000, 0.000000000000000000, 1.000000000000000000 ) ) ;
#20117=CARTESIAN_POINT ( 'NONE',  ( 0.5839879882012681822, 33.86758487442402554, 33.86754218494311175 ) ) ;
#20131=CARTESIAN_POINT ( 'NONE',  ( 0.5807400328401637335, -38.33001520688971198, 28.72484455891626709 ) ) ;
#20134=CARTESIAN_POINT ( 'NONE',  ( 5.959547316686252039, -12.49803383497738807, -16.28190225198614627 ) ) ;
#20135=ORIENTED_EDGE ( 'NONE', *, *, #34172, .T. ) ;
#20143=CARTESIAN_POINT ( 'NONE',  ( 3.270143674763207553, -0.2742231296308566546, -13.68510027222513692 ) ) ;
#20151=CARTESIAN_POINT ( 'NONE',  ( 5.960721111146673579, -16.28787783074218964, -12.49016043756465422 ) ) ;
#20157=ADVANCED_FACE ( 'NONE', ( #33757 ), #50051, .F. ) ;
#20160=ORIENTED_EDGE ( 'NONE', *, *, #22290, .T. ) ;
#20161=FACE_OUTER_BOUND ( 'NONE', #30710, .T. ) ;
#20168=CARTESIAN_POINT ( 'NONE',  ( 2.624215991343620935, -38.92973006074493725, -28.09277600149258447 ) ) ;
#20175=CARTESIAN_POINT ( 'NONE',  ( 4.967162193818130511, 0.000000000000000000, 0.000000000000000000 ) ) ;
#20177=CARTESIAN_POINT ( 'NONE',  ( 0.9730545539215883499, 37.40983423658502716, -21.01499094264509893 ) ) ;
#20178=CARTESIAN_POINT ( 'NONE',  ( 0.5807400328401574052, -37.66660715020886840, 29.58941477093001993 ) ) ;
#20179=EDGE_CURVE ( 'NONE', #51998, #57230, #39696, .T. ) ;
#20181=B_SPLINE_CURVE_WITH_KNOTS ( 'NONE', 3,
 ( #48753, #16175, #1732, #44399, #57824, #1425 ),
 .UNSPECIFIED., .F., .F.,
 ( 4, 2, 4 ),
 ( 9.745765416140531346E-18, 0.0002291978881530162685, 0.0004583957763060227792 ),
 .UNSPECIFIED. ) ;
#20189=CARTESIAN_POINT ( 'NONE',  ( 0.5838002273316419410, -41.54704836736068074, 23.82993264414549373 ) ) ;
#20197=CARTESIAN_POINT ( 'NONE',  ( 0.9730545539215883499, 10.61654491617563423, 41.57420493492389113 ) ) ;
#20205=CARTESIAN_POINT ( 'NONE',  ( 4.967162193818130511, 23.56777426397228936, -36.06913038482774425 ) ) ;
#20207=CARTESIAN_POINT ( 'NONE',  ( 5.974727161628367256, 7.868887636447348122, 18.95664195401520402 ) ) ;
#20208=B_SPLINE_CURVE_WITH_KNOTS ( 'NONE', 3,
 ( #50332, #35960, #50945, #45659, #36570, #3022 ),
 .UNSPECIFIED., .F., .F.,
 ( 4, 2, 4 ),
 ( 1.097135458930219133E-17, 0.0002291978881530148590, 0.0004583957763060187134 ),
 .UNSPECIFIED. ) ;
#20209=EDGE_LOOP ( 'NONE', ( #23883, #26729, #30987, #4315 ) ) ;
#20210=ORIENTED_EDGE ( 'NONE', *, *, #33178, .T. ) ;
#20212=FACE_OUTER_BOUND ( 'NONE', #60814, .T. ) ;
#20218=CARTESIAN_POINT ( 'NONE',  ( 0.9756354156337463390, 42.52418499698895005, 5.729847988735494724 ) ) ;
#20227=EDGE_CURVE ( 'NONE', #31789, #5687, #26373, .T. ) ;
#20236=CARTESIAN_POINT ( 'NONE',  ( 0.7762777257811899201, -46.49451973287609263, 11.53708189756924618 ) ) ;
#20237=EDGE_CURVE ( 'NONE', #49382, #9581, #59065, .T. ) ;
#20240=CARTESIAN_POINT ( 'NONE',  ( 0.5839880159502340851, 23.98728323041108013, -41.45643525694580944 ) ) ;
#20242=( BOUNDED_SURFACE ( )  B_SPLINE_SURFACE ( 3, 1, ( 
 ( #46649, #41044 ),
 ( #3693, #60107 ),
 ( #37254, #17213 ),
 ( #36334, #31611 ) ),
 .UNSPECIFIED., .F., .F., .F. ) 
 B_SPLINE_SURFACE_WITH_KNOTS ( ( 4, 4 ),
 ( 2, 2 ),
 ( 0.000000000000000000, 1.000000000000000000 ),
 ( 0.000000000000000000, 1.000000000000000000 ),
 .UNSPECIFIED. ) 
 GEOMETRIC_REPRESENTATION_ITEM ( )  RATIONAL_B_SPLINE_SURFACE ( (
 ( 1.000000000000000000, 1.000000000000000000),
 ( 0.9953390228620291325, 0.8624445117760984880),
 ( 0.9953390228620291325, 0.8624445117760984880),
 ( 1.000000000000000000, 1.000000000000000000) ) ) 
 REPRESENTATION_ITEM ( '' )  SURFACE ( )  );
#20257=EDGE_CURVE ( 'NONE', #44894, #3092, #17466, .T. ) ;
#20261=CARTESIAN_POINT ( 'NONE',  ( 0.5786265663353153954, -5.535668456754276434, 47.58023467411537410 ) ) ;
#20266=DIRECTION ( 'NONE',  ( 0.07836865515943411409, -0.9240274869783839939, 0.3742079063794805371 ) ) ;
#20272=ORIENTED_EDGE ( 'NONE', *, *, #56624, .F. ) ;
#20273=VERTEX_POINT ( 'NONE', #5209 ) ;
#20275=CARTESIAN_POINT ( 'NONE',  ( 5.981074661064941900, 20.34795181394745001, 2.687517936920068351 ) ) ;
#20279=CARTESIAN_POINT ( 'NONE',  ( 0.5827359174754822568, -47.53228759166452733, 5.891371786504793207 ) ) ;
#20280=CARTESIAN_POINT ( 'NONE',  ( 0.9722240741986364343, 30.74950262511642052, -29.92651525529343814 ) ) ;
#20300=EDGE_LOOP ( 'NONE', ( #33621, #39981, #33812, #29193 ) ) ;
#20308=CARTESIAN_POINT ( 'NONE',  ( 5.960221823109900008, -5.307149561568222929, 19.82761049839333012 ) ) ;
#20313=CARTESIAN_POINT ( 'NONE',  ( 0.7057020205115085432, 41.05685587925835023, 24.67553336431198829 ) ) ;
#20314=ORIENTED_EDGE ( 'NONE', *, *, #6617, .T. ) ;
#20317=CARTESIAN_POINT ( 'NONE',  ( 0.8557997880470599172, 11.51622788066458369, 46.50333260518563350 ) ) ;
#20320=ORIENTED_EDGE ( 'NONE', *, *, #17734, .T. ) ;
#20330=ORIENTED_EDGE ( 'NONE', *, *, #24526, .F. ) ;
#20332=CARTESIAN_POINT ( 'NONE',  ( 2.526552050251864134, 42.96196914573631886, 1.212569781798080726 ) ) ;
#20334=LINE ( 'NONE', #39454, #9669 ) ;
#20338=CARTESIAN_POINT ( 'NONE',  ( 0.5809828226811556418, 44.03860873105722362, -18.83114015454650314 ) ) ;
#20341=B_SPLINE_CURVE_WITH_KNOTS ( 'NONE', 3,
 ( #14180, #33285, #52356, #15407, #53282, #24795 ),
 .UNSPECIFIED., .F., .F.,
 ( 4, 2, 4 ),
 ( 2.168404344971008868E-19, 0.0002445244328975376192, 0.0004890488657950750216 ),
 .UNSPECIFIED. ) ;
#20342=DIRECTION ( 'NONE',  ( -0.07836865515943411409, 0.9968932487286223942, -0.007886984708660891782 ) ) ;
#20345=CARTESIAN_POINT ( 'NONE',  ( 5.959547316686252039, 20.34955788964373014, 2.682663672454983050 ) ) ;
#20349=ORIENTED_EDGE ( 'NONE', *, *, #58371, .F. ) ;
#20351=CARTESIAN_POINT ( 'NONE',  ( 0.5850706913938533704, 29.01314519953797699, 38.10903744847151842 ) ) ;
#20352=CARTESIAN_POINT ( 'NONE',  ( 0.5832366564991506852, 18.07697797533149853, -44.35361744978919774 ) ) ;
#20355=EDGE_LOOP ( 'NONE', ( #51081, #11195, #52489, #61943 ) ) ;
#20356=CARTESIAN_POINT ( 'NONE',  ( 0.9730545539215883499, -21.89037132892409687, -36.90443313492354349 ) ) ;
#20359=B_SPLINE_CURVE_WITH_KNOTS ( 'NONE', 3,
 ( #55568, #47132, #41206, #60576, #33037, #60892, #46832, #27704, #61201, #32103, #52109, #32411, #51486, #12695, #36815, #23016, #28313, #42145, #13935 ),
 .UNSPECIFIED., .F., .F.,
 ( 4, 3, 3, 3, 3, 3, 4 ),
 ( 0.000000000000000000, 0.0002724573126191823149, 0.0004086839781548524345, 0.0005449106435901870157, 0.0006811373090491508074, 0.0008459866663933821680, 0.001010840725717217052 ),
 .UNSPECIFIED. ) ;
#20363=ORIENTED_EDGE ( 'NONE', *, *, #52475, .T. ) ;
#20367=ORIENTED_EDGE ( 'NONE', *, *, #36070, .T. ) ;
#20370=EDGE_LOOP ( 'NONE', ( #57926, #18135, #50097, #28376 ) ) ;
#20378=CARTESIAN_POINT ( 'NONE',  ( 3.270143674763207553, -8.548517033725183012, -10.69018354892896205 ) ) ;
#20390=CARTESIAN_POINT ( 'NONE',  ( 4.963659409799330291, -39.92545197189564732, 20.22157859941717462 ) ) ;
#20413=CARTESIAN_POINT ( 'NONE',  ( 0.6067099128993242996, 44.51753430581941018, 17.67241243535499251 ) ) ;
#20415=EDGE_CURVE ( 'NONE', #56211, #13708, #13634, .T. ) ;
#20416=DIRECTION ( 'NONE',  ( -1.000000000000000000, -0.000000000000000000, -0.000000000000000000 ) ) ;
#20422=CARTESIAN_POINT ( 'NONE',  ( 2.526552050251863246, 9.948123361606842963, 41.81191169914599470 ) ) ;
#20427=ORIENTED_EDGE ( 'NONE', *, *, #34394, .F. ) ;
#20429=VERTEX_POINT ( 'NONE', #22724 ) ;
#20441=ORIENTED_EDGE ( 'NONE', *, *, #38642, .T. ) ;
#20445=B_SPLINE_CURVE_WITH_KNOTS ( 'NONE', 3,
 ( #26524, #45651, #2706, #36256 ),
 .UNSPECIFIED., .F., .F.,
 ( 4, 4 ),
 ( 8.673617379884035472E-19, 0.004050076154993002484 ),
 .UNSPECIFIED. ) ;
#20458=CARTESIAN_POINT ( 'NONE',  ( 5.960721111146673579, -17.77882586010660049, -10.25731071096576486 ) ) ;
#20462=ORIENTED_EDGE ( 'NONE', *, *, #47612, .F. ) ;
#20463=CARTESIAN_POINT ( 'NONE',  ( 0.9972139404380295780, 39.38665787682688091, -17.02682566833142630 ) ) ;
#20466=EDGE_CURVE ( 'NONE', #10980, #25968, #12087, .T. ) ;
#20467=CARTESIAN_POINT ( 'NONE',  ( 0.9972139404380309102, -33.63772329383400006, 26.64066783422323681 ) ) ;
#20468=CARTESIAN_POINT ( 'NONE',  ( 3.660087539127328871, -30.71416465583032007, -36.93668088065476951 ) ) ;
#20470=CARTESIAN_POINT ( 'NONE',  ( 0.5807400328401637335, -41.75144119563903189, 23.47602859900699457 ) ) ;
#20471=B_SPLINE_CURVE_WITH_KNOTS ( 'NONE', 3,
 ( #37144, #8596, #32430, #37451 ),
 .UNSPECIFIED., .F., .F.,
 ( 4, 4 ),
 ( 7.757919228897728493E-18, 0.005004741218457447495 ),
 .UNSPECIFIED. ) ;
#20472=LINE ( 'NONE', #11382, #48793 ) ;
#20476=CARTESIAN_POINT ( 'NONE',  ( 5.958863334805807099, -14.51296551801793200, -14.51469124124474597 ) ) ;
#20491=DIRECTION ( 'NONE',  ( 0.000000000000000000, 0.000000000000000000, 1.000000000000000000 ) ) ;
#20504=VERTEX_POINT ( 'NONE', #39615 ) ;
#20509=( BOUNDED_SURFACE ( )  B_SPLINE_SURFACE ( 3, 1, ( 
 ( #37528, #32824 ),
 ( #32197, #14331 ),
 ( #28404, #8362 ),
 ( #51904, #51279 ) ),
 .UNSPECIFIED., .F., .F., .F. ) 
 B_SPLINE_SURFACE_WITH_KNOTS ( ( 4, 4 ),
 ( 2, 2 ),
 ( 0.000000000000000000, 1.000000000000000000 ),
 ( 0.000000000000000000, 1.000000000000000000 ),
 .UNSPECIFIED. ) 
 GEOMETRIC_REPRESENTATION_ITEM ( )  RATIONAL_B_SPLINE_SURFACE ( (
 ( 1.000000000000000000, 1.000000000000000000),
 ( 0.7269869731126821222, 0.9931720237060910339),
 ( 0.7269869731126821222, 0.9931720237060910339),
 ( 1.000000000000000000, 1.000000000000000000) ) ) 
 REPRESENTATION_ITEM ( '' )  SURFACE ( )  );
#20519=EDGE_CURVE ( 'NONE', #55413, #28131, #57627, .T. ) ;
#20520=VERTEX_POINT ( 'NONE', #53064 ) ;
#20522=VECTOR ( 'NONE', #8299, 1000.000000000000114 ) ;
#20523=ORIENTED_EDGE ( 'NONE', *, *, #29968, .T. ) ;
#20524=CARTESIAN_POINT ( 'NONE',  ( 4.956653778116990594, -32.11725092155016625, -35.79382859084151391 ) ) ;
#20528=ADVANCED_FACE ( 'NONE', ( #15797 ), #2832, .F. ) ;
#20533=ADVANCED_FACE ( 'NONE', ( #34594 ), #56802, .F. ) ;
#20540=CARTESIAN_POINT ( 'NONE',  ( 5.965394784446458765, 18.96850062921623703, 7.841344330025009413 ) ) ;
#20541=ORIENTED_EDGE ( 'NONE', *, *, #40918, .T. ) ;
#20543=CARTESIAN_POINT ( 'NONE',  ( 4.956653778116966613, 0.000000000000000000, 0.000000000000000000 ) ) ;
#20546=CARTESIAN_POINT ( 'NONE',  ( 0.6067099128993209689, -18.98236771638427101, -43.97493306231482535 ) ) ;
#20550=CARTESIAN_POINT ( 'NONE',  ( 0.9968887458511633826, 34.43855515351805963, -25.59699785741752365 ) ) ;
#20555=EDGE_LOOP ( 'NONE', ( #50050, #52325, #57448, #27477 ) ) ;
#20557=CARTESIAN_POINT ( 'NONE',  ( 1.088313998177381503, -17.14007796983261755, 39.34193117255247785 ) ) ;
#20561=CARTESIAN_POINT ( 'NONE',  ( 3.270143674763207553, 12.74832469035459681, -4.983712007628090745 ) ) ;
#20568=VERTEX_POINT ( 'NONE', #26721 ) ;
#20570=CARTESIAN_POINT ( 'NONE',  ( 0.5839254288179567265, -12.48406597209070945, 46.24038938821428246 ) ) ;
#20571=VECTOR ( 'NONE', #10727, 1000.000000000000227 ) ;
#20572=CARTESIAN_POINT ( 'NONE',  ( 5.960721111146673579, -14.51823969584109619, 14.50930005614991813 ) ) ;
#20588=CARTESIAN_POINT ( 'NONE',  ( 5.965394784446460541, -20.52536205633085231, -0.01447339372445936509 ) ) ;
#20589=( BOUNDED_SURFACE ( )  B_SPLINE_SURFACE ( 3, 1, ( 
 ( #32905, #51984 ),
 ( #4345, #9075 ),
 ( #28180, #23800 ),
 ( #23481, #61673 ) ),
 .UNSPECIFIED., .F., .F., .F. ) 
 B_SPLINE_SURFACE_WITH_KNOTS ( ( 4, 4 ),
 ( 2, 2 ),
 ( 0.000000000000000000, 1.000000000000000000 ),
 ( 0.000000000000000000, 1.000000000000000000 ),
 .UNSPECIFIED. ) 
 GEOMETRIC_REPRESENTATION_ITEM ( )  RATIONAL_B_SPLINE_SURFACE ( (
 ( 1.000000000000000000, 1.000000000000000000),
 ( 0.7269869731126821222, 0.9931720237060910339),
 ( 0.7269869731126821222, 0.9931720237060910339),
 ( 1.000000000000000000, 1.000000000000000000) ) ) 
 REPRESENTATION_ITEM ( '' )  SURFACE ( )  );
#20592=B_SPLINE_CURVE_WITH_KNOTS ( 'NONE', 3,
 ( #34741, #53806, #10939, #7118 ),
 .UNSPECIFIED., .F., .F.,
 ( 4, 4 ),
 ( 0.000000000000000000, 0.005004741218457408464 ),
 .UNSPECIFIED. ) ;
#20596=CARTESIAN_POINT ( 'NONE',  ( 1.227938101723748288, -33.52879263017845091, -26.79402671879361364 ) ) ;
#20605=CARTESIAN_POINT ( 'NONE',  ( 5.974727161628367256, -18.95664195401523244, 7.868887636447281508 ) ) ;
#20609=CARTESIAN_POINT ( 'NONE',  ( 5.960721111146673579, -5.306302591836717930, 19.82781442290488627 ) ) ;
#20610=ORIENTED_EDGE ( 'NONE', *, *, #49674, .T. ) ;
#20614=CARTESIAN_POINT ( 'NONE',  ( 4.967162193818130511, -42.16965968614200477, 8.839793687085075291 ) ) ;
#20617=CARTESIAN_POINT ( 'NONE',  ( 0.5827357941260216112, -5.891356987507951004, 47.53228940613937681 ) ) ;
#20620=ORIENTED_EDGE ( 'NONE', *, *, #31114, .T. ) ;
#20623=CARTESIAN_POINT ( 'NONE',  ( -4.473699999999997345, 0.000000000000000000, -12.50000000000000000 ) ) ;
#20629=EDGE_LOOP ( 'NONE', ( #38145, #59185, #41592, #41985 ) ) ;
#20631=CARTESIAN_POINT ( 'NONE',  ( 0.8557997880470690211, 7.156447707085701104, 47.37054680076709445 ) ) ;
#20639=CARTESIAN_POINT ( 'NONE',  ( 2.526552050251864578, -9.948123361606551640, -41.81191169914605865 ) ) ;
#20650=ORIENTED_EDGE ( 'NONE', *, *, #21584, .F. ) ;
#20654=ADVANCED_FACE ( 'NONE', ( #46783 ), #50411, .F. ) ;
#20663=CARTESIAN_POINT ( 'NONE',  ( 2.624215991343620935, -37.21129343241625520, 30.33228621715021944 ) ) ;
#20664=CARTESIAN_POINT ( 'NONE',  ( 0.9730545539215883499, 16.88610103448612065, -39.44597740938043273 ) ) ;
#20670=EDGE_CURVE ( 'NONE', #36860, #11517, #6818, .T. ) ;
#20673=AXIS2_PLACEMENT_3D ( 'NONE', #56139, #38005, #14187 ) ;
#20674=CARTESIAN_POINT ( 'NONE',  ( 3.270143674763207553, -13.14781761974172092, 3.806843787665870060 ) ) ;
#20675=ORIENTED_EDGE ( 'NONE', *, *, #55562, .T. ) ;
#20676=CARTESIAN_POINT ( 'NONE',  ( 5.974727161628367256, -12.50710176109996574, -16.27409205901371791 ) ) ;
#20687=CARTESIAN_POINT ( 'NONE',  ( 0.5832367798473377940, 34.05962365606865916, -33.67436043247226962 ) ) ;
#20695=VERTEX_POINT ( 'NONE', #27650 ) ;
#20696=CARTESIAN_POINT ( 'NONE',  ( 0.9752132459055852243, 33.89922943039213266, -26.30543738863311276 ) ) ;
#20702=CARTESIAN_POINT ( 'NONE',  ( -17.97369999999976642, -12.32233744059949210, 2.099999999999994760 ) ) ;
#20713=B_SPLINE_CURVE_WITH_KNOTS ( 'NONE', 3,
 ( #44044, #19595, #5754, #57150 ),
 .UNSPECIFIED., .F., .F.,
 ( 4, 4 ),
 ( 0.000000000000000000, 0.005004741218457414535 ),
 .UNSPECIFIED. ) ;
#20717=CARTESIAN_POINT ( 'NONE',  ( -17.97369999999976642, -7.719455939378113030, 2.099999999999994760 ) ) ;
#20721=CARTESIAN_POINT ( 'NONE',  ( 0.5786265663353196143, -28.58414684753461188, -38.43785771743232260 ) ) ;
#20723=ADVANCED_FACE ( 'NONE', ( #17959 ), #1186, .F. ) ;
#20730=CARTESIAN_POINT ( 'NONE',  ( 4.967162193818130511, 0.000000000000000000, 0.000000000000000000 ) ) ;
#20731=EDGE_CURVE ( 'NONE', #30005, #58891, #33835, .T. ) ;
#20732=EDGE_LOOP ( 'NONE', ( #35633, #2224, #7467, #16815 ) ) ;
#20733=FACE_OUTER_BOUND ( 'NONE', #13543, .T. ) ;
#20739=CARTESIAN_POINT ( 'NONE',  ( 5.960721111146673579, 5.306302591836580262, -19.82781442290492890 ) ) ;
#20756=EDGE_LOOP ( 'NONE', ( #60700, #39624, #22985, #16143 ) ) ;
#20761=ORIENTED_EDGE ( 'NONE', *, *, #10604, .T. ) ;
#20767=EDGE_CURVE ( 'NONE', #51225, #34606, #15959, .T. ) ;
#20768=DIRECTION ( 'NONE',  ( -1.000000000000000000, -0.000000000000000000, -0.000000000000000000 ) ) ;
#20770=CARTESIAN_POINT ( 'NONE',  ( 1.227938101723756947, 42.65467462194918369, 4.762198645644581951 ) ) ;
#20779=CARTESIAN_POINT ( 'NONE',  ( 0.9730545539215883499, -33.73144377768576874, 26.52009130076758225 ) ) ;
#20780=B_SPLINE_CURVE_WITH_KNOTS ( 'NONE', 3,
 ( #57252, #46985, #42286, #28459, #33808, #28154, #9356, #19093, #32884, #38204, #4625, #57559, #14386 ),
 .UNSPECIFIED., .F., .F.,
 ( 4, 3, 3, 3, 4 ),
 ( 0.0005054209210070093961, 0.0005449106435901839799, 0.0006811373090491489642, 0.0008459866663933690491, 0.001010840725717212715 ),
 .UNSPECIFIED. ) ;
#20785=CARTESIAN_POINT ( 'NONE',  ( 0.5850706913938533704, -38.10903744847161789, 29.01314519953784554 ) ) ;
#20795=CARTESIAN_POINT ( 'NONE',  ( 0.5839879882012690704, -41.47910964649813081, 23.94800997596668779 ) ) ;
#20796=CARTESIAN_POINT ( 'NONE',  ( 0.6846871229502932144, 47.37786444808393327, 7.109010606687553135 ) ) ;
#20797=CARTESIAN_POINT ( 'NONE',  ( 0.9757402383260943557, -26.18833306844175723, 33.98983788393810102 ) ) ;
#20825=CARTESIAN_POINT ( 'NONE',  ( 0.9749527285493297946, 42.50314808877163131, 5.883724875809256183 ) ) ;
#20839=CARTESIAN_POINT ( 'NONE',  ( 4.967162193818130511, 0.000000000000000000, 0.000000000000000000 ) ) ;
#20843=CARTESIAN_POINT ( 'NONE',  ( 5.959547316686252039, -10.25972575517542396, 17.77749189599199653 ) ) ;
#20849=ORIENTED_EDGE ( 'NONE', *, *, #37047, .F. ) ;
#20851=CARTESIAN_POINT ( 'NONE',  ( 4.963659409799330291, -40.34793212403957341, -19.36487359954742971 ) ) ;
#20853=ADVANCED_FACE ( 'NONE', ( #1513 ), #14037, .F. ) ;
#20856=CARTESIAN_POINT ( 'NONE',  ( 0.5834872094924180574, 46.32218741137614160, -12.17696997821474625 ) ) ;
#20858=EDGE_CURVE ( 'NONE', #41370, #3302, #19197, .T. ) ;
#20864=CARTESIAN_POINT ( 'NONE',  ( 4.303969348037246512, 35.51084504003240738, -32.45857549159264721 ) ) ;
#20867=CARTESIAN_POINT ( 'NONE',  ( 2.526552050251864134, -4.405466163647019151, -42.75269566045970748 ) ) ;
#20875=ORIENTED_EDGE ( 'NONE', *, *, #22373, .T. ) ;
#20877=CARTESIAN_POINT ( 'NONE',  ( 5.960721111146673579, 17.77882586010667154, -10.25731071096564051 ) ) ;
#20880=CARTESIAN_POINT ( 'NONE',  ( 5.958863334805807099, -16.28483817244731213, -12.49425770716481487 ) ) ;
#20881=EDGE_CURVE ( 'NONE', #51998, #56250, #1604, .T. ) ;
#20896=ORIENTED_EDGE ( 'NONE', *, *, #13784, .F. ) ;
#20897=CARTESIAN_POINT ( 'NONE',  ( 0.9758171775293918992, 41.44488232057081945, -11.11125068417950601 ) ) ;
#20898=ORIENTED_EDGE ( 'NONE', *, *, #41027, .F. ) ;
#20900=CARTESIAN_POINT ( 'NONE',  ( 5.965394784446460541, 19.82972329408686107, -5.298374383010430400 ) ) ;
#20904=CARTESIAN_POINT ( 'NONE',  ( 0.5839254288179566155, 41.52446060675855222, -23.86932519546686038 ) ) ;
#20905=CARTESIAN_POINT ( 'NONE',  ( 3.783278058412225864, 33.06594414781534397, -27.54892951149511049 ) ) ;
#20921=CARTESIAN_POINT ( 'NONE',  ( 0.5832367798473389042, 5.981481162905716076, 47.52096797443089571 ) ) ;
#20922=EDGE_CURVE ( 'NONE', #57497, #24606, #60375, .T. ) ;
#20936=EDGE_CURVE ( 'NONE', #36860, #36466, #55679, .T. ) ;
#20940=VERTEX_POINT ( 'NONE', #7766 ) ;
#20947=CARTESIAN_POINT ( 'NONE',  ( 5.965394784446458765, -19.82223131420057882, 5.326334832595306601 ) ) ;
#20951=EDGE_CURVE ( 'NONE', #5687, #37326, #18061, .T. ) ;
#20959=DIRECTION ( 'NONE',  ( -0.000000000000000000, 1.000000000000000000, -0.000000000000000000 ) ) ;
#20970=CARTESIAN_POINT ( 'NONE',  ( 5.974727161628367256, 10.27590650342012779, 17.76736931401863373 ) ) ;
#20972=DIRECTION ( 'NONE',  ( 0.000000000000000000, 0.000000000000000000, -1.000000000000000000 ) ) ;
#20974=CARTESIAN_POINT ( 'NONE',  ( 5.959547316686252039, -20.34955788964374790, -2.682663672454841386 ) ) ;
#20977=VERTEX_POINT ( 'NONE', #50080 ) ;
#20978=CARTESIAN_POINT ( 'NONE',  ( 2.526464513654345545, -40.15570173027679601, -15.32058692775033570 ) ) ;
#20988=CARTESIAN_POINT ( 'NONE',  ( 0.5807400328401574052, -12.92266817606047269, 46.12278621143493496 ) ) ;
#20991=CARTESIAN_POINT ( 'NONE',  ( 0.9757954354143110187, -0.03224588977114339200, -42.90846090505964838 ) ) ;
#20993=CARTESIAN_POINT ( 'NONE',  ( 0.5832366564991509073, 33.67434452455960070, -34.05963937630765770 ) ) ;
#20996=ORIENTED_EDGE ( 'NONE', *, *, #28778, .T. ) ;
#21001=VERTEX_POINT ( 'NONE', #21889 ) ;
#21011=LINE ( 'NONE', #40155, #52695 ) ;
#21012=CARTESIAN_POINT ( 'NONE',  ( -19.79687759653248946, -12.45625484602615529, 1.051131599843221132 ) ) ;
#21014=EDGE_CURVE ( 'NONE', #12545, #25700, #49304, .T. ) ;
#21025=CARTESIAN_POINT ( 'NONE',  ( 4.963659409799330291, -3.403493583737023265, -44.62477100936220609 ) ) ;
#21028=CARTESIAN_POINT ( 'NONE',  ( 4.956653778117001252, 45.71126949320271393, -14.93973939759840519 ) ) ;
#21031=CARTESIAN_POINT ( 'NONE',  ( 4.956653778116970166, 36.51451553856417576, 31.29546495791861460 ) ) ;
#21032=CARTESIAN_POINT ( 'NONE',  ( 0.5839879327111922036, 33.93179405280490357, 33.80333292213272500 ) ) ;
#21036=B_SPLINE_CURVE_WITH_KNOTS ( 'NONE', 3,
 ( #23380, #56571, #31861, #55952, #46901, #42507, #8038, #36884, #27150, #51553, #46277, #60639, #3935, #60333, #36568, #37188 ),
 .UNSPECIFIED., .F., .F.,
 ( 4, 3, 3, 3, 3, 4 ),
 ( 1.250973872328959318E-17, 0.0002724568934985507223, 0.0004086836638483677328, 0.0005449104342063536104, 0.0008173270854453667817, 0.001089761613562691177 ),
 .UNSPECIFIED. ) ;
#21041=CARTESIAN_POINT ( 'NONE',  ( 0.9972139404380286898, -4.947665363829067076, 42.62325912566431896 ) ) ;
#21047=CARTESIAN_POINT ( 'NONE',  ( 0.5809828226811617480, -41.20389530892290253, -24.41822904836968178 ) ) ;
#21049=CONICAL_SURFACE ( 'NONE', #49931, 43.08621763946400307, 1.568696531533066763 ) ;
#21051=VERTEX_POINT ( 'NONE', #8693 ) ;
#21052=ORIENTED_EDGE ( 'NONE', *, *, #6981, .T. ) ;
#21053=CARTESIAN_POINT ( 'NONE',  ( 0.9758171775293916772, -5.594812732687391765, 42.54217005300509413 ) ) ;
#21055=CARTESIAN_POINT ( 'NONE',  ( 3.270143674763207553, -7.080034332678346587, 11.71453292426876835 ) ) ;
#21060=CARTESIAN_POINT ( 'NONE',  ( 4.967162193818130511, 42.16965968614205451, -8.839793687084773310 ) ) ;
#21061=ORIENTED_EDGE ( 'NONE', *, *, #15989, .T. ) ;
#21065=CARTESIAN_POINT ( 'NONE',  ( 3.407937589446178528, -7.243367523630944049, -11.62731850632891550 ) ) ;
#21068=CARTESIAN_POINT ( 'NONE',  ( 4.956653778116996811, 40.28700667097716348, -26.26162724282331951 ) ) ;
#21071=CARTESIAN_POINT ( 'NONE',  ( 3.660176727303348532, -16.63097650367944880, -45.06760739764693824 ) ) ;
#21072=ORIENTED_EDGE ( 'NONE', *, *, #40830, .T. ) ;
#21089=CARTESIAN_POINT ( 'NONE',  ( 4.967162193818130511, 2.375726030842579828, 43.02067033766019932 ) ) ;
#21096=CARTESIAN_POINT ( 'NONE',  ( 0.7762783648524370639, 29.86325223097011161, 37.45705264446588956 ) ) ;
#21097=CARTESIAN_POINT ( 'NONE',  ( 1.088908134280558659, 29.78762923590010914, -30.89124834763357796 ) ) ;
#21099=CARTESIAN_POINT ( 'NONE',  ( 2.624215991343608501, -47.76052319582219496, 4.864192649745223918 ) ) ;
#21100=CARTESIAN_POINT ( 'NONE',  ( 5.959547316686252039, -2.675599016784684814, 20.35048796920732173 ) ) ;
#21109=DIRECTION ( 'NONE',  ( 0.000000000000000000, 0.000000000000000000, 1.000000000000000000 ) ) ;
#21117=ORIENTED_EDGE ( 'NONE', *, *, #19180, .T. ) ;
#21138=CARTESIAN_POINT ( 'NONE',  ( 0.5838002273316434954, 12.52789267095249492, -46.22850660674009049 ) ) ;
#21142=( BOUNDED_SURFACE ( )  B_SPLINE_SURFACE ( 3, 1, ( 
 ( #25956, #50071 ),
 ( #7128, #26255 ),
 ( #45394, #35999 ),
 ( #55060, #31272 ) ),
 .UNSPECIFIED., .F., .F., .F. ) 
 B_SPLINE_SURFACE_WITH_KNOTS ( ( 4, 4 ),
 ( 2, 2 ),
 ( 0.000000000000000000, 1.000000000000000000 ),
 ( 0.000000000000000000, 1.000000000000000000 ),
 .UNSPECIFIED. ) 
 GEOMETRIC_REPRESENTATION_ITEM ( )  RATIONAL_B_SPLINE_SURFACE ( (
 ( 1.000000000000000000, 1.000000000000000000),
 ( 0.9732289882329797637, 0.9999525324661233672),
 ( 0.9732289882329797637, 0.9999525324661233672),
 ( 1.000000000000000000, 1.000000000000000000) ) ) 
 REPRESENTATION_ITEM ( '' )  SURFACE ( )  );
#21147=CARTESIAN_POINT ( 'NONE',  ( 5.958863334805807099, 20.52565293643016275, -0.001220270595957195347 ) ) ;
#21148=EDGE_CURVE ( 'NONE', #31436, #6995, #53449, .T. ) ;
#21152=CARTESIAN_POINT ( 'NONE',  ( 1.227938101723748288, 36.73927144310511750, 22.18841447410732215 ) ) ;
#21157=CARTESIAN_POINT ( 'NONE',  ( 5.965394784446458765, -20.34787558161488974, 2.693446924985283264 ) ) ;
#21164=CARTESIAN_POINT ( 'NONE',  ( 0.5836750258453372586, 37.88760409476694235, 29.30109045202400608 ) ) ;
#21167=VERTEX_POINT ( 'NONE', #49078 ) ;
#21168=CARTESIAN_POINT ( 'NONE',  ( 5.860006189529234355, 36.25227510158507727, -31.81514841426720608 ) ) ;
#21174=CARTESIAN_POINT ( 'NONE',  ( 5.960721111146673579, 20.34914600876575363, -2.685391721745826299 ) ) ;
#21179=B_SPLINE_CURVE_WITH_KNOTS ( 'NONE', 3,
 ( #9815, #35730, #11928, #51025, #12229, #36648, #26301, #59494, #20991, #50115 ),
 .UNSPECIFIED., .F., .F.,
 ( 4, 3, 3, 4 ),
 ( 4.878909776184769953E-18, 0.0002724573126191764060, 0.0004086839781548492903, 0.0005054209210070093961 ),
 .UNSPECIFIED. ) ;
#21180=CARTESIAN_POINT ( 'NONE',  ( 4.956653778116991482, 20.77844580450620526, -43.37017594958032873 ) ) ;
#21182=ORIENTED_EDGE ( 'NONE', *, *, #36378, .T. ) ;
#21184=CARTESIAN_POINT ( 'NONE',  ( 0.9972139404380327976, 42.45145681504345703, -6.252633471302944557 ) ) ;
#21186=DIRECTION ( 'NONE',  ( 0.000000000000000000, 0.000000000000000000, 1.000000000000000000 ) ) ;
#21188=CARTESIAN_POINT ( 'NONE',  ( 0.5807400328401574052, -11.87003418057210880, -46.40483864045157958 ) ) ;
#21198=VERTEX_POINT ( 'NONE', #6131 ) ;
#21206=VERTEX_POINT ( 'NONE', #49379 ) ;
#21217=ORIENTED_EDGE ( 'NONE', *, *, #13655, .F. ) ;
#21219=ORIENTED_EDGE ( 'NONE', *, *, #44239, .F. ) ;
#21220=CARTESIAN_POINT ( 'NONE',  ( 5.959547316686252039, -5.308980600728594013, 19.82715097195153220 ) ) ;
#21223=CARTESIAN_POINT ( 'NONE',  ( 0.8557997880470606944, 19.17299735372068525, -43.90420959842161608 ) ) ;
#21225=( BOUNDED_SURFACE ( )  B_SPLINE_SURFACE ( 3, 1, ( 
 ( #1928, #45201 ),
 ( #54536, #60479 ),
 ( #50782, #11663 ),
 ( #50478, #12600 ) ),
 .UNSPECIFIED., .F., .F., .F. ) 
 B_SPLINE_SURFACE_WITH_KNOTS ( ( 4, 4 ),
 ( 2, 2 ),
 ( 0.000000000000000000, 1.000000000000000000 ),
 ( 0.000000000000000000, 1.000000000000000000 ),
 .UNSPECIFIED. ) 
 GEOMETRIC_REPRESENTATION_ITEM ( )  RATIONAL_B_SPLINE_SURFACE ( (
 ( 1.000000000000000000, 1.000000000000000000),
 ( 0.9953390228620291325, 0.8624445117761032620),
 ( 0.9953390228620291325, 0.8624445117761032620),
 ( 1.000000000000000000, 1.000000000000000000) ) ) 
 REPRESENTATION_ITEM ( '' )  SURFACE ( )  );
#21228=ORIENTED_EDGE ( 'NONE', *, *, #53938, .T. ) ;
#21230=EDGE_CURVE ( 'NONE', #36314, #36654, #12719, .T. ) ;
#21231=CARTESIAN_POINT ( 'NONE',  ( 0.8551540677456739292, 47.90804413217340851, 0.9122407826477398896 ) ) ;
#21233=ORIENTED_EDGE ( 'NONE', *, *, #9414, .T. ) ;
#21234=B_SPLINE_CURVE_WITH_KNOTS ( 'NONE', 3,
 ( #39083, #44697, #16177, #30561 ),
 .UNSPECIFIED., .F., .F.,
 ( 4, 4 ),
 ( 0.000000000000000000, 0.004444878191957686922 ),
 .UNSPECIFIED. ) ;
#21238=CIRCLE ( 'NONE', #49218, 43.08621763946400307 ) ;
#21243=DIRECTION ( 'NONE',  ( 0.07439287786467664587, -0.6174937095821814159, 0.7830499462674445077 ) ) ;
#21253=CARTESIAN_POINT ( 'NONE',  ( -48.95476116535499500, 0.000000000000000000, 0.000000000000000000 ) ) ;
#21257=( BOUNDED_SURFACE ( )  B_SPLINE_SURFACE ( 3, 1, ( 
 ( #19774, #49491 ),
 ( #38894, #16295 ),
 ( #6545, #35418 ),
 ( #1869, #25379 ) ),
 .UNSPECIFIED., .F., .F., .F. ) 
 B_SPLINE_SURFACE_WITH_KNOTS ( ( 4, 4 ),
 ( 2, 2 ),
 ( 0.000000000000000000, 1.000000000000000000 ),
 ( 0.000000000000000000, 1.000000000000000000 ),
 .UNSPECIFIED. ) 
 GEOMETRIC_REPRESENTATION_ITEM ( )  RATIONAL_B_SPLINE_SURFACE ( (
 ( 1.000000000000000000, 1.000000000000000000),
 ( 0.9953390228620291325, 0.8624445117761032620),
 ( 0.9953390228620291325, 0.8624445117761032620),
 ( 1.000000000000000000, 1.000000000000000000) ) ) 
 REPRESENTATION_ITEM ( '' )  SURFACE ( )  );
#21259=CARTESIAN_POINT ( 'NONE',  ( 0.5809828226811556418, -5.711058609465654357, 47.55412398569204413 ) ) ;
#21260=CARTESIAN_POINT ( 'NONE',  ( 0.5850706913938533704, -18.49682194437995975, 44.18063951072215190 ) ) ;
#21264=DIRECTION ( 'NONE',  ( 0.07836865515943411409, 0.2503967164834395298, 0.9649662368512245125 ) ) ;
#21265=CARTESIAN_POINT ( 'NONE',  ( 0.5809828226811617480, -47.41188724015875522, -6.791453954330822107 ) ) ;
#21271=B_SPLINE_CURVE_WITH_KNOTS ( 'NONE', 3,
 ( #11197, #2071, #1768, #40042, #49395, #54693, #25589, #6448, #20897, #16203, #35944, #54382, #11828, #59401, #7078, #26203, #45344, #37482, #23063 ),
 .UNSPECIFIED., .F., .F.,
 ( 4, 3, 3, 3, 3, 3, 4 ),
 ( 5.204170427930421283E-18, 0.0002724573126191728281, 0.0004086839781548437609, 0.0005449106435901761736, 0.0006811373090491400738, 0.0008459866663933635197, 0.001010840725717212065 ),
 .UNSPECIFIED. ) ;
#21272=CARTESIAN_POINT ( 'NONE',  ( 2.281448460670572942, 17.13756432392898077, -44.80776276180753825 ) ) ;
#21273=ORIENTED_EDGE ( 'NONE', *, *, #28979, .T. ) ;
#21276=CARTESIAN_POINT ( 'NONE',  ( 0.9736507210033050752, 16.83559693395318391, -39.46762617149617824 ) ) ;
#21279=EDGE_CURVE ( 'NONE', #15433, #23834, #16523, .T. ) ;
#21283=B_SPLINE_CURVE_WITH_KNOTS ( 'NONE', 3,
 ( #26581, #59465, #59789, #7451, #30980, #60092 ),
 .UNSPECIFIED., .F., .F.,
 ( 4, 2, 4 ),
 ( 7.757919228897728493E-18, 0.0002291978881530210932, 0.0004583957763060344344 ),
 .UNSPECIFIED. ) ;
#21287=CARTESIAN_POINT ( 'NONE',  ( 0.8551540677456834771, -0.9122407826472416215, -47.90804413217341562 ) ) ;
#21288=CARTESIAN_POINT ( 'NONE',  ( 0.8557997880470599172, 7.156447707086380561, -47.37054680076698077 ) ) ;
#21290=CARTESIAN_POINT ( 'NONE',  ( 5.965394784446458765, -12.50653125158996204, -16.27505370423077125 ) ) ;
#21291=ORIENTED_EDGE ( 'NONE', *, *, #56859, .F. ) ;
#21304=B_SPLINE_CURVE_WITH_KNOTS ( 'NONE', 3,
 ( #35565, #24924, #1385, #20524 ),
 .UNSPECIFIED., .F., .F.,
 ( 4, 4 ),
 ( 0.000000000000000000, 0.005004741218457415403 ),
 .UNSPECIFIED. ) ;
#21311=ADVANCED_FACE ( 'NONE', ( #30887 ), #10528, .F. ) ;
#21312=ORIENTED_EDGE ( 'NONE', *, *, #3597, .T. ) ;
#21321=ORIENTED_EDGE ( 'NONE', *, *, #34521, .F. ) ;
#21333=CARTESIAN_POINT ( 'NONE',  ( 5.960721111146673579, -16.28787783074235662, 12.49016043756443750 ) ) ;
#21335=CARTESIAN_POINT ( 'NONE',  ( 0.5786265663353153954, -47.39171391660397603, 6.967625775955545109 ) ) ;
#21337=CARTESIAN_POINT ( 'NONE',  ( 1.154321713695926732, -37.57248787340954266, 20.73950268329812374 ) ) ;
#21339=CARTESIAN_POINT ( 'NONE',  ( 0.5263152470540364281, 0.000000000000000000, 0.000000000000000000 ) ) ;
#21366=VECTOR ( 'NONE', #36368, 1000.000000000000114 ) ;
#21369=EDGE_CURVE ( 'NONE', #36409, #30700, #14523, .T. ) ;
#21384=CARTESIAN_POINT ( 'NONE',  ( 0.5839880159502349732, -46.25220722086336167, -12.44022138820733936 ) ) ;
#21387=CARTESIAN_POINT ( 'NONE',  ( 0.5809828226811626362, 29.58751527316234231, -37.66417181417519799 ) ) ;
#21390=CARTESIAN_POINT ( 'NONE',  ( 4.963659409799330291, 24.46566636552876517, -37.47512675766667911 ) ) ;
#21392=CARTESIAN_POINT ( 'NONE',  ( 4.956653778116987041, -47.27023054223747067, -8.845409907521421644 ) ) ;
#21401=CARTESIAN_POINT ( 'NONE',  ( 0.5800708119828335008, 0.6275298934114975635, 47.89175345941821149 ) ) ;
#21407=CARTESIAN_POINT ( 'NONE',  ( 4.303969348037246512, -47.93217632892351077, 4.133486515473138390 ) ) ;
#21409=CARTESIAN_POINT ( 'NONE',  ( 0.8551540677456834771, 44.61036085020950992, 17.49081417858803533 ) ) ;
#21412=LINE ( 'NONE', #12043, #61332 ) ;
#21414=B_SPLINE_CURVE_WITH_KNOTS ( 'NONE', 3,
 ( #2964, #22088, #54646, #59981, #21780, #30855 ),
 .UNSPECIFIED., .F., .F.,
 ( 4, 2, 4 ),
 ( 0.000000000000000000, 0.0002291966416970778317, 0.0004583932833941556633 ),
 .UNSPECIFIED. ) ;
#21417=CARTESIAN_POINT ( 'NONE',  ( 3.660087539127329759, -20.10768839917373541, -43.62750476736573546 ) ) ;
#21418=CARTESIAN_POINT ( 'NONE',  ( 4.963659409799330291, -44.68724496494572662, -2.450325214228857629 ) ) ;
#21419=ORIENTED_EDGE ( 'NONE', *, *, #60740, .F. ) ;
#21421=ORIENTED_EDGE ( 'NONE', *, *, #11279, .F. ) ;
#21423=CARTESIAN_POINT ( 'NONE',  ( 5.959828726073459926, 5.308046411394975017, 19.82738831247215217 ) ) ;
#21427=CARTESIAN_POINT ( 'NONE',  ( 0.5819845901640493535, 47.89381229371849713, 0.4540519722832492833 ) ) ;
#21443=CARTESIAN_POINT ( 'NONE',  ( 5.960721111146673579, 14.51823969584099672, -14.50930005615001583 ) ) ;
#21450=CARTESIAN_POINT ( 'NONE',  ( 4.956653778116973719, 21.75875759808707244, 42.88673967249138741 ) ) ;
#21451=CARTESIAN_POINT ( 'NONE',  ( 0.9754642270333678811, -21.30186789325730601, -37.24735125696678040 ) ) ;
#21453=VERTEX_POINT ( 'NONE', #56232 ) ;
#21454=CARTESIAN_POINT ( 'NONE',  ( 5.958863334805807099, 20.52565293643016275, 0.001220270596240801819 ) ) ;
#21455=CARTESIAN_POINT ( 'NONE',  ( 0.8551540677456715978, -5.348818140990585057, -47.61725548905996419 ) ) ;
#21467=CARTESIAN_POINT ( 'NONE',  ( 0.9756008150404607004, -5.741579752919358626, -42.52260101821270410 ) ) ;
#21468=CARTESIAN_POINT ( 'NONE',  ( 5.959547316686252039, -5.315863417546194292, -19.82530672674360517 ) ) ;
#21471=FACE_OUTER_BOUND ( 'NONE', #28535, .T. ) ;
#21472=VERTEX_POINT ( 'NONE', #56845 ) ;
#21483=CARTESIAN_POINT ( 'NONE',  ( 5.974727161628367256, -5.327229920347289926, -19.82156119440443476 ) ) ;
#21485=ORIENTED_EDGE ( 'NONE', *, *, #677, .F. ) ;
#21491=CARTESIAN_POINT ( 'NONE',  ( 0.5807400328401637335, 44.45848844984443815, 17.82553128098424366 ) ) ;
#21492=DIRECTION ( 'NONE',  ( -1.000000000000000000, -0.000000000000000000, -0.000000000000000000 ) ) ;
#21494=( BOUNDED_SURFACE ( )  B_SPLINE_SURFACE ( 3, 1, ( 
 ( #58406, #29922 ),
 ( #49032, #48117 ),
 ( #23995, #24301 ),
 ( #53700, #29609 ) ),
 .UNSPECIFIED., .F., .F., .F. ) 
 B_SPLINE_SURFACE_WITH_KNOTS ( ( 4, 4 ),
 ( 2, 2 ),
 ( 0.000000000000000000, 1.000000000000000000 ),
 ( 0.000000000000000000, 1.000000000000000000 ),
 .UNSPECIFIED. ) 
 GEOMETRIC_REPRESENTATION_ITEM ( )  RATIONAL_B_SPLINE_SURFACE ( (
 ( 1.000000000000000000, 1.000000000000000000),
 ( 0.9732289882329797637, 0.9999525324661233672),
 ( 0.9732289882329797637, 0.9999525324661233672),
 ( 1.000000000000000000, 1.000000000000000000) ) ) 
 REPRESENTATION_ITEM ( '' )  SURFACE ( )  );
#21499=CARTESIAN_POINT ( 'NONE',  ( 0.5809828226811553087, -44.03860873105708151, 18.83114015454682999 ) ) ;
#21500=AXIS2_PLACEMENT_3D ( 'NONE', #9313, #519, #14655 ) ;
#21501=DIRECTION ( 'NONE',  ( 0.07836865515943411409, 0.9968932487286222832, 0.007886984708667934760 ) ) ;
#21508=CARTESIAN_POINT ( 'NONE',  ( 2.526464513654345545, -33.34586834545791589, 27.11556434133536087 ) ) ;
#21509=ORIENTED_EDGE ( 'NONE', *, *, #3288, .T. ) ;
#21513=VERTEX_POINT ( 'NONE', #49301 ) ;
#21521=FACE_OUTER_BOUND ( 'NONE', #11813, .T. ) ;
#21522=EDGE_CURVE ( 'NONE', #18062, #46608, #6005, .T. ) ;
#21526=ORIENTED_EDGE ( 'NONE', *, *, #39856, .F. ) ;
#21531=CARTESIAN_POINT ( 'NONE',  ( 0.9722240750034564227, 26.58024222649045498, 33.68410530487882681 ) ) ;
#21537=CARTESIAN_POINT ( 'NONE',  ( 3.407937589446174087, 12.82481284928210563, -4.815089211104917943 ) ) ;
#21542=VERTEX_POINT ( 'NONE', #54288 ) ;
#21543=CARTESIAN_POINT ( 'NONE',  ( 3.660176727303402711, 16.63097650367969749, 45.06760739764692403 ) ) ;
#21544=CARTESIAN_POINT ( 'NONE',  ( 5.959828726073459926, 19.82504517499712904, -5.316791119500882346 ) ) ;
#21551=EDGE_LOOP ( 'NONE', ( #52408, #6884, #53166, #48417 ) ) ;
#21552=CARTESIAN_POINT ( 'NONE',  ( 0.6067375320500746350, -23.33187539052098813, -41.82999795871630511 ) ) ;
#21555=VECTOR ( 'NONE', #11646, 1000.000000000000114 ) ;
#21556=CARTESIAN_POINT ( 'NONE',  ( 5.960721111146673579, -7.848955554238637333, 18.96557324978273940 ) ) ;
#21566=CARTESIAN_POINT ( 'NONE',  ( 0.5807400328401574052, -33.48217046439087596, -34.25275203086270182 ) ) ;
#21569=CARTESIAN_POINT ( 'NONE',  ( 4.967162193818131399, -35.57684288741960899, -24.30453456948146851 ) ) ;
#21577=CARTESIAN_POINT ( 'NONE',  ( 0.9730545539215883499, 37.40983423658472873, 21.01499094264562473 ) ) ;
#21580=CARTESIAN_POINT ( 'NONE',  ( 0.9754642270333698795, -25.98138239028835628, -34.14824330022355525 ) ) ;
#21581=CARTESIAN_POINT ( 'NONE',  ( 0.7762783648524387292, 28.45155609988383461, -38.54028518467388409 ) ) ;
#21584=EDGE_CURVE ( 'NONE', #12427, #35241, #33695, .T. ) ;
#21601=VERTEX_POINT ( 'NONE', #58074 ) ;
#21607=ORIENTED_EDGE ( 'NONE', *, *, #54028, .F. ) ;
#21610=CARTESIAN_POINT ( 'NONE',  ( 0.5263152470540346517, 0.000000000000000000, 0.000000000000000000 ) ) ;
#21614=CARTESIAN_POINT ( 'NONE',  ( 0.9754642270333685472, 10.93570046136908402, 41.49150764699761140 ) ) ;
#21618=ORIENTED_EDGE ( 'NONE', *, *, #4533, .F. ) ;
#21619=CARTESIAN_POINT ( 'NONE',  ( 0.9745511491811743587, 34.24777528633319434, -25.84997388131824891 ) ) ;
#21620=( BOUNDED_SURFACE ( )  B_SPLINE_SURFACE ( 3, 1, ( 
 ( #25216, #54622 ),
 ( #35255, #15521 ),
 ( #39653, #49954 ),
 ( #30835, #59333 ) ),
 .UNSPECIFIED., .F., .F., .F. ) 
 B_SPLINE_SURFACE_WITH_KNOTS ( ( 4, 4 ),
 ( 2, 2 ),
 ( 0.000000000000000000, 1.000000000000000000 ),
 ( 0.000000000000000000, 1.000000000000000000 ),
 .UNSPECIFIED. ) 
 GEOMETRIC_REPRESENTATION_ITEM ( )  RATIONAL_B_SPLINE_SURFACE ( (
 ( 1.000000000000000000, 1.000000000000000000),
 ( 0.7269869731126817891, 0.9931720237060910339),
 ( 0.7269869731126817891, 0.9931720237060910339),
 ( 1.000000000000000000, 1.000000000000000000) ) ) 
 REPRESENTATION_ITEM ( '' )  SURFACE ( )  );
#21626=CARTESIAN_POINT ( 'NONE',  ( -20.00618396018216671, -12.48880663681880954, -0.5456665274875781568 ) ) ;
#21628=CARTESIAN_POINT ( 'NONE',  ( 4.967162193818130511, -40.93989340068619498, 13.42934394584149871 ) ) ;
#21629=VERTEX_POINT ( 'NONE', #6057 ) ;
#21632=CARTESIAN_POINT ( 'NONE',  ( 5.974727161628369032, -20.35137732084678319, 2.663664384318439105 ) ) ;
#21634=LINE ( 'NONE', #36676, #23808 ) ;
#21636=CARTESIAN_POINT ( 'NONE',  ( 0.9754402186311952327, 21.29160191075049369, -37.25324696807206237 ) ) ;
#21643=CARTESIAN_POINT ( 'NONE',  ( 0.9758171775293921213, 37.15687890897648771, -21.45936886481755934 ) ) ;
#21645=CARTESIAN_POINT ( 'NONE',  ( 5.959828726073459926, 18.96145866559671589, -7.858992891709945638 ) ) ;
#21647=CARTESIAN_POINT ( 'NONE',  ( 0.8557997880470599172, 47.89938907511594124, 0.9121262075947815795 ) ) ;
#21649=CARTESIAN_POINT ( 'NONE',  ( 5.860006189529246790, 15.52021937683337605, -45.66786516969914800 ) ) ;
#21651=AXIS2_PLACEMENT_3D ( 'NONE', #3673, #13732, #51600 ) ;
#21653=CARTESIAN_POINT ( 'NONE',  ( 4.967162193818130511, -7.970725651239513709, -42.34252806656601820 ) ) ;
#21658=CARTESIAN_POINT ( 'NONE',  ( 3.783278058412226308, -42.86118820526427697, -3.901118461247271352 ) ) ;
#21662=CARTESIAN_POINT ( 'NONE',  ( 0.6067375320500733027, -33.36326114377794028, -34.36594163291744053 ) ) ;
#21663=CARTESIAN_POINT ( 'NONE',  ( 0.8557997880470599172, -41.02602466100761802, -24.73961900479294584 ) ) ;
#21668=CARTESIAN_POINT ( 'NONE',  ( 0.9752570700956808558, -5.829291291128961383, 42.51066151201238341 ) ) ;
#21682=ORIENTED_EDGE ( 'NONE', *, *, #14938, .T. ) ;
#21687=CARTESIAN_POINT ( 'NONE',  ( 0.9756950546413937220, 26.19769393035369021, 33.98259063592730200 ) ) ;
#21710=CARTESIAN_POINT ( 'NONE',  ( 1.154321713695928509, 4.782433421670080342, 42.64911660416108674 ) ) ;
#21727=CARTESIAN_POINT ( 'NONE',  ( 0.5809828226811553087, -18.83114015454665946, -44.03860873105715967 ) ) ;
#21728=CARTESIAN_POINT ( 'NONE',  ( 0.9730545539215883499, 6.101350888305258735, -42.47233286818610054 ) ) ;
#21746=EDGE_CURVE ( 'NONE', #10214, #37705, #42558, .T. ) ;
#21749=VECTOR ( 'NONE', #1829, 1000.000000000000114 ) ;
#21757=DIRECTION ( 'NONE',  ( -0.07439287786467650709, 0.9597484305373229496, -0.2708295585864967658 ) ) ;
#21764=CARTESIAN_POINT ( 'NONE',  ( 5.959547316686252039, 7.851524054666140451, 18.96456592444103606 ) ) ;
#21769=( BOUNDED_SURFACE ( )  B_SPLINE_SURFACE ( 3, 1, ( 
 ( #59793, #12823 ),
 ( #46332, #21900 ),
 ( #55387, #2459 ),
 ( #17203, #31916 ) ),
 .UNSPECIFIED., .F., .F., .F. ) 
 B_SPLINE_SURFACE_WITH_KNOTS ( ( 4, 4 ),
 ( 2, 2 ),
 ( 0.000000000000000000, 1.000000000000000000 ),
 ( 0.000000000000000000, 1.000000000000000000 ),
 .UNSPECIFIED. ) 
 GEOMETRIC_REPRESENTATION_ITEM ( )  RATIONAL_B_SPLINE_SURFACE ( (
 ( 1.000000000000000000, 1.000000000000000000),
 ( 0.9953390228620291325, 0.8624445117761032620),
 ( 0.9953390228620291325, 0.8624445117761032620),
 ( 1.000000000000000000, 1.000000000000000000) ) ) 
 REPRESENTATION_ITEM ( '' )  SURFACE ( )  );
#21771=ORIENTED_EDGE ( 'NONE', *, *, #34883, .F. ) ;
#21775=EDGE_CURVE ( 'NONE', #10287, #59424, #61160, .T. ) ;
#21776=CARTESIAN_POINT ( 'NONE',  ( 0.8557997880470599172, -0.9121262075949487791, 47.89938907511593413 ) ) ;
#21780=CARTESIAN_POINT ( 'NONE',  ( 1.154321713695927398, -15.65787958845389305, -39.95809834491020496 ) ) ;
#21784=CARTESIAN_POINT ( 'NONE',  ( 0.9756950546413942771, -5.696573146291698642, -42.52863374229713145 ) ) ;
#21805=ORIENTED_EDGE ( 'NONE', *, *, #5343, .F. ) ;
#21807=CARTESIAN_POINT ( 'NONE',  ( 0.9730545539215883499, 42.47233286818625686, -6.101350888304211573 ) ) ;
#21811=DIRECTION ( 'NONE',  ( 0.000000000000000000, 0.000000000000000000, 1.000000000000000000 ) ) ;
#21842=ORIENTED_EDGE ( 'NONE', *, *, #38177, .T. ) ;
#21851=CARTESIAN_POINT ( 'NONE',  ( 0.5786265663353153954, 33.35675271369586881, -34.37803667029777444 ) ) ;
#21859=CARTESIAN_POINT ( 'NONE',  ( 0.9730545539215883499, -30.69604515769671949, 29.98130006528850444 ) ) ;
#21862=EDGE_CURVE ( 'NONE', #1609, #30886, #50741, .T. ) ;
#21873=FACE_OUTER_BOUND ( 'NONE', #46415, .T. ) ;
#21882=CARTESIAN_POINT ( 'NONE',  ( 5.958863334805807099, 7.853699934219900314, -18.96369761673811638 ) ) ;
#21889=CARTESIAN_POINT ( 'NONE',  ( 1.227938101723748288, -41.23019537246701560, -11.92353943227992197 ) ) ;
#21890=CARTESIAN_POINT ( 'NONE',  ( 0.5800708057587400379, -47.40012370174856926, -6.873290064481863304 ) ) ;
#21891=( BOUNDED_SURFACE ( )  B_SPLINE_SURFACE ( 3, 1, ( 
 ( #39003, #58359 ),
 ( #12646, #50523 ),
 ( #2277, #55521 ),
 ( #21100, #45245 ) ),
 .UNSPECIFIED., .F., .F., .F. ) 
 B_SPLINE_SURFACE_WITH_KNOTS ( ( 4, 4 ),
 ( 2, 2 ),
 ( 0.000000000000000000, 1.000000000000000000 ),
 ( 0.000000000000000000, 1.000000000000000000 ),
 .UNSPECIFIED. ) 
 GEOMETRIC_REPRESENTATION_ITEM ( )  RATIONAL_B_SPLINE_SURFACE ( (
 ( 1.000000000000000000, 1.000000000000000000),
 ( 0.9732289882329797637, 0.9999525324661233672),
 ( 0.9732289882329797637, 0.9999525324661233672),
 ( 1.000000000000000000, 1.000000000000000000) ) ) 
 REPRESENTATION_ITEM ( '' )  SURFACE ( )  );
#21899=CARTESIAN_POINT ( 'NONE',  ( 5.965394784446460541, 20.52536205633085231, 0.01447339372460269141 ) ) ;
#21900=CARTESIAN_POINT ( 'NONE',  ( 0.5786265663353196143, -34.37803667029834287, 33.35675271369526484 ) ) ;
#21901=DIRECTION ( 'NONE',  ( 1.000000000000000000, 0.000000000000000000, 0.000000000000000000 ) ) ;
#21903=EDGE_CURVE ( 'NONE', #44595, #30566, #19360, .T. ) ;
#21908=CIRCLE ( 'NONE', #3857, 48.09070567114147110 ) ;
#21926=CARTESIAN_POINT ( 'NONE',  ( 4.956653778116961284, 40.28700667097682953, 26.26162724282386662 ) ) ;
#21932=VERTEX_POINT ( 'NONE', #14808 ) ;
#21940=ADVANCED_FACE ( 'NONE', ( #30117 ), #16956, .F. ) ;
#21958=CARTESIAN_POINT ( 'NONE',  ( 0.9757402383260946888, 37.20221273948040164, -21.38067434779540932 ) ) ;
#21963=CARTESIAN_POINT ( 'NONE',  ( 2.281351352603296245, 7.562287671717891513, -47.37344280316137457 ) ) ;
#21965=CARTESIAN_POINT ( 'NONE',  ( 0.5809828226811553087, 23.47450554821769231, -41.74875432577623258 ) ) ;
#21973=EDGE_LOOP ( 'NONE', ( #3049, #10716, #32723, #2783 ) ) ;
#21975=CARTESIAN_POINT ( 'NONE',  ( 5.860006189529234355, -26.78264244998126742, 40.11385274514673682 ) ) ;
#21978=FACE_OUTER_BOUND ( 'NONE', #48352, .T. ) ;
#22003=ORIENTED_EDGE ( 'NONE', *, *, #53256, .F. ) ;
#22004=CARTESIAN_POINT ( 'NONE',  ( 5.965394784446460541, 12.48356622107654879, 16.29267539192346703 ) ) ;
#22008=CARTESIAN_POINT ( 'NONE',  ( 0.5837374860065636106, -46.31070423340723607, -12.22086613152811196 ) ) ;
#22015=ORIENTED_EDGE ( 'NONE', *, *, #58446, .T. ) ;
#22018=EDGE_CURVE ( 'NONE', #53354, #50613, #52954, .T. ) ;
#22021=B_SPLINE_CURVE_WITH_KNOTS ( 'NONE', 3,
 ( #53971, #38691, #1656, #10473, #57748, #43392, #48372, #19574, #44021, #48677, #20797, #29876, #24572, #16101, #39934, #29568, #58991, #25178, #44320 ),
 .UNSPECIFIED., .F., .F.,
 ( 4, 3, 3, 3, 3, 3, 4 ),
 ( 9.813676791237319219E-18, 0.0002724573126191821523, 0.0004086839781548627887, 0.0005449106435902062060, 0.0006811373090491684799, 0.0008459866663933775059, 0.001010840725717205993 ),
 .UNSPECIFIED. ) ;
#22024=CARTESIAN_POINT ( 'NONE',  ( 4.963659409799330291, 2.450325214228396664, 44.68724496494573373 ) ) ;
#22031=CARTESIAN_POINT ( 'NONE',  ( 0.5786265663353153954, -47.58023467411535279, -5.535668456754443412 ) ) ;
#22036=B_SPLINE_CURVE_WITH_KNOTS ( 'NONE', 3,
 ( #13028, #41529, #60285, #41225 ),
 .UNSPECIFIED., .F., .F.,
 ( 4, 4 ),
 ( 9.757819552369539906E-19, 0.004444878191957645289 ),
 .UNSPECIFIED. ) ;
#22040=ORIENTED_EDGE ( 'NONE', *, *, #11084, .T. ) ;
#22050=VERTEX_POINT ( 'NONE', #35776 ) ;
#22051=ORIENTED_EDGE ( 'NONE', *, *, #7104, .F. ) ;
#22052=DIRECTION ( 'NONE',  ( -1.000000000000000000, -0.000000000000000000, -0.000000000000000000 ) ) ;
#22057=FACE_OUTER_BOUND ( 'NONE', #30813, .T. ) ;
#22058=ADVANCED_FACE ( 'NONE', ( #20733 ), #57697, .F. ) ;
#22062=ORIENTED_EDGE ( 'NONE', *, *, #19734, .T. ) ;
#22063=EDGE_CURVE ( 'NONE', #14998, #55315, #8926, .T. ) ;
#22065=FACE_OUTER_BOUND ( 'NONE', #35233, .T. ) ;
#22068=CARTESIAN_POINT ( 'NONE',  ( 0.9972139404380306882, 20.88226186415282015, -37.48536715150202525 ) ) ;
#22072=CARTESIAN_POINT ( 'NONE',  ( 0.5839880159502345292, 12.44022138820751167, -46.25220722086333325 ) ) ;
#22081=EDGE_CURVE ( 'NONE', #26674, #57948, #7337, .T. ) ;
#22086=CARTESIAN_POINT ( 'NONE',  ( 2.526464513654346433, 37.81242626108694793, 20.43088802552575700 ) ) ;
#22088=CARTESIAN_POINT ( 'NONE',  ( 0.9722240741986374335, -15.88116971565358959, -39.86121768686903977 ) ) ;
#22091=CARTESIAN_POINT ( 'NONE',  ( 0.9741495583595166652, -5.208308905147834622, -42.59115242362814513 ) ) ;
#22101=CARTESIAN_POINT ( 'NONE',  ( 0.8551540677456715978, -46.51172240253112733, -11.51835730326528306 ) ) ;
#22106=CARTESIAN_POINT ( 'NONE',  ( 4.956653778116991482, 20.77844580450620526, -43.37017594958032873 ) ) ;
#22114=VERTEX_POINT ( 'NONE', #33228 ) ;
#22116=CARTESIAN_POINT ( 'NONE',  ( 0.7056555295713323739, -23.21854706865607554, 41.89804573586724956 ) ) ;
#22124=EDGE_LOOP ( 'NONE', ( #1169, #50108, #59833, #54220 ) ) ;
#22126=CARTESIAN_POINT ( 'NONE',  ( 0.9730545539215892381, 39.44597740938061037, 16.88610103448572630 ) ) ;
#22134=( BOUNDED_SURFACE ( )  B_SPLINE_SURFACE ( 3, 1, ( 
 ( #1771, #59717 ),
 ( #7081, #16833 ),
 ( #12142, #31223 ),
 ( #53764, #6149 ) ),
 .UNSPECIFIED., .F., .F., .F. ) 
 B_SPLINE_SURFACE_WITH_KNOTS ( ( 4, 4 ),
 ( 2, 2 ),
 ( 0.000000000000000000, 1.000000000000000000 ),
 ( 0.000000000000000000, 1.000000000000000000 ),
 .UNSPECIFIED. ) 
 GEOMETRIC_REPRESENTATION_ITEM ( )  RATIONAL_B_SPLINE_SURFACE ( (
 ( 1.000000000000000000, 1.000000000000000000),
 ( 0.9732289882329797637, 0.9999525324661233672),
 ( 0.9732289882329797637, 0.9999525324661233672),
 ( 1.000000000000000000, 1.000000000000000000) ) ) 
 REPRESENTATION_ITEM ( '' )  SURFACE ( )  );
#22135=EDGE_CURVE ( 'NONE', #58704, #355, #18579, .T. ) ;
#22143=ORIENTED_EDGE ( 'NONE', *, *, #27421, .T. ) ;
#22151=ORIENTED_EDGE ( 'NONE', *, *, #22530, .F. ) ;
#22152=CARTESIAN_POINT ( 'NONE',  ( 5.981074661064941900, -12.48781255314301397, 16.28853686865577544 ) ) ;
#22161=CARTESIAN_POINT ( 'NONE',  ( 1.154321713695930507, -11.90271797554042976, 41.23280394713391672 ) ) ;
#22169=CARTESIAN_POINT ( 'NONE',  ( 3.783278058412223199, 41.98530666033914827, 9.462251542473966381 ) ) ;
#22170=CARTESIAN_POINT ( 'NONE',  ( 4.956653778116827169, 32.11725092155053574, 35.79382859084104496 ) ) ;
#22173=CARTESIAN_POINT ( 'NONE',  ( 0.8557997880470690211, -46.50333260518550560, -11.51622788066506686 ) ) ;
#22175=CARTESIAN_POINT ( 'NONE',  ( 0.9752132459055847802, -30.17566824627268218, 30.50512806189400550 ) ) ;
#22176=CARTESIAN_POINT ( 'NONE',  ( 0.9968887458511644928, 42.90440775986218114, 0.6574002966409985271 ) ) ;
#22180=CARTESIAN_POINT ( 'NONE',  ( 0.5807400328401637335, 23.47602859900714023, 41.75144119563894662 ) ) ;
#22188=CARTESIAN_POINT ( 'NONE',  ( 0.9754642270333679921, -39.70914670678644853, 16.25787253057921689 ) ) ;
#22192=CARTESIAN_POINT ( 'NONE',  ( 4.956653778116966613, 0.000000000000000000, 0.000000000000000000 ) ) ;
#22201=CARTESIAN_POINT ( 'NONE',  ( 0.9736507210033057413, -39.46762617149622798, -16.83559693395306311 ) ) ;
#22203=ORIENTED_EDGE ( 'NONE', *, *, #24470, .T. ) ;
#22204=EDGE_CURVE ( 'NONE', #23496, #47332, #53872, .T. ) ;
#22226=B_SPLINE_CURVE_WITH_KNOTS ( 'NONE', 3,
 ( #53396, #53094, #28369, #19607, #38728, #787 ),
 .UNSPECIFIED., .F., .F.,
 ( 4, 2, 4 ),
 ( 1.738108305489988542E-18, 0.0002291966416970804066, 0.0004583932833941590785 ),
 .UNSPECIFIED. ) ;
#22230=ORIENTED_EDGE ( 'NONE', *, *, #24282, .T. ) ;
#22232=CARTESIAN_POINT ( 'NONE',  ( 0.8557997880470697982, 11.51622788066522851, -46.50333260518546297 ) ) ;
#22237=ORIENTED_EDGE ( 'NONE', *, *, #51749, .F. ) ;
#22240=CARTESIAN_POINT ( 'NONE',  ( 4.956653778116992370, 3.690426056930664611, -47.94889704119048446 ) ) ;
#22241=VERTEX_POINT ( 'NONE', #20356 ) ;
#22252=CARTESIAN_POINT ( 'NONE',  ( 4.967162193818130511, 40.93989340068610261, 13.42934394584178648 ) ) ;
#22253=ORIENTED_EDGE ( 'NONE', *, *, #57953, .T. ) ;
#22254=B_SPLINE_CURVE_WITH_KNOTS ( 'NONE', 3,
 ( #15537, #5785, #34641, #1102, #44074, #24937, #53110, #5484, #20240, #24622, #39354, #43758, #39053, #58110, #15231, #58413 ),
 .UNSPECIFIED., .F., .F.,
 ( 4, 3, 3, 3, 3, 4 ),
 ( 1.250973872328959318E-17, 0.0002724568934985518065, 0.0004086836638483732080, 0.0005449104342063575135, 0.0008173270854453600597, 0.001089761613562685756 ),
 .UNSPECIFIED. ) ;
#22256=CARTESIAN_POINT ( 'NONE',  ( 0.9749527285493297946, -34.21468599366731667, 25.89384247702557929 ) ) ;
#22262=DIRECTION ( 'NONE',  ( -0.07439287786467650709, 0.2453289374370270781, -0.9665813013808153276 ) ) ;
#22275=CARTESIAN_POINT ( 'NONE',  ( 5.960221823109900008, -18.96526051813986413, 7.849768660536222242 ) ) ;
#22277=CARTESIAN_POINT ( 'NONE',  ( 0.5809828226811617480, 44.45562576850627323, -17.82437196699632054 ) ) ;
#22284=CARTESIAN_POINT ( 'NONE',  ( 0.9752570700956806338, -41.38610171411350080, -11.32817567195955810 ) ) ;
#22285=EDGE_CURVE ( 'NONE', #1532, #49867, #52440, .T. ) ;
#22287=ORIENTED_EDGE ( 'NONE', *, *, #53780, .T. ) ;
#22289=ORIENTED_EDGE ( 'NONE', *, *, #49945, .T. ) ;
#22290=EDGE_CURVE ( 'NONE', #35128, #22938, #34493, .T. ) ;
#22294=CARTESIAN_POINT ( 'NONE',  ( 5.958863334805807099, -0.001220270596028860026, -20.52565293643016275 ) ) ;
#22310=CARTESIAN_POINT ( 'NONE',  ( 0.9756008150404595902, -42.90824081423206593, 0.1421465480001363191 ) ) ;
#22314=ORIENTED_EDGE ( 'NONE', *, *, #20936, .F. ) ;
#22315=CARTESIAN_POINT ( 'NONE',  ( 0.5827359174754822568, -46.16863801597755668, -12.74690115177656224 ) ) ;
#22318=ORIENTED_EDGE ( 'NONE', *, *, #7150, .T. ) ;
#22321=CARTESIAN_POINT ( 'NONE',  ( 5.974727161628369032, 18.96851388233658398, -7.840226266082345852 ) ) ;
#22334=CARTESIAN_POINT ( 'NONE',  ( 4.967162193818130511, 3.259922920618364639, -42.96271701169381885 ) ) ;
#22345=ORIENTED_EDGE ( 'NONE', *, *, #25432, .T. ) ;
#22357=ADVANCED_FACE ( 'NONE', ( #2769 ), #42560, .F. ) ;
#22368=CARTESIAN_POINT ( 'NONE',  ( 0.5837374860065644988, 44.18034382476647437, -18.49670552082908159 ) ) ;
#22373=EDGE_CURVE ( 'NONE', #35226, #61413, #56871, .T. ) ;
#22382=LINE ( 'NONE', #13615, #31659 ) ;
#22386=CARTESIAN_POINT ( 'NONE',  ( 5.974727161628369032, 10.24903993264984514, 17.78288073588506180 ) ) ;
#22387=CARTESIAN_POINT ( 'NONE',  ( 4.967162193818131399, 35.57684288741977241, 24.30453456948122692 ) ) ;
#22389=CONICAL_SURFACE ( 'NONE', #14405, 48.09070567114147110, 0.04450589592585947607 ) ;
#22392=CARTESIAN_POINT ( 'NONE',  ( 0.9749527285493316819, 42.90750796893246388, 0.2856147164660120530 ) ) ;
#22396=CARTESIAN_POINT ( 'NONE',  ( 2.281351352603295357, -47.37344280316140299, -7.562287671717704995 ) ) ;
#22397=ORIENTED_EDGE ( 'NONE', *, *, #12883, .F. ) ;
#22398=ADVANCED_FACE ( 'NONE', ( #54768 ), #34145, .F. ) ;
#22401=CARTESIAN_POINT ( 'NONE',  ( 4.956653778116987041, -47.94889704119048446, -3.690426056930470988 ) ) ;
#22402=DIRECTION ( 'NONE',  ( -0.07439287786467650709, 0.8569499480575054617, -0.5100024374914788883 ) ) ;
#22406=CARTESIAN_POINT ( 'NONE',  ( 5.959547316686252039, 20.34955788964376566, -2.682663672454702830 ) ) ;
#22407=EDGE_CURVE ( 'NONE', #49553, #32791, #44805, .T. ) ;
#22414=CARTESIAN_POINT ( 'NONE',  ( 2.624215991343608501, 11.05657803851045529, 46.71702075422656009 ) ) ;
#22415=VERTEX_POINT ( 'NONE', #2458 ) ;
#22416=ORIENTED_EDGE ( 'NONE', *, *, #23344, .F. ) ;
#22426=ORIENTED_EDGE ( 'NONE', *, *, #659, .F. ) ;
#22428=ADVANCED_FACE ( 'NONE', ( #59792 ), #6840, .F. ) ;
#22431=ORIENTED_EDGE ( 'NONE', *, *, #45416, .F. ) ;
#22437=ADVANCED_FACE ( 'NONE', ( #4839 ), #43579, .T. ) ;
#22442=CARTESIAN_POINT ( 'NONE',  ( 0.5786265663353196143, -47.39171391660386234, -6.967625775956209466 ) ) ;
#22447=DIRECTION ( 'NONE',  ( 0.000000000000000000, 0.000000000000000000, 1.000000000000000000 ) ) ;
#22449=AXIS2_PLACEMENT_3D ( 'NONE', #36649, #55105, #8414 ) ;
#22450=ORIENTED_EDGE ( 'NONE', *, *, #53326, .F. ) ;
#22452=CARTESIAN_POINT ( 'NONE',  ( 5.960721111146673579, -7.848955554238637333, 18.96557324978273940 ) ) ;
#22464=LINE ( 'NONE', #12161, #44684 ) ;
#22473=CARTESIAN_POINT ( 'NONE',  ( 2.624215991343620935, 7.662883702704664124, 47.39206852872460018 ) ) ;
#22477=EDGE_CURVE ( 'NONE', #27319, #54223, #24052, .T. ) ;
#22486=EDGE_CURVE ( 'NONE', #34885, #24606, #57524, .T. ) ;
#22494=AXIS2_PLACEMENT_3D ( 'NONE', #22192, #7762, #36002 ) ;
#22495=CARTESIAN_POINT ( 'NONE',  ( 5.860006189529234355, 21.34829429597467509, 43.25137511473258911 ) ) ;
#22503=ORIENTED_EDGE ( 'NONE', *, *, #40907, .T. ) ;
#22504=B_SPLINE_CURVE_WITH_KNOTS ( 'NONE', 3,
 ( #19483, #38599, #39529, #24476 ),
 .UNSPECIFIED., .F., .F.,
 ( 4, 4 ),
 ( 0.000000000000000000, 0.004446090762761374660 ),
 .UNSPECIFIED. ) ;
#22505=CARTESIAN_POINT ( 'NONE',  ( 4.956653778116996811, 45.35992544608552635, -15.97476558431834626 ) ) ;
#22506=ADVANCED_FACE ( 'NONE', ( #29588 ), #14940, .F. ) ;
#22507=( BOUNDED_SURFACE ( )  B_SPLINE_SURFACE ( 3, 1, ( 
 ( #44008, #20178 ),
 ( #49903, #11704 ),
 ( #30783, #20785 ),
 ( #25466, #59286 ) ),
 .UNSPECIFIED., .F., .F., .F. ) 
 B_SPLINE_SURFACE_WITH_KNOTS ( ( 4, 4 ),
 ( 2, 2 ),
 ( 0.000000000000000000, 1.000000000000000000 ),
 ( 0.000000000000000000, 1.000000000000000000 ),
 .UNSPECIFIED. ) 
 GEOMETRIC_REPRESENTATION_ITEM ( )  RATIONAL_B_SPLINE_SURFACE ( (
 ( 1.000000000000000000, 1.000000000000000000),
 ( 0.9732289882329797637, 0.9999525324661233672),
 ( 0.9732289882329797637, 0.9999525324661233672),
 ( 1.000000000000000000, 1.000000000000000000) ) ) 
 REPRESENTATION_ITEM ( '' )  SURFACE ( )  );
#22513=CARTESIAN_POINT ( 'NONE',  ( 5.981074661064941900, 10.26976685693798608, 17.77058762078881315 ) ) ;
#22519=VERTEX_POINT ( 'NONE', #30500 ) ;
#22520=( BOUNDED_SURFACE ( )  B_SPLINE_SURFACE ( 3, 1, ( 
 ( #57742, #19881 ),
 ( #14874, #17878 ),
 ( #22570, #37002 ),
 ( #37296, #41093 ) ),
 .UNSPECIFIED., .F., .F., .F. ) 
 B_SPLINE_SURFACE_WITH_KNOTS ( ( 4, 4 ),
 ( 2, 2 ),
 ( 0.000000000000000000, 1.000000000000000000 ),
 ( 0.000000000000000000, 1.000000000000000000 ),
 .UNSPECIFIED. ) 
 GEOMETRIC_REPRESENTATION_ITEM ( )  RATIONAL_B_SPLINE_SURFACE ( (
 ( 1.000000000000000000, 1.000000000000000000),
 ( 0.9732289882329797637, 0.9999525324661233672),
 ( 0.9732289882329797637, 0.9999525324661233672),
 ( 1.000000000000000000, 1.000000000000000000) ) ) 
 REPRESENTATION_ITEM ( '' )  SURFACE ( )  );
#22528=CARTESIAN_POINT ( 'NONE',  ( 4.967162193818131399, -14.26841313271251543, -40.65506779172179108 ) ) ;
#22530=EDGE_CURVE ( 'NONE', #20695, #49095, #10637, .T. ) ;
#22531=VERTEX_POINT ( 'NONE', #1370 ) ;
#22536=VERTEX_POINT ( 'NONE', #24592 ) ;
#22541=CIRCLE ( 'NONE', #55551, 48.09070567114147110 ) ;
#22557=CARTESIAN_POINT ( 'NONE',  ( 0.5839879327111925367, 47.49806740880208622, 6.161619650335476095 ) ) ;
#22560=CARTESIAN_POINT ( 'NONE',  ( 0.9740398440564312921, -33.78760696452724233, 26.44872719679357687 ) ) ;
#22566=CARTESIAN_POINT ( 'NONE',  ( 0.8551540677456715978, 38.56334384152469852, -28.44084013485079154 ) ) ;
#22567=EDGE_CURVE ( 'NONE', #35268, #17533, #26264, .T. ) ;
#22570=CARTESIAN_POINT ( 'NONE',  ( 5.958863334805807099, -12.49425770716499784, 16.28483817244718068 ) ) ;
#22571=ADVANCED_FACE ( 'NONE', ( #20212 ), #19975, .T. ) ;
#22575=CARTESIAN_POINT ( 'NONE',  ( 0.6846871229502899947, -11.56285438919665154, 46.49193983736587654 ) ) ;
#22576=EDGE_CURVE ( 'NONE', #28235, #30729, #32273, .T. ) ;
#22580=CARTESIAN_POINT ( 'NONE',  ( 0.5836750258453351492, -29.01293504009516866, -38.10871351907219662 ) ) ;
#22584=CARTESIAN_POINT ( 'NONE',  ( 0.5839879882012681822, 46.26395995854837651, 12.39635945868979050 ) ) ;
#22590=CARTESIAN_POINT ( 'NONE',  ( 0.8557997880470599172, -47.89938907511592703, -0.9121262075951160897 ) ) ;
#22597=CARTESIAN_POINT ( 'NONE',  ( 3.270143674763207553, -12.53844339339238445, 5.490410281242732893 ) ) ;
#22600=CARTESIAN_POINT ( 'NONE',  ( 0.5836750258453350382, -6.071582023533952821, -47.50958153310757837 ) ) ;
#22601=ORIENTED_EDGE ( 'NONE', *, *, #4754, .T. ) ;
#22606=EDGE_CURVE ( 'NONE', #42072, #31462, #6823, .T. ) ;
#22613=EDGE_LOOP ( 'NONE', ( #56496, #48479, #50061, #4448 ) ) ;
#22616=CARTESIAN_POINT ( 'NONE',  ( 0.8551540677456834771, -29.88829867897789683, -37.45266983663526617 ) ) ;
#22640=ADVANCED_FACE ( 'NONE', ( #55540 ), #23703, .F. ) ;
#22644=CARTESIAN_POINT ( 'NONE',  ( 4.967162193818132288, -24.30453456948087521, -35.57684288742000689 ) ) ;
#22651=CARTESIAN_POINT ( 'NONE',  ( 0.9745511491811756910, 39.51062171155258795, 16.73445648040586420 ) ) ;
#22653=VERTEX_POINT ( 'NONE', #35548 ) ;
#22658=ORIENTED_EDGE ( 'NONE', *, *, #29550, .T. ) ;
#22667=LINE ( 'NONE', #47705, #7957 ) ;
#22668=CARTESIAN_POINT ( 'NONE',  ( 0.9736507210033057413, -41.56063510425039453, 10.66979144439354421 ) ) ;
#22669=B_SPLINE_CURVE_WITH_KNOTS ( 'NONE', 3,
 ( #33792, #9650, #52871, #29073 ),
 .UNSPECIFIED., .F., .F.,
 ( 4, 4 ),
 ( 0.000000000000000000, 0.005004741218457411066 ),
 .UNSPECIFIED. ) ;
#22677=VERTEX_POINT ( 'NONE', #45563 ) ;
#22680=CARTESIAN_POINT ( 'NONE',  ( 2.624215991343608501, -19.66774719433009722, 43.79392271049062657 ) ) ;
#22682=CARTESIAN_POINT ( 'NONE',  ( 0.5807400328401637335, -33.48217046439135203, 34.25275203086223286 ) ) ;
#22697=CARTESIAN_POINT ( 'NONE',  ( 0.6846871229502932144, -43.92355552798024121, -19.12907057981251313 ) ) ;
#22698=CARTESIAN_POINT ( 'NONE',  ( 4.967162193818131399, 35.57684288741977241, 24.30453456948122692 ) ) ;
#22699=DIRECTION ( 'NONE',  ( 0.000000000000000000, 0.000000000000000000, 1.000000000000000000 ) ) ;
#22700=CARTESIAN_POINT ( 'NONE',  ( 5.981074661064941900, -14.50705827991436081, -14.51919955600730638 ) ) ;
#22704=CARTESIAN_POINT ( 'NONE',  ( 1.088313998177381281, 20.77783415101626829, 37.54798835078467789 ) ) ;
#22713=EDGE_CURVE ( 'NONE', #23510, #27918, #36788, .T. ) ;
#22719=CARTESIAN_POINT ( 'NONE',  ( 5.959828726073459926, 0.004526594003093787483, 20.52560994243598813 ) ) ;
#22724=CARTESIAN_POINT ( 'NONE',  ( 0.8557997880470690211, -33.22501220301925429, 34.51495345639537504 ) ) ;
#22728=ORIENTED_EDGE ( 'NONE', *, *, #31282, .T. ) ;
#22731=ADVANCED_FACE ( 'NONE', ( #31766 ), #36904, .F. ) ;
#22736=ORIENTED_EDGE ( 'NONE', *, *, #12964, .T. ) ;
#22738=B_SPLINE_CURVE_WITH_KNOTS ( 'NONE', 3,
 ( #24086, #249, #37911, #38513, #14394, #33502 ),
 .UNSPECIFIED., .F., .F.,
 ( 4, 2, 4 ),
 ( 6.946513017424995024E-18, 0.0002291966416970849874, 0.0004583932833941630359 ),
 .UNSPECIFIED. ) ;
#22739=CARTESIAN_POINT ( 'NONE',  ( 0.9756008150404588131, 41.48296819691553594, 10.96816689273711809 ) ) ;
#22740=B_SPLINE_CURVE_WITH_KNOTS ( 'NONE', 3,
 ( #35263, #20236, #44667, #49336, #34637, #6388 ),
 .UNSPECIFIED., .F., .F.,
 ( 4, 2, 4 ),
 ( 1.534030753529914427E-16, 0.0002445252820015203824, 0.0004890505640028873502 ),
 .UNSPECIFIED. ) ;
#22755=CARTESIAN_POINT ( 'NONE',  ( 4.967162193818129623, -18.65818244221285127, 38.83676580803761169 ) ) ;
#22767=CARTESIAN_POINT ( 'NONE',  ( 4.956653778116994147, 39.67974989265076857, -27.17045123668430406 ) ) ;
#22774=( BOUNDED_SURFACE ( )  B_SPLINE_SURFACE ( 3, 1, ( 
 ( #29146, #10360 ),
 ( #58873, #44822 ),
 ( #5926, #35103 ),
 ( #54162, #20988 ) ),
 .UNSPECIFIED., .F., .F., .F. ) 
 B_SPLINE_SURFACE_WITH_KNOTS ( ( 4, 4 ),
 ( 2, 2 ),
 ( 0.000000000000000000, 1.000000000000000000 ),
 ( 0.000000000000000000, 1.000000000000000000 ),
 .UNSPECIFIED. ) 
 GEOMETRIC_REPRESENTATION_ITEM ( )  RATIONAL_B_SPLINE_SURFACE ( (
 ( 1.000000000000000000, 1.000000000000000000),
 ( 0.9732289882329797637, 0.9999525324661233672),
 ( 0.9732289882329797637, 0.9999525324661233672),
 ( 1.000000000000000000, 1.000000000000000000) ) ) 
 REPRESENTATION_ITEM ( '' )  SURFACE ( )  );
#22791=FACE_OUTER_BOUND ( 'NONE', #36163, .T. ) ;
#22797=( BOUNDED_SURFACE ( )  B_SPLINE_SURFACE ( 3, 1, ( 
 ( #20345, #592 ),
 ( #14418, #275 ),
 ( #57909, #19730 ),
 ( #5586, #19423 ) ),
 .UNSPECIFIED., .F., .F., .F. ) 
 B_SPLINE_SURFACE_WITH_KNOTS ( ( 4, 4 ),
 ( 2, 2 ),
 ( 0.000000000000000000, 1.000000000000000000 ),
 ( 0.000000000000000000, 1.000000000000000000 ),
 .UNSPECIFIED. ) 
 GEOMETRIC_REPRESENTATION_ITEM ( )  RATIONAL_B_SPLINE_SURFACE ( (
 ( 1.000000000000000000, 1.000000000000000000),
 ( 0.9732289882329797637, 0.9999525324661233672),
 ( 0.9732289882329797637, 0.9999525324661233672),
 ( 1.000000000000000000, 1.000000000000000000) ) ) 
 REPRESENTATION_ITEM ( '' )  SURFACE ( )  );
#22798=CARTESIAN_POINT ( 'NONE',  ( 0.8551540677456715978, 41.03346287276462334, -24.74404575822732610 ) ) ;
#22803=CARTESIAN_POINT ( 'NONE',  ( 0.8551540677456739292, 23.16399837394546424, 41.94570365541211032 ) ) ;
#22804=CARTESIAN_POINT ( 'NONE',  ( 0.6846871229502899947, -44.58493949243992915, -17.53234844287788974 ) ) ;
#22806=EDGE_CURVE ( 'NONE', #2408, #53354, #22667, .T. ) ;
#22818=CONICAL_SURFACE ( 'NONE', #3790, 43.08621763946400307, 1.568696531533066763 ) ;
#22834=DIRECTION ( 'NONE',  ( -0.07836865515943411409, -0.2656332009267247662, -0.9608836331491571459 ) ) ;
#22836=CARTESIAN_POINT ( 'NONE',  ( 0.8551540677456715978, -28.44084013485144524, 38.56334384152421535 ) ) ;
#22837=ORIENTED_EDGE ( 'NONE', *, *, #14428, .T. ) ;
#22848=CARTESIAN_POINT ( 'NONE',  ( 0.9754402186311941225, 11.28658745892519022, 41.39745964575698878 ) ) ;
#22851=ORIENTED_EDGE ( 'NONE', *, *, #59385, .T. ) ;
#22861=VERTEX_POINT ( 'NONE', #4750 ) ;
#22862=CARTESIAN_POINT ( 'NONE',  ( 0.5837374860065648319, 47.50965286059334858, 6.071555045024764397 ) ) ;
#22873=CARTESIAN_POINT ( 'NONE',  ( 0.9730545539215883499, 21.89037132892487847, -36.90443313492307453 ) ) ;
#22874=DIRECTION ( 'NONE',  ( 0.000000000000000000, 0.000000000000000000, 1.000000000000000000 ) ) ;
#22875=( BOUNDED_SURFACE ( )  B_SPLINE_SURFACE ( 3, 1, ( 
 ( #4076, #47331 ),
 ( #9725, #18519 ),
 ( #18215, #18842 ),
 ( #56095, #37965 ) ),
 .UNSPECIFIED., .F., .F., .F. ) 
 B_SPLINE_SURFACE_WITH_KNOTS ( ( 4, 4 ),
 ( 2, 2 ),
 ( 0.000000000000000000, 1.000000000000000000 ),
 ( 0.000000000000000000, 1.000000000000000000 ),
 .UNSPECIFIED. ) 
 GEOMETRIC_REPRESENTATION_ITEM ( )  RATIONAL_B_SPLINE_SURFACE ( (
 ( 1.000000000000000000, 1.000000000000000000),
 ( 0.9953390228620291325, 0.8624445117760984880),
 ( 0.9953390228620291325, 0.8624445117760984880),
 ( 1.000000000000000000, 1.000000000000000000) ) ) 
 REPRESENTATION_ITEM ( '' )  SURFACE ( )  );
#22885=B_SPLINE_CURVE_WITH_KNOTS ( 'NONE', 3,
 ( #41720, #3456, #28503, #47631 ),
 .UNSPECIFIED., .F., .F.,
 ( 4, 4 ),
 ( 0.000000000000000000, 0.005004741218457452699 ),
 .UNSPECIFIED. ) ;
#22886=ADVANCED_FACE ( 'NONE', ( #38905 ), #29728, .F. ) ;
#22894=CARTESIAN_POINT ( 'NONE',  ( 0.8551540677456739292, 41.94570365541235191, -23.16399837394502725 ) ) ;
#22897=CARTESIAN_POINT ( 'NONE',  ( 0.5800708119828337228, 46.09746484493497576, -13.00144522946610515 ) ) ;
#22899=B_SPLINE_CURVE_WITH_KNOTS ( 'NONE', 3,
 ( #10919, #30004, #20313, #5861, #49115, #48491 ),
 .UNSPECIFIED., .F., .F.,
 ( 4, 2, 4 ),
 ( 1.495080201624372079E-16, 0.0002445252820015202740, 0.0004890505640028910365 ),
 .UNSPECIFIED. ) ;
#22900=( NAMED_UNIT ( * ) PLANE_ANGLE_UNIT ( ) SI_UNIT ( $, .RADIAN. ) );
#22902=CARTESIAN_POINT ( 'NONE',  ( 4.956653778116991482, -2.599733001514001440, -48.02038484091103498 ) ) ;
#22906=DIRECTION ( 'NONE',  ( -0.07836865515943411409, -0.9179910502197385913, 0.3887811538706100745 ) ) ;
#22910=CARTESIAN_POINT ( 'NONE',  ( 0.5809828226811617480, -5.711058609464997105, -47.55412398569212939 ) ) ;
#22913=VERTEX_POINT ( 'NONE', #1564 ) ;
#22916=EDGE_CURVE ( 'NONE', #51439, #46801, #32152, .T. ) ;
#22923=EDGE_CURVE ( 'NONE', #34886, #59557, #59086, .T. ) ;
#22933=CARTESIAN_POINT ( 'NONE',  ( 0.9749527285493307938, -42.90750796893248520, -0.2856147164663118132 ) ) ;
#22934=ORIENTED_EDGE ( 'NONE', *, *, #6875, .F. ) ;
#22936=ADVANCED_FACE ( 'NONE', ( #26014 ), #58077, .F. ) ;
#22937=CARTESIAN_POINT ( 'NONE',  ( 0.8551540677456715978, -23.16399837394516581, -41.94570365541226664 ) ) ;
#22938=VERTEX_POINT ( 'NONE', #2179 ) ;
#22940=CARTESIAN_POINT ( 'NONE',  ( 4.956653778116949738, -36.51451553856396970, -31.29546495791881000 ) ) ;
#22944=ORIENTED_EDGE ( 'NONE', *, *, #1727, .T. ) ;
#22945=CARTESIAN_POINT ( 'NONE',  ( 1.154321485836933281, 41.66001465002027970, 10.30834589251726285 ) ) ;
#22946=FACE_OUTER_BOUND ( 'NONE', #60230, .T. ) ;
#22947=CARTESIAN_POINT ( 'NONE',  ( 5.959547316686252039, -12.49238070347965035, -16.28624005235095495 ) ) ;
#22949=CARTESIAN_POINT ( 'NONE',  ( 0.9730545539215883499, 42.60426903087353878, 5.099196237955034405 ) ) ;
#22951=CARTESIAN_POINT ( 'NONE',  ( 0.5819845079324655890, -46.14435090135486206, 12.83441846783114570 ) ) ;
#22953=VECTOR ( 'NONE', #25625, 1000.000000000000114 ) ;
#22955=CARTESIAN_POINT ( 'NONE',  ( 2.526552050251864134, 6.809858322089650251, -42.43615142762118353 ) ) ;
#22960=CARTESIAN_POINT ( 'NONE',  ( 4.967162193818130511, 43.02067033766019932, -2.375726030842729486 ) ) ;
#22964=CARTESIAN_POINT ( 'NONE',  ( 0.9749527285493325701, -37.01618455594557133, -21.70110358462078182 ) ) ;
#22970=CARTESIAN_POINT ( 'NONE',  ( 0.5809828226811553087, 24.41822904836923058, 41.20389530892317254 ) ) ;
#22974=CARTESIAN_POINT ( 'NONE',  ( 0.5832367798473377940, -34.05962365606842468, 33.67436043247250410 ) ) ;
#22985=ORIENTED_EDGE ( 'NONE', *, *, #36962, .T. ) ;
#22988=ORIENTED_EDGE ( 'NONE', *, *, #23615, .T. ) ;
#22992=VERTEX_POINT ( 'NONE', #49815 ) ;
#23003=CARTESIAN_POINT ( 'NONE',  ( 2.281448460670563616, 38.84544723616143358, 28.15071835136410883 ) ) ;
#23010=B_SPLINE_CURVE_WITH_KNOTS ( 'NONE', 3,
 ( #1440, #52534, #53747, #9628, #24041, #57843 ),
 .UNSPECIFIED., .F., .F.,
 ( 4, 2, 4 ),
 ( 1.527179101177669750E-16, 0.0002445252820015209245, 0.0004890505640028891933 ),
 .UNSPECIFIED. ) ;
#23013=VERTEX_POINT ( 'NONE', #55120 ) ;
#23014=CARTESIAN_POINT ( 'NONE',  ( 0.5786265663353153954, -18.99608782658000905, -43.97352617418637521 ) ) ;
#23016=CARTESIAN_POINT ( 'NONE',  ( 0.9745511491811750249, 30.09905547141354276, 30.58068216140344120 ) ) ;
#23018=EDGE_CURVE ( 'NONE', #50394, #37784, #49328, .T. ) ;
#23026=CARTESIAN_POINT ( 'NONE',  ( 0.8551540677456715978, 11.51835730326544649, -46.51172240253109180 ) ) ;
#23028=CARTESIAN_POINT ( 'NONE',  ( 1.154321713695929175, -22.16897764010631633, 36.74718012229649844 ) ) ;
#23030=CARTESIAN_POINT ( 'NONE',  ( 0.5807400328401574052, -24.41979442053140303, -41.20655774452995246 ) ) ;
#23031=VERTEX_POINT ( 'NONE', #58890 ) ;
#23043=CARTESIAN_POINT ( 'NONE',  ( 1.154321485836933725, -36.74718014677581834, 22.16897757994461671 ) ) ;
#23045=ORIENTED_EDGE ( 'NONE', *, *, #16560, .T. ) ;
#23047=CARTESIAN_POINT ( 'NONE',  ( 0.5800708119828332787, -37.61306658477494125, 29.65250521075930834 ) ) ;
#23049=CARTESIAN_POINT ( 'NONE',  ( 2.624215991343608501, 32.93378783738849336, 34.92983774302978617 ) ) ;
#23057=CARTESIAN_POINT ( 'NONE',  ( 0.9745511491811748028, 41.35688774886286723, 11.43411988112617372 ) ) ;
#23063=CARTESIAN_POINT ( 'NONE',  ( 0.9730545539215883499, 41.57420493492400482, -10.61654491617520080 ) ) ;
#23070=FACE_OUTER_BOUND ( 'NONE', #19135, .T. ) ;
#23073=DIRECTION ( 'NONE',  ( -0.000000000000000000, 1.000000000000000000, -0.000000000000000000 ) ) ;
#23076=CARTESIAN_POINT ( 'NONE',  ( 0.9752132459055842251, 0.2329632697543913833, 42.90780255730426518 ) ) ;
#23079=AXIS2_PLACEMENT_3D ( 'NONE', #48868, #941, #52942 ) ;
#23080=VERTEX_POINT ( 'NONE', #41369 ) ;
#23081=CARTESIAN_POINT ( 'NONE',  ( 5.960721111146673579, -12.49016043756483363, 16.28787783074205819 ) ) ;
#23088=CARTESIAN_POINT ( 'NONE',  ( 0.5809828226811617480, -47.41188724015875522, -6.791453954330822107 ) ) ;
#23091=CARTESIAN_POINT ( 'NONE',  ( 1.227938101723756947, -42.91134962331487657, 0.8460948827223682134 ) ) ;
#23093=CARTESIAN_POINT ( 'NONE',  ( 0.5839879327111922036, -18.41291455875270344, -44.21534283185622627 ) ) ;
#23098=CARTESIAN_POINT ( 'NONE',  ( 3.270143674763207553, 0.2742231296309522448, 13.68510027222513514 ) ) ;
#23119=CARTESIAN_POINT ( 'NONE',  ( 5.981074661064941900, -2.670494474392148376, 20.35019299530684123 ) ) ;
#23125=CARTESIAN_POINT ( 'NONE',  ( 3.270143674763207553, -12.53844339339230451, -5.490410281242913193 ) ) ;
#23128=CARTESIAN_POINT ( 'NONE',  ( -19.36110035657940287, -7.842565309080231195, -1.582362494774802730 ) ) ;
#23129=ORIENTED_EDGE ( 'NONE', *, *, #27805, .T. ) ;
#23150=EDGE_LOOP ( 'NONE', ( #47324, #46052, #39309, #51880 ) ) ;
#23152=VERTEX_POINT ( 'NONE', #17859 ) ;
#23155=FACE_OUTER_BOUND ( 'NONE', #38116, .T. ) ;
#23156=CARTESIAN_POINT ( 'NONE',  ( 0.5800708119828336118, 46.42229822050698118, 11.78915056783724502 ) ) ;
#23157=FACE_OUTER_BOUND ( 'NONE', #36622, .T. ) ;
#23158=VERTEX_POINT ( 'NONE', #36984 ) ;
#23159=CARTESIAN_POINT ( 'NONE',  ( 0.8557997880470599172, -46.03118133706016835, -13.27832040216687304 ) ) ;
#23161=ADVANCED_FACE ( 'NONE', ( #56044 ), #27731, .F. ) ;
#23172=CARTESIAN_POINT ( 'NONE',  ( 0.5827359174754822568, 47.43746338751532932, 6.611633125156963331 ) ) ;
#23193=CARTESIAN_POINT ( 'NONE',  ( 2.281351352603295357, 13.68106635380627800, -45.98107981851849502 ) ) ;
#23196=CARTESIAN_POINT ( 'NONE',  ( 5.965394784446458765, -17.76824826579361982, 10.27521535480955528 ) ) ;
#23201=SURFACE_STYLE_USAGE ( .BOTH. , #42629 ) ;
#23204=CARTESIAN_POINT ( 'NONE',  ( 3.270143674763207553, 5.490410281242775525, 12.53844339339236491 ) ) ;
#23205=CARTESIAN_POINT ( 'NONE',  ( 4.960156602257184133, 2.524999074838214508, -46.35381625054453991 ) ) ;
#23211=ORIENTED_EDGE ( 'NONE', *, *, #30141, .F. ) ;
#23212=CARTESIAN_POINT ( 'NONE',  ( 0.5832366564991502411, -6.521686574605801923, -47.44984844891996545 ) ) ;
#23214=ORIENTED_EDGE ( 'NONE', *, *, #6697, .F. ) ;
#23219=B_SPLINE_CURVE_WITH_KNOTS ( 'NONE', 3,
 ( #26978, #55459, #56083, #22590 ),
 .UNSPECIFIED., .F., .F.,
 ( 4, 4 ),
 ( 0.000000000000000000, 0.004446090762761370323 ),
 .UNSPECIFIED. ) ;
#23221=CARTESIAN_POINT ( 'NONE',  ( 2.624215991343608501, 44.87417713512112982, -17.05978231157355296 ) ) ;
#23231=ORIENTED_EDGE ( 'NONE', *, *, #40952, .T. ) ;
#23232=CARTESIAN_POINT ( 'NONE',  ( 0.9758171775293923433, -42.90848549292462621, 0.005919131624846820337 ) ) ;
#23234=B_SPLINE_CURVE_WITH_KNOTS ( 'NONE', 3,
 ( #37251, #3998, #7464, #41342, #46341, #17210, #36949, #55700, #26912, #3385 ),
 .UNSPECIFIED., .F., .F.,
 ( 4, 3, 3, 4 ),
 ( 0.0005448802484329447627, 0.0005449104342063602240, 0.0008173270854453676491, 0.001089761613562688792 ),
 .UNSPECIFIED. ) ;
#23237=CARTESIAN_POINT ( 'NONE',  ( 4.967162193818130511, 32.68434214048205888, -28.07411493385260925 ) ) ;
#23241=CARTESIAN_POINT ( 'NONE',  ( 5.974727161628367256, 14.52429704002343769, 14.50236057684849911 ) ) ;
#23242=DIRECTION ( 'NONE',  ( -1.000000000000000000, 0.000000000000000000, 0.000000000000000000 ) ) ;
#23247=CARTESIAN_POINT ( 'NONE',  ( 5.981074661064941900, -10.25489689131142867, 17.77917279944614393 ) ) ;
#23249=CARTESIAN_POINT ( 'NONE',  ( 4.967162193818130511, 28.07411493385340862, -32.68434214048137676 ) ) ;
#23253=B_SPLINE_CURVE_WITH_KNOTS ( 'NONE', 3,
 ( #33570, #61722, #37979, #42657, #56727, #57634 ),
 .UNSPECIFIED., .F., .F.,
 ( 4, 2, 4 ),
 ( 8.787390050835121380E-18, 0.0002445244328975383239, 0.0004890488657950678658 ),
 .UNSPECIFIED. ) ;
#23268=ORIENTED_EDGE ( 'NONE', *, *, #48642, .T. ) ;
#23270=CARTESIAN_POINT ( 'NONE',  ( 0.5837374860065626114, 24.10515569139049674, 41.38807031854324947 ) ) ;
#23272=CARTESIAN_POINT ( 'NONE',  ( 0.8557997880470690211, 41.93815086860257679, 23.15977007032337553 ) ) ;
#23273=EDGE_LOOP ( 'NONE', ( #23214, #47346, #22143, #44459 ) ) ;
#23274=ORIENTED_EDGE ( 'NONE', *, *, #45112, .F. ) ;
#23276=CARTESIAN_POINT ( 'NONE',  ( 4.967162193818129623, -19.45289607368849616, 38.44485641567065670 ) ) ;
#23278=EDGE_LOOP ( 'NONE', ( #19215, #37894, #15188, #55171 ) ) ;
#23279=ORIENTED_EDGE ( 'NONE', *, *, #55791, .T. ) ;
#23283=ADVANCED_FACE ( 'NONE', ( #38515 ), #14966, .T. ) ;
#23285=CARTESIAN_POINT ( 'NONE',  ( 0.9757892942422834448, -41.43309903783660531, 11.15510465568985587 ) ) ;
#23289=VERTEX_POINT ( 'NONE', #57887 ) ;
#23297=ORIENTED_EDGE ( 'NONE', *, *, #32461, .T. ) ;
#23301=CARTESIAN_POINT ( 'NONE',  ( 1.088908134280559326, 17.14055988408919617, 39.34174992079760358 ) ) ;
#23302=CARTESIAN_POINT ( 'NONE',  ( 0.9757954354143124620, -0.01316335317099341304, 42.90846090505963417 ) ) ;
#23319=ORIENTED_EDGE ( 'NONE', *, *, #48428, .T. ) ;
#23325=CARTESIAN_POINT ( 'NONE',  ( 0.5807400328401637335, 46.12278621143515522, -12.92266817605966978 ) ) ;
#23327=CARTESIAN_POINT ( 'NONE',  ( 0.5850706913938534814, -29.01314519953824700, 38.10903744847131236 ) ) ;
#23335=CARTESIAN_POINT ( 'NONE',  ( 0.8551540677456739292, -13.28067116677233805, 46.03951182599424641 ) ) ;
#23339=CARTESIAN_POINT ( 'NONE',  ( 4.960156602257181468, -34.56254177294292873, 30.99165383632755066 ) ) ;
#23344=EDGE_CURVE ( 'NONE', #23911, #27511, #44050, .T. ) ;
#23347=CARTESIAN_POINT ( 'NONE',  ( 4.967162193818130511, 0.000000000000000000, 0.000000000000000000 ) ) ;
#23349=VERTEX_POINT ( 'NONE', #21859 ) ;
#23358=CARTESIAN_POINT ( 'NONE',  ( 4.967162193818130511, 0.000000000000000000, 0.000000000000000000 ) ) ;
#23378=ORIENTED_EDGE ( 'NONE', *, *, #11192, .F. ) ;
#23380=CARTESIAN_POINT ( 'NONE',  ( 0.5809828226811617480, 41.20389530892307306, 24.41822904836939401 ) ) ;
#23384=CARTESIAN_POINT ( 'NONE',  ( 0.6067099128993235224, 41.82996792600780367, 23.33192673707546660 ) ) ;
#23390=CARTESIAN_POINT ( 'NONE',  ( 0.5834872094924179464, -47.45604551759231526, -6.476680342367071574 ) ) ;
#23394=B_SPLINE_CURVE_WITH_KNOTS ( 'NONE', 3,
 ( #53051, #14562, #19258, #47150 ),
 .UNSPECIFIED., .F., .F.,
 ( 4, 4 ),
 ( 0.000000000000000000, 0.004048833967417082152 ),
 .UNSPECIFIED. ) ;
#23403=ORIENTED_EDGE ( 'NONE', *, *, #21903, .F. ) ;
#23404=CARTESIAN_POINT ( 'NONE',  ( 0.5800708119828335008, 38.37709857409269887, 28.65679933661808221 ) ) ;
#23405=CARTESIAN_POINT ( 'NONE',  ( 0.5809828226811617480, 0.5448590168539207967, -47.89273459658652854 ) ) ;
#23406=EDGE_CURVE ( 'NONE', #33579, #46829, #45377, .T. ) ;
#23407=CARTESIAN_POINT ( 'NONE',  ( 0.9757402383260943557, 5.684842778069837621, -42.53022961222597331 ) ) ;
#23410=CARTESIAN_POINT ( 'NONE',  ( 0.6846871229502899947, -43.92355552798050411, 19.12907057981189496 ) ) ;
#23416=CARTESIAN_POINT ( 'NONE',  ( 4.960156602257182357, 15.40604254112643723, 43.79161740034479777 ) ) ;
#23418=EDGE_LOOP ( 'NONE', ( #2694, #51702, #57366, #10517 ) ) ;
#23428=CARTESIAN_POINT ( 'NONE',  ( 0.9757787079277433495, 11.14366644276469032, -41.43615150473004860 ) ) ;
#23429=EDGE_CURVE ( 'NONE', #29382, #42725, #55983, .T. ) ;
#23431=ORIENTED_EDGE ( 'NONE', *, *, #57047, .F. ) ;
#23447=ORIENTED_EDGE ( 'NONE', *, *, #38321, .F. ) ;
#23449=VERTEX_POINT ( 'NONE', #18399 ) ;
#23464=CARTESIAN_POINT ( 'NONE',  ( 2.624215991343608501, 45.98641578154030185, 13.78323291683799212 ) ) ;
#23469=ORIENTED_EDGE ( 'NONE', *, *, #57047, .T. ) ;
#23470=ORIENTED_EDGE ( 'NONE', *, *, #8440, .F. ) ;
#23471=LINE ( 'NONE', #42603, #25343 ) ;
#23475=CARTESIAN_POINT ( 'NONE',  ( 0.5786265663353153954, 5.535668456754629041, -47.58023467411533147 ) ) ;
#23476=CARTESIAN_POINT ( 'NONE',  ( 2.624215991343608501, -44.87417713512100192, 17.05978231157389047 ) ) ;
#23478=CARTESIAN_POINT ( 'NONE',  ( 4.956653778116475451, 47.27023054223744225, 8.845409907520236814 ) ) ;
#23480=EDGE_CURVE ( 'NONE', #40820, #28284, #19393, .T. ) ;
#23481=CARTESIAN_POINT ( 'NONE',  ( 5.981074661064941900, -20.35019299530686610, -2.670494474391926332 ) ) ;
#23483=CARTESIAN_POINT ( 'NONE',  ( 0.8551540677456834771, 19.17641535420853316, 43.91216198251545677 ) ) ;
#23486=FACE_OUTER_BOUND ( 'NONE', #3719, .T. ) ;
#23496=VERTEX_POINT ( 'NONE', #28709 ) ;
#23506=B_SPLINE_CURVE_WITH_KNOTS ( 'NONE', 3,
 ( #10823, #35254, #6376, #44655, #1694, #39973, #59024, #54310, #11433, #50255, #7959, #22368, #41498, #13291, #32090, #45576 ),
 .UNSPECIFIED., .F., .F.,
 ( 4, 3, 3, 3, 3, 4 ),
 ( 3.469446951953614189E-18, 0.0002724568934985621064, 0.0004086836638483854595, 0.0005449104342063774628, 0.0008173270854453849963, 0.001089761613562692478 ),
 .UNSPECIFIED. ) ;
#23507=CARTESIAN_POINT ( 'NONE',  ( 4.963659409799326738, -14.83726297270310823, 42.22332985082307744 ) ) ;
#23508=VECTOR ( 'NONE', #17413, 1000.000000000000227 ) ;
#23509=ORIENTED_EDGE ( 'NONE', *, *, #41247, .T. ) ;
#23510=VERTEX_POINT ( 'NONE', #43451 ) ;
#23511=CARTESIAN_POINT ( 'NONE',  ( 0.5832367798473389042, -5.981481162905404325, -47.52096797443093834 ) ) ;
#23512=CARTESIAN_POINT ( 'NONE',  ( 4.956653778116966613, 0.000000000000000000, 0.000000000000000000 ) ) ;
#23514=CARTESIAN_POINT ( 'NONE',  ( 3.660176727303398714, 27.72864483302518224, 39.22755245663856982 ) ) ;
#23517=CARTESIAN_POINT ( 'NONE',  ( 0.5827357941260203900, 0.3632531319014370430, 47.89462047563813485 ) ) ;
#23520=VERTEX_POINT ( 'NONE', #4565 ) ;
#23521=CARTESIAN_POINT ( 'NONE',  ( 0.9758171775293917882, -16.42583507057837622, -39.64000636436379210 ) ) ;
#23525=CARTESIAN_POINT ( 'NONE',  ( 5.959828726073459926, -5.308046411395112685, -19.82738831247212019 ) ) ;
#23526=CARTESIAN_POINT ( 'NONE',  ( 0.5850706913938533704, -29.01314519953773186, -38.10903744847171026 ) ) ;
#23529=CARTESIAN_POINT ( 'NONE',  ( 5.960721111146673579, -16.28018152803701213, 12.50019045452710742 ) ) ;
#23532=EDGE_LOOP ( 'NONE', ( #14229, #11429, #52645, #2686 ) ) ;
#23542=VERTEX_POINT ( 'NONE', #61888 ) ;
#23543=CARTESIAN_POINT ( 'NONE',  ( 0.9730545539215883499, 41.57420493492384850, 10.61654491617579055 ) ) ;
#23544=CARTESIAN_POINT ( 'NONE',  ( 0.8551540677456715978, -41.03346287276445992, 24.74404575822761032 ) ) ;
#23546=CARTESIAN_POINT ( 'NONE',  ( 0.5838002273316419410, -44.19779719735685575, -18.45474575185561505 ) ) ;
#23555=EDGE_CURVE ( 'NONE', #19529, #58674, #12635, .T. ) ;
#23557=CARTESIAN_POINT ( 'NONE',  ( 0.9730545539215883499, 30.69604515769692554, -29.98130006528829483 ) ) ;
#23561=CARTESIAN_POINT ( 'NONE',  ( 0.9752132459055854463, 37.27572867006962554, 21.25214916889604666 ) ) ;
#23564=CARTESIAN_POINT ( 'NONE',  ( 0.8551540677456715978, -23.16399837394575556, 41.94570365541196111 ) ) ;
#23567=CARTESIAN_POINT ( 'NONE',  ( 0.9754642270333695464, 39.57465882553928793, 16.58255499746090322 ) ) ;
#23586=ORIENTED_EDGE ( 'NONE', *, *, #12776, .F. ) ;
#23588=ORIENTED_EDGE ( 'NONE', *, *, #6617, .F. ) ;
#23595=VERTEX_POINT ( 'NONE', #58423 ) ;
#23600=VERTEX_POINT ( 'NONE', #30543 ) ;
#23603=CARTESIAN_POINT ( 'NONE',  ( 5.958863334805807099, 16.28335246510350842, 12.49619391867187801 ) ) ;
#23609=LINE ( 'NONE', #4779, #879 ) ;
#23613=ORIENTED_EDGE ( 'NONE', *, *, #51058, .T. ) ;
#23615=EDGE_CURVE ( 'NONE', #6126, #58704, #27589, .T. ) ;
#23617=CARTESIAN_POINT ( 'NONE',  ( 2.281448460670560952, -4.956513608981508945, 47.71650330356585101 ) ) ;
#23618=AXIS2_PLACEMENT_3D ( 'NONE', #2820, #60147, #44548 ) ;
#23625=CARTESIAN_POINT ( 'NONE',  ( 3.783278058412224976, 7.325100730114287195, 42.41041238787298084 ) ) ;
#23627=CARTESIAN_POINT ( 'NONE',  ( 5.965394784446460541, 10.27521535480986614, -17.76824826579344574 ) ) ;
#23639=CARTESIAN_POINT ( 'NONE',  ( 5.981074661064941900, 5.303881226583676778, -19.82752479807522406 ) ) ;
#23647=CARTESIAN_POINT ( 'NONE',  ( 0.5827359174754831450, 12.04517879102136924, 46.35666395585276689 ) ) ;
#23650=CARTESIAN_POINT ( 'NONE',  ( 3.407937589446174087, -11.62731850632879116, -7.243367523631146554 ) ) ;
#23663=EDGE_CURVE ( 'NONE', #58552, #12007, #24597, .T. ) ;
#23671=CARTESIAN_POINT ( 'NONE',  ( 0.5809828226811553087, 37.66417181417592275, -29.58751527316140795 ) ) ;
#23673=DIRECTION ( 'NONE',  ( -1.000000000000000000, -0.000000000000000000, -0.000000000000000000 ) ) ;
#23675=EDGE_LOOP ( 'NONE', ( #19424, #50331, #53026, #60044 ) ) ;
#23685=EDGE_CURVE ( 'NONE', #59114, #45338, #50006, .T. ) ;
#23686=CARTESIAN_POINT ( 'NONE',  ( 4.956653778116995035, 36.51451553856460919, -31.29546495791814209 ) ) ;
#23689=VECTOR ( 'NONE', #8907, 1000.000000000000114 ) ;
#23696=CARTESIAN_POINT ( 'NONE',  ( 0.5809828226811553087, -47.55412398569202281, -5.711058609465819558 ) ) ;
#23700=CARTESIAN_POINT ( 'NONE',  ( 0.9745511491811748028, 26.39034508612584062, -33.83313387735761779 ) ) ;
#23702=CARTESIAN_POINT ( 'NONE',  ( 0.5809828226811553087, -18.83114015454665946, -44.03860873105715967 ) ) ;
#23703=( BOUNDED_SURFACE ( )  B_SPLINE_SURFACE ( 3, 1, ( 
 ( #35854, #40566 ),
 ( #55859, #12358 ),
 ( #17659, #2300 ),
 ( #26748, #3533 ) ),
 .UNSPECIFIED., .F., .F., .F. ) 
 B_SPLINE_SURFACE_WITH_KNOTS ( ( 4, 4 ),
 ( 2, 2 ),
 ( 0.000000000000000000, 1.000000000000000000 ),
 ( 0.000000000000000000, 1.000000000000000000 ),
 .UNSPECIFIED. ) 
 GEOMETRIC_REPRESENTATION_ITEM ( )  RATIONAL_B_SPLINE_SURFACE ( (
 ( 1.000000000000000000, 1.000000000000000000),
 ( 0.9732289882329797637, 0.9999525324661233672),
 ( 0.9732289882329797637, 0.9999525324661233672),
 ( 1.000000000000000000, 1.000000000000000000) ) ) 
 REPRESENTATION_ITEM ( '' )  SURFACE ( )  );
#23706=ADVANCED_FACE ( 'NONE', ( #27096 ), #46957, .F. ) ;
#23721=VECTOR ( 'NONE', #59450, 1000.000000000000000 ) ;
#23722=CARTESIAN_POINT ( 'NONE',  ( 0.5837374860065642768, -47.89569815517035067, 0.1816420316513765454 ) ) ;
#23726=CARTESIAN_POINT ( 'NONE',  ( 1.227938101723748288, -39.96870412324346944, 15.63977281655828300 ) ) ;
#23728=VERTEX_POINT ( 'NONE', #41217 ) ;
#23733=CARTESIAN_POINT ( 'NONE',  ( 0.9757892942422828897, 42.53466646637867399, -5.651566539685394908 ) ) ;
#23736=ORIENTED_EDGE ( 'NONE', *, *, #35691, .T. ) ;
#23740=CARTESIAN_POINT ( 'NONE',  ( -19.02812962168027511, -7.790324327006077354, -1.821248266840887364 ) ) ;
#23743=ORIENTED_EDGE ( 'NONE', *, *, #3280, .T. ) ;
#23748=CARTESIAN_POINT ( 'NONE',  ( 0.7057020205115013267, 28.48867101281825498, 38.50899875908065439 ) ) ;
#23750=CARTESIAN_POINT ( 'NONE',  ( 0.9972139404380298000, 42.90441115546387607, -0.6581143129161796113 ) ) ;
#23758=ADVANCED_FACE ( 'NONE', ( #13020 ), #49306, .F. ) ;
#23767=EDGE_CURVE ( 'NONE', #7563, #14241, #58193, .T. ) ;
#23768=CARTESIAN_POINT ( 'NONE',  ( 0.5809828226811553087, 46.40184912890838831, 11.86925843957183879 ) ) ;
#23773=CARTESIAN_POINT ( 'NONE',  ( 0.5786265663353153954, -38.43785771743185364, -28.58414684753526558 ) ) ;
#23774=ORIENTED_EDGE ( 'NONE', *, *, #60365, .F. ) ;
#23775=B_SPLINE_CURVE_WITH_KNOTS ( 'NONE', 3,
 ( #34416, #58800, #34725, #20921, #44453, #882, #48809, #49730, #5863, #2096, #30006, #44151, #40364, #59115, #35040, #1178 ),
 .UNSPECIFIED., .F., .F.,
 ( 4, 3, 3, 3, 3, 4 ),
 ( 1.301087781288862954E-17, 0.0002724568934985555470, 0.0004086836638483815022, 0.0005449104342063617419, 0.0008173270854453690585, 0.001089761613562690093 ),
 .UNSPECIFIED. ) ;
#23781=CARTESIAN_POINT ( 'NONE',  ( 5.960721111146673579, 12.49016043756471284, -16.28787783074214701 ) ) ;
#23787=VECTOR ( 'NONE', #53190, 1000.000000000000114 ) ;
#23794=DIRECTION ( 'NONE',  ( -1.000000000000000000, -0.000000000000000000, -0.000000000000000000 ) ) ;
#23800=CARTESIAN_POINT ( 'NONE',  ( 4.303969348037246512, 47.36875205922773091, 8.413118729224215997 ) ) ;
#23801=B_SPLINE_CURVE_WITH_KNOTS ( 'NONE', 3,
 ( #39149, #5576, #53205, #25326, #10310, #24713 ),
 .UNSPECIFIED., .F., .F.,
 ( 4, 2, 4 ),
 ( 1.492775917167880503E-16, 0.0002445252820015208161, 0.0004890505640028923375 ),
 .UNSPECIFIED. ) ;
#23806=CARTESIAN_POINT ( 'NONE',  ( 3.270143674763207553, -10.69018354892881462, -8.548517033725367753 ) ) ;
#23808=VECTOR ( 'NONE', #13175, 1000.000000000000114 ) ;
#23812=CARTESIAN_POINT ( 'NONE',  ( 0.5807400328401574052, -41.20655774452952613, -24.41979442053212779 ) ) ;
#23825=CARTESIAN_POINT ( 'NONE',  ( 4.967162193818130511, -14.26841313271309808, 40.65506779172159924 ) ) ;
#23829=ORIENTED_EDGE ( 'NONE', *, *, #39633, .T. ) ;
#23834=VERTEX_POINT ( 'NONE', #53348 ) ;
#23841=CARTESIAN_POINT ( 'NONE',  ( 0.9730545539215883499, 36.90443313492362165, -21.89037132892396897 ) ) ;
#23848=CARTESIAN_POINT ( 'NONE',  ( 5.974727161628367256, -16.27409205901383871, 12.50710176109980409 ) ) ;
#23849=VERTEX_POINT ( 'NONE', #9520 ) ;
#23851=CARTESIAN_POINT ( 'NONE',  ( 0.5786265663353196143, -23.32245830378999329, -41.83999636203343186 ) ) ;
#23852=EDGE_LOOP ( 'NONE', ( #59416, #39881, #37194, #9912 ) ) ;
#23853=CARTESIAN_POINT ( 'NONE',  ( 3.407937589446178528, 0.4592810312471982126, 13.69123696618924590 ) ) ;
#23858=EDGE_CURVE ( 'NONE', #58674, #12140, #14070, .T. ) ;
#23862=ADVANCED_FACE ( 'NONE', ( #29552 ), #48662, .F. ) ;
#23863=CARTESIAN_POINT ( 'NONE',  ( 4.303969348037246512, 25.89994482339426440, -40.54345935592751715 ) ) ;
#23866=CARTESIAN_POINT ( 'NONE',  ( 5.959547316686252039, -16.28190225198627061, 12.49803383497722642 ) ) ;
#23873=CARTESIAN_POINT ( 'NONE',  ( 0.9758171775293915662, 30.33669560438110935, -30.34506652060211351 ) ) ;
#23875=CARTESIAN_POINT ( 'NONE',  ( 0.9722240741986376555, -34.39263045016073761, 25.65687427836892454 ) ) ;
#23876=CARTESIAN_POINT ( 'NONE',  ( 0.9730545539215883499, -41.57420493492377744, -10.61654491617608009 ) ) ;
#23879=CARTESIAN_POINT ( 'NONE',  ( 0.8557997880470599172, -46.03118133706016835, -13.27832040216687304 ) ) ;
#23883=ORIENTED_EDGE ( 'NONE', *, *, #57457, .F. ) ;
#23890=LINE ( 'NONE', #52687, #38958 ) ;
#23891=CARTESIAN_POINT ( 'NONE',  ( 0.7762783648524402835, 34.49689442177346876, 33.23866576554850383 ) ) ;
#23893=ORIENTED_EDGE ( 'NONE', *, *, #1913, .T. ) ;
#23894=ORIENTED_EDGE ( 'NONE', *, *, #26239, .T. ) ;
#23895=CARTESIAN_POINT ( 'NONE',  ( 0.9730545539215883499, -11.59290486963477562, -41.31259007387244253 ) ) ;
#23900=ORIENTED_EDGE ( 'NONE', *, *, #9533, .F. ) ;
#23904=CARTESIAN_POINT ( 'NONE',  ( 0.9730545539215883499, -29.98130006528883129, 30.69604515769640329 ) ) ;
#23908=CARTESIAN_POINT ( 'NONE',  ( 0.9730545539215883499, -33.73144377768539215, -26.52009130076805832 ) ) ;
#23910=ADVANCED_FACE ( 'NONE', ( #16953 ), #36161, .F. ) ;
#23911=VERTEX_POINT ( 'NONE', #31965 ) ;
#23918=CARTESIAN_POINT ( 'NONE',  ( 3.783278058412226752, -14.86148287637761634, 40.39104487792936737 ) ) ;
#23921=DIRECTION ( 'NONE',  ( 0.07836865515943411409, -0.9893941468723573829, 0.1223011693452750320 ) ) ;
#23923=ADVANCED_FACE ( 'NONE', ( #59838 ), #48945, .F. ) ;
#23925=AXIS2_PLACEMENT_3D ( 'NONE', #4874, #14937, #42517 ) ;
#23929=CARTESIAN_POINT ( 'NONE',  ( 4.956653778116960396, -3.690426056930336429, 47.94889704119049867 ) ) ;
#23935=CARTESIAN_POINT ( 'NONE',  ( 1.088908134280557327, -17.14055988408889064, -39.34174992079771016 ) ) ;
#23936=ADVANCED_FACE ( 'NONE', ( #50140 ), #55329, .F. ) ;
#23939=CARTESIAN_POINT ( 'NONE',  ( 0.9756950546413921677, -42.52863374229713855, 5.696573146291832757 ) ) ;
#23941=CARTESIAN_POINT ( 'NONE',  ( 0.6067375320500716374, 0.7090021732340618943, -47.89177856776003495 ) ) ;
#23945=B_SPLINE_CURVE_WITH_KNOTS ( 'NONE', 3,
 ( #44004, #30781, #20468, #35509 ),
 .UNSPECIFIED., .F., .F.,
 ( 4, 4 ),
 ( 1.084202172485504434E-19, 0.004444878191957687789 ),
 .UNSPECIFIED. ) ;
#23948=CARTESIAN_POINT ( 'NONE',  ( 5.959547316686252039, -10.26589671991375674, 17.77392908783916070 ) ) ;
#23959=CARTESIAN_POINT ( 'NONE',  ( 5.981074661064941900, 0.008585178657332563981, 20.52466374824937034 ) ) ;
#23960=CARTESIAN_POINT ( 'NONE',  ( 0.9972139404380295780, -36.82725283858625431, 22.02214929131128329 ) ) ;
#23962=ORIENTED_EDGE ( 'NONE', *, *, #58050, .T. ) ;
#23968=ORIENTED_EDGE ( 'NONE', *, *, #36222, .F. ) ;
#23982=CARTESIAN_POINT ( 'NONE',  ( 0.7056555295713303755, -11.58338207350432825, 46.47980662829228748 ) ) ;
#23985=CARTESIAN_POINT ( 'NONE',  ( 0.9972139404380286898, -37.48536715150211052, -20.88226186415268870 ) ) ;
#23988=FACE_OUTER_BOUND ( 'NONE', #3604, .T. ) ;
#23993=CARTESIAN_POINT ( 'NONE',  ( 0.9722240750034587542, 10.54237121715143388, -41.59310803641446341 ) ) ;
#23995=CARTESIAN_POINT ( 'NONE',  ( 5.958863334805807099, 2.677925489610637921, -20.35021240744032411 ) ) ;
#24002=FACE_OUTER_BOUND ( 'NONE', #30498, .T. ) ;
#24009=ORIENTED_EDGE ( 'NONE', *, *, #17548, .T. ) ;
#24010=CARTESIAN_POINT ( 'NONE',  ( 0.8557997880470697982, 29.88293891557470516, 37.44587306708108088 ) ) ;
#24011=CARTESIAN_POINT ( 'NONE',  ( 0.9730545539215883499, 15.95224156741828914, 39.83279466599044838 ) ) ;
#24012=CARTESIAN_POINT ( 'NONE',  ( 4.967162193818130511, -36.06913038482816347, 23.56777426397165698 ) ) ;
#24022=CARTESIAN_POINT ( 'NONE',  ( 0.5839879882104923592, 0.04539914087015842203, -47.89596766822081264 ) ) ;
#24024=CARTESIAN_POINT ( 'NONE',  ( 5.974727161628367256, 2.694421823322646237, 20.34732802718248479 ) ) ;
#24036=CARTESIAN_POINT ( 'NONE',  ( 3.783198216974391404, -33.06596988314780106, -27.54889409286111857 ) ) ;
#24040=CARTESIAN_POINT ( 'NONE',  ( 0.9754642270333688803, 42.56393738774957569, -5.426415525315391619 ) ) ;
#24041=CARTESIAN_POINT ( 'NONE',  ( 0.5800708057587381505, -11.78915002112689692, -46.42229836006548283 ) ) ;
#24052=B_SPLINE_CURVE_WITH_KNOTS ( 'NONE', 3,
 ( #139, #28667, #52776, #9880 ),
 .UNSPECIFIED., .F., .F.,
 ( 4, 4 ),
 ( 7.790820618110713323E-17, 0.005004741218457486526 ),
 .UNSPECIFIED. ) ;
#24064=ORIENTED_EDGE ( 'NONE', *, *, #8546, .T. ) ;
#24086=CARTESIAN_POINT ( 'NONE',  ( 0.9730545539215883499, 16.88610103448612065, -39.44597740938043273 ) ) ;
#24092=VERTEX_POINT ( 'NONE', #25327 ) ;
#24097=CARTESIAN_POINT ( 'NONE',  ( 0.6846871229502899947, 5.395516691087876460, -47.60345020167345353 ) ) ;
#24098=CARTESIAN_POINT ( 'NONE',  ( 3.660176727303401378, 10.60619300811871746, 46.85282580473582215 ) ) ;
#24106=DIRECTION ( 'NONE',  ( -1.000000000000000000, -0.000000000000000000, -0.000000000000000000 ) ) ;
#24107=LINE ( 'NONE', #909, #41158 ) ;
#24108=FACE_OUTER_BOUND ( 'NONE', #26124, .T. ) ;
#24117=EDGE_LOOP ( 'NONE', ( #46423, #38946 ) ) ;
#24125=CARTESIAN_POINT ( 'NONE',  ( 0.9722240750034566448, -6.177112354444842524, -42.46141201102052776 ) ) ;
#24128=ORIENTED_EDGE ( 'NONE', *, *, #36222, .T. ) ;
#24137=( BOUNDED_SURFACE ( )  B_SPLINE_SURFACE ( 3, 1, ( 
 ( #8029, #27141 ),
 ( #46268, #22442 ),
 ( #41567, #17746 ),
 ( #36873, #8635 ) ),
 .UNSPECIFIED., .F., .F., .F. ) 
 B_SPLINE_SURFACE_WITH_KNOTS ( ( 4, 4 ),
 ( 2, 2 ),
 ( 0.000000000000000000, 1.000000000000000000 ),
 ( 0.000000000000000000, 1.000000000000000000 ),
 .UNSPECIFIED. ) 
 GEOMETRIC_REPRESENTATION_ITEM ( )  RATIONAL_B_SPLINE_SURFACE ( (
 ( 1.000000000000000000, 1.000000000000000000),
 ( 0.9953390228620291325, 0.8624445117761032620),
 ( 0.9953390228620291325, 0.8624445117761032620),
 ( 1.000000000000000000, 1.000000000000000000) ) ) 
 REPRESENTATION_ITEM ( '' )  SURFACE ( )  );
#24141=CARTESIAN_POINT ( 'NONE',  ( 1.227938101723756947, 36.73927144310543014, -22.18841447410681411 ) ) ;
#24142=ORIENTED_EDGE ( 'NONE', *, *, #38097, .T. ) ;
#24143=CARTESIAN_POINT ( 'NONE',  ( 0.5839879327111928697, -33.93179405280464778, -33.80333292213293106 ) ) ;
#24157=( BOUNDED_SURFACE ( )  B_SPLINE_SURFACE ( 3, 1, ( 
 ( #29573, #48683 ),
 ( #59302, #35219 ),
 ( #40862, #50528 ),
 ( #12651, #3213 ) ),
 .UNSPECIFIED., .F., .F., .F. ) 
 B_SPLINE_SURFACE_WITH_KNOTS ( ( 4, 4 ),
 ( 2, 2 ),
 ( 0.000000000000000000, 1.000000000000000000 ),
 ( 0.000000000000000000, 1.000000000000000000 ),
 .UNSPECIFIED. ) 
 GEOMETRIC_REPRESENTATION_ITEM ( )  RATIONAL_B_SPLINE_SURFACE ( (
 ( 1.000000000000000000, 1.000000000000000000),
 ( 0.7269869731126817891, 0.9931720237060910339),
 ( 0.7269869731126817891, 0.9931720237060910339),
 ( 1.000000000000000000, 1.000000000000000000) ) ) 
 REPRESENTATION_ITEM ( '' )  SURFACE ( )  );
#24158=ORIENTED_EDGE ( 'NONE', *, *, #14675, .F. ) ;
#24160=( BOUNDED_SURFACE ( )  B_SPLINE_SURFACE ( 3, 1, ( 
 ( #33194, #47282 ),
 ( #4329, #23464 ),
 ( #18786, #37912 ),
 ( #9363, #28465 ) ),
 .UNSPECIFIED., .F., .F., .F. ) 
 B_SPLINE_SURFACE_WITH_KNOTS ( ( 4, 4 ),
 ( 2, 2 ),
 ( 0.000000000000000000, 1.000000000000000000 ),
 ( 0.000000000000000000, 1.000000000000000000 ),
 .UNSPECIFIED. ) 
 GEOMETRIC_REPRESENTATION_ITEM ( )  RATIONAL_B_SPLINE_SURFACE ( (
 ( 1.000000000000000000, 1.000000000000000000),
 ( 0.7269869731126821222, 0.9931720237060910339),
 ( 0.7269869731126821222, 0.9931720237060910339),
 ( 1.000000000000000000, 1.000000000000000000) ) ) 
 REPRESENTATION_ITEM ( '' )  SURFACE ( )  );
#24163=CARTESIAN_POINT ( 'NONE',  ( 0.5786265663353153954, 41.83999636203319028, 23.32245830379044094 ) ) ;
#24167=CARTESIAN_POINT ( 'NONE',  ( 3.270143674763207553, 9.870732238228656641, -9.482922169187856909 ) ) ;
#24170=CARTESIAN_POINT ( 'NONE',  ( 0.9740398440564311811, 30.04629765303432620, -30.63262235044597759 ) ) ;
#24175=CARTESIAN_POINT ( 'NONE',  ( 0.5832367798473389042, -23.71165515427687609, -41.61463593465329325 ) ) ;
#24181=ORIENTED_EDGE ( 'NONE', *, *, #27341, .T. ) ;
#24187=CARTESIAN_POINT ( 'NONE',  ( 0.9745511491811765792, 5.262846425219600555, 42.58443036172445773 ) ) ;
#24191=B_SPLINE_CURVE_WITH_KNOTS ( 'NONE', 3,
 ( #39566, #44576, #58945, #53313 ),
 .UNSPECIFIED., .F., .F.,
 ( 4, 4 ),
 ( 2.602085213965210642E-18, 0.004050076154992997279 ),
 .UNSPECIFIED. ) ;
#24196=ADVANCED_FACE ( 'NONE', ( #7120 ), #36528, .F. ) ;
#24203=CARTESIAN_POINT ( 'NONE',  ( 1.088313998177382391, 11.85828975620065684, -41.24258460930624892 ) ) ;
#24206=ORIENTED_EDGE ( 'NONE', *, *, #50072, .T. ) ;
#24207=CARTESIAN_POINT ( 'NONE',  ( 4.956653778116971054, 47.05699031914949160, 9.917440902361329691 ) ) ;
#24215=CARTESIAN_POINT ( 'NONE',  ( 4.960156602257182357, 15.40604254112701810, -43.79161740034457750 ) ) ;
#24233=CARTESIAN_POINT ( 'NONE',  ( 0.6067375320500731917, -13.08014790719059128, 46.07640252006475379 ) ) ;
#24255=( BOUNDED_SURFACE ( )  B_SPLINE_SURFACE ( 3, 1, ( 
 ( #9008, #57211 ),
 ( #47237, #33766 ),
 ( #4587, #3979 ),
 ( #23119, #4283 ) ),
 .UNSPECIFIED., .F., .F., .F. ) 
 B_SPLINE_SURFACE_WITH_KNOTS ( ( 4, 4 ),
 ( 2, 2 ),
 ( 0.000000000000000000, 1.000000000000000000 ),
 ( 0.000000000000000000, 1.000000000000000000 ),
 .UNSPECIFIED. ) 
 GEOMETRIC_REPRESENTATION_ITEM ( )  RATIONAL_B_SPLINE_SURFACE ( (
 ( 1.000000000000000000, 1.000000000000000000),
 ( 0.7269869731126821222, 0.9931720237060910339),
 ( 0.7269869731126821222, 0.9931720237060910339),
 ( 1.000000000000000000, 1.000000000000000000) ) ) 
 REPRESENTATION_ITEM ( '' )  SURFACE ( )  );
#24257=CARTESIAN_POINT ( 'NONE',  ( 0.8557997880470690211, 33.22501220301949587, -34.51495345639514767 ) ) ;
#24263=VERTEX_POINT ( 'NONE', #54741 ) ;
#24276=B_SPLINE_CURVE_WITH_KNOTS ( 'NONE', 3,
 ( #10960, #15349, #53224, #49154 ),
 .UNSPECIFIED., .F., .F.,
 ( 4, 4 ),
 ( 1.301042606982605321E-18, 0.004444878191957692126 ),
 .UNSPECIFIED. ) ;
#24277=CARTESIAN_POINT ( 'NONE',  ( 0.9749527285493319040, -39.53206838353031571, -16.68386601451079443 ) ) ;
#24282=EDGE_CURVE ( 'NONE', #60198, #46592, #31247, .T. ) ;
#24300=CARTESIAN_POINT ( 'NONE',  ( 0.9747592971366240144, -42.58247319705098022, -5.279515277919826666 ) ) ;
#24301=CARTESIAN_POINT ( 'NONE',  ( 0.5850706913938533704, -6.431767090163146960, 47.46255051844951822 ) ) ;
#24304=CARTESIAN_POINT ( 'NONE',  ( 4.963659409799329403, 33.96111158240244521, 29.14784479683121887 ) ) ;
#24305=ORIENTED_EDGE ( 'NONE', *, *, #50141, .T. ) ;
#24312=B_SPLINE_CURVE_WITH_KNOTS ( 'NONE', 3,
 ( #46680, #46079, #23172, #55738, #3728, #56355, #56050, #13473, #61059, #60429, #22557, #22862, #41994, #32268, #41680, #51659 ),
 .UNSPECIFIED., .F., .F.,
 ( 4, 3, 3, 3, 3, 4 ),
 ( 9.541595121948225732E-18, 0.0002724568934985560349, 0.0004086836638483799301, 0.0005449104342063581640, 0.0008173270854453656975, 0.001089761613562689226 ),
 .UNSPECIFIED. ) ;
#24318=DIRECTION ( 'NONE',  ( 0.000000000000000000, 0.000000000000000000, 1.000000000000000000 ) ) ;
#24322=EDGE_LOOP ( 'NONE', ( #58411, #54210, #61151, #10896 ) ) ;
#24324=CARTESIAN_POINT ( 'NONE',  ( 0.5839254288179572816, -24.02657516616534750, 41.43367229384574557 ) ) ;
#24325=CARTESIAN_POINT ( 'NONE',  ( 3.407937589446174087, -13.34359005742691373, 3.099921468254956736 ) ) ;
#24328=CARTESIAN_POINT ( 'NONE',  ( 0.9730545539215883499, -30.69604515769671949, 29.98130006528850444 ) ) ;
#24331=DIRECTION ( 'NONE',  ( 0.07836865515943411409, 0.6993330359244814831, 0.7104869166657112878 ) ) ;
#24338=DIRECTION ( 'NONE',  ( -1.000000000000000000, -0.000000000000000000, -0.000000000000000000 ) ) ;
#24341=DIRECTION ( 'NONE',  ( 0.000000000000000000, 0.000000000000000000, 1.000000000000000000 ) ) ;
#24344=CARTESIAN_POINT ( 'NONE',  ( 0.5834872094924177244, -12.61552836343323314, 46.20467604622297131 ) ) ;
#24349=CARTESIAN_POINT ( 'NONE',  ( 1.227938101723756947, 30.94118573761312874, 29.74462687941236538 ) ) ;
#24352=EDGE_CURVE ( 'NONE', #12149, #884, #44694, .T. ) ;
#24354=CARTESIAN_POINT ( 'NONE',  ( 4.956653778116994147, 35.79382859084161339, -32.11725092155005967 ) ) ;
#24359=B_SPLINE_CURVE_WITH_KNOTS ( 'NONE', 3,
 ( #11177, #2052, #25882, #21184, #40626, #21807 ),
 .UNSPECIFIED., .F., .F.,
 ( 4, 2, 4 ),
 ( 8.434507579685065902E-18, 0.0002291978881530156180, 0.0004583957763060228334 ),
 .UNSPECIFIED. ) ;
#24361=CARTESIAN_POINT ( 'NONE',  ( 4.967162193818130511, 0.000000000000000000, 0.000000000000000000 ) ) ;
#24362=CARTESIAN_POINT ( 'NONE',  ( 0.5832366564991511293, 47.44984844891997255, -6.521686574605630504 ) ) ;
#24363=ORIENTED_EDGE ( 'NONE', *, *, #41715, .T. ) ;
#24369=CARTESIAN_POINT ( 'NONE',  ( 0.8557997880470599172, 0.9121262075952832893, -47.89938907511592703 ) ) ;
#24370=ORIENTED_EDGE ( 'NONE', *, *, #38008, .F. ) ;
#24382=ADVANCED_FACE ( 'NONE', ( #5199 ), #15303, .F. ) ;
#24384=ORIENTED_EDGE ( 'NONE', *, *, #38247, .T. ) ;
#24386=EDGE_CURVE ( 'NONE', #36850, #36264, #14643, .T. ) ;
#24403=CARTESIAN_POINT ( 'NONE',  ( 0.9757787079277461251, -21.48842038179459735, 37.14005577278813064 ) ) ;
#24419=CARTESIAN_POINT ( 'NONE',  ( 0.7762777257811881437, 47.37038525518534726, 7.133808567472427420 ) ) ;
#24422=VERTEX_POINT ( 'NONE', #5505 ) ;
#24426=B_SPLINE_CURVE_WITH_KNOTS ( 'NONE', 3,
 ( #46759, #22945, #37057, #28542, #42992, #23543 ),
 .UNSPECIFIED., .F., .F.,
 ( 4, 2, 4 ),
 ( 1.056081928668503685E-17, 0.0002291978881530176780, 0.0004583957763060247850 ),
 .UNSPECIFIED. ) ;
#24431=EDGE_CURVE ( 'NONE', #37022, #23510, #51420, .T. ) ;
#24432=CARTESIAN_POINT ( 'NONE',  ( 0.5800708057587384836, 23.40241940841957202, 41.78924035064532205 ) ) ;
#24447=AXIS2_PLACEMENT_3D ( 'NONE', #13843, #57318, #18225 ) ;
#24451=CARTESIAN_POINT ( 'NONE',  ( 0.8557997880470599172, -29.88293891557496096, 37.44587306708088192 ) ) ;
#24452=ORIENTED_EDGE ( 'NONE', *, *, #20237, .F. ) ;
#24455=CARTESIAN_POINT ( 'NONE',  ( 0.5837374860065638327, -33.99581326751410870, -33.73893264285585047 ) ) ;
#24456=CARTESIAN_POINT ( 'NONE',  ( 3.660087539127326206, -40.62968541507459719, 25.63019641081313438 ) ) ;
#24461=ORIENTED_EDGE ( 'NONE', *, *, #4934, .F. ) ;
#24462=CARTESIAN_POINT ( 'NONE',  ( 0.9741495583595161101, 25.80610403442907952, 34.28086552274301368 ) ) ;
#24463=CARTESIAN_POINT ( 'NONE',  ( 4.963659409799332067, 29.14784479683110163, 33.96111158240255889 ) ) ;
#24470=EDGE_CURVE ( 'NONE', #58260, #23595, #17833, .T. ) ;
#24471=EDGE_LOOP ( 'NONE', ( #34530, #32846, #60176, #57408 ) ) ;
#24475=CARTESIAN_POINT ( 'NONE',  ( 0.5839880159502333079, -44.23273844814451650, -18.37091806000283967 ) ) ;
#24476=CARTESIAN_POINT ( 'NONE',  ( 0.8557997880470599172, 0.9121262075952832893, -47.89938907511592703 ) ) ;
#24481=CARTESIAN_POINT ( 'NONE',  ( 3.660176727303401378, -25.63023984566673974, 40.62966184289481220 ) ) ;
#24488=FACE_OUTER_BOUND ( 'NONE', #47964, .T. ) ;
#24490=ORIENTED_EDGE ( 'NONE', *, *, #4012, .T. ) ;
#24492=AXIS2_PLACEMENT_3D ( 'NONE', #17114, #45326, #46549 ) ;
#24496=CARTESIAN_POINT ( 'NONE',  ( 5.960721111146673579, -20.35079619394247885, 2.672857320902960243 ) ) ;
#24497=LINE ( 'NONE', #4436, #7940 ) ;
#24499=ORIENTED_EDGE ( 'NONE', *, *, #42718, .T. ) ;
#24501=( BOUNDED_SURFACE ( )  B_SPLINE_SURFACE ( 3, 1, ( 
 ( #44860, #40787 ),
 ( #58589, #30722 ),
 ( #12266, #35451 ),
 ( #54509, #11022 ) ),
 .UNSPECIFIED., .F., .F., .F. ) 
 B_SPLINE_SURFACE_WITH_KNOTS ( ( 4, 4 ),
 ( 2, 2 ),
 ( 0.000000000000000000, 1.000000000000000000 ),
 ( 0.000000000000000000, 1.000000000000000000 ),
 .UNSPECIFIED. ) 
 GEOMETRIC_REPRESENTATION_ITEM ( )  RATIONAL_B_SPLINE_SURFACE ( (
 ( 1.000000000000000000, 1.000000000000000000),
 ( 0.7269869731126817891, 0.9931720237060910339),
 ( 0.7269869731126817891, 0.9931720237060910339),
 ( 1.000000000000000000, 1.000000000000000000) ) ) 
 REPRESENTATION_ITEM ( '' )  SURFACE ( )  );
#24505=ORIENTED_EDGE ( 'NONE', *, *, #7228, .T. ) ;
#24511=ORIENTED_EDGE ( 'NONE', *, *, #60317, .T. ) ;
#24514=CARTESIAN_POINT ( 'NONE',  ( 0.9757892942422830007, -34.07281211842306590, -26.08029006934572180 ) ) ;
#24526=EDGE_CURVE ( 'NONE', #20520, #1247, #7247, .T. ) ;
#24531=ADVANCED_FACE ( 'NONE', ( #50587 ), #3962, .T. ) ;
#24542=CIRCLE ( 'NONE', #29540, 43.08621763946400307 ) ;
#24547=CARTESIAN_POINT ( 'NONE',  ( 0.9730545539215883499, -21.01499094264522682, -37.40983423658496321 ) ) ;
#24548=CARTESIAN_POINT ( 'NONE',  ( 1.154321485836933059, -17.18284940416421591, -39.32643515542051915 ) ) ;
#24551=B_SPLINE_CURVE_WITH_KNOTS ( 'NONE', 3,
 ( #12377, #46202, #54316, #7639, #31786, #11439, #30521, #49958, #49638, #7011, #45281, #7321, #26145, #2323, #35874, #42734, #8895, #51796, #37120 ),
 .UNSPECIFIED., .F., .F.,
 ( 4, 3, 3, 3, 3, 3, 4 ),
 ( 0.000000000000000000, 0.0002724573126191774902, 0.0004086839781548475556, 0.0005449106435901796431, 0.0006811373090491484221, 0.0008459866663933725186, 0.001010840725717214450 ),
 .UNSPECIFIED. ) ;
#24559=CARTESIAN_POINT ( 'NONE',  ( 1.227938101723756947, 11.92353943227949387, 41.23019537246713639 ) ) ;
#24561=ORIENTED_EDGE ( 'NONE', *, *, #53581, .T. ) ;
#24562=CARTESIAN_POINT ( 'NONE',  ( 0.9722240750034567558, -42.46141201102050644, 6.177112354444973086 ) ) ;
#24572=CARTESIAN_POINT ( 'NONE',  ( 0.9754642270333674370, -26.26019354539063144, 33.93430397636404905 ) ) ;
#24573=CARTESIAN_POINT ( 'NONE',  ( 5.958863334805807099, 12.49425770716465678, 16.28483817244743292 ) ) ;
#24574=CARTESIAN_POINT ( 'NONE',  ( 0.9745511491811743587, -11.43411988112632471, 41.35688774886285302 ) ) ;
#24586=CARTESIAN_POINT ( 'NONE',  ( 0.5838002273316443835, -41.41085122398235541, -24.06583301632245409 ) ) ;
#24588=EDGE_LOOP ( 'NONE', ( #35784, #368, #35265, #7320 ) ) ;
#24591=LINE ( 'NONE', #38105, #18343 ) ;
#24592=CARTESIAN_POINT ( 'NONE',  ( 0.8557997880470697982, -41.02602466100796619, 24.73961900479237386 ) ) ;
#24593=AXIS2_PLACEMENT_3D ( 'NONE', #27367, #45568, #31772 ) ;
#24597=B_SPLINE_CURVE_WITH_KNOTS ( 'NONE', 3,
 ( #30858, #7034, #35894, #26162, #2343, #45299, #42154, #13628, #3262, #36511, #60277, #56204, #32733, #32113, #22392, #37442, #8588, #46222, #61209 ),
 .UNSPECIFIED., .F., .F.,
 ( 4, 3, 3, 3, 3, 3, 4 ),
 ( 4.878909776184769953E-18, 0.0002724573126191761892, 0.0004086839781548490735, 0.0005449106435901837631, 0.0006811373090491487474, 0.0008459866663933690491, 0.001010840725717212715 ),
 .UNSPECIFIED. ) ;
#24600=CARTESIAN_POINT ( 'NONE',  ( 5.959828726073459926, 2.674641840415901139, 20.35060134307035540 ) ) ;
#24602=CIRCLE ( 'NONE', #32615, 8.000000000000000000 ) ;
#24606=VERTEX_POINT ( 'NONE', #46854 ) ;
#24611=ORIENTED_EDGE ( 'NONE', *, *, #40922, .F. ) ;
#24615=( BOUNDED_SURFACE ( )  B_SPLINE_SURFACE ( 3, 1, ( 
 ( #58831, #30335 ),
 ( #54124, #44782 ),
 ( #40094, #38849 ),
 ( #35067, #15338 ) ),
 .UNSPECIFIED., .F., .F., .F. ) 
 B_SPLINE_SURFACE_WITH_KNOTS ( ( 4, 4 ),
 ( 2, 2 ),
 ( 0.000000000000000000, 1.000000000000000000 ),
 ( 0.000000000000000000, 1.000000000000000000 ),
 .UNSPECIFIED. ) 
 GEOMETRIC_REPRESENTATION_ITEM ( )  RATIONAL_B_SPLINE_SURFACE ( (
 ( 1.000000000000000000, 1.000000000000000000),
 ( 0.9953390228620291325, 0.8624445117761032620),
 ( 0.9953390228620291325, 0.8624445117761032620),
 ( 1.000000000000000000, 1.000000000000000000) ) ) 
 REPRESENTATION_ITEM ( '' )  SURFACE ( )  );
#24616=CARTESIAN_POINT ( 'NONE',  ( 0.5819845901640484653, 28.79568196372268574, 38.27312528999442520 ) ) ;
#24619=EDGE_CURVE ( 'NONE', #2619, #51439, #4196, .T. ) ;
#24622=CARTESIAN_POINT ( 'NONE',  ( 0.5839879882012682932, 23.94795769224444726, -41.47913983251925885 ) ) ;
#24624=VERTEX_POINT ( 'NONE', #31815 ) ;
#24632=CARTESIAN_POINT ( 'NONE',  ( 3.660176727303419586, 47.83637937224830949, -4.399934609596090951 ) ) ;
#24633=CARTESIAN_POINT ( 'NONE',  ( 0.6067375320500718594, 47.89177856776005626, 0.7090021732335601845 ) ) ;
#24635=CARTESIAN_POINT ( 'NONE',  ( 0.9745511491811736926, 39.77127619790164914, -16.10518088436863238 ) ) ;
#24641=CARTESIAN_POINT ( 'NONE',  ( 5.959547316686252039, 2.682663672454912440, -20.34955788964373724 ) ) ;
#24645=CARTESIAN_POINT ( 'NONE',  ( 0.8551540677456739292, -5.348818140990592163, -47.61725548905996419 ) ) ;
#24653=EDGE_LOOP ( 'NONE', ( #57373, #58229, #6628, #14779 ) ) ;
#24658=CARTESIAN_POINT ( 'NONE',  ( 0.9730545539215883499, 0.5054011016612682816, 42.90536227157002003 ) ) ;
#24662=CARTESIAN_POINT ( 'NONE',  ( -17.97369999999976642, -7.719455939378113030, 2.099999999999994760 ) ) ;
#24667=B_SPLINE_CURVE_WITH_KNOTS ( 'NONE', 3,
 ( #9334, #14986, #13756, #10274, #9643, #33473 ),
 .UNSPECIFIED., .F., .F.,
 ( 4, 2, 4 ),
 ( 3.511543213478341086E-18, 0.0002445244328975359387, 0.0004890488657950682995 ),
 .UNSPECIFIED. ) ;
#24668=CARTESIAN_POINT ( 'NONE',  ( 5.960721111146673579, -12.49016043756459915, -16.28787783074223228 ) ) ;
#24669=CARTESIAN_POINT ( 'NONE',  ( 0.5837374860065647209, 47.46223477511620814, -6.431731162805296442 ) ) ;
#24670=VERTEX_POINT ( 'NONE', #5120 ) ;
#24673=VECTOR ( 'NONE', #43456, 1000.000000000000227 ) ;
#24677=( GEOMETRIC_REPRESENTATION_CONTEXT ( 3 ) GLOBAL_UNCERTAINTY_ASSIGNED_CONTEXT ( ( #52377 ) ) GLOBAL_UNIT_ASSIGNED_CONTEXT ( ( #27903, #22900, #41409 ) ) REPRESENTATION_CONTEXT ( 'NONE', 'WORKASPACE' ) );
#24678=VERTEX_POINT ( 'NONE', #42767 ) ;
#24685=CARTESIAN_POINT ( 'NONE',  ( 5.981074661064941900, 16.28853686865582517, 12.48781255314294469 ) ) ;
#24686=ORIENTED_EDGE ( 'NONE', *, *, #43239, .T. ) ;
#24693=CARTESIAN_POINT ( 'NONE',  ( 5.981074661064941900, 17.77917279944618301, 10.25489689131136650 ) ) ;
#24699=CARTESIAN_POINT ( 'NONE',  ( 0.6067375320500733027, 11.71046088714751399, 46.44340905096866834 ) ) ;
#24702=EDGE_LOOP ( 'NONE', ( #1674, #26029, #13587, #49040 ) ) ;
#24703=CIRCLE ( 'NONE', #4669, 43.08621763946400307 ) ;
#24711=ORIENTED_EDGE ( 'NONE', *, *, #2527, .F. ) ;
#24713=CARTESIAN_POINT ( 'NONE',  ( 0.5809828226811617480, -38.32755012159166341, 28.72298383114474518 ) ) ;
#24732=VECTOR ( 'NONE', #38315, 1000.000000000000000 ) ;
#24736=CARTESIAN_POINT ( 'NONE',  ( 2.526552050251863246, 39.22765360404650181, 17.56110221699841745 ) ) ;
#24739=CARTESIAN_POINT ( 'NONE',  ( 0.9749527285493305717, -37.30179927241191251, 21.20640438431177444 ) ) ;
#24740=CARTESIAN_POINT ( 'NONE',  ( 0.8557997880470599172, 46.03118133706026072, 13.27832040216655507 ) ) ;
#24741=EDGE_CURVE ( 'NONE', #42439, #27088, #28128, .T. ) ;
#24746=CARTESIAN_POINT ( 'NONE',  ( 0.8551540677456715978, 7.157691013574362771, 47.37911285756622704 ) ) ;
#24750=CARTESIAN_POINT ( 'NONE',  ( 0.5809828226811617480, 37.66417181417551774, 29.58751527316192664 ) ) ;
#24753=CARTESIAN_POINT ( 'NONE',  ( 0.5809828226811617480, 23.47450554821709900, 41.74875432577658074 ) ) ;
#24755=CARTESIAN_POINT ( 'NONE',  ( 3.783278058412226308, -39.06943705276843559, 18.05212641201958590 ) ) ;
#24758=CARTESIAN_POINT ( 'NONE',  ( 4.956653778116991482, -14.93973939759855263, -45.71126949320266419 ) ) ;
#24773=VERTEX_POINT ( 'NONE', #29253 ) ;
#24782=CARTESIAN_POINT ( 'NONE',  ( 0.5809828226811544205, -28.72298383114515374, 38.32755012159135077 ) ) ;
#24784=ORIENTED_EDGE ( 'NONE', *, *, #51062, .T. ) ;
#24786=CARTESIAN_POINT ( 'NONE',  ( 0.9722240741986389878, 33.68410525900284114, 26.58024228478306483 ) ) ;
#24788=AXIS2_PLACEMENT_3D ( 'NONE', #51500, #4492, #56820 ) ;
#24789=B_SPLINE_CURVE_WITH_KNOTS ( 'NONE', 3,
 ( #15897, #50315, #21508, #7383 ),
 .UNSPECIFIED., .F., .F.,
 ( 4, 4 ),
 ( 6.254634441385501517E-18, 0.004050076154993002484 ),
 .UNSPECIFIED. ) ;
#24791=CARTESIAN_POINT ( 'NONE',  ( 0.5832366564991509073, -44.14509737861659033, 18.58038995918336767 ) ) ;
#24792=CARTESIAN_POINT ( 'NONE',  ( 0.8557997880470599172, 46.03118133706026072, 13.27832040216655507 ) ) ;
#24795=CARTESIAN_POINT ( 'NONE',  ( 0.8557997880470690211, 33.22501220301949587, -34.51495345639514767 ) ) ;
#24797=CARTESIAN_POINT ( 'NONE',  ( 0.5807400328401637335, -46.12278621143506285, 12.92266817605998952 ) ) ;
#24802=( BOUNDED_SURFACE ( )  B_SPLINE_SURFACE ( 3, 1, ( 
 ( #17177, #41012 ),
 ( #46015, #50365 ),
 ( #13100, #60674 ),
 ( #27485, #55360 ) ),
 .UNSPECIFIED., .F., .F., .F. ) 
 B_SPLINE_SURFACE_WITH_KNOTS ( ( 4, 4 ),
 ( 2, 2 ),
 ( 0.000000000000000000, 1.000000000000000000 ),
 ( 0.000000000000000000, 1.000000000000000000 ),
 .UNSPECIFIED. ) 
 GEOMETRIC_REPRESENTATION_ITEM ( )  RATIONAL_B_SPLINE_SURFACE ( (
 ( 1.000000000000000000, 1.000000000000000000),
 ( 0.9732289882329797637, 0.9999525324661233672),
 ( 0.9732289882329797637, 0.9999525324661233672),
 ( 1.000000000000000000, 1.000000000000000000) ) ) 
 REPRESENTATION_ITEM ( '' )  SURFACE ( )  );
#24810=ORIENTED_EDGE ( 'NONE', *, *, #33673, .T. ) ;
#24823=AXIS2_PLACEMENT_3D ( 'NONE', #2972, #45926, #17705 ) ;
#24825=ORIENTED_EDGE ( 'NONE', *, *, #6901, .T. ) ;
#24833=VERTEX_POINT ( 'NONE', #50215 ) ;
#24836=EDGE_CURVE ( 'NONE', #13813, #52796, #1266, .T. ) ;
#24841=DIRECTION ( 'NONE',  ( -1.000000000000000000, -0.000000000000000000, -0.000000000000000000 ) ) ;
#24849=CARTESIAN_POINT ( 'NONE',  ( 4.967162193818130511, 0.000000000000000000, 0.000000000000000000 ) ) ;
#24851=CARTESIAN_POINT ( 'NONE',  ( 2.624215991343608501, 40.85210347989531243, 25.21574086439720119 ) ) ;
#24853=CARTESIAN_POINT ( 'NONE',  ( 4.967162193818131399, -19.45289607368795259, -38.44485641567092671 ) ) ;
#24854=CARTESIAN_POINT ( 'NONE',  ( 4.967162193818130511, -32.68434214048149045, -28.07411493385329138 ) ) ;
#24855=VECTOR ( 'NONE', #30991, 1000.000000000000114 ) ;
#24857=VERTEX_POINT ( 'NONE', #6336 ) ;
#24868=CARTESIAN_POINT ( 'NONE',  ( 4.960156602257182357, 35.23783291257208106, -30.22163187094351144 ) ) ;
#24869=FACE_OUTER_BOUND ( 'NONE', #14701, .T. ) ;
#24871=CARTESIAN_POINT ( 'NONE',  ( 4.303969348037258058, 4.133486515473990153, -47.93217632892343971 ) ) ;
#24884=CARTESIAN_POINT ( 'NONE',  ( 4.963659409799330291, 29.86601237216407156, 33.33129552235096327 ) ) ;
#24888=ORIENTED_EDGE ( 'NONE', *, *, #56856, .T. ) ;
#24892=VECTOR ( 'NONE', #15873, 999.9999999999998863 ) ;
#24897=CARTESIAN_POINT ( 'NONE',  ( 5.960721111146673579, 7.860635756377621242, 18.96073515164551537 ) ) ;
#24900=B_SPLINE_CURVE_WITH_KNOTS ( 'NONE', 3,
 ( #8453, #46710, #23193, #50761 ),
 .UNSPECIFIED., .F., .F.,
 ( 4, 4 ),
 ( 0.000000000000000000, 0.004446090762761377262 ),
 .UNSPECIFIED. ) ;
#24904=ADVANCED_FACE ( 'NONE', ( #60215 ), #28093, .F. ) ;
#24908=( BOUNDED_SURFACE ( )  B_SPLINE_SURFACE ( 3, 1, ( 
 ( #55666, #50973 ),
 ( #8070, #35680 ),
 ( #27180, #54740 ),
 ( #49747, #6809 ) ),
 .UNSPECIFIED., .F., .F., .F. ) 
 B_SPLINE_SURFACE_WITH_KNOTS ( ( 4, 4 ),
 ( 2, 2 ),
 ( 0.000000000000000000, 1.000000000000000000 ),
 ( 0.000000000000000000, 1.000000000000000000 ),
 .UNSPECIFIED. ) 
 GEOMETRIC_REPRESENTATION_ITEM ( )  RATIONAL_B_SPLINE_SURFACE ( (
 ( 1.000000000000000000, 1.000000000000000000),
 ( 0.9953390228620291325, 0.8624445117761032620),
 ( 0.9953390228620291325, 0.8624445117761032620),
 ( 1.000000000000000000, 1.000000000000000000) ) ) 
 REPRESENTATION_ITEM ( '' )  SURFACE ( )  );
#24914=( BOUNDED_SURFACE ( )  B_SPLINE_SURFACE ( 3, 1, ( 
 ( #61707, #1167 ),
 ( #4081, #23221 ),
 ( #20605, #56712 ),
 ( #52322, #58477 ) ),
 .UNSPECIFIED., .F., .F., .F. ) 
 B_SPLINE_SURFACE_WITH_KNOTS ( ( 4, 4 ),
 ( 2, 2 ),
 ( 0.000000000000000000, 1.000000000000000000 ),
 ( 0.000000000000000000, 1.000000000000000000 ),
 .UNSPECIFIED. ) 
 GEOMETRIC_REPRESENTATION_ITEM ( )  RATIONAL_B_SPLINE_SURFACE ( (
 ( 1.000000000000000000, 1.000000000000000000),
 ( 0.7269869731126821222, 0.9931720237060910339),
 ( 0.7269869731126821222, 0.9931720237060910339),
 ( 1.000000000000000000, 1.000000000000000000) ) ) 
 REPRESENTATION_ITEM ( '' )  SURFACE ( )  );
#24921=CARTESIAN_POINT ( 'NONE',  ( 2.281448460670567169, 19.56578495220171021, 43.80196084514285815 ) ) ;
#24922=VECTOR ( 'NONE', #38683, 1000.000000000000000 ) ;
#24923=ORIENTED_EDGE ( 'NONE', *, *, #4675, .F. ) ;
#24924=CARTESIAN_POINT ( 'NONE',  ( 4.963659409799330291, -29.86601237216385485, -33.33129552235118354 ) ) ;
#24931=CARTESIAN_POINT ( 'NONE',  ( 0.5809828226811553087, -0.5448590168529036104, -47.89273459658654275 ) ) ;
#24932=CARTESIAN_POINT ( 'NONE',  ( 4.303969348037258058, 40.54345935592815664, -25.89994482339327320 ) ) ;
#24934=CARTESIAN_POINT ( 'NONE',  ( 0.5807400328401574052, -47.89582301953902999, -0.5448834511094979849 ) ) ;
#24937=CARTESIAN_POINT ( 'NONE',  ( 0.5836750258453350382, 24.10509086647810051, -41.38803015411981789 ) ) ;
#24954=CARTESIAN_POINT ( 'NONE',  ( 5.960221823109900008, 2.684531185214417803, -20.34928172836727711 ) ) ;
#24962=CARTESIAN_POINT ( 'NONE',  ( 1.154321713695927176, 29.75729669971110880, 30.92445811446658510 ) ) ;
#24964=CARTESIAN_POINT ( 'NONE',  ( 4.963659409799330291, -29.14784479683089558, -33.96111158240276495 ) ) ;
#24968=FACE_OUTER_BOUND ( 'NONE', #27451, .T. ) ;
#24970=CARTESIAN_POINT ( 'NONE',  ( 0.8551540677456834771, 33.23105123575948028, -34.52115452272894203 ) ) ;
#24971=CARTESIAN_POINT ( 'NONE',  ( 5.959547316686252039, -16.28190225198610008, -12.49803383497744136 ) ) ;
#24977=ORIENTED_EDGE ( 'NONE', *, *, #61263, .T. ) ;
#24978=EDGE_CURVE ( 'NONE', #18352, #33579, #54291, .T. ) ;
#24985=CARTESIAN_POINT ( 'NONE',  ( 0.5827357941260212781, 47.43746130990125920, -6.611647889510720688 ) ) ;
#24998=CARTESIAN_POINT ( 'NONE',  ( 3.660087539127327982, -47.34518630204117073, 8.130906407639885813 ) ) ;
#25004=ORIENTED_EDGE ( 'NONE', *, *, #52828, .T. ) ;
#25009=CARTESIAN_POINT ( 'NONE',  ( 0.9749527285493315709, 33.86694354778357052, 26.34702925571509624 ) ) ;
#25012=CARTESIAN_POINT ( 'NONE',  ( 0.5809828226811556418, -5.711058609465654357, 47.55412398569204413 ) ) ;
#25020=EDGE_CURVE ( 'NONE', #36409, #58875, #8521, .T. ) ;
#25029=CARTESIAN_POINT ( 'NONE',  ( 5.959547316686252039, -18.96183906913549322, 7.858107265727413804 ) ) ;
#25036=LINE ( 'NONE', #19727, #40267 ) ;
#25039=ORIENTED_EDGE ( 'NONE', *, *, #48770, .F. ) ;
#25040=EDGE_CURVE ( 'NONE', #39239, #54529, #18491, .T. ) ;
#25043=CARTESIAN_POINT ( 'NONE',  ( 0.5834872094924155039, 18.53852119651626396, -44.16273175734626477 ) ) ;
#25048=CARTESIAN_POINT ( 'NONE',  ( 0.9756950546413950542, -37.11135009583540523, 21.53795086961250149 ) ) ;
#25049=CARTESIAN_POINT ( 'NONE',  ( 0.9745511491811745808, 16.73445648040624789, -39.51062171155243874 ) ) ;
#25054=CARTESIAN_POINT ( 'NONE',  ( 1.227938101723748288, -41.23019537246701560, -11.92353943227992197 ) ) ;
#25069=CARTESIAN_POINT ( 'NONE',  ( 4.963659409799328515, -39.92545197189537021, -20.22157859941772529 ) ) ;
#25078=CIRCLE ( 'NONE', #23079, 48.09070567114147110 ) ;
#25080=CARTESIAN_POINT ( 'NONE',  ( 5.960221823109900008, 0.005450390361721958211, -20.52559243573973546 ) ) ;
#25090=B_SPLINE_CURVE_WITH_KNOTS ( 'NONE', 3,
 ( #36248, #27137, #50617, #3007 ),
 .UNSPECIFIED., .F., .F.,
 ( 4, 4 ),
 ( 0.000000000000000000, 0.004446090762761357312 ),
 .UNSPECIFIED. ) ;
#25094=CARTESIAN_POINT ( 'NONE',  ( 0.7057020205115043243, 46.04437542275044137, 13.20843872046504330 ) ) ;
#25095=( BOUNDED_SURFACE ( )  B_SPLINE_SURFACE ( 3, 1, ( 
 ( #44982, #25225 ),
 ( #39350, #30227 ),
 ( #1704, #44368 ),
 ( #20843, #44071 ) ),
 .UNSPECIFIED., .F., .F., .F. ) 
 B_SPLINE_SURFACE_WITH_KNOTS ( ( 4, 4 ),
 ( 2, 2 ),
 ( 0.000000000000000000, 1.000000000000000000 ),
 ( 0.000000000000000000, 1.000000000000000000 ),
 .UNSPECIFIED. ) 
 GEOMETRIC_REPRESENTATION_ITEM ( )  RATIONAL_B_SPLINE_SURFACE ( (
 ( 1.000000000000000000, 1.000000000000000000),
 ( 0.9732289882329797637, 0.9999525324661233672),
 ( 0.9732289882329797637, 0.9999525324661233672),
 ( 1.000000000000000000, 1.000000000000000000) ) ) 
 REPRESENTATION_ITEM ( '' )  SURFACE ( )  );
#25098=CARTESIAN_POINT ( 'NONE',  ( 0.8551540677456715978, 41.94570365541235901, -23.16399837394502015 ) ) ;
#25099=CARTESIAN_POINT ( 'NONE',  ( -15.88746099330916373, -7.996356313915863545, -0.2766558318553649642 ) ) ;
#25105=CARTESIAN_POINT ( 'NONE',  ( 0.8551540677456715978, -28.44084013485092655, -38.56334384152460615 ) ) ;
#25113=VERTEX_POINT ( 'NONE', #58587 ) ;
#25117=EDGE_CURVE ( 'NONE', #47332, #17815, #489, .T. ) ;
#25133=CARTESIAN_POINT ( 'NONE',  ( 0.9730545539215892381, 39.83279466599039154, 15.95224156741843835 ) ) ;
#25135=EDGE_LOOP ( 'NONE', ( #49560, #59560, #38425, #42916 ) ) ;
#25139=DIRECTION ( 'NONE',  ( -0.07439287786467652097, -0.5100024374914818859, -0.8569499480575037964 ) ) ;
#25150=ORIENTED_EDGE ( 'NONE', *, *, #10126, .F. ) ;
#25157=AXIS2_PLACEMENT_3D ( 'NONE', #15609, #53180, #10285 ) ;
#25163=CARTESIAN_POINT ( 'NONE',  ( 0.8551540677456834771, -34.52115452272905571, -33.23105123575936659 ) ) ;
#25165=DIRECTION ( 'NONE',  ( 1.000000000000000000, -0.000000000000000000, -0.000000000000000000 ) ) ;
#25170=ADVANCED_FACE ( 'NONE', ( #59217 ), #51308, .F. ) ;
#25173=CARTESIAN_POINT ( 'NONE',  ( 0.5800708119828333897, 29.65250521075944334, 37.61306658477484888 ) ) ;
#25175=CARTESIAN_POINT ( 'NONE',  ( 0.5839880159502348622, -41.50181427378120702, 23.90868446765462707 ) ) ;
#25178=CARTESIAN_POINT ( 'NONE',  ( 0.9736507210033049642, -26.47691119766813728, 33.76542629919396887 ) ) ;
#25183=DIRECTION ( 'NONE',  ( -1.000000000000000000, -0.000000000000000000, -0.000000000000000000 ) ) ;
#25186=B_SPLINE_CURVE_WITH_KNOTS ( 'NONE', 3,
 ( #3953, #46917, #47210, #42519 ),
 .UNSPECIFIED., .F., .F.,
 ( 4, 4 ),
 ( 7.296157027441120170E-17, 0.005004741218457514282 ),
 .UNSPECIFIED. ) ;
#25191=EDGE_LOOP ( 'NONE', ( #50412, #48482, #41438, #18981 ) ) ;
#25196=VERTEX_POINT ( 'NONE', #59849 ) ;
#25209=EDGE_CURVE ( 'NONE', #7463, #49001, #40035, .T. ) ;
#25212=ORIENTED_EDGE ( 'NONE', *, *, #11084, .F. ) ;
#25216=CARTESIAN_POINT ( 'NONE',  ( 5.981074661064941900, 14.51919955600735612, -14.50705827991430930 ) ) ;
#25225=CARTESIAN_POINT ( 'NONE',  ( 0.5807400328401574052, 23.47602859900773353, -41.75144119563861267 ) ) ;
#25226=CARTESIAN_POINT ( 'NONE',  ( 5.960221823109900008, 2.684531185214145577, 20.34928172836731619 ) ) ;
#25247=CARTESIAN_POINT ( 'NONE',  ( 4.956653778116987930, -47.05699031914942054, -9.917440902361647659 ) ) ;
#25251=CARTESIAN_POINT ( 'NONE',  ( 4.956653778116989706, -40.28700667097662347, -26.26162724282415084 ) ) ;
#25252=CARTESIAN_POINT ( 'NONE',  ( 4.956653778116975495, -9.917440902361487787, 47.05699031914946318 ) ) ;
#25256=LINE ( 'NONE', #38769, #10607 ) ;
#25258=LINE ( 'NONE', #44401, #48899 ) ;
#25262=B_SPLINE_CURVE_WITH_KNOTS ( 'NONE', 3,
 ( #2914, #12047, #31121, #7289 ),
 .UNSPECIFIED., .F., .F.,
 ( 4, 4 ),
 ( 0.000000000000000000, 0.004446090762761356445 ),
 .UNSPECIFIED. ) ;
#25271=CARTESIAN_POINT ( 'NONE',  ( 0.5827357941260216112, -47.43746130990120236, 6.611647889511030662 ) ) ;
#25277=CARTESIAN_POINT ( 'NONE',  ( -19.65183073023187532, -7.897491201526634974, 1.291549906873825870 ) ) ;
#25281=CARTESIAN_POINT ( 'NONE',  ( 4.956653778117001252, 47.27023054223765541, -8.845409907520457082 ) ) ;
#25283=EDGE_CURVE ( 'NONE', #38360, #57884, #54959, .T. ) ;
#25287=CARTESIAN_POINT ( 'NONE',  ( 0.9730545539215883499, 42.90536227157002003, -0.5054011016614180507 ) ) ;
#25296=VERTEX_POINT ( 'NONE', #51988 ) ;
#25298=ORIENTED_EDGE ( 'NONE', *, *, #5935, .T. ) ;
#25300=VERTEX_POINT ( 'NONE', #58752 ) ;
#25303=CARTESIAN_POINT ( 'NONE',  ( 0.9745511491811754690, 33.83313387735789490, 26.39034508612545693 ) ) ;
#25306=CARTESIAN_POINT ( 'NONE',  ( 3.270143674763207553, -8.113405361969434182, -11.02405647745178641 ) ) ;
#25307=ADVANCED_FACE ( 'NONE', ( #24968 ), #55694, .F. ) ;
#25311=B_SPLINE_CURVE_WITH_KNOTS ( 'NONE', 3,
 ( #13253, #42385, #32667, #51129 ),
 .UNSPECIFIED., .F., .F.,
 ( 4, 4 ),
 ( 0.000000000000000000, 0.004446090762761359047 ),
 .UNSPECIFIED. ) ;
#25313=CARTESIAN_POINT ( 'NONE',  ( 0.8557997880470690211, -24.73961900479222820, -41.02602466100805145 ) ) ;
#25321=CARTESIAN_POINT ( 'NONE',  ( 0.5809828226811553087, 6.791453954330313181, 47.41188724015881917 ) ) ;
#25326=CARTESIAN_POINT ( 'NONE',  ( 0.6067375320500727476, -38.42671567536872601, 28.59217831627001516 ) ) ;
#25327=CARTESIAN_POINT ( 'NONE',  ( 4.967162193818131399, -42.34252806656588319, -7.970725651240238463 ) ) ;
#25328=B_SPLINE_CURVE_WITH_KNOTS ( 'NONE', 3,
 ( #10283, #11515, #54087, #34710 ),
 .UNSPECIFIED., .F., .F.,
 ( 4, 4 ),
 ( 4.470280076681872512E-19, 0.004048833967417084755 ),
 .UNSPECIFIED. ) ;
#25329=CARTESIAN_POINT ( 'NONE',  ( 5.965394784446458765, -18.96850062921629743, -7.841344330024877074 ) ) ;
#25331=B_SPLINE_CURVE_WITH_KNOTS ( 'NONE', 3,
 ( #52634, #38888, #43276, #33560 ),
 .UNSPECIFIED., .F., .F.,
 ( 4, 4 ),
 ( 1.939479807224432123E-18, 0.004050076154992998147 ),
 .UNSPECIFIED. ) ;
#25333=B_SPLINE_CURVE_WITH_KNOTS ( 'NONE', 3,
 ( #5216, #52846, #24036, #201 ),
 .UNSPECIFIED., .F., .F.,
 ( 4, 4 ),
 ( 1.734723475976807094E-18, 0.004048833967417087357 ),
 .UNSPECIFIED. ) ;
#25339=CARTESIAN_POINT ( 'NONE',  ( 4.956653778116966613, 0.000000000000000000, 0.000000000000000000 ) ) ;
#25341=EDGE_CURVE ( 'NONE', #41494, #23520, #48218, .T. ) ;
#25343=VECTOR ( 'NONE', #61665, 1000.000000000000114 ) ;
#25353=CARTESIAN_POINT ( 'NONE',  ( 0.5809828226811553087, -24.41822904836894637, -41.20389530892332886 ) ) ;
#25355=CARTESIAN_POINT ( 'NONE',  ( 5.981074661064941900, 16.28853686865598860, -12.48781255314272087 ) ) ;
#25360=ADVANCED_FACE ( 'NONE', ( #838 ), #19320, .F. ) ;
#25363=DIRECTION ( 'NONE',  ( 0.07836865515943411409, -0.007886984708671416350, 0.9968932487286222832 ) ) ;
#25379=CARTESIAN_POINT ( 'NONE',  ( 0.8551540677456715978, 17.49081417858787191, 44.61036085020956676 ) ) ;
#25383=DIRECTION ( 'NONE',  ( 0.000000000000000000, 0.000000000000000000, 1.000000000000000000 ) ) ;
#25386=CARTESIAN_POINT ( 'NONE',  ( 0.6846871229502899947, 0.8641397935259540475, 47.90045233486064546 ) ) ;
#25391=CARTESIAN_POINT ( 'NONE',  ( -19.86127894103453073, -12.46596387912833315, 0.9305556580907108355 ) ) ;
#25396=CARTESIAN_POINT ( 'NONE',  ( 3.270143674763207553, -0.2742231296310536637, 13.68510027222513159 ) ) ;
#25402=CARTESIAN_POINT ( 'NONE',  ( 4.967162193818130511, 0.000000000000000000, 0.000000000000000000 ) ) ;
#25403=CARTESIAN_POINT ( 'NONE',  ( 4.967162193818130511, 14.26841313271336809, -40.65506779172149976 ) ) ;
#25425=ORIENTED_EDGE ( 'NONE', *, *, #20415, .T. ) ;
#25426=FACE_OUTER_BOUND ( 'NONE', #23418, .T. ) ;
#25427=ORIENTED_EDGE ( 'NONE', *, *, #1960, .F. ) ;
#25432=EDGE_CURVE ( 'NONE', #46904, #31029, #57166, .T. ) ;
#25435=CARTESIAN_POINT ( 'NONE',  ( 4.960156602257185909, -45.42786611289321286, 9.558288641081595927 ) ) ;
#25437=EDGE_CURVE ( 'NONE', #58998, #56168, #24359, .T. ) ;
#25438=ORIENTED_EDGE ( 'NONE', *, *, #38088, .T. ) ;
#25442=CARTESIAN_POINT ( 'NONE',  ( 4.967162193818131399, 18.65818244221258126, 38.83676580803773248 ) ) ;
#25445=EDGE_LOOP ( 'NONE', ( #8098, #4926, #6311, #51384 ) ) ;
#25446=CARTESIAN_POINT ( 'NONE',  ( 0.5850706913938534814, -23.79070617305411162, 41.56998471741220413 ) ) ;
#25449=EDGE_LOOP ( 'NONE', ( #40423, #20320, #15631, #37564 ) ) ;
#25450=CARTESIAN_POINT ( 'NONE',  ( 5.959828726073459926, -17.77796293532166061, -10.25888482581853012 ) ) ;
#25460=ADVANCED_FACE ( 'NONE', ( #59692 ), #58015, .T. ) ;
#25465=CARTESIAN_POINT ( 'NONE',  ( 4.963659409799330291, 33.96111158240283601, -29.14784479683076412 ) ) ;
#25466=CARTESIAN_POINT ( 'NONE',  ( 5.959547316686252039, 16.28190225198618535, -12.49803383497733122 ) ) ;
#25469=CARTESIAN_POINT ( 'NONE',  ( 0.5850706913938533704, 33.73916126769452006, 33.99603398296602563 ) ) ;
#25478=CARTESIAN_POINT ( 'NONE',  ( 5.960721111146673579, -20.35079619394244332, -2.672857320903232470 ) ) ;
#25485=CARTESIAN_POINT ( 'NONE',  ( 1.088313998177381503, 10.35171213034691995, 41.64627086748857465 ) ) ;
#25504=EDGE_LOOP ( 'NONE', ( #60720, #15741, #29787, #10519 ) ) ;
#25534=CARTESIAN_POINT ( 'NONE',  ( 0.8557997880470599172, 33.22501220301901270, 34.51495345639560952 ) ) ;
#25542=ADVANCED_FACE ( 'NONE', ( #19544 ), #13042, .T. ) ;
#25552=CARTESIAN_POINT ( 'NONE',  ( -17.97369999999976642, -12.32233744059949210, 2.099999999999994760 ) ) ;
#25557=CARTESIAN_POINT ( 'NONE',  ( 2.526464513654348654, 36.59988118252434219, -22.53107770806383314 ) ) ;
#25558=B_SPLINE_CURVE_WITH_KNOTS ( 'NONE', 3,
 ( #15153, #34261, #45222, #44598 ),
 .UNSPECIFIED., .F., .F.,
 ( 4, 4 ),
 ( 0.000000000000000000, 0.004048833967417087357 ),
 .UNSPECIFIED. ) ;
#25576=FACE_OUTER_BOUND ( 'NONE', #42061, .T. ) ;
#25585=EDGE_CURVE ( 'NONE', #52183, #2408, #1929, .T. ) ;
#25587=FACE_OUTER_BOUND ( 'NONE', #27756, .T. ) ;
#25589=CARTESIAN_POINT ( 'NONE',  ( 0.9756950546413930558, 41.42124338356092750, -11.19893879603404940 ) ) ;
#25593=FACE_OUTER_BOUND ( 'NONE', #20732, .T. ) ;
#25594=CARTESIAN_POINT ( 'NONE',  ( 5.860006189529246790, -45.67886430272042020, 15.48781697582032102 ) ) ;
#25599=CARTESIAN_POINT ( 'NONE',  ( 0.5832366564991507962, 41.34220239954017728, -24.18352361336783929 ) ) ;
#25601=ORIENTED_EDGE ( 'NONE', *, *, #39998, .F. ) ;
#25614=CARTESIAN_POINT ( 'NONE',  ( 0.9730545539215883499, 33.73144377768558400, 26.52009130076782739 ) ) ;
#25616=CARTESIAN_POINT ( 'NONE',  ( 4.963659409799330291, -8.262218268420788547, 43.98510776953406776 ) ) ;
#25621=ORIENTED_EDGE ( 'NONE', *, *, #17586, .T. ) ;
#25622=CARTESIAN_POINT ( 'NONE',  ( 0.5832367798473389042, 18.07699868820190048, 44.35360901387653598 ) ) ;
#25624=CARTESIAN_POINT ( 'NONE',  ( 0.9730545539215883499, 34.34678117142556175, 25.71816799638790840 ) ) ;
#25625=DIRECTION ( 'NONE',  ( -0.07836865515943411409, 0.7860872967108267773, -0.6131273243286146091 ) ) ;
#25631=ORIENTED_EDGE ( 'NONE', *, *, #19826, .T. ) ;
#25635=EDGE_CURVE ( 'NONE', #31335, #23849, #13079, .T. ) ;
#25636=CARTESIAN_POINT ( 'NONE',  ( 5.958863334805807099, -18.96276366205799135, 7.855954700275283642 ) ) ;
#25647=CARTESIAN_POINT ( 'NONE',  ( 0.5807400328401574052, 47.89582301953903709, -0.5448834511091605881 ) ) ;
#25648=CARTESIAN_POINT ( 'NONE',  ( -17.97369999999976642, 0.000000000000000000, -2.099999999999997424 ) ) ;
#25652=CARTESIAN_POINT ( 'NONE',  ( 0.5800708057587377064, 5.628966369369036826, 47.56394202401740046 ) ) ;
#25654=CARTESIAN_POINT ( 'NONE',  ( 0.9730545539215883499, -39.83279466599027785, -15.95224156741871546 ) ) ;
#25657=VECTOR ( 'NONE', #41139, 1000.000000000000000 ) ;
#25659=CARTESIAN_POINT ( 'NONE',  ( 5.960721111146673579, 16.28787783074227136, -12.49016043756454231 ) ) ;
#25660=DIRECTION ( 'NONE',  ( 0.000000000000000000, 0.000000000000000000, 1.000000000000000000 ) ) ;
#25676=ORIENTED_EDGE ( 'NONE', *, *, #42881, .T. ) ;
#25682=FACE_OUTER_BOUND ( 'NONE', #79, .T. ) ;
#25685=VERTEX_POINT ( 'NONE', #23237 ) ;
#25687=CARTESIAN_POINT ( 'NONE',  ( 0.9730545539215883499, -39.83279466599050522, 15.95224156741815236 ) ) ;
#25696=CARTESIAN_POINT ( 'NONE',  ( 0.8557997880470599172, 41.93815086860288943, -23.15977007032279289 ) ) ;
#25698=CARTESIAN_POINT ( 'NONE',  ( 4.956653778116968390, 48.02038484091101367, -2.599733001514498376 ) ) ;
#25699=CARTESIAN_POINT ( 'NONE',  ( 4.967162193818130511, 19.45289607368822615, 38.44485641567079881 ) ) ;
#25700=VERTEX_POINT ( 'NONE', #28534 ) ;
#25712=CARTESIAN_POINT ( 'NONE',  ( 0.5800708057587394828, -5.628966369368725076, -47.56394202401742888 ) ) ;
#25720=DIRECTION ( 'NONE',  ( 0.07836865515943411409, 0.9240274869783812184, -0.3742079063794873650 ) ) ;
#25724=B_SPLINE_CURVE_WITH_KNOTS ( 'NONE', 3,
 ( #60066, #11871, #50060, #40689 ),
 .UNSPECIFIED., .F., .F.,
 ( 4, 4 ),
 ( 1.734723475976807094E-18, 0.004050076154993002484 ),
 .UNSPECIFIED. ) ;
#25736=ORIENTED_EDGE ( 'NONE', *, *, #11743, .F. ) ;
#25737=CARTESIAN_POINT ( 'NONE',  ( 5.974727161628367256, 12.50710176109986094, 16.27409205901379963 ) ) ;
#25738=CARTESIAN_POINT ( 'NONE',  ( 0.8551540677456715978, -13.28067116677234694, 46.03951182599423930 ) ) ;
#25739=ADVANCED_FACE ( 'NONE', ( #47658 ), #16569, .F. ) ;
#25742=CARTESIAN_POINT ( 'NONE',  ( 0.8551540677456715978, -29.88829867897790038, -37.45266983663525906 ) ) ;
#25759=EDGE_CURVE ( 'NONE', #32445, #25918, #15243, .T. ) ;
#25780=CARTESIAN_POINT ( 'NONE',  ( 0.9730545539215892381, -15.95224156741857691, 39.83279466599033469 ) ) ;
#25786=LINE ( 'NONE', #7588, #13243 ) ;
#25789=CARTESIAN_POINT ( 'NONE',  ( 2.624215991343620935, 4.864192649746072128, -47.76052319582212391 ) ) ;
#25795=CARTESIAN_POINT ( 'NONE',  ( 0.5809828226811617480, 0.5448590168539207967, -47.89273459658652854 ) ) ;
#25800=CARTESIAN_POINT ( 'NONE',  ( 5.959547316686252039, 10.25972575517505270, 17.77749189599220969 ) ) ;
#25817=CARTESIAN_POINT ( 'NONE',  ( 3.660087539127330203, -47.83637163185225205, -4.399983418616626452 ) ) ;
#25819=ADVANCED_FACE ( 'NONE', ( #8421 ), #8047, .F. ) ;
#25821=CARTESIAN_POINT ( 'NONE',  ( 4.956653778116975495, 14.93973939759886704, 45.71126949320255761 ) ) ;
#25828=VERTEX_POINT ( 'NONE', #32570 ) ;
#25833=CARTESIAN_POINT ( 'NONE',  ( 3.660176727303418698, 42.51126973288313593, -22.37119938028445176 ) ) ;
#25836=CARTESIAN_POINT ( 'NONE',  ( 3.407937589446178528, 13.10584870154472092, -3.987184287467649746 ) ) ;
#25850=CARTESIAN_POINT ( 'NONE',  ( 4.967162193818129623, -40.65506779172174845, 14.26841313271267886 ) ) ;
#25855=CARTESIAN_POINT ( 'NONE',  ( 0.5839880159502331969, 46.27569712847351013, -12.35255585954135427 ) ) ;
#25857=CARTESIAN_POINT ( 'NONE',  ( 0.5786265663353196143, 11.69877690266654824, 46.45062944555897388 ) ) ;
#25864=CARTESIAN_POINT ( 'NONE',  ( -15.87380398270803106, -12.49998253090622313, 0.2752802063126107979 ) ) ;
#25867=DIRECTION ( 'NONE',  ( 0.000000000000000000, 0.000000000000000000, 1.000000000000000000 ) ) ;
#25876=ADVANCED_FACE ( 'NONE', ( #9667 ), #18967, .F. ) ;
#25879=CARTESIAN_POINT ( 'NONE',  ( 3.660087539127330647, -39.22752134874899355, -27.72868323267848822 ) ) ;
#25882=CARTESIAN_POINT ( 'NONE',  ( 1.088908134280559992, 42.43751564162690215, -6.374115321932653622 ) ) ;
#25888=CARTESIAN_POINT ( 'NONE',  ( 0.5837374860065650539, -47.46223477511615130, 6.431731162805607305 ) ) ;
#25891=ORIENTED_EDGE ( 'NONE', *, *, #20466, .F. ) ;
#25896=CARTESIAN_POINT ( 'NONE',  ( 4.956653778116480780, -21.75875759808806720, 42.88673967249081898 ) ) ;
#25898=CARTESIAN_POINT ( 'NONE',  ( 0.7762777257811908083, 41.92424087089342066, -23.17763256463726762 ) ) ;
#25910=CARTESIAN_POINT ( 'NONE',  ( 4.303969348037258058, 14.52400616872369632, 45.86537346639062918 ) ) ;
#25918=VERTEX_POINT ( 'NONE', #52574 ) ;
#25924=CARTESIAN_POINT ( 'NONE',  ( 0.5838002273316438284, -18.45474575185545163, 44.19779719735692680 ) ) ;
#25932=CARTESIAN_POINT ( 'NONE',  ( 0.9968887458511694888, -11.73947777183250096, 41.27232779986115929 ) ) ;
#25935=VERTEX_POINT ( 'NONE', #242 ) ;
#25940=CARTESIAN_POINT ( 'NONE',  ( 0.5809828226811553087, -44.45562576850588243, -17.82437196699728332 ) ) ;
#25950=CARTESIAN_POINT ( 'NONE',  ( 0.8551540677456715978, 24.74404575822833507, -41.03346287276401938 ) ) ;
#25951=FACE_OUTER_BOUND ( 'NONE', #14054, .T. ) ;
#25956=CARTESIAN_POINT ( 'NONE',  ( 5.959547316686252039, -2.675599016784394379, -20.35048796920736081 ) ) ;
#25968=VERTEX_POINT ( 'NONE', #30311 ) ;
#25969=CARTESIAN_POINT ( 'NONE',  ( 4.967162193818130511, 0.000000000000000000, 0.000000000000000000 ) ) ;
#25973=CARTESIAN_POINT ( 'NONE',  ( 0.9756950546413926117, -39.67916378221926266, -16.33093981194364019 ) ) ;
#25982=ORIENTED_EDGE ( 'NONE', *, *, #31347, .T. ) ;
#25987=CARTESIAN_POINT ( 'NONE',  ( 5.974727161628367256, 12.48248968439928674, -16.29297756969635458 ) ) ;
#25993=ORIENTED_EDGE ( 'NONE', *, *, #7899, .F. ) ;
#25994=CARTESIAN_POINT ( 'NONE',  ( 4.960156602257181468, -15.40604254112611216, -43.79161740034492567 ) ) ;
#25995=CARTESIAN_POINT ( 'NONE',  ( 0.5809828226811553087, -38.32755012159125840, -28.72298383114528519 ) ) ;
#25996=B_SPLINE_CURVE_WITH_KNOTS ( 'NONE', 3,
 ( #45714, #12203, #36318, #59788, #54137, #45405, #1838, #16574, #49461, #55383, #39797, #58846, #21580, #55078, #11255, #35702, #40403, #6511, #59464 ),
 .UNSPECIFIED., .F., .F.,
 ( 4, 3, 3, 3, 3, 3, 4 ),
 ( 9.813676791237319219E-18, 0.0002724573126191676240, 0.0004086839781548304794, 0.0005449106435901656569, 0.0006811373090491328096, 0.0008459866663933593997, 0.001010840725717213366 ),
 .UNSPECIFIED. ) ;
#26003=CARTESIAN_POINT ( 'NONE',  ( 3.270143674763207553, 13.14781761974169072, 3.806843787665967760 ) ) ;
#26008=B_SPLINE_CURVE_WITH_KNOTS ( 'NONE', 3,
 ( #4463, #38343, #57393, #52716, #5085, #15140 ),
 .UNSPECIFIED., .F., .F.,
 ( 4, 2, 4 ),
 ( 9.543442895606953578E-18, 0.0002291978881530156451, 0.0004583957763060217492 ),
 .UNSPECIFIED. ) ;
#26009=ORIENTED_EDGE ( 'NONE', *, *, #52932, .F. ) ;
#26014=FACE_OUTER_BOUND ( 'NONE', #36105, .T. ) ;
#26024=CARTESIAN_POINT ( 'NONE',  ( 0.5850706913938533704, -33.99603398296613932, 33.73916126769439217 ) ) ;
#26028=AXIS2_PLACEMENT_3D ( 'NONE', #45192, #40186, #50769 ) ;
#26029=ORIENTED_EDGE ( 'NONE', *, *, #13257, .F. ) ;
#26031=DIRECTION ( 'NONE',  ( -1.000000000000000000, -0.000000000000000000, -0.000000000000000000 ) ) ;
#26036=CARTESIAN_POINT ( 'NONE',  ( 0.9754402186311934564, 37.06569162601132206, -21.61645729243075209 ) ) ;
#26042=CARTESIAN_POINT ( 'NONE',  ( 5.974727161628369032, -7.868887636447738920, 18.95664195401504060 ) ) ;
#26050=CARTESIAN_POINT ( 'NONE',  ( 0.9722240750034573109, -5.023189755349235064, 42.61332880321398875 ) ) ;
#26056=CARTESIAN_POINT ( 'NONE',  ( 0.6846871229502899947, -29.84551600520608616, -37.47592888575278636 ) ) ;
#26057=ORIENTED_EDGE ( 'NONE', *, *, #5351, .T. ) ;
#26058=ORIENTED_EDGE ( 'NONE', *, *, #4488, .F. ) ;
#26063=EDGE_LOOP ( 'NONE', ( #42142, #48214, #41071, #4219 ) ) ;
#26070=CARTESIAN_POINT ( 'NONE',  ( 5.959547316686252039, -19.82715097195158194, -5.308980600728387067 ) ) ;
#26075=EDGE_LOOP ( 'NONE', ( #54177, #56966, #50402, #23274 ) ) ;
#26076=CARTESIAN_POINT ( 'NONE',  ( 5.958863334805807099, 10.26176968287945179, -17.77634700750918384 ) ) ;
#26083=CARTESIAN_POINT ( 'NONE',  ( 4.956653778116966613, 0.000000000000000000, 0.000000000000000000 ) ) ;
#26085=VERTEX_POINT ( 'NONE', #53789 ) ;
#26092=CARTESIAN_POINT ( 'NONE',  ( 5.959547316686252039, 18.96456592444089395, 7.851524054666477959 ) ) ;
#26093=CARTESIAN_POINT ( 'NONE',  ( 4.967162193818129623, -43.02067033766018511, 2.375726030842427061 ) ) ;
#26107=CARTESIAN_POINT ( 'NONE',  ( 0.8557997880470599172, -43.90420959842167292, -19.17299735372055736 ) ) ;
#26114=CARTESIAN_POINT ( 'NONE',  ( 0.8557997880470697982, -46.03118133706034598, 13.27832040216623355 ) ) ;
#26115=CARTESIAN_POINT ( 'NONE',  ( 0.9722240741986363233, 6.177112427866467748, -42.46141200043694397 ) ) ;
#26117=EDGE_CURVE ( 'NONE', #16449, #21472, #41441, .T. ) ;
#26118=ORIENTED_EDGE ( 'NONE', *, *, #44450, .T. ) ;
#26121=CARTESIAN_POINT ( 'NONE',  ( 5.959547316686252039, 5.308980600728181010, 19.82715097195164233 ) ) ;
#26124=EDGE_LOOP ( 'NONE', ( #8553, #54003, #4427, #49474 ) ) ;
#26125=CARTESIAN_POINT ( 'NONE',  ( 0.5809828226811617480, 47.89273459658653564, 0.5448590168534191980 ) ) ;
#26138=ORIENTED_EDGE ( 'NONE', *, *, #55295, .F. ) ;
#26145=CARTESIAN_POINT ( 'NONE',  ( 0.9754642270333674370, -30.21634823122148106, -30.46484943293189218 ) ) ;
#26149=CARTESIAN_POINT ( 'NONE',  ( 0.9757892942422823346, -21.49867881049921081, -37.13414688883487713 ) ) ;
#26152=CARTESIAN_POINT ( 'NONE',  ( 5.960721111146673579, 2.685391721745764571, 20.34914600876576074 ) ) ;
#26162=CARTESIAN_POINT ( 'NONE',  ( 0.9752132459055877778, 42.90780255730422255, -0.2329632697545410136 ) ) ;
#26163=CARTESIAN_POINT ( 'NONE',  ( 0.6067099128993237445, -47.57459301987699263, -5.548253864790892997 ) ) ;
#26165=LINE ( 'NONE', #2346, #46862 ) ;
#26168=DIRECTION ( 'NONE',  ( 0.000000000000000000, 0.000000000000000000, -1.000000000000000000 ) ) ;
#26173=CARTESIAN_POINT ( 'NONE',  ( 0.7056555295713275999, -13.20840017674985845, -46.04438433984169876 ) ) ;
#26176=CARTESIAN_POINT ( 'NONE',  ( 5.960221823109900008, 19.82478916873567698, 5.317678907195506177 ) ) ;
#26177=FACE_OUTER_BOUND ( 'NONE', #34995, .T. ) ;
#26181=ORIENTED_EDGE ( 'NONE', *, *, #16646, .F. ) ;
#26182=ORIENTED_EDGE ( 'NONE', *, *, #2605, .F. ) ;
#26184=CARTESIAN_POINT ( 'NONE',  ( 5.965394784446460541, 17.76824826579340666, 10.27521535480992654 ) ) ;
#26193=ORIENTED_EDGE ( 'NONE', *, *, #26602, .F. ) ;
#26196=CARTESIAN_POINT ( 'NONE',  ( 5.860006189529246790, -15.52021937683308295, 45.66786516969924747 ) ) ;
#26197=ORIENTED_EDGE ( 'NONE', *, *, #33249, .F. ) ;
#26203=CARTESIAN_POINT ( 'NONE',  ( 0.9745511491811753579, 41.53317535253989234, -10.77620558745893931 ) ) ;
#26204=EDGE_LOOP ( 'NONE', ( #43828, #7226, #31375, #10873 ) ) ;
#26205=CARTESIAN_POINT ( 'NONE',  ( 0.9730545539215883499, -33.73144377768539215, -26.52009130076805832 ) ) ;
#26209=FACE_OUTER_BOUND ( 'NONE', #40495, .T. ) ;
#26210=CARTESIAN_POINT ( 'NONE',  ( 0.5809828226811617480, 41.74875432577682233, -23.47450554821666202 ) ) ;
#26217=ORIENTED_EDGE ( 'NONE', *, *, #19977, .T. ) ;
#26226=CARTESIAN_POINT ( 'NONE',  ( 0.5807400328401637335, 33.48217046439159361, -34.25275203086200548 ) ) ;
#26228=ORIENTED_EDGE ( 'NONE', *, *, #42887, .F. ) ;
#26233=FACE_OUTER_BOUND ( 'NONE', #26273, .T. ) ;
#26239=EDGE_CURVE ( 'NONE', #33551, #56726, #49612, .T. ) ;
#26242=ORIENTED_EDGE ( 'NONE', *, *, #23480, .T. ) ;
#26244=CARTESIAN_POINT ( 'NONE',  ( 0.8551540677456715978, 41.94570365541202506, 23.16399837394560635 ) ) ;
#26248=DIRECTION ( 'NONE',  ( 0.000000000000000000, 0.000000000000000000, 1.000000000000000000 ) ) ;
#26249=CARTESIAN_POINT ( 'NONE',  ( 3.660176727303400934, -20.10773453922317344, 43.62748706623516171 ) ) ;
#26255=CARTESIAN_POINT ( 'NONE',  ( 0.5850706913938534814, 6.431767090162812117, 47.46255051844956085 ) ) ;
#26257=CARTESIAN_POINT ( 'NONE',  ( 5.974727161628369032, 7.840226266082271245, 18.96851388233661595 ) ) ;
#26263=CARTESIAN_POINT ( 'NONE',  ( 0.7057020205115004385, -47.37450661940665242, -7.085441699094105594 ) ) ;
#26264=B_SPLINE_CURVE_WITH_KNOTS ( 'NONE', 3,
 ( #1075, #19916, #29282, #57772, #58082, #5756 ),
 .UNSPECIFIED., .F., .F.,
 ( 4, 2, 4 ),
 ( 0.000000000000000000, 0.0002291966416970790514, 0.0004583932833941581028 ),
 .UNSPECIFIED. ) ;
#26268=B_SPLINE_CURVE_WITH_KNOTS ( 'NONE', 3,
 ( #25940, #30948, #50056, #45680, #3569, #42751 ),
 .UNSPECIFIED., .F., .F.,
 ( 4, 2, 4 ),
 ( 1.084202172485504434E-19, 0.0002445244328975360471, 0.0004890488657950719858 ),
 .UNSPECIFIED. ) ;
#26273=EDGE_LOOP ( 'NONE', ( #45324, #31308, #15189, #3397 ) ) ;
#26274=CARTESIAN_POINT ( 'NONE',  ( 3.660176727303400046, -30.71420464230597247, 36.93665184075209851 ) ) ;
#26281=EDGE_CURVE ( 'NONE', #59424, #46608, #2890, .T. ) ;
#26282=CARTESIAN_POINT ( 'NONE',  ( 1.227938101723756947, -39.96870412324324917, -15.63977281655884077 ) ) ;
#26290=VERTEX_POINT ( 'NONE', #19316 ) ;
#26301=CARTESIAN_POINT ( 'NONE',  ( 0.9756950546413932779, -0.09673755062766570267, -42.90834738653779823 ) ) ;
#26302=CARTESIAN_POINT ( 'NONE',  ( 4.967162193818130511, 0.000000000000000000, 0.000000000000000000 ) ) ;
#26308=CARTESIAN_POINT ( 'NONE',  ( 0.9757402383260944667, 11.02350435907904469, 41.46830379850858606 ) ) ;
#26309=CARTESIAN_POINT ( 'NONE',  ( 5.981074661064941900, 2.687517936919997741, -20.34795181394746066 ) ) ;
#26319=CARTESIAN_POINT ( 'NONE',  ( -19.85996189817664259, -12.46576327517147043, -0.9332767033992659389 ) ) ;
#26324=EDGE_CURVE ( 'NONE', #8570, #33938, #40665, .T. ) ;
#26325=CARTESIAN_POINT ( 'NONE',  ( 0.9756008150404616996, -33.95486284030242530, 26.23365443298902377 ) ) ;
#26326=CARTESIAN_POINT ( 'NONE',  ( 5.981074661064941900, -20.35019299530690162, 2.670494474391653661 ) ) ;
#26331=CARTESIAN_POINT ( 'NONE',  ( 0.9757402383260955769, 21.52772413548534658, -37.11731350497332471 ) ) ;
#26333=FACE_OUTER_BOUND ( 'NONE', #22613, .T. ) ;
#26335=CARTESIAN_POINT ( 'NONE',  ( 0.5850706913938534814, 12.22095376872101546, -46.31100969101474618 ) ) ;
#26339=CARTESIAN_POINT ( 'NONE',  ( 4.956653778116975495, 20.77844580450561551, 43.37017594958062006 ) ) ;
#26340=CIRCLE ( 'NONE', #7307, 43.08621763946400307 ) ;
#26344=CARTESIAN_POINT ( 'NONE',  ( 0.5832367798473383491, -28.94059862654968640, -38.16362489683119463 ) ) ;
#26345=ORIENTED_EDGE ( 'NONE', *, *, #24741, .F. ) ;
#26347=LINE ( 'NONE', #40177, #21555 ) ;
#26349=VERTEX_POINT ( 'NONE', #15851 ) ;
#26353=ORIENTED_EDGE ( 'NONE', *, *, #38511, .T. ) ;
#26354=CARTESIAN_POINT ( 'NONE',  ( 0.8557997880470606944, -33.22501220301877112, -34.51495345639583689 ) ) ;
#26355=CARTESIAN_POINT ( 'NONE',  ( 0.8557997880470599172, -46.03118133706016835, -13.27832040216687304 ) ) ;
#26360=CARTESIAN_POINT ( 'NONE',  ( 0.9757402383260942447, -5.684842778069517877, 42.53022961222601594 ) ) ;
#26371=ADVANCED_FACE ( 'NONE', ( #40601 ), #5370, .F. ) ;
#26373=B_SPLINE_CURVE_WITH_KNOTS ( 'NONE', 3,
 ( #54053, #53735, #29646, #10868, #24962, #30258 ),
 .UNSPECIFIED., .F., .F.,
 ( 4, 2, 4 ),
 ( 0.000000000000000000, 0.0002291966416970795664, 0.0004583932833941591328 ),
 .UNSPECIFIED. ) ;
#26377=VERTEX_POINT ( 'NONE', #1106 ) ;
#26393=CARTESIAN_POINT ( 'NONE',  ( 5.960721111146673579, -19.82454228767742066, -5.318514366754864220 ) ) ;
#26395=CARTESIAN_POINT ( 'NONE',  ( 0.9758171775293927874, -16.41489794146152548, 39.64453667157740568 ) ) ;
#26398=CARTESIAN_POINT ( 'NONE',  ( 4.956653778116966613, 0.000000000000000000, 0.000000000000000000 ) ) ;
#26399=LINE ( 'NONE', #40235, #16717 ) ;
#26401=CARTESIAN_POINT ( 'NONE',  ( 0.8557997880470697982, -23.15977007032352475, 41.93815086860250574 ) ) ;
#26402=CARTESIAN_POINT ( 'NONE',  ( 0.6067375320500711933, -41.82999795871622695, 23.33187539052113380 ) ) ;
#26404=CARTESIAN_POINT ( 'NONE',  ( 5.960221823109900008, 20.34928172836727356, 2.684531185214488413 ) ) ;
#26405=CIRCLE ( 'NONE', #40441, 43.08621763946400307 ) ;
#26408=CARTESIAN_POINT ( 'NONE',  ( 1.227938101723756947, -26.79402671879305231, -33.52879263017890565 ) ) ;
#26419=VERTEX_POINT ( 'NONE', #16159 ) ;
#26425=ORIENTED_EDGE ( 'NONE', *, *, #5654, .F. ) ;
#26430=ORIENTED_EDGE ( 'NONE', *, *, #53256, .T. ) ;
#26431=CARTESIAN_POINT ( 'NONE',  ( 0.5809828226811553087, -38.32755012159125840, -28.72298383114528519 ) ) ;
#26432=B_SPLINE_CURVE_WITH_KNOTS ( 'NONE', 3,
 ( #48073, #19887, #15486, #53363 ),
 .UNSPECIFIED., .F., .F.,
 ( 4, 4 ),
 ( 0.000000000000000000, 0.004446090762761378129 ),
 .UNSPECIFIED. ) ;
#26435=( BOUNDED_SURFACE ( )  B_SPLINE_SURFACE ( 3, 1, ( 
 ( #5882, #48829 ),
 ( #25329, #2432 ),
 ( #45087, #59446 ),
 ( #11556, #40385 ) ),
 .UNSPECIFIED., .F., .F., .F. ) 
 B_SPLINE_SURFACE_WITH_KNOTS ( ( 4, 4 ),
 ( 2, 2 ),
 ( 0.000000000000000000, 1.000000000000000000 ),
 ( 0.000000000000000000, 1.000000000000000000 ),
 .UNSPECIFIED. ) 
 GEOMETRIC_REPRESENTATION_ITEM ( )  RATIONAL_B_SPLINE_SURFACE ( (
 ( 1.000000000000000000, 1.000000000000000000),
 ( 0.7269869731126821222, 0.9931720237060910339),
 ( 0.7269869731126821222, 0.9931720237060910339),
 ( 1.000000000000000000, 1.000000000000000000) ) ) 
 REPRESENTATION_ITEM ( '' )  SURFACE ( )  );
#26437=EDGE_CURVE ( 'NONE', #1494, #29154, #56331, .T. ) ;
#26438=EDGE_LOOP ( 'NONE', ( #57304, #44064, #14627, #4252 ) ) ;
#26440=ADVANCED_FACE ( 'NONE', ( #55265 ), #34817, .T. ) ;
#26446=EDGE_CURVE ( 'NONE', #47520, #3369, #30144, .T. ) ;
#26456=ORIENTED_EDGE ( 'NONE', *, *, #54598, .F. ) ;
#26457=FACE_OUTER_BOUND ( 'NONE', #28579, .T. ) ;
#26459=CARTESIAN_POINT ( 'NONE',  ( 0.8557997880470606944, 29.88293891557523807, -37.44587306708065455 ) ) ;
#26460=CARTESIAN_POINT ( 'NONE',  ( 1.088313998177382169, 36.76812638579230708, 22.12859469727350614 ) ) ;
#26466=DIRECTION ( 'NONE',  ( -1.000000000000000000, -0.000000000000000000, -0.000000000000000000 ) ) ;
#26468=FACE_OUTER_BOUND ( 'NONE', #3099, .T. ) ;
#26470=CARTESIAN_POINT ( 'NONE',  ( 0.5837374860065656090, 46.21667939904230593, -12.57177159055114046 ) ) ;
#26471=CARTESIAN_POINT ( 'NONE',  ( 0.9740398440564312921, -6.011466167923821935, -42.48528956276143731 ) ) ;
#26476=CARTESIAN_POINT ( 'NONE',  ( 5.959547316686252039, 17.77392908783919978, 10.26589671991369457 ) ) ;
#26503=CARTESIAN_POINT ( 'NONE',  ( 0.6067099128993203028, -43.97493306231474719, 18.98236771638443443 ) ) ;
#26504=AXIS2_PLACEMENT_3D ( 'NONE', #53594, #34221, #48920 ) ;
#26507=ORIENTED_EDGE ( 'NONE', *, *, #16853, .T. ) ;
#26508=VECTOR ( 'NONE', #58016, 1000.000000000000114 ) ;
#26509=ORIENTED_EDGE ( 'NONE', *, *, #13734, .F. ) ;
#26511=CARTESIAN_POINT ( 'NONE',  ( 4.967162193818130511, 0.000000000000000000, 0.000000000000000000 ) ) ;
#26513=CARTESIAN_POINT ( 'NONE',  ( 0.5809828226811553087, 34.25055090842153760, 33.48000389720628789 ) ) ;
#26517=( BOUNDED_SURFACE ( )  B_SPLINE_SURFACE ( 3, 1, ( 
 ( #50206, #39920 ),
 ( #1647, #58979 ),
 ( #7270, #6959 ),
 ( #26092, #55200 ) ),
 .UNSPECIFIED., .F., .F., .F. ) 
 B_SPLINE_SURFACE_WITH_KNOTS ( ( 4, 4 ),
 ( 2, 2 ),
 ( 0.000000000000000000, 1.000000000000000000 ),
 ( 0.000000000000000000, 1.000000000000000000 ),
 .UNSPECIFIED. ) 
 GEOMETRIC_REPRESENTATION_ITEM ( )  RATIONAL_B_SPLINE_SURFACE ( (
 ( 1.000000000000000000, 1.000000000000000000),
 ( 0.9732289882329797637, 0.9999525324661233672),
 ( 0.9732289882329797637, 0.9999525324661233672),
 ( 1.000000000000000000, 1.000000000000000000) ) ) 
 REPRESENTATION_ITEM ( '' )  SURFACE ( )  );
#26524=CARTESIAN_POINT ( 'NONE',  ( 4.967162193818130511, 24.30453456948160351, -35.57684288741949530 ) ) ;
#26526=B_SPLINE_CURVE_WITH_KNOTS ( 'NONE', 3,
 ( #21628, #54495, #11622, #17246 ),
 .UNSPECIFIED., .F., .F.,
 ( 4, 4 ),
 ( 4.670885906470169924E-18, 0.004050076154993003351 ),
 .UNSPECIFIED. ) ;
#26534=CARTESIAN_POINT ( 'NONE',  ( 0.5809828226811626362, -18.83114015454730961, 44.03860873105688967 ) ) ;
#26535=ORIENTED_EDGE ( 'NONE', *, *, #22063, .T. ) ;
#26540=ORIENTED_EDGE ( 'NONE', *, *, #22713, .T. ) ;
#26542=CARTESIAN_POINT ( 'NONE',  ( 1.088313998177386166, -11.85828975620036552, 41.24258460930634129 ) ) ;
#26547=EDGE_LOOP ( 'NONE', ( #32556, #53300, #6539, #19615, #1100, #31378, #47941, #53534, #13385, #28283, #52314, #59104, #22944, #21182, #25425, #44577, #6657, #46194, #51334, #11074, #36363, #15569, #16527, #8979, #50784, #59930, #23962, #29144, #46494, #53885, #43138, #9685, #50014, #37573, #51789, #23129, #9542, #52418, #29509, #3760, #52879, #52690, #46283, #59691, #40989, #51219, #40802, #39435, #15441, #15089, #56539, #4249, #15193, #22253, #19834, #32366, #29064, #59620, #23268, #28717, #58105, #8393, #18170, #401, #18464, #47721, #25631, #43221, #19011, #17591, #6136, #44965, #14744, #14075, #47931, #59039, #24181, #26921, #2530, #17834, #20541, #49223, #8335, #45724, #26242, #17013, #22988, #31612, #34805, #15762, #52545, #52101, #15213, #55469, #41746, #45402, #13267, #26118, #14439, #8538, #49029, #45973, #39164, #10977, #32414, #59964, #25298, #58173, #20135, #16847, #50493, #59089, #19664, #40417, #30920, #20363, #21312, #42355, #17853, #4141, #42762, #58470, #8988, #26865, #33270, #34928, #954, #24977, #51395, #20160, #43111, #17056, #31311, #53141, #18591, #16632, #13025, #39503, #11861, #10927, #55009, #59267, #58380, #9891, #43210, #5666, #55884, #16284 ) ) ;
#26552=CARTESIAN_POINT ( 'NONE',  ( 5.974727161628369032, -14.50236057684835522, -14.52429704002358690 ) ) ;
#26553=CARTESIAN_POINT ( 'NONE',  ( 0.5850706913938534814, 46.21698775168663076, -12.57184842331969143 ) ) ;
#26559=CARTESIAN_POINT ( 'NONE',  ( 5.960721111146673579, 19.82454228767738158, 5.318514366755001888 ) ) ;
#26562=AXIS2_PLACEMENT_3D ( 'NONE', #14705, #29094, #57888 ) ;
#26564=CARTESIAN_POINT ( 'NONE',  ( 5.860006189529246790, 26.81109398084765161, -40.09484204000572305 ) ) ;
#26565=DIRECTION ( 'NONE',  ( -0.07439287786467650709, 0.5965490341031379762, -0.7991213610169762838 ) ) ;
#26568=ADVANCED_FACE ( 'NONE', ( #26781 ), #54961, .F. ) ;
#26569=CARTESIAN_POINT ( 'NONE',  ( 0.9758171775293925654, -39.64000636436369263, 16.42583507057852898 ) ) ;
#26580=CARTESIAN_POINT ( 'NONE',  ( 4.303969348037258058, -47.36875205922778065, 8.413118729223894476 ) ) ;
#26581=CARTESIAN_POINT ( 'NONE',  ( 1.227938101723756947, -25.45152231597080927, 34.55893248994497924 ) ) ;
#26583=CARTESIAN_POINT ( 'NONE',  ( 5.960721111146673579, 20.52557019979492026, 0.006321279846891981850 ) ) ;
#26602=EDGE_CURVE ( 'NONE', #3069, #20568, #52558, .T. ) ;
#26606=ORIENTED_EDGE ( 'NONE', *, *, #55612, .T. ) ;
#26608=DIRECTION ( 'NONE',  ( -0.07836865515943412797, -0.6993330359244914751, 0.7104869166657016288 ) ) ;
#26612=CARTESIAN_POINT ( 'NONE',  ( 5.959828726073459926, -14.51699876360190267, -14.51059719297111705 ) ) ;
#26615=CARTESIAN_POINT ( 'NONE',  ( 5.965394784446460541, 2.693446924985626101, -20.34787558161484355 ) ) ;
#26617=CARTESIAN_POINT ( 'NONE',  ( 0.5834872094924150598, -44.33648115256914224, 18.11905305011503842 ) ) ;
#26633=CARTESIAN_POINT ( 'NONE',  ( 5.960721111146673579, 17.77250458025991975, -10.26825948882907191 ) ) ;
#26635=CARTESIAN_POINT ( 'NONE',  ( 0.8557997880470599172, -5.347802024196930404, -47.60865952217005059 ) ) ;
#26636=ORIENTED_EDGE ( 'NONE', *, *, #45461, .F. ) ;
#26640=CARTESIAN_POINT ( 'NONE',  ( 4.303969348037258058, 36.81598326424592216, -30.97035057417624060 ) ) ;
#26654=CONICAL_SURFACE ( 'NONE', #20673, 43.08621763946400307, 1.568696531533066763 ) ;
#26660=CARTESIAN_POINT ( 'NONE',  ( 3.783198216974394068, -14.86152287314652476, -40.39102707215872812 ) ) ;
#26661=CARTESIAN_POINT ( 'NONE',  ( 5.981074661064941900, 10.25489689131130611, -17.77917279944622209 ) ) ;
#26665=CARTESIAN_POINT ( 'NONE',  ( 0.9736507210033050752, -41.32746151989292116, -11.54000710819857822 ) ) ;
#26669=CARTESIAN_POINT ( 'NONE',  ( 0.5807400328401574052, -47.55718917606846929, 5.711437504335798998 ) ) ;
#26670=EDGE_CURVE ( 'NONE', #29930, #49867, #50791, .T. ) ;
#26673=LINE ( 'NONE', #47035, #1705 ) ;
#26674=VERTEX_POINT ( 'NONE', #14550 ) ;
#26678=EDGE_CURVE ( 'NONE', #55702, #31335, #8509, .T. ) ;
#26679=CARTESIAN_POINT ( 'NONE',  ( 0.9730545539215883499, 36.90443313492362165, -21.89037132892396897 ) ) ;
#26686=CARTESIAN_POINT ( 'NONE',  ( 0.6067375320500721925, 18.98242280073624144, -43.97491060910868299 ) ) ;
#26691=ORIENTED_EDGE ( 'NONE', *, *, #31773, .F. ) ;
#26692=CARTESIAN_POINT ( 'NONE',  ( 0.9736507210033054083, -42.90603603725248405, -0.4504567742785494100 ) ) ;
#26693=DIRECTION ( 'NONE',  ( 0.000000000000000000, 0.000000000000000000, 1.000000000000000000 ) ) ;
#26695=EDGE_LOOP ( 'NONE', ( #47710, #36576, #9979, #41278 ) ) ;
#26696=FACE_OUTER_BOUND ( 'NONE', #31950, .T. ) ;
#26697=CARTESIAN_POINT ( 'NONE',  ( 4.963659409799330291, -29.86601237216433447, 33.33129552235077853 ) ) ;
#26698=CARTESIAN_POINT ( 'NONE',  ( 3.407937589446178528, -7.970324840162034796, 11.14158115674370642 ) ) ;
#26702=FACE_OUTER_BOUND ( 'NONE', #20355, .T. ) ;
#26704=CARTESIAN_POINT ( 'NONE',  ( 3.407937589446178528, 1.331713209622699567, -13.63405474014706975 ) ) ;
#26707=DIRECTION ( 'NONE',  ( 0.000000000000000000, 0.000000000000000000, 1.000000000000000000 ) ) ;
#26711=LINE ( 'NONE', #49908, #16230 ) ;
#26712=CARTESIAN_POINT ( 'NONE',  ( 0.5800708057587374844, -41.78924035064540021, 23.40241940841941570 ) ) ;
#26721=CARTESIAN_POINT ( 'NONE',  ( 0.9730545539215883499, -16.88610103448528221, -39.44597740938079511 ) ) ;
#26729=ORIENTED_EDGE ( 'NONE', *, *, #48770, .T. ) ;
#26730=CIRCLE ( 'NONE', #61712, 48.09070567114147110 ) ;
#26736=ORIENTED_EDGE ( 'NONE', *, *, #2312, .T. ) ;
#26746=EDGE_CURVE ( 'NONE', #57526, #61588, #31727, .T. ) ;
#26748=CARTESIAN_POINT ( 'NONE',  ( 5.959547316686252039, -18.96456592444095435, -7.851524054666348285 ) ) ;
#26749=ORIENTED_EDGE ( 'NONE', *, *, #23858, .F. ) ;
#26756=CARTESIAN_POINT ( 'NONE',  ( 5.960721111146673579, 7.848955554238515653, -18.96557324978279624 ) ) ;
#26757=VERTEX_POINT ( 'NONE', #21392 ) ;
#26758=CARTESIAN_POINT ( 'NONE',  ( 5.959828726073459926, 14.51699876360200214, -14.51059719297101758 ) ) ;
#26759=CARTESIAN_POINT ( 'NONE',  ( 4.956653778116991482, -21.75875759808677046, -42.88673967249153662 ) ) ;
#26765=ORIENTED_EDGE ( 'NONE', *, *, #56199, .T. ) ;
#26766=CARTESIAN_POINT ( 'NONE',  ( 0.5809828226811617480, 44.45562576850627323, -17.82437196699632054 ) ) ;
#26771=ORIENTED_EDGE ( 'NONE', *, *, #17148, .F. ) ;
#26774=CARTESIAN_POINT ( 'NONE',  ( 0.5809828226811617480, 33.48000389720616710, 34.25055090842165839 ) ) ;
#26777=EDGE_LOOP ( 'NONE', ( #7875, #44947, #21217, #7800 ) ) ;
#26778=CARTESIAN_POINT ( 'NONE',  ( 5.965394784446460541, 10.25014670152090268, 17.78272165951804595 ) ) ;
#26781=FACE_OUTER_BOUND ( 'NONE', #4368, .T. ) ;
#26785=CARTESIAN_POINT ( 'NONE',  ( 5.959547316686252039, 12.49238070347976226, -16.28624005235086614 ) ) ;
#26787=CARTESIAN_POINT ( 'NONE',  ( 0.5807400328401637335, 11.87003418057242321, 46.40483864045149431 ) ) ;
#26791=CARTESIAN_POINT ( 'NONE',  ( -16.08632264266780609, -12.46593278125092219, -0.9310146124893876607 ) ) ;
#26797=CARTESIAN_POINT ( 'NONE',  ( 0.8551540677456715978, -47.61725548905994287, 5.348818140990729830 ) ) ;
#26800=EDGE_CURVE ( 'NONE', #14380, #39397, #35821, .T. ) ;
#26814=DIRECTION ( 'NONE',  ( -1.000000000000000000, -0.000000000000000000, -0.000000000000000000 ) ) ;
#26822=CIRCLE ( 'NONE', #29852, 12.50000000000000000 ) ;
#26834=ORIENTED_EDGE ( 'NONE', *, *, #30141, .T. ) ;
#26837=CARTESIAN_POINT ( 'NONE',  ( 0.5827359174754822568, 41.65957726278070083, -23.63273677570873232 ) ) ;
#26855=CARTESIAN_POINT ( 'NONE',  ( 0.9730545539215892381, -11.59290486963536360, 41.31259007387227911 ) ) ;
#26865=ORIENTED_EDGE ( 'NONE', *, *, #18626, .T. ) ;
#26868=CARTESIAN_POINT ( 'NONE',  ( 3.660087539127326206, -46.85281175970447975, -10.60624038924642143 ) ) ;
#26876=CARTESIAN_POINT ( 'NONE',  ( 0.6067099128993229673, -47.38952184036239856, 6.954009037735986887 ) ) ;
#26880=EDGE_CURVE ( 'NONE', #30283, #41860, #44400, .T. ) ;
#26884=CARTESIAN_POINT ( 'NONE',  ( 2.526464513654345989, -9.948146339971524199, 41.81190200959800052 ) ) ;
#26885=CARTESIAN_POINT ( 'NONE',  ( 0.8551540677456834771, -19.17641535420820631, -43.91216198251559888 ) ) ;
#26890=CARTESIAN_POINT ( 'NONE',  ( 0.5819845079324652559, -24.34013310064366564, -41.25022834067375754 ) ) ;
#26891=CARTESIAN_POINT ( 'NONE',  ( 4.967162193818130511, 28.74031574030012237, 32.10009971360082659 ) ) ;
#26892=CARTESIAN_POINT ( 'NONE',  ( 4.956653778116991482, -2.599733001514001440, -48.02038484091103498 ) ) ;
#26893=B_SPLINE_CURVE_WITH_KNOTS ( 'NONE', 3,
 ( #26205, #59403, #15289, #5840, #44432, #20596 ),
 .UNSPECIFIED., .F., .F.,
 ( 4, 2, 4 ),
 ( 3.476216610979977084E-18, 0.0002291966416970833069, 0.0004583932833941631443 ),
 .UNSPECIFIED. ) ;
#26895=ORIENTED_EDGE ( 'NONE', *, *, #38350, .F. ) ;
#26896=CARTESIAN_POINT ( 'NONE',  ( 0.9972139404380286898, 37.48536715150224552, 20.88226186415244001 ) ) ;
#26902=ORIENTED_EDGE ( 'NONE', *, *, #29681, .T. ) ;
#26906=CARTESIAN_POINT ( 'NONE',  ( 2.526552050251864134, 42.75269566045972169, -4.405466163646869049 ) ) ;
#26912=CARTESIAN_POINT ( 'NONE',  ( 0.5819845079324651449, -0.4540594263149760890, -47.89381220525412175 ) ) ;
#26919=LINE ( 'NONE', #3089, #51320 ) ;
#26921=ORIENTED_EDGE ( 'NONE', *, *, #55415, .T. ) ;
#26922=LINE ( 'NONE', #31617, #48732 ) ;
#26925=ADVANCED_FACE ( 'NONE', ( #9138 ), #12562, .F. ) ;
#26930=CARTESIAN_POINT ( 'NONE',  ( 0.5800708057587404820, 44.00606528161386422, 18.90714313908675237 ) ) ;
#26931=FACE_BOUND ( 'NONE', #56337, .T. ) ;
#26932=CARTESIAN_POINT ( 'NONE',  ( 0.5807400328401574052, 46.12278621143497048, 12.92266817606031104 ) ) ;
#26945=CARTESIAN_POINT ( 'NONE',  ( 0.5809828226811617480, -17.82437196699647686, -44.45562576850621639 ) ) ;
#26950=CARTESIAN_POINT ( 'NONE',  ( 0.9741495583595161101, -34.28086552274312737, 25.80610403442896228 ) ) ;
#26951=CARTESIAN_POINT ( 'NONE',  ( 5.965394784446460541, 14.50338846149112904, 14.52385693119007648 ) ) ;
#26955=CARTESIAN_POINT ( 'NONE',  ( 0.9757892942422816684, 21.40977514834436235, -37.18547544211192246 ) ) ;
#26956=CARTESIAN_POINT ( 'NONE',  ( 0.5786265663353196143, 38.43785771743242208, -28.58414684753446977 ) ) ;
#26961=CARTESIAN_POINT ( 'NONE',  ( 0.9756008150404604784, 37.08855330282530360, -21.57722292874418812 ) ) ;
#26965=CARTESIAN_POINT ( 'NONE',  ( 4.960156602257181468, 45.62767441207046204, 8.553784487773027578 ) ) ;
#26966=CARTESIAN_POINT ( 'NONE',  ( 4.956653778116988818, -43.37017594958040689, -20.77844580450608447 ) ) ;
#26978=CARTESIAN_POINT ( 'NONE',  ( 4.956653778116987041, -48.02038484091099235, -2.599733001514835884 ) ) ;
#26983=CARTESIAN_POINT ( 'NONE',  ( 4.956653778117001252, 47.05699031914963371, -9.917440902360649346 ) ) ;
#26984=ORIENTED_EDGE ( 'NONE', *, *, #40002, .T. ) ;
#26989=CARTESIAN_POINT ( 'NONE',  ( 0.9754402186311932343, -5.414674803234063027, 42.56545569314710775 ) ) ;
#26993=( BOUNDED_SURFACE ( )  B_SPLINE_SURFACE ( 3, 1, ( 
 ( #60987, #12795 ),
 ( #16872, #60669 ),
 ( #8360, #55051 ),
 ( #21556, #31889 ) ),
 .UNSPECIFIED., .F., .F., .F. ) 
 B_SPLINE_SURFACE_WITH_KNOTS ( ( 4, 4 ),
 ( 2, 2 ),
 ( 0.000000000000000000, 1.000000000000000000 ),
 ( 0.000000000000000000, 1.000000000000000000 ),
 .UNSPECIFIED. ) 
 GEOMETRIC_REPRESENTATION_ITEM ( )  RATIONAL_B_SPLINE_SURFACE ( (
 ( 1.000000000000000000, 1.000000000000000000),
 ( 0.9953390228620291325, 0.8624445117761032620),
 ( 0.9953390228620291325, 0.8624445117761032620),
 ( 1.000000000000000000, 1.000000000000000000) ) ) 
 REPRESENTATION_ITEM ( '' )  SURFACE ( )  );
#27001=ORIENTED_EDGE ( 'NONE', *, *, #34900, .T. ) ;
#27002=EDGE_CURVE ( 'NONE', #38495, #6221, #25724, .T. ) ;
#27003=CARTESIAN_POINT ( 'NONE',  ( 3.407937589446174087, 5.663729899985241012, -12.47329436636623257 ) ) ;
#27005=CARTESIAN_POINT ( 'NONE',  ( 4.303969348037258058, -30.97035057417636850, -36.81598326424581558 ) ) ;
#27009=EDGE_LOOP ( 'NONE', ( #41208, #43440, #36645, #37716 ) ) ;
#27011=B_SPLINE_CURVE_WITH_KNOTS ( 'NONE', 3,
 ( #4902, #5815, #24964, #43471 ),
 .UNSPECIFIED., .F., .F.,
 ( 4, 4 ),
 ( 6.397344083151129036E-17, 0.005004741218457477853 ),
 .UNSPECIFIED. ) ;
#27013=ORIENTED_EDGE ( 'NONE', *, *, #43706, .T. ) ;
#27014=CARTESIAN_POINT ( 'NONE',  ( 5.960221823109900008, 2.673723662181335392, -20.35070456576731956 ) ) ;
#27015=CARTESIAN_POINT ( 'NONE',  ( 4.960156602257177028, 8.553784487773508971, -45.62767441207027730 ) ) ;
#27024=CARTESIAN_POINT ( 'NONE',  ( 0.6067375320500707492, 6.954068056451403912, -47.38951440911009882 ) ) ;
#27031=CARTESIAN_POINT ( 'NONE',  ( 0.9730545539215883499, 33.73144377768594637, -26.52009130076736554 ) ) ;
#27036=EDGE_CURVE ( 'NONE', #24857, #19642, #19744, .T. ) ;
#27047=ORIENTED_EDGE ( 'NONE', *, *, #45557, .F. ) ;
#27053=AXIS2_PLACEMENT_3D ( 'NONE', #56857, #18366, #33704 ) ;
#27057=CARTESIAN_POINT ( 'NONE',  ( 5.959547316686252039, 7.851524054666140451, 18.96456592444103606 ) ) ;
#27064=EDGE_LOOP ( 'NONE', ( #26540, #35088, #42212, #45430 ) ) ;
#27066=CARTESIAN_POINT ( 'NONE',  ( 1.088313998177381503, -0.7798619649924283248, 42.90642884828984904 ) ) ;
#27070=CARTESIAN_POINT ( 'NONE',  ( 4.967162193818130511, 0.000000000000000000, 0.000000000000000000 ) ) ;
#27082=CARTESIAN_POINT ( 'NONE',  ( 5.959828726073459926, 7.850628836606585281, 18.96492317065697009 ) ) ;
#27088=VERTEX_POINT ( 'NONE', #27793 ) ;
#27091=CARTESIAN_POINT ( 'NONE',  ( 1.227938101723756947, 37.58536632582779191, 20.72293514920763258 ) ) ;
#27096=FACE_OUTER_BOUND ( 'NONE', #55275, .T. ) ;
#27097=CARTESIAN_POINT ( 'NONE',  ( 0.9747592971366210168, -5.921534893733859661, -42.49794971112905984 ) ) ;
#27100=CARTESIAN_POINT ( 'NONE',  ( 4.956653778116975495, 8.845409907520915382, 47.27023054223757015 ) ) ;
#27101=CARTESIAN_POINT ( 'NONE',  ( 0.7057020205115018818, -19.10543569325825430, 43.92641219669825148 ) ) ;
#27104=DIRECTION ( 'NONE',  ( 0.000000000000000000, 0.000000000000000000, 1.000000000000000000 ) ) ;
#27112=( BOUNDED_SURFACE ( )  B_SPLINE_SURFACE ( 3, 1, ( 
 ( #21220, #39741 ),
 ( #40060, #45059 ),
 ( #20308, #50039 ),
 ( #20609, #45360 ) ),
 .UNSPECIFIED., .F., .F., .F. ) 
 B_SPLINE_SURFACE_WITH_KNOTS ( ( 4, 4 ),
 ( 2, 2 ),
 ( 0.000000000000000000, 1.000000000000000000 ),
 ( 0.000000000000000000, 1.000000000000000000 ),
 .UNSPECIFIED. ) 
 GEOMETRIC_REPRESENTATION_ITEM ( )  RATIONAL_B_SPLINE_SURFACE ( (
 ( 1.000000000000000000, 1.000000000000000000),
 ( 0.9953390228620291325, 0.8624445117761032620),
 ( 0.9953390228620291325, 0.8624445117761032620),
 ( 1.000000000000000000, 1.000000000000000000) ) ) 
 REPRESENTATION_ITEM ( '' )  SURFACE ( )  );
#27116=ORIENTED_EDGE ( 'NONE', *, *, #27361, .T. ) ;
#27119=CARTESIAN_POINT ( 'NONE',  ( 1.227938101723748288, -25.45152231597034387, -34.55893248994532030 ) ) ;
#27123=CARTESIAN_POINT ( 'NONE',  ( 4.956653778116966613, 0.000000000000000000, 0.000000000000000000 ) ) ;
#27124=DIRECTION ( 'NONE',  ( 0.000000000000000000, 0.000000000000000000, 1.000000000000000000 ) ) ;
#27128=ORIENTED_EDGE ( 'NONE', *, *, #54942, .T. ) ;
#27133=ORIENTED_EDGE ( 'NONE', *, *, #43178, .T. ) ;
#27134=CARTESIAN_POINT ( 'NONE',  ( 0.6846871229502899947, 47.60345020167351038, 5.395516691087355099 ) ) ;
#27136=CIRCLE ( 'NONE', #56142, 43.08621763946400307 ) ;
#27137=CARTESIAN_POINT ( 'NONE',  ( 3.660176727303400934, -39.22755245663866930, 27.72864483302505434 ) ) ;
#27141=CARTESIAN_POINT ( 'NONE',  ( 0.5807400328401637335, -47.41494605191439149, -6.791881299636087554 ) ) ;
#27142=ORIENTED_EDGE ( 'NONE', *, *, #58830, .T. ) ;
#27145=CARTESIAN_POINT ( 'NONE',  ( 3.660176727303414257, 39.22755245663885404, -27.72864483302478078 ) ) ;
#27146=EDGE_CURVE ( 'NONE', #17051, #27319, #32387, .T. ) ;
#27150=CARTESIAN_POINT ( 'NONE',  ( 0.5839880159502343071, 41.45643525694605103, 23.98728323041064314 ) ) ;
#27161=CARTESIAN_POINT ( 'NONE',  ( 3.660176727303401822, -8.130955556894797098, 47.34518114598556338 ) ) ;
#27165=CARTESIAN_POINT ( 'NONE',  ( 4.303969348037246512, 48.06163817123226067, 2.158280495710376279 ) ) ;
#27168=EDGE_LOOP ( 'NONE', ( #48768, #4572, #57300, #46787 ) ) ;
#27178=CARTESIAN_POINT ( 'NONE',  ( 5.981074661064941900, 19.82308078259083572, 5.320466518161004466 ) ) ;
#27180=CARTESIAN_POINT ( 'NONE',  ( 5.960221823109900008, -18.96526051813975045, -7.849768660536494025 ) ) ;
#27181=CARTESIAN_POINT ( 'NONE',  ( 0.9968887458511656030, 41.61262323391482454, -10.46947792236050923 ) ) ;
#27184=VECTOR ( 'NONE', #56875, 1000.000000000000000 ) ;
#27186=CARTESIAN_POINT ( 'NONE',  ( 1.227938101723756947, -42.65467462194914816, -4.762198645644879491 ) ) ;
#27191=CARTESIAN_POINT ( 'NONE',  ( 0.8557997880470697982, -47.89938907511594834, 0.9121262075944505110 ) ) ;
#27195=CARTESIAN_POINT ( 'NONE',  ( 0.5839879327111916485, -24.02664985973677148, -41.43370681949804890 ) ) ;
#27198=DIRECTION ( 'NONE',  ( 0.000000000000000000, 0.000000000000000000, -1.000000000000000000 ) ) ;
#27203=CARTESIAN_POINT ( 'NONE',  ( 0.9757402383260933565, 11.18751708556368918, -41.42435672089860788 ) ) ;
#27205=CARTESIAN_POINT ( 'NONE',  ( 0.9741495583595181085, -39.48917442789106502, -16.78504838919925035 ) ) ;
#27206=CARTESIAN_POINT ( 'NONE',  ( 4.967162193818131399, -3.259922920618036901, 42.96271701169384016 ) ) ;
#27209=CARTESIAN_POINT ( 'NONE',  ( 3.270143674763207553, -13.68510027222513514, 0.2742231296309043942 ) ) ;
#27213=CARTESIAN_POINT ( 'NONE',  ( 0.8557997880470599172, 47.89938907511594124, 0.9121262075947815795 ) ) ;
#27214=CARTESIAN_POINT ( 'NONE',  ( 4.963659409799330291, 37.47512675766729018, -24.46566636552785212 ) ) ;
#27218=CARTESIAN_POINT ( 'NONE',  ( 0.5839880159502323087, -29.19321933421524307, 37.97080096460575049 ) ) ;
#27219=VERTEX_POINT ( 'NONE', #18093 ) ;
#27231=ORIENTED_EDGE ( 'NONE', *, *, #28279, .F. ) ;
#27240=EDGE_CURVE ( 'NONE', #3856, #11901, #3181, .T. ) ;
#27241=CARTESIAN_POINT ( 'NONE',  ( 0.8551540677456739292, -46.51172240253128365, 11.51835730326464180 ) ) ;
#27246=DIRECTION ( 'NONE',  ( 0.000000000000000000, 0.000000000000000000, 1.000000000000000000 ) ) ;
#27254=ORIENTED_EDGE ( 'NONE', *, *, #37365, .F. ) ;
#27258=CARTESIAN_POINT ( 'NONE',  ( 4.960156602257182357, -20.07163247083116886, -41.85906677498982020 ) ) ;
#27265=CARTESIAN_POINT ( 'NONE',  ( 5.974727161628369032, -16.29297756969656419, 12.48248968439901674 ) ) ;
#27267=CARTESIAN_POINT ( 'NONE',  ( 5.960721111146673579, -7.848955554238384202, -18.96557324978284242 ) ) ;
#27269=CARTESIAN_POINT ( 'NONE',  ( 4.967162193818129623, -32.10009971360051395, -28.74031574030045633 ) ) ;
#27273=CARTESIAN_POINT ( 'NONE',  ( 0.5809828226811617480, -28.72298383114462439, -38.32755012159175578 ) ) ;
#27275=CARTESIAN_POINT ( 'NONE',  ( 0.7762783648524375080, 47.89627393592490989, -0.8897020150999853660 ) ) ;
#27287=ORIENTED_EDGE ( 'NONE', *, *, #17492, .F. ) ;
#27301=CARTESIAN_POINT ( 'NONE',  ( 5.959828726073459926, -19.82738831247209532, -5.308046411395180186 ) ) ;
#27317=CARTESIAN_POINT ( 'NONE',  ( 0.6067099128993246326, 24.55985149487322161, 41.12102523654863262 ) ) ;
#27318=CARTESIAN_POINT ( 'NONE',  ( -48.95476116535499500, 0.000000000000000000, 0.000000000000000000 ) ) ;
#27319=VERTEX_POINT ( 'NONE', #25247 ) ;
#27323=CARTESIAN_POINT ( 'NONE',  ( 0.9747592971366256798, -16.12077520819477527, 39.76507150545825908 ) ) ;
#27324=ADVANCED_FACE ( 'NONE', ( #34656 ), #57801, .T. ) ;
#27327=CONICAL_SURFACE ( 'NONE', #34361, 43.08621763946400307, 1.568696531533066763 ) ;
#27328=CARTESIAN_POINT ( 'NONE',  ( 0.5800708057587373734, -29.65250565429469276, 37.61306623599830345 ) ) ;
#27333=CARTESIAN_POINT ( 'NONE',  ( 0.8557997880470690211, 0.9121262075946178216, 47.89938907511594124 ) ) ;
#27340=CARTESIAN_POINT ( 'NONE',  ( 0.9756008150404608115, -37.23069985082527467, -21.33101788548767175 ) ) ;
#27341=EDGE_CURVE ( 'NONE', #40152, #9472, #33840, .T. ) ;
#27353=CARTESIAN_POINT ( 'NONE',  ( 1.227938101723756947, 4.762198645645047357, -42.65467462194912684 ) ) ;
#27361=EDGE_CURVE ( 'NONE', #24606, #34885, #14816, .T. ) ;
#27363=CARTESIAN_POINT ( 'NONE',  ( 0.9730545539215883499, -41.31259007387239279, 11.59290486963492128 ) ) ;
#27364=ORIENTED_EDGE ( 'NONE', *, *, #58906, .F. ) ;
#27367=CARTESIAN_POINT ( 'NONE',  ( 4.967162193818130511, 0.000000000000000000, 0.000000000000000000 ) ) ;
#27371=ORIENTED_EDGE ( 'NONE', *, *, #15426, .F. ) ;
#27379=EDGE_LOOP ( 'NONE', ( #3654, #3565, #7558, #10093 ) ) ;
#27388=CARTESIAN_POINT ( 'NONE',  ( 3.783198216974389627, 33.06596988314798580, 27.54889409286091251 ) ) ;
#27393=ADVANCED_FACE ( 'NONE', ( #21471 ), #54815, .T. ) ;
#27394=CIRCLE ( 'NONE', #358, 43.08621763946400307 ) ;
#27397=CARTESIAN_POINT ( 'NONE',  ( 5.960221823109900008, -5.317678907195576343, 19.82478916873565922 ) ) ;
#27398=CARTESIAN_POINT ( 'NONE',  ( 0.8557997880470697982, -7.156447707085392018, -47.37054680076713709 ) ) ;
#27399=CARTESIAN_POINT ( 'NONE',  ( 1.088313998177382391, -22.12859469727364470, 36.76812638579223602 ) ) ;
#27409=CARTESIAN_POINT ( 'NONE',  ( 1.088908134280558437, -39.34174992079763911, 17.14055988408905762 ) ) ;
#27412=CARTESIAN_POINT ( 'NONE',  ( 0.5809828226811617480, 11.86925843957166471, 46.40184912890843805 ) ) ;
#27418=CARTESIAN_POINT ( 'NONE',  ( 0.7056555295713246023, -37.48482836297252163, 29.82339362082581502 ) ) ;
#27419=LINE ( 'NONE', #36853, #20522 ) ;
#27420=CARTESIAN_POINT ( 'NONE',  ( 0.9730545539215883499, 41.57420493492400482, -10.61654491617520080 ) ) ;
#27421=EDGE_CURVE ( 'NONE', #7786, #1247, #19829, .T. ) ;
#27425=DIRECTION ( 'NONE',  ( -0.07439287786467650709, 0.4871392060438144989, -0.8701500408883593440 ) ) ;
#27440=EDGE_CURVE ( 'NONE', #26290, #5464, #56219, .T. ) ;
#27446=EDGE_CURVE ( 'NONE', #26757, #9163, #53989, .T. ) ;
#27451=EDGE_LOOP ( 'NONE', ( #26902, #59486, #41355, #10684 ) ) ;
#27464=VERTEX_POINT ( 'NONE', #32738 ) ;
#27471=CARTESIAN_POINT ( 'NONE',  ( 4.967162193818130511, 40.93989340068628024, -13.42934394584121094 ) ) ;
#27472=CARTESIAN_POINT ( 'NONE',  ( 0.6067375320500720814, -6.954068056451050417, 47.38951440911012725 ) ) ;
#27477=ORIENTED_EDGE ( 'NONE', *, *, #61913, .F. ) ;
#27478=B_SPLINE_CURVE_WITH_KNOTS ( 'NONE', 3,
 ( #55845, #35534, #21417, #11725 ),
 .UNSPECIFIED., .F., .F.,
 ( 4, 4 ),
 ( 0.000000000000000000, 0.004444878191957686055 ),
 .UNSPECIFIED. ) ;
#27481=CARTESIAN_POINT ( 'NONE',  ( 0.5786265663353153954, 17.66171603226140974, -44.52624106864126219 ) ) ;
#27482=CARTESIAN_POINT ( 'NONE',  ( 4.967162193818130511, 24.30453456948110613, 35.57684288741985768 ) ) ;
#27485=CARTESIAN_POINT ( 'NONE',  ( 5.959547316686252039, 2.682663672454640658, 20.34955788964377632 ) ) ;
#27502=ADVANCED_FACE ( 'NONE', ( #41842 ), #52593, .F. ) ;
#27509=CARTESIAN_POINT ( 'NONE',  ( 4.960156602257181468, -3.546989772330209512, 46.28683144126592452 ) ) ;
#27511=VERTEX_POINT ( 'NONE', #34277 ) ;
#27514=ORIENTED_EDGE ( 'NONE', *, *, #28205, .T. ) ;
#27516=EDGE_CURVE ( 'NONE', #7786, #23911, #6156, .T. ) ;
#27519=B_SPLINE_CURVE_WITH_KNOTS ( 'NONE', 3,
 ( #4476, #23617, #33348, #23929 ),
 .UNSPECIFIED., .F., .F.,
 ( 4, 4 ),
 ( 2.168404344971008868E-19, 0.004444878191957648758 ),
 .UNSPECIFIED. ) ;
#27525=VERTEX_POINT ( 'NONE', #24559 ) ;
#27526=CARTESIAN_POINT ( 'NONE',  ( 0.9754402186311942335, 21.61645729243112868, 37.06569162601108047 ) ) ;
#27528=B_SPLINE_CURVE_WITH_KNOTS ( 'NONE', 3,
 ( #27646, #46780, #37072, #23561, #61749, #42088, #57059, #4420, #41775, #42689, #61140, #37688, #32359, #13560, #8220, #43007, #27960, #51432, #8526 ),
 .UNSPECIFIED., .F., .F.,
 ( 4, 3, 3, 3, 3, 3, 4 ),
 ( 3.469446951953614189E-18, 0.0002724573126191751050, 0.0004086839781548431104, 0.0005449106435901767157, 0.0006811373090491364959, 0.0008459866663933654713, 0.001010840725717215317 ),
 .UNSPECIFIED. ) ;
#27533=CARTESIAN_POINT ( 'NONE',  ( 0.5850706913938534814, 47.46255051844963191, -6.431767090162336054 ) ) ;
#27539=LINE ( 'NONE', #15226, #38472 ) ;
#27541=CARTESIAN_POINT ( 'NONE',  ( 0.8557997880470599172, 23.15977007032323343, 41.93815086860265495 ) ) ;
#27543=CARTESIAN_POINT ( 'NONE',  ( 0.9758171775293916772, 11.11125068417994122, 41.44488232057071997 ) ) ;
#27546=CONICAL_SURFACE ( 'NONE', #26562, 43.08621763946400307, 1.568696531533066763 ) ;
#27547=EDGE_CURVE ( 'NONE', #8543, #12597, #23394, .T. ) ;
#27551=( BOUNDED_SURFACE ( )  B_SPLINE_SURFACE ( 3, 1, ( 
 ( #11395, #48676 ),
 ( #53060, #29874 ),
 ( #39613, #20796 ),
 ( #25478, #39932 ) ),
 .UNSPECIFIED., .F., .F., .F. ) 
 B_SPLINE_SURFACE_WITH_KNOTS ( ( 4, 4 ),
 ( 2, 2 ),
 ( 0.000000000000000000, 1.000000000000000000 ),
 ( 0.000000000000000000, 1.000000000000000000 ),
 .UNSPECIFIED. ) 
 GEOMETRIC_REPRESENTATION_ITEM ( )  RATIONAL_B_SPLINE_SURFACE ( (
 ( 1.000000000000000000, 1.000000000000000000),
 ( 0.9953390228620291325, 0.8624445117761032620),
 ( 0.9953390228620291325, 0.8624445117761032620),
 ( 1.000000000000000000, 1.000000000000000000) ) ) 
 REPRESENTATION_ITEM ( '' )  SURFACE ( )  );
#27559=DIRECTION ( 'NONE',  ( 0.000000000000000000, 0.000000000000000000, 1.000000000000000000 ) ) ;
#27563=CARTESIAN_POINT ( 'NONE',  ( 1.088908134280553552, 22.12904883058554617, 36.76788378223834286 ) ) ;
#27566=CARTESIAN_POINT ( 'NONE',  ( 0.9730545539215883499, 21.01499094264601908, -37.40983423658450846 ) ) ;
#27568=CARTESIAN_POINT ( 'NONE',  ( 4.956653778116991482, -31.29546495791826644, -36.51451553856450971 ) ) ;
#27571=CARTESIAN_POINT ( 'NONE',  ( 0.5839880159502323087, 6.296669079378848011, -47.48028790449882308 ) ) ;
#27584=ADVANCED_FACE ( 'NONE', ( #13952 ), #14201, .F. ) ;
#27585=ORIENTED_EDGE ( 'NONE', *, *, #10325, .T. ) ;
#27588=CARTESIAN_POINT ( 'NONE',  ( 5.974727161628367256, 10.24903993265009206, -17.78288073588492324 ) ) ;
#27589=B_SPLINE_CURVE_WITH_KNOTS ( 'NONE', 3,
 ( #16784, #7341, #59048, #29942, #20856, #35274, #35589, #49049, #25855, #40604, #54334, #26470, #2651, #16460, #12095, #1412 ),
 .UNSPECIFIED., .F., .F.,
 ( 4, 3, 3, 3, 3, 4 ),
 ( 1.214354834101861570E-17, 0.0002724568934985554386, 0.0004086836638483811227, 0.0005449104342063607661, 0.0008173270854453699259, 0.001089761613562689876 ),
 .UNSPECIFIED. ) ;
#27606=DIRECTION ( 'NONE',  ( -0.07439287786467652097, 0.9971416435352943308, -0.01320009283086595250 ) ) ;
#27607=CARTESIAN_POINT ( 'NONE',  ( 0.8557997880470697982, 13.27832040216639520, 46.03118133706031045 ) ) ;
#27618=FACE_OUTER_BOUND ( 'NONE', #58548, .T. ) ;
#27623=ORIENTED_EDGE ( 'NONE', *, *, #6009, .F. ) ;
#27624=DIRECTION ( 'NONE',  ( 0.000000000000000000, 0.000000000000000000, 1.000000000000000000 ) ) ;
#27628=( BOUNDED_SURFACE ( )  B_SPLINE_SURFACE ( 3, 1, ( 
 ( #55170, #41119 ),
 ( #12292, #3166 ),
 ( #22294, #13834 ),
 ( #57309, #42344 ) ),
 .UNSPECIFIED., .F., .F., .F. ) 
 B_SPLINE_SURFACE_WITH_KNOTS ( ( 4, 4 ),
 ( 2, 2 ),
 ( 0.000000000000000000, 1.000000000000000000 ),
 ( 0.000000000000000000, 1.000000000000000000 ),
 .UNSPECIFIED. ) 
 GEOMETRIC_REPRESENTATION_ITEM ( )  RATIONAL_B_SPLINE_SURFACE ( (
 ( 1.000000000000000000, 1.000000000000000000),
 ( 0.9732289882329797637, 0.9999525324661233672),
 ( 0.9732289882329797637, 0.9999525324661233672),
 ( 1.000000000000000000, 1.000000000000000000) ) ) 
 REPRESENTATION_ITEM ( '' )  SURFACE ( )  );
#27632=CARTESIAN_POINT ( 'NONE',  ( 0.8551540677456715978, 38.56334384152431483, 28.44084013485131024 ) ) ;
#27639=CARTESIAN_POINT ( 'NONE',  ( 0.5827357941260203900, -46.16863402900289515, 12.74691551863615224 ) ) ;
#27646=CARTESIAN_POINT ( 'NONE',  ( 0.9730545539215883499, 37.40983423658472873, 21.01499094264562473 ) ) ;
#27650=CARTESIAN_POINT ( 'NONE',  ( 0.8557997880470697982, -47.60865952216995822, -5.347802024197736870 ) ) ;
#27657=CARTESIAN_POINT ( 'NONE',  ( 4.960156602257180580, 20.99019478193107346, -41.40608197274610802 ) ) ;
#27660=ADVANCED_FACE ( 'NONE', ( #15474 ), #58992, .F. ) ;
#27668=CARTESIAN_POINT ( 'NONE',  ( 0.9736507210033062965, -10.66979144439339500, -41.56063510425041585 ) ) ;
#27671=DIRECTION ( 'NONE',  ( 0.07439287786467664587, 0.3693942911085579262, 0.9262902123089810091 ) ) ;
#27672=CARTESIAN_POINT ( 'NONE',  ( 0.5809828226811626362, -18.83114015454730961, 44.03860873105688967 ) ) ;
#27673=CONICAL_SURFACE ( 'NONE', #5592, 43.08621763946400307, 1.568696531533066763 ) ;
#27677=EDGE_CURVE ( 'NONE', #58998, #28511, #11088, .T. ) ;
#27687=CARTESIAN_POINT ( 'NONE',  ( 5.960721111146673579, 17.77882586010652943, 10.25731071096588920 ) ) ;
#27689=CARTESIAN_POINT ( 'NONE',  ( 0.8557997880470697982, 34.51495345639548873, 33.22501220301912639 ) ) ;
#27701=ORIENTED_EDGE ( 'NONE', *, *, #35083, .F. ) ;
#27704=CARTESIAN_POINT ( 'NONE',  ( 0.9757892942422823346, 30.37715353261994977, 30.30456399643803067 ) ) ;
#27707=CARTESIAN_POINT ( 'NONE',  ( 0.5786265663353196143, -43.97352617418602705, -18.99608782658079775 ) ) ;
#27709=CARTESIAN_POINT ( 'NONE',  ( 0.5809828226811617480, -0.5448590168535863976, 47.89273459658653564 ) ) ;
#27714=CARTESIAN_POINT ( 'NONE',  ( 3.660176727303390276, 40.62966184289491878, 25.63023984566660118 ) ) ;
#27716=B_SPLINE_CURVE_WITH_KNOTS ( 'NONE', 3,
 ( #55753, #55446, #16640, #59847, #26036, #26961, #7840, #45171, #21643, #45780, #21958, #49519, #2197, #1899, #30403, #50450, #40167, #60447, #17567 ),
 .UNSPECIFIED., .F., .F.,
 ( 4, 3, 3, 3, 3, 3, 4 ),
 ( 9.813676791237319219E-18, 0.0002724573126191774360, 0.0004086839781548490193, 0.0005449106435901849557, 0.0006811373090491581800, 0.0008459866663933742533, 0.001010840725717204692 ),
 .UNSPECIFIED. ) ;
#27723=FACE_OUTER_BOUND ( 'NONE', #22124, .T. ) ;
#27728=CARTESIAN_POINT ( 'NONE',  ( 5.960221823109900008, 0.005450390361438351740, 20.52559243573973546 ) ) ;
#27731=( BOUNDED_SURFACE ( )  B_SPLINE_SURFACE ( 3, 1, ( 
 ( #61055, #37282 ),
 ( #42293, #32576 ),
 ( #51655, #8746 ),
 ( #56661, #4027 ) ),
 .UNSPECIFIED., .F., .F., .F. ) 
 B_SPLINE_SURFACE_WITH_KNOTS ( ( 4, 4 ),
 ( 2, 2 ),
 ( 0.000000000000000000, 1.000000000000000000 ),
 ( 0.000000000000000000, 1.000000000000000000 ),
 .UNSPECIFIED. ) 
 GEOMETRIC_REPRESENTATION_ITEM ( )  RATIONAL_B_SPLINE_SURFACE ( (
 ( 1.000000000000000000, 1.000000000000000000),
 ( 0.7269869731126821222, 0.9931720237060910339),
 ( 0.7269869731126821222, 0.9931720237060910339),
 ( 1.000000000000000000, 1.000000000000000000) ) ) 
 REPRESENTATION_ITEM ( '' )  SURFACE ( )  );
#27738=CARTESIAN_POINT ( 'NONE',  ( 0.9972139404380298000, -42.90441115546387607, 0.6581143129158801841 ) ) ;
#27740=ADVANCED_FACE ( 'NONE', ( #40236 ), #37825, .F. ) ;
#27751=EDGE_CURVE ( 'NONE', #58674, #52304, #59914, .T. ) ;
#27756=EDGE_LOOP ( 'NONE', ( #49468, #41650, #59303, #42478 ) ) ;
#27763=CARTESIAN_POINT ( 'NONE',  ( 4.303969348037246512, -48.06163817123224646, -2.158280495710712454 ) ) ;
#27765=DIRECTION ( 'NONE',  ( -1.000000000000000000, -0.000000000000000000, -0.000000000000000000 ) ) ;
#27774=CARTESIAN_POINT ( 'NONE',  ( 1.088313998177379949, -4.827222641554953064, -42.64115081428568743 ) ) ;
#27785=CARTESIAN_POINT ( 'NONE',  ( 4.967162193818130511, 0.000000000000000000, 0.000000000000000000 ) ) ;
#27793=CARTESIAN_POINT ( 'NONE',  ( 4.967162193818130511, 24.30453456948110613, 35.57684288741985768 ) ) ;
#27799=CARTESIAN_POINT ( 'NONE',  ( 5.960721111146673579, -10.26825948882913586, -17.77250458025988422 ) ) ;
#27803=CARTESIAN_POINT ( 'NONE',  ( 0.5786265663353153954, 41.11783955080273500, -24.57327059187355189 ) ) ;
#27805=EDGE_CURVE ( 'NONE', #34886, #18589, #48877, .T. ) ;
#27818=CARTESIAN_POINT ( 'NONE',  ( 0.9747592971366234593, 10.79247637456177245, -41.52905920980973775 ) ) ;
#27832=B_SPLINE_CURVE_WITH_KNOTS ( 'NONE', 3,
 ( #5704, #58963, #22315, #40834, #31092, #45832, #46139, #31401, #21384, #51106, #2569, #22008, #60815, #35810, #2254, #2876 ),
 .UNSPECIFIED., .F., .F.,
 ( 4, 3, 3, 3, 3, 4 ),
 ( 1.040890552917501732E-17, 0.0002724568934985567396, 0.0004086836638483815564, 0.0005449104342063605493, 0.0008173270854453664564, 0.001089761613562688141 ),
 .UNSPECIFIED. ) ;
#27833=CARTESIAN_POINT ( 'NONE',  ( 2.281351352603287364, 47.95523304704249057, 1.314116150903620106 ) ) ;
#27838=CARTESIAN_POINT ( 'NONE',  ( 0.9756950546413940550, 21.53795086961263650, 37.11135009583534128 ) ) ;
#27842=ORIENTED_EDGE ( 'NONE', *, *, #23018, .T. ) ;
#27843=CARTESIAN_POINT ( 'NONE',  ( 0.5850706913938533704, 47.50996714391791187, -6.071602062250133436 ) ) ;
#27860=SURFACE_STYLE_FILL_AREA ( #43215 ) ;
#27867=CIRCLE ( 'NONE', #5829, 43.08621763946400307 ) ;
#27871=DIRECTION ( 'NONE',  ( -1.000000000000000000, -0.000000000000000000, -0.000000000000000000 ) ) ;
#27877=ORIENTED_EDGE ( 'NONE', *, *, #5543, .T. ) ;
#27878=CARTESIAN_POINT ( 'NONE',  ( 0.8557997880470606944, 47.37054680076706603, 7.156447707085862753 ) ) ;
#27880=EDGE_CURVE ( 'NONE', #7019, #54529, #18554, .T. ) ;
#27881=CARTESIAN_POINT ( 'NONE',  ( 0.8557997880470599172, 46.50333260518575429, -11.51622788066409697 ) ) ;
#27885=LINE ( 'NONE', #39160, #32241 ) ;
#27887=CARTESIAN_POINT ( 'NONE',  ( 5.960221823109900008, 19.82761049839334788, 5.307149561568152762 ) ) ;
#27888=CARTESIAN_POINT ( 'NONE',  ( 0.8557997880470690211, -0.9121262075942833114, -47.89938907511595545 ) ) ;
#27889=CARTESIAN_POINT ( 'NONE',  ( 4.967162193818130511, -38.83676580803754064, -18.65818244221298983 ) ) ;
#27894=FACE_OUTER_BOUND ( 'NONE', #47151, .T. ) ;
#27899=CARTESIAN_POINT ( 'NONE',  ( 0.5809828226811617480, 18.83114015454759738, -44.03860873105676177 ) ) ;
#27900=EDGE_CURVE ( 'NONE', #61413, #41443, #13871, .T. ) ;
#27903=( LENGTH_UNIT ( ) NAMED_UNIT ( * ) SI_UNIT ( .MILLI., .METRE. ) );
#27904=ORIENTED_EDGE ( 'NONE', *, *, #58044, .T. ) ;
#27914=CARTESIAN_POINT ( 'NONE',  ( 0.5819845901640494645, -5.801229454883635839, -47.54333976522122640 ) ) ;
#27918=VERTEX_POINT ( 'NONE', #9762 ) ;
#27921=CARTESIAN_POINT ( 'NONE',  ( 0.9968887458511638267, 0.6574002966414476123, -42.90440775986216693 ) ) ;
#27929=CARTESIAN_POINT ( 'NONE',  ( 5.960221823109900008, -5.307149561567947593, -19.82761049839340117 ) ) ;
#27930=CARTESIAN_POINT ( 'NONE',  ( 0.5850706913938534814, -29.30134895053029709, -37.88789093229835458 ) ) ;
#27933=EDGE_CURVE ( 'NONE', #4978, #38949, #32978, .T. ) ;
#27934=ORIENTED_EDGE ( 'NONE', *, *, #42109, .F. ) ;
#27938=CARTESIAN_POINT ( 'NONE',  ( 0.6846871229502932144, -7.109010606687719225, 47.37786444808391906 ) ) ;
#27947=EDGE_CURVE ( 'NONE', #22992, #3856, #56928, .T. ) ;
#27948=CARTESIAN_POINT ( 'NONE',  ( 0.5807400328401637335, -41.20655774452986719, 24.41979442053154870 ) ) ;
#27950=CARTESIAN_POINT ( 'NONE',  ( 5.959547316686252039, -10.25972575517517704, -17.77749189599214219 ) ) ;
#27952=DIRECTION ( 'NONE',  ( -0.07836865515943411409, -0.7956898808744429230, -0.6006129930017468643 ) ) ;
#27953=CARTESIAN_POINT ( 'NONE',  ( 4.967162193818130511, 28.74031574030056646, -32.10009971360042158 ) ) ;
#27956=FACE_OUTER_BOUND ( 'NONE', #33165, .T. ) ;
#27960=CARTESIAN_POINT ( 'NONE',  ( 0.9741495583595177754, 36.96045061395533793, 21.79582154536815608 ) ) ;
#27966=DIRECTION ( 'NONE',  ( 0.000000000000000000, 0.000000000000000000, 1.000000000000000000 ) ) ;
#27967=LINE ( 'NONE', #46474, #11494 ) ;
#27968=CARTESIAN_POINT ( 'NONE',  ( 0.5850706913938534814, -46.31100969101478881, -12.22095376872085382 ) ) ;
#27970=ORIENTED_EDGE ( 'NONE', *, *, #659, .T. ) ;
#27971=CARTESIAN_POINT ( 'NONE',  ( 4.960156602257180580, 26.21519897043481961, -38.31207700265922256 ) ) ;
#27972=B_SPLINE_CURVE_WITH_KNOTS ( 'NONE', 3,
 ( #53537, #29434, #39486, #15672, #24432, #14743 ),
 .UNSPECIFIED., .F., .F.,
 ( 4, 2, 4 ),
 ( 1.487699617223508360E-16, 0.0002445252820015211956, 0.0004890505640028936386 ),
 .UNSPECIFIED. ) ;
#27981=CARTESIAN_POINT ( 'NONE',  ( 0.9754402186311951217, -41.39745964575704562, 11.28658745892504456 ) ) ;
#27982=ORIENTED_EDGE ( 'NONE', *, *, #7618, .F. ) ;
#27993=ORIENTED_EDGE ( 'NONE', *, *, #40002, .F. ) ;
#27995=AXIS2_PLACEMENT_3D ( 'NONE', #10774, #12251, #7198 ) ;
#27999=CARTESIAN_POINT ( 'NONE',  ( 5.974727161628369032, 2.663664384318509715, 20.35137732084677253 ) ) ;
#28002=EDGE_CURVE ( 'NONE', #36997, #55413, #20341, .T. ) ;
#28006=EDGE_CURVE ( 'NONE', #10306, #2188, #61465, .T. ) ;
#28023=B_SPLINE_CURVE_WITH_KNOTS ( 'NONE', 3,
 ( #10682, #34806, #30082, #20696, #39836, #7181, #51035, #17857, #36053, #55422, #2497, #51342, #50725, #3720, #7816, #21619, #8425, #35740, #41670 ),
 .UNSPECIFIED., .F., .F.,
 ( 4, 3, 3, 3, 3, 3, 4 ),
 ( 9.813676791237319219E-18, 0.0002724573126191667566, 0.0004086839781548390988, 0.0005449106435901880999, 0.0006811373090491526505, 0.0008459866663933667723, 0.001010840725717211197 ),
 .UNSPECIFIED. ) ;
#28025=CARTESIAN_POINT ( 'NONE',  ( 5.959547316686252039, 12.49803383497749820, -16.28190225198605745 ) ) ;
#28031=ADVANCED_FACE ( 'NONE', ( #5648 ), #40200, .F. ) ;
#28036=EDGE_CURVE ( 'NONE', #25685, #26377, #7868, .T. ) ;
#28043=CARTESIAN_POINT ( 'NONE',  ( 2.281351352603211424, 32.98025003937418376, 34.83869092251570265 ) ) ;
#28046=CARTESIAN_POINT ( 'NONE',  ( 0.7762783648524372859, -37.45705264446598193, 29.86325223096999082 ) ) ;
#28048=CARTESIAN_POINT ( 'NONE',  ( 0.7762777257811896980, 17.50713318242637584, 44.59086130178256724 ) ) ;
#28053=ORIENTED_EDGE ( 'NONE', *, *, #40618, .F. ) ;
#28056=EDGE_CURVE ( 'NONE', #1247, #26085, #57684, .T. ) ;
#28064=CARTESIAN_POINT ( 'NONE',  ( 0.9730545539215883499, 26.52009130076770305, 33.73144377768567637 ) ) ;
#28067=B_SPLINE_CURVE_WITH_KNOTS ( 'NONE', 3,
 ( #53171, #34099, #10276, #29369, #28440, #28759 ),
 .UNSPECIFIED., .F., .F.,
 ( 4, 2, 4 ),
 ( 7.023086426956682172E-18, 0.0002445244328975374024, 0.0004890488657950677574 ),
 .UNSPECIFIED. ) ;
#28089=EDGE_CURVE ( 'NONE', #13993, #38729, #27867, .T. ) ;
#28093=( BOUNDED_SURFACE ( )  B_SPLINE_SURFACE ( 3, 1, ( 
 ( #7918, #32051 ),
 ( #45854, #12332 ),
 ( #61137, #41153 ),
 ( #8846, #18258 ) ),
 .UNSPECIFIED., .F., .F., .F. ) 
 B_SPLINE_SURFACE_WITH_KNOTS ( ( 4, 4 ),
 ( 2, 2 ),
 ( 0.000000000000000000, 1.000000000000000000 ),
 ( 0.000000000000000000, 1.000000000000000000 ),
 .UNSPECIFIED. ) 
 GEOMETRIC_REPRESENTATION_ITEM ( )  RATIONAL_B_SPLINE_SURFACE ( (
 ( 1.000000000000000000, 1.000000000000000000),
 ( 0.9953390228620291325, 0.8624445117761032620),
 ( 0.9953390228620291325, 0.8624445117761032620),
 ( 1.000000000000000000, 1.000000000000000000) ) ) 
 REPRESENTATION_ITEM ( '' )  SURFACE ( )  );
#28098=ORIENTED_EDGE ( 'NONE', *, *, #23663, .T. ) ;
#28103=CARTESIAN_POINT ( 'NONE',  ( 4.956653778116975495, 20.77844580450561551, 43.37017594958062006 ) ) ;
#28106=B_SPLINE_CURVE_WITH_KNOTS ( 'NONE', 3,
 ( #2721, #32175, #45667, #31239 ),
 .UNSPECIFIED., .F., .F.,
 ( 4, 4 ),
 ( 0.000000000000000000, 0.005004741218457420607 ),
 .UNSPECIFIED. ) ;
#28116=CARTESIAN_POINT ( 'NONE',  ( 5.860006189529246790, 21.34829429597527550, -43.25137511473229068 ) ) ;
#28120=CARTESIAN_POINT ( 'NONE',  ( 2.526464513654347321, -25.19161096467252747, 34.82216969498457360 ) ) ;
#28122=VERTEX_POINT ( 'NONE', #35447 ) ;
#28125=CARTESIAN_POINT ( 'NONE',  ( -20.07373396512872787, -8.000008915846105850, 0.1379583681271069062 ) ) ;
#28128=B_SPLINE_CURVE_WITH_KNOTS ( 'NONE', 3,
 ( #58353, #52750, #38080, #28639 ),
 .UNSPECIFIED., .F., .F.,
 ( 4, 4 ),
 ( 0.000000000000000000, 0.004048833967417087357 ),
 .UNSPECIFIED. ) ;
#28130=CARTESIAN_POINT ( 'NONE',  ( 4.963659409799330291, -29.14784479683135743, 33.96111158240236705 ) ) ;
#28131=VERTEX_POINT ( 'NONE', #39534 ) ;
#28142=VERTEX_POINT ( 'NONE', #13180 ) ;
#28149=CARTESIAN_POINT ( 'NONE',  ( 1.154321713695928064, -42.43366804783610746, -6.418927679456075452 ) ) ;
#28151=CARTESIAN_POINT ( 'NONE',  ( 0.7056555295713290432, 46.47980662829232301, 11.58338207350417015 ) ) ;
#28154=CARTESIAN_POINT ( 'NONE',  ( 0.9756354156337461170, 0.1303083999672954851, -42.90827993934335893 ) ) ;
#28166=CARTESIAN_POINT ( 'NONE',  ( 4.967162193818130511, -32.68434214048189546, 28.07411493385282242 ) ) ;
#28167=CARTESIAN_POINT ( 'NONE',  ( 0.5807400328401637335, -29.58941477093042494, 37.66660715020854866 ) ) ;
#28168=( BOUNDED_SURFACE ( )  B_SPLINE_SURFACE ( 3, 1, ( 
 ( #50465, #3451 ),
 ( #50766, #31676 ),
 ( #27588, #55154 ),
 ( #26661, #21975 ) ),
 .UNSPECIFIED., .F., .F., .F. ) 
 B_SPLINE_SURFACE_WITH_KNOTS ( ( 4, 4 ),
 ( 2, 2 ),
 ( 0.000000000000000000, 1.000000000000000000 ),
 ( 0.000000000000000000, 1.000000000000000000 ),
 .UNSPECIFIED. ) 
 GEOMETRIC_REPRESENTATION_ITEM ( )  RATIONAL_B_SPLINE_SURFACE ( (
 ( 1.000000000000000000, 1.000000000000000000),
 ( 0.7269869731126821222, 0.9931720237060910339),
 ( 0.7269869731126821222, 0.9931720237060910339),
 ( 1.000000000000000000, 1.000000000000000000) ) ) 
 REPRESENTATION_ITEM ( '' )  SURFACE ( )  );
#28174=CARTESIAN_POINT ( 'NONE',  ( 4.967162193818130511, 43.02067033766019932, -2.375726030842729486 ) ) ;
#28180=CARTESIAN_POINT ( 'NONE',  ( 5.974727161628367256, -20.35137732084674056, -2.663664384318710887 ) ) ;
#28181=B_SPLINE_CURVE_WITH_KNOTS ( 'NONE', 3,
 ( #6249, #11302, #49200, #31025, #8351, #30088, #3645, #46597, #49820, #54813, #26319, #36903, #21626, #54492, #16624, #6881, #51266, #32183, #58895, #25391, #21012, #49507, #41910, #60977, #34814, #39842, #44538, #40765, #59830, #20702 ),
 .UNSPECIFIED., .F., .F.,
 ( 4, 2, 2, 2, 2, 2, 2, 2, 2, 2, 2, 2, 2, 2, 4 ),
 ( 0.006577215611807306177, 0.007399161751817349281, 0.007810134821822366062, 0.008221107891827382844, 0.008632080961832398758, 0.009043054031837416407, 0.009454027101842432321, 0.009865000171847449970, 0.01027597324185246588, 0.01068694631185748180, 0.01109791938186249771, 0.01150889245186751536, 0.01233083859187754892, 0.01274181166188256484, 0.01315278473188758249 ),
 .UNSPECIFIED. ) ;
#28185=CARTESIAN_POINT ( 'NONE',  ( 4.956653778116990594, -35.79382859084093127, -32.11725092155079864 ) ) ;
#28187=ORIENTED_EDGE ( 'NONE', *, *, #18964, .F. ) ;
#28188=EDGE_CURVE ( 'NONE', #51030, #39564, #12566, .T. ) ;
#28202=VERTEX_POINT ( 'NONE', #27568 ) ;
#28205=EDGE_CURVE ( 'NONE', #24773, #4220, #48728, .T. ) ;
#28211=CARTESIAN_POINT ( 'NONE',  ( 0.5809828226811626362, -12.92184523170236510, 46.11980934799335330 ) ) ;
#28214=CARTESIAN_POINT ( 'NONE',  ( 4.967162193818130511, -3.259922920617460029, -42.96271701169388280 ) ) ;
#28218=FACE_OUTER_BOUND ( 'NONE', #1083, .T. ) ;
#28219=ADVANCED_FACE ( 'NONE', ( #26333 ), #50576, .F. ) ;
#28220=VERTEX_POINT ( 'NONE', #31974 ) ;
#28223=CARTESIAN_POINT ( 'NONE',  ( 0.8551540677456715978, 19.17641535420853671, 43.91216198251545677 ) ) ;
#28225=EDGE_LOOP ( 'NONE', ( #23968, #46330, #59085, #31097 ) ) ;
#28226=ADVANCED_FACE ( 'NONE', ( #31656 ), #29361, .F. ) ;
#28227=CARTESIAN_POINT ( 'NONE',  ( 5.960721111146673579, -5.306302591836445259, -19.82781442290496443 ) ) ;
#28233=CARTESIAN_POINT ( 'NONE',  ( 1.227938101723748288, 11.92353943228006585, -41.23019537246697297 ) ) ;
#28235=VERTEX_POINT ( 'NONE', #42006 ) ;
#28239=FACE_BOUND ( 'NONE', #18911, .T. ) ;
#28242=CARTESIAN_POINT ( 'NONE',  ( 0.5807400328401637335, 38.33001520688950592, 28.72484455891654065 ) ) ;
#28244=CARTESIAN_POINT ( 'NONE',  ( 0.5807400328401637335, 24.41979442053169436, 41.20655774452978193 ) ) ;
#28248=CARTESIAN_POINT ( 'NONE',  ( 5.958863334805807099, -16.28483817244747556, 12.49425770716459994 ) ) ;
#28255=CARTESIAN_POINT ( 'NONE',  ( 0.9756354156337452288, 30.43287766742290046, -30.24859376089789009 ) ) ;
#28257=CARTESIAN_POINT ( 'NONE',  ( 1.227938101723748288, -34.55893248994524214, 25.45152231597044690 ) ) ;
#28261=CARTESIAN_POINT ( 'NONE',  ( 0.9754642270333709897, -37.07163437210430601, -21.60621846558674974 ) ) ;
#28265=ORIENTED_EDGE ( 'NONE', *, *, #27880, .F. ) ;
#28267=CARTESIAN_POINT ( 'NONE',  ( 0.5839879327111934249, 24.02664985973703793, 41.43370681949784995 ) ) ;
#28271=CARTESIAN_POINT ( 'NONE',  ( 5.960721111146673579, -16.28787783074235662, 12.49016043756443750 ) ) ;
#28274=EDGE_LOOP ( 'NONE', ( #5267, #5020, #38961, #26771 ) ) ;
#28279=EDGE_CURVE ( 'NONE', #45339, #17051, #7664, .T. ) ;
#28280=CARTESIAN_POINT ( 'NONE',  ( 0.5807400328401574052, -18.83234461715150587, -44.04145271122585115 ) ) ;
#28283=ORIENTED_EDGE ( 'NONE', *, *, #37365, .T. ) ;
#28284=VERTEX_POINT ( 'NONE', #27881 ) ;
#28286=VERTEX_POINT ( 'NONE', #10015 ) ;
#28294=CARTESIAN_POINT ( 'NONE',  ( 0.9756354156337452288, -33.96210048825357575, -26.22428641656288306 ) ) ;
#28297=CARTESIAN_POINT ( 'NONE',  ( 0.5850706913938533704, -44.31965802246118358, 18.16120156791865270 ) ) ;
#28302=DIRECTION ( 'NONE',  ( 0.000000000000000000, 0.000000000000000000, 1.000000000000000000 ) ) ;
#28308=B_SPLINE_CURVE_WITH_KNOTS ( 'NONE', 3,
 ( #58664, #47766, #43078, #115 ),
 .UNSPECIFIED., .F., .F.,
 ( 4, 4 ),
 ( 2.927345865710861972E-18, 0.004444878191957672177 ),
 .UNSPECIFIED. ) ;
#28312=CARTESIAN_POINT ( 'NONE',  ( 0.5800708119828336118, -38.37709857409249992, -28.65679933661834511 ) ) ;
#28313=CARTESIAN_POINT ( 'NONE',  ( 0.9741495583595173313, 30.05988007970395870, 30.61921547032163815 ) ) ;
#28322=B_SPLINE_CURVE_WITH_KNOTS ( 'NONE', 3,
 ( #42046, #18221, #13839, #61706 ),
 .UNSPECIFIED., .F., .F.,
 ( 4, 4 ),
 ( 1.951563910473907981E-18, 0.004048833967417086489 ),
 .UNSPECIFIED. ) ;
#28324=CARTESIAN_POINT ( 'NONE',  ( 5.860006189529246790, -21.34829429597497708, 43.25137511473244700 ) ) ;
#28326=ADVANCED_FACE ( 'NONE', ( #56675 ), #20589, .F. ) ;
#28330=CARTESIAN_POINT ( 'NONE',  ( 5.958863334805807099, -5.311251202228716828, -19.82657410201440840 ) ) ;
#28337=LINE ( 'NONE', #18342, #1096 ) ;
#28347=CARTESIAN_POINT ( 'NONE',  ( 0.8557997880470606944, 43.90420959842181503, 19.17299735372024827 ) ) ;
#28348=CARTESIAN_POINT ( 'NONE',  ( 5.965394784446458765, -14.52385693118993082, -14.50338846149128358 ) ) ;
#28354=ORIENTED_EDGE ( 'NONE', *, *, #53261, .F. ) ;
#28356=ADVANCED_FACE ( 'NONE', ( #43543 ), #24615, .F. ) ;
#28357=CARTESIAN_POINT ( 'NONE',  ( 0.9757402383260933565, 41.42435672089872867, 11.18751708556325397 ) ) ;
#28359=CARTESIAN_POINT ( 'NONE',  ( 5.960721111146673579, 7.860635756377621242, 18.96073515164551537 ) ) ;
#28360=CARTESIAN_POINT ( 'NONE',  ( 1.088908134280557105, -34.51503525510833015, -25.50067491870075287 ) ) ;
#28364=CARTESIAN_POINT ( 'NONE',  ( 0.5819845079324661441, 37.72030202710114821, -29.51613512130344574 ) ) ;
#28369=CARTESIAN_POINT ( 'NONE',  ( 0.9968887458511668243, 42.45154664631704833, 6.251925120321585538 ) ) ;
#28372=CARTESIAN_POINT ( 'NONE',  ( 0.7762777257811900311, -47.89627391089017294, -0.8897018348891000405 ) ) ;
#28374=CARTESIAN_POINT ( 'NONE',  ( 0.9730545539215883499, 15.95224156741828914, 39.83279466599044838 ) ) ;
#28376=ORIENTED_EDGE ( 'NONE', *, *, #34026, .F. ) ;
#28378=CARTESIAN_POINT ( 'NONE',  ( 0.5786265663353153954, -17.66171603226112197, 44.52624106864138298 ) ) ;
#28379=CARTESIAN_POINT ( 'NONE',  ( 4.967162193818130511, 0.000000000000000000, 0.000000000000000000 ) ) ;
#28382=( BOUNDED_SURFACE ( )  B_SPLINE_SURFACE ( 3, 1, ( 
 ( #20275, #58444 ),
 ( #39393, #15572 ),
 ( #34678, #10876 ),
 ( #29966, #49075 ) ),
 .UNSPECIFIED., .F., .F., .F. ) 
 B_SPLINE_SURFACE_WITH_KNOTS ( ( 4, 4 ),
 ( 2, 2 ),
 ( 0.000000000000000000, 1.000000000000000000 ),
 ( 0.000000000000000000, 1.000000000000000000 ),
 .UNSPECIFIED. ) 
 GEOMETRIC_REPRESENTATION_ITEM ( )  RATIONAL_B_SPLINE_SURFACE ( (
 ( 1.000000000000000000, 1.000000000000000000),
 ( 0.7269869731126817891, 0.9931720237060910339),
 ( 0.7269869731126817891, 0.9931720237060910339),
 ( 1.000000000000000000, 1.000000000000000000) ) ) 
 REPRESENTATION_ITEM ( '' )  SURFACE ( )  );
#28391=CARTESIAN_POINT ( 'NONE',  ( 0.9754402186311941225, 25.97197377940605989, -34.15542855230911101 ) ) ;
#28399=EDGE_LOOP ( 'NONE', ( #48644, #18500, #23774, #54386 ) ) ;
#28404=CARTESIAN_POINT ( 'NONE',  ( 5.974727161628367256, -2.694421823322779019, -20.34732802718246703 ) ) ;
#28409=CARTESIAN_POINT ( 'NONE',  ( 0.5838002273316411639, -47.89576566046789452, -0.1361971433783075169 ) ) ;
#28415=FACE_OUTER_BOUND ( 'NONE', #28839, .T. ) ;
#28418=CARTESIAN_POINT ( 'NONE',  ( 0.9730545539215883499, 42.47233286818625686, -6.101350888304211573 ) ) ;
#28423=CARTESIAN_POINT ( 'NONE',  ( 0.9758171775293909000, 11.09981579996865264, -41.44794628856068641 ) ) ;
#28428=CARTESIAN_POINT ( 'NONE',  ( 0.9730545539215883499, -25.71816799638755668, -34.34678117142582465 ) ) ;
#28438=CARTESIAN_POINT ( 'NONE',  ( 1.088908134280556661, 42.90644581410506220, -0.7803765577543299026 ) ) ;
#28440=CARTESIAN_POINT ( 'NONE',  ( 0.7762783648524360647, -24.71864151483687166, -41.03453896757969943 ) ) ;
#28444=EDGE_CURVE ( 'NONE', #21051, #42119, #2333, .T. ) ;
#28450=( BOUNDED_SURFACE ( )  B_SPLINE_SURFACE ( 3, 1, ( 
 ( #35370, #54427 ),
 ( #10943, #30024 ),
 ( #25636, #6811 ),
 ( #25029, #49136 ) ),
 .UNSPECIFIED., .F., .F., .F. ) 
 B_SPLINE_SURFACE_WITH_KNOTS ( ( 4, 4 ),
 ( 2, 2 ),
 ( 0.000000000000000000, 1.000000000000000000 ),
 ( 0.000000000000000000, 1.000000000000000000 ),
 .UNSPECIFIED. ) 
 GEOMETRIC_REPRESENTATION_ITEM ( )  RATIONAL_B_SPLINE_SURFACE ( (
 ( 1.000000000000000000, 1.000000000000000000),
 ( 0.9732289882329797637, 0.9999525324661233672),
 ( 0.9732289882329797637, 0.9999525324661233672),
 ( 1.000000000000000000, 1.000000000000000000) ) ) 
 REPRESENTATION_ITEM ( '' )  SURFACE ( )  );
#28451=VECTOR ( 'NONE', #46322, 1000.000000000000227 ) ;
#28452=ORIENTED_EDGE ( 'NONE', *, *, #16102, .F. ) ;
#28453=ORIENTED_EDGE ( 'NONE', *, *, #29300, .T. ) ;
#28455=CARTESIAN_POINT ( 'NONE',  ( 5.960721111146673579, -20.34914600876577140, 2.685391721745692628 ) ) ;
#28459=CARTESIAN_POINT ( 'NONE',  ( 0.9757787079277446818, 0.03949005143961138026, -42.90844198810273014 ) ) ;
#28465=CARTESIAN_POINT ( 'NONE',  ( 5.860006189529234355, 45.67886430272030651, 15.48781697582063366 ) ) ;
#28471=VERTEX_POINT ( 'NONE', #27191 ) ;
#28472=ORIENTED_EDGE ( 'NONE', *, *, #59404, .F. ) ;
#28477=CARTESIAN_POINT ( 'NONE',  ( 0.9756008150404614776, -21.33101788548756161, 37.23069985082535993 ) ) ;
#28483=CARTESIAN_POINT ( 'NONE',  ( 5.959547316686252039, 17.77749189599217416, -10.25972575517511487 ) ) ;
#28499=EDGE_CURVE ( 'NONE', #5464, #61588, #16561, .T. ) ;
#28503=CARTESIAN_POINT ( 'NONE',  ( 4.960156602257184133, -26.21519897043405223, -38.31207700265980520 ) ) ;
#28504=AXIS2_PLACEMENT_3D ( 'NONE', #11942, #12240, #27246 ) ;
#28505=CARTESIAN_POINT ( 'NONE',  ( 0.9730545539215883499, -33.73144377768576874, 26.52009130076758225 ) ) ;
#28506=ORIENTED_EDGE ( 'NONE', *, *, #51058, .F. ) ;
#28511=VERTEX_POINT ( 'NONE', #45396 ) ;
#28512=CARTESIAN_POINT ( 'NONE',  ( 0.5839879882012694035, -6.251708210201749161, -47.48620708510745914 ) ) ;
#28520=CARTESIAN_POINT ( 'NONE',  ( 4.967162193818129623, -13.42934394584134949, -40.93989340068622340 ) ) ;
#28525=CARTESIAN_POINT ( 'NONE',  ( 5.960721111146673579, -7.848955554238384202, -18.96557324978284242 ) ) ;
#28534=CARTESIAN_POINT ( 'NONE',  ( 0.9730545539215883499, 30.69604515769650632, 29.98130006528872826 ) ) ;
#28535=EDGE_LOOP ( 'NONE', ( #6989, #40651, #3311, #30733 ) ) ;
#28542=CARTESIAN_POINT ( 'NONE',  ( 0.9972139404380298000, 41.61281131482461859, 10.46878911444690452 ) ) ;
#28543=ADVANCED_FACE ( 'NONE', ( #2441 ), #11825, .F. ) ;
#28549=B_SPLINE_CURVE_WITH_KNOTS ( 'NONE', 3,
 ( #42996, #28551, #47672, #29478, #13868, #5646 ),
 .UNSPECIFIED., .F., .F.,
 ( 4, 2, 4 ),
 ( 1.499559393730840704E-16, 0.0002445252820015210871, 0.0004890505640028922291 ),
 .UNSPECIFIED. ) ;
#28551=CARTESIAN_POINT ( 'NONE',  ( 0.7762777257811892540, 46.49451973287617790, -11.53708189756892466 ) ) ;
#28558=DIRECTION ( 'NONE',  ( 0.07439287786467665975, -0.3693942911085648095, -0.9262902123089783446 ) ) ;
#28564=CARTESIAN_POINT ( 'NONE',  ( 5.959547316686252039, -7.851524054666280783, -18.96456592444097922 ) ) ;
#28571=DIRECTION ( 'NONE',  ( -0.07439287786467650709, -0.1170659376278904151, 0.9903339163990669824 ) ) ;
#28572=LINE ( 'NONE', #19204, #24732 ) ;
#28579=EDGE_LOOP ( 'NONE', ( #54206, #26009, #42268, #26193 ) ) ;
#28584=CARTESIAN_POINT ( 'NONE',  ( 3.270143674763207553, -9.870732238228589139, 9.482922169187926187 ) ) ;
#28596=CARTESIAN_POINT ( 'NONE',  ( 0.9757787079277435716, -34.01751575780804870, -26.15233402543304919 ) ) ;
#28599=CARTESIAN_POINT ( 'NONE',  ( 0.5807400328401574052, -44.45848844984454473, 17.82553128098393103 ) ) ;
#28600=CONICAL_SURFACE ( 'NONE', #24593, 43.08621763946400307, 1.568696531533066763 ) ;
#28601=VERTEX_POINT ( 'NONE', #5126 ) ;
#28604=CARTESIAN_POINT ( 'NONE',  ( 0.9745511491811756910, -0.3405614984923568400, 42.90705396078542577 ) ) ;
#28605=CARTESIAN_POINT ( 'NONE',  ( 4.967162193818129623, 32.68434214048168940, 28.07411493385305334 ) ) ;
#28606=AXIS2_PLACEMENT_3D ( 'NONE', #29955, #29641, #6116 ) ;
#28613=CARTESIAN_POINT ( 'NONE',  ( 4.963659409799330291, -9.199077662858595517, -43.79875484948457398 ) ) ;
#28617=ORIENTED_EDGE ( 'NONE', *, *, #34521, .T. ) ;
#28619=ADVANCED_FACE ( 'NONE', ( #43393 ), #31759, .F. ) ;
#28620=CARTESIAN_POINT ( 'NONE',  ( 0.5807400328401574052, 23.47602859900714733, 41.75144119563893952 ) ) ;
#28624=CARTESIAN_POINT ( 'NONE',  ( 0.9730545539215883499, -42.47233286818622133, 6.101350888304490461 ) ) ;
#28626=CARTESIAN_POINT ( 'NONE',  ( 4.963659409799330291, 8.262218268420474132, 43.98510776953411749 ) ) ;
#28629=FACE_OUTER_BOUND ( 'NONE', #42962, .T. ) ;
#28635=EDGE_CURVE ( 'NONE', #37784, #15622, #10569, .T. ) ;
#28636=CARTESIAN_POINT ( 'NONE',  ( 0.5786265663353153954, 23.32245830379087081, -41.83999636203295580 ) ) ;
#28639=CARTESIAN_POINT ( 'NONE',  ( 4.967162193818130511, 24.30453456948110613, 35.57684288741985768 ) ) ;
#28651=ORIENTED_EDGE ( 'NONE', *, *, #40419, .F. ) ;
#28655=CARTESIAN_POINT ( 'NONE',  ( 4.967162193818130511, -32.10009971360091896, 28.74031574030002645 ) ) ;
#28658=CARTESIAN_POINT ( 'NONE',  ( 0.8551540677456834771, 11.51835730326545004, -46.51172240253108470 ) ) ;
#28659=ORIENTED_EDGE ( 'NONE', *, *, #50141, .F. ) ;
#28663=ORIENTED_EDGE ( 'NONE', *, *, #38983, .F. ) ;
#28667=CARTESIAN_POINT ( 'NONE',  ( 4.960156602257181468, -45.42786611289307075, -9.558288641082238968 ) ) ;
#28674=ADVANCED_FACE ( 'NONE', ( #18530 ), #14916, .T. ) ;
#28675=B_SPLINE_CURVE_WITH_KNOTS ( 'NONE', 3,
 ( #27482, #60670, #51903, #60069 ),
 .UNSPECIFIED., .F., .F.,
 ( 4, 4 ),
 ( 0.000000000000000000, 0.005004741218457404994 ),
 .UNSPECIFIED. ) ;
#28676=CARTESIAN_POINT ( 'NONE',  ( 0.5819845901640493535, 38.27312528999471652, -28.79568196372230204 ) ) ;
#28681=CARTESIAN_POINT ( 'NONE',  ( 1.227938101723756947, -37.58536632582764980, -20.72293514920789903 ) ) ;
#28687=CARTESIAN_POINT ( 'NONE',  ( 0.8551540677456715978, -17.49081417858818455, 44.61036085020945308 ) ) ;
#28691=VERTEX_POINT ( 'NONE', #8817 ) ;
#28698=ORIENTED_EDGE ( 'NONE', *, *, #56199, .F. ) ;
#28701=AXIS2_PLACEMENT_3D ( 'NONE', #29, #14470, #10069 ) ;
#28703=CARTESIAN_POINT ( 'NONE',  ( 0.9756950546413942771, 26.04419981250937610, -34.10037081504532352 ) ) ;
#28704=ORIENTED_EDGE ( 'NONE', *, *, #17684, .T. ) ;
#28706=CARTESIAN_POINT ( 'NONE',  ( 0.5838002273316436064, -18.20308624554797916, -44.30203797796956877 ) ) ;
#28707=DIRECTION ( 'NONE',  ( 0.000000000000000000, 0.000000000000000000, 1.000000000000000000 ) ) ;
#28709=CARTESIAN_POINT ( 'NONE',  ( 0.9730545539215883499, -36.90443313492345823, 21.89037132892422832 ) ) ;
#28710=B_SPLINE_CURVE_WITH_KNOTS ( 'NONE', 3,
 ( #42680, #18553, #56131, #37681, #37064, #52355, #51121, #51425, #46457, #61431, #61741, #13869, #32976, #27639, #22951, #9447 ),
 .UNSPECIFIED., .F., .F.,
 ( 4, 3, 3, 3, 3, 4 ),
 ( 1.040890552917501732E-17, 0.0002724568934985535954, 0.0004086836638483777617, 0.0005449104342063600072, 0.0008173270854453693838, 0.001089761613562689659 ),
 .UNSPECIFIED. ) ;
#28717=ORIENTED_EDGE ( 'NONE', *, *, #15938, .T. ) ;
#28718=B_SPLINE_CURVE_WITH_KNOTS ( 'NONE', 3,
 ( #35061, #54116, #26876, #12482, #16876, #7433 ),
 .UNSPECIFIED., .F., .F.,
 ( 4, 2, 4 ),
 ( 6.149443329761888550E-18, 0.0002445244328975374566, 0.0004890488657950688416 ),
 .UNSPECIFIED. ) ;
#28722=CARTESIAN_POINT ( 'NONE',  ( 0.6067099128993260759, 18.98236771638461562, 43.97493306231469745 ) ) ;
#28726=VECTOR ( 'NONE', #53440, 1000.000000000000114 ) ;
#28727=CARTESIAN_POINT ( 'NONE',  ( 0.5819845079324655890, -47.89381220525412175, 0.4540594263151432886 ) ) ;
#28732=DIRECTION ( 'NONE',  ( 0.07836865515943411409, -0.7860872967108184506, -0.6131273243286252672 ) ) ;
#28736=FACE_OUTER_BOUND ( 'NONE', #61478, .T. ) ;
#28739=DIRECTION ( 'NONE',  ( -1.000000000000000000, -0.000000000000000000, -0.000000000000000000 ) ) ;
#28742=VECTOR ( 'NONE', #53847, 1000.000000000000114 ) ;
#28759=CARTESIAN_POINT ( 'NONE',  ( 0.8557997880470690211, -24.73961900479222820, -41.02602466100805145 ) ) ;
#28763=ORIENTED_EDGE ( 'NONE', *, *, #53666, .T. ) ;
#28770=CARTESIAN_POINT ( 'NONE',  ( 0.5786265663353196143, 47.58023467411546648, -5.535668456753460198 ) ) ;
#28771=CARTESIAN_POINT ( 'NONE',  ( 0.9756950546413930558, 34.10037081504560064, 26.04419981250898886 ) ) ;
#28772=ORIENTED_EDGE ( 'NONE', *, *, #10926, .T. ) ;
#28773=CARTESIAN_POINT ( 'NONE',  ( 0.5809828226811617480, -46.11980934799329646, -12.92184523170252497 ) ) ;
#28774=CARTESIAN_POINT ( 'NONE',  ( 0.9730545539215883499, 10.61654491617622398, -41.57420493492374192 ) ) ;
#28775=EDGE_CURVE ( 'NONE', #17561, #42072, #14459, .T. ) ;
#28776=CARTESIAN_POINT ( 'NONE',  ( 0.6846871229502899947, -38.52803883689281150, -28.47437962186167582 ) ) ;
#28778=EDGE_CURVE ( 'NONE', #42119, #10980, #58349, .T. ) ;
#28786=EDGE_CURVE ( 'NONE', #22536, #55130, #5322, .T. ) ;
#28789=CIRCLE ( 'NONE', #60646, 12.50000000000000000 ) ;
#28794=CARTESIAN_POINT ( 'NONE',  ( 0.9745511491811764682, -21.74846188963803684, 36.98831798234368762 ) ) ;
#28800=CARTESIAN_POINT ( 'NONE',  ( 5.958863334805807099, 17.77634700750928687, -10.26176968287926528 ) ) ;
#28808=VERTEX_POINT ( 'NONE', #59502 ) ;
#28823=ORIENTED_EDGE ( 'NONE', *, *, #54028, .T. ) ;
#28824=CARTESIAN_POINT ( 'NONE',  ( 4.967162193818130511, -28.07411493385273715, -32.68434214048198072 ) ) ;
#28827=CARTESIAN_POINT ( 'NONE',  ( 0.7057020205114981071, -17.55108080125414460, -44.57024707370732841 ) ) ;
#28829=CARTESIAN_POINT ( 'NONE',  ( 4.967162193818130511, 0.000000000000000000, 0.000000000000000000 ) ) ;
#28833=CARTESIAN_POINT ( 'NONE',  ( 4.963659409799331179, -20.22157859941701830, -39.92545197189572548 ) ) ;
#28837=CARTESIAN_POINT ( 'NONE',  ( 3.407937589446174087, -0.4592810312472936363, 13.69123696618924235 ) ) ;
#28839=EDGE_LOOP ( 'NONE', ( #47508, #60966, #61401, #27982 ) ) ;
#28842=CARTESIAN_POINT ( 'NONE',  ( 0.8551540677456739292, -7.157691013574685179, 47.37911285756618440 ) ) ;
#28845=CARTESIAN_POINT ( 'NONE',  ( 0.5839880159502346402, -33.83547574026603399, -33.89965136132180845 ) ) ;
#28849=ORIENTED_EDGE ( 'NONE', *, *, #57668, .T. ) ;
#28852=CARTESIAN_POINT ( 'NONE',  ( 5.960721111146673579, 0.006321279846820317821, -20.52557019979492026 ) ) ;
#28863=CARTESIAN_POINT ( 'NONE',  ( 0.5827359174754822568, -44.10985444762171426, -18.66406616558025888 ) ) ;
#28864=CARTESIAN_POINT ( 'NONE',  ( 0.5850706913938533704, 38.10903744847180974, -29.01314519953759685 ) ) ;
#28872=CARTESIAN_POINT ( 'NONE',  ( 0.9757787079277441267, 30.36877398309943388, -30.31292661677461098 ) ) ;
#28887=CARTESIAN_POINT ( 'NONE',  ( 0.9756354156337447847, 5.471460801653407202, 42.55820231551292920 ) ) ;
#28888=CARTESIAN_POINT ( 'NONE',  ( 5.959828726073459926, -16.28681682518072549, 12.49160845136007580 ) ) ;
#28890=ORIENTED_EDGE ( 'NONE', *, *, #52462, .T. ) ;
#28910=EDGE_CURVE ( 'NONE', #24624, #45383, #41992, .T. ) ;
#28911=ORIENTED_EDGE ( 'NONE', *, *, #17167, .F. ) ;
#28916=CARTESIAN_POINT ( 'NONE',  ( 2.281448460670567613, 34.83871297539704415, 32.98023336626246049 ) ) ;
#28917=CARTESIAN_POINT ( 'NONE',  ( 3.270143674763207553, 8.548517033725413938, -10.69018354892878264 ) ) ;
#28918=CARTESIAN_POINT ( 'NONE',  ( 0.5850706913938534814, -38.10903744847121288, -29.01314519953837845 ) ) ;
#28923=CARTESIAN_POINT ( 'NONE',  ( 3.270143674763207553, 8.113405361969672214, -11.02405647745161410 ) ) ;
#28932=VERTEX_POINT ( 'NONE', #53574 ) ;
#28936=CARTESIAN_POINT ( 'NONE',  ( 4.956653778116999476, 43.37017594958085454, -20.77844580450516077 ) ) ;
#28937=B_SPLINE_CURVE_WITH_KNOTS ( 'NONE', 3,
 ( #25321, #49744, #11546, #35055, #15020, #20631 ),
 .UNSPECIFIED., .F., .F.,
 ( 4, 2, 4 ),
 ( 5.275955480050202716E-18, 0.0002445244328975366434, 0.0004890488657950680827 ),
 .UNSPECIFIED. ) ;
#28957=LINE ( 'NONE', #51590, #15632 ) ;
#28961=CARTESIAN_POINT ( 'NONE',  ( 0.9757402383260965761, -11.18751708556339253, 41.42435672089863630 ) ) ;
#28966=ORIENTED_EDGE ( 'NONE', *, *, #7899, .T. ) ;
#28973=CARTESIAN_POINT ( 'NONE',  ( 4.967162193818130511, 40.65506779172185503, -14.26841313271238221 ) ) ;
#28975=CARTESIAN_POINT ( 'NONE',  ( 0.8557997880470697982, 24.73961900479251952, 41.02602466100786671 ) ) ;
#28977=ORIENTED_EDGE ( 'NONE', *, *, #60740, .T. ) ;
#28979=EDGE_CURVE ( 'NONE', #4433, #51079, #57969, .T. ) ;
#28981=CARTESIAN_POINT ( 'NONE',  ( 4.967162193818130511, 0.000000000000000000, 0.000000000000000000 ) ) ;
#28983=ADVANCED_FACE ( 'NONE', ( #20103 ), #1351, .F. ) ;
#28987=CARTESIAN_POINT ( 'NONE',  ( 0.9754402186311934564, 42.56545569314712907, 5.414674803233914702 ) ) ;
#28989=EDGE_CURVE ( 'NONE', #54909, #7563, #22504, .T. ) ;
#29000=ORIENTED_EDGE ( 'NONE', *, *, #43914, .T. ) ;
#29002=CARTESIAN_POINT ( 'NONE',  ( 0.9745511491811751359, -42.49552597049454761, -5.938142320543777330 ) ) ;
#29005=CARTESIAN_POINT ( 'NONE',  ( 0.5839880159502331969, 29.12121614504463096, 38.02605095487687947 ) ) ;
#29011=EDGE_CURVE ( 'NONE', #19785, #57948, #19795, .T. ) ;
#29016=B_SPLINE_CURVE_WITH_KNOTS ( 'NONE', 3,
 ( #58249, #58876, #25069, #44213 ),
 .UNSPECIFIED., .F., .F.,
 ( 4, 4 ),
 ( 7.919159918457849946E-17, 0.005004741218457501271 ),
 .UNSPECIFIED. ) ;
#29019=ADVANCED_FACE ( 'NONE', ( #38296 ), #44579, .F. ) ;
#29025=CARTESIAN_POINT ( 'NONE',  ( 0.9749527285493297946, 39.75066842359309760, -16.15611883305602703 ) ) ;
#29029=ORIENTED_EDGE ( 'NONE', *, *, #22923, .T. ) ;
#29033=CARTESIAN_POINT ( 'NONE',  ( 5.960721111146673579, 2.685391721745764571, 20.34914600876576074 ) ) ;
#29034=ADVANCED_FACE ( 'NONE', ( #35987 ), #26993, .F. ) ;
#29049=FACE_OUTER_BOUND ( 'NONE', #20629, .T. ) ;
#29057=B_SPLINE_CURVE_WITH_KNOTS ( 'NONE', 3,
 ( #42148, #61205, #32726, #22387 ),
 .UNSPECIFIED., .F., .F.,
 ( 4, 4 ),
 ( 1.734723475976807094E-17, 0.005004741218457424944 ),
 .UNSPECIFIED. ) ;
#29058=ADVANCED_FACE ( 'NONE', ( #18095 ), #31016, .F. ) ;
#29059=FACE_OUTER_BOUND ( 'NONE', #58003, .T. ) ;
#29060=DIRECTION ( 'NONE',  ( -1.000000000000000000, -0.000000000000000000, -0.000000000000000000 ) ) ;
#29063=CARTESIAN_POINT ( 'NONE',  ( 0.9730545539215883499, -5.099196237955184507, 42.60426903087352457 ) ) ;
#29064=ORIENTED_EDGE ( 'NONE', *, *, #35946, .T. ) ;
#29071=EDGE_CURVE ( 'NONE', #929, #23349, #40502, .T. ) ;
#29073=CARTESIAN_POINT ( 'NONE',  ( 4.956653778116970166, 43.37017594958054900, 20.77844580450576117 ) ) ;
#29077=VERTEX_POINT ( 'NONE', #14028 ) ;
#29079=EDGE_CURVE ( 'NONE', #44331, #27918, #3070, .T. ) ;
#29081=ORIENTED_EDGE ( 'NONE', *, *, #20097, .F. ) ;
#29085=CARTESIAN_POINT ( 'NONE',  ( 0.7762777257811889209, -46.03397617421218513, -13.25585385760155432 ) ) ;
#29086=DIRECTION ( 'NONE',  ( -1.000000000000000000, 0.000000000000000000, 0.000000000000000000 ) ) ;
#29094=DIRECTION ( 'NONE',  ( -1.000000000000000000, -0.000000000000000000, -0.000000000000000000 ) ) ;
#29095=CARTESIAN_POINT ( 'NONE',  ( 5.960221823109900008, 12.49086489703227798, -16.28736530777577585 ) ) ;
#29114=CARTESIAN_POINT ( 'NONE',  ( 5.960721111146673579, 20.52557019979492026, -0.006321279846608376246 ) ) ;
#29115=( BOUNDED_SURFACE ( )  B_SPLINE_SURFACE ( 3, 1, ( 
 ( #20458, #53629 ),
 ( #45219, #24851 ),
 ( #6316, #19857 ),
 ( #38971, #53335 ) ),
 .UNSPECIFIED., .F., .F., .F. ) 
 B_SPLINE_SURFACE_WITH_KNOTS ( ( 4, 4 ),
 ( 2, 2 ),
 ( 0.000000000000000000, 1.000000000000000000 ),
 ( 0.000000000000000000, 1.000000000000000000 ),
 .UNSPECIFIED. ) 
 GEOMETRIC_REPRESENTATION_ITEM ( )  RATIONAL_B_SPLINE_SURFACE ( (
 ( 1.000000000000000000, 1.000000000000000000),
 ( 0.7269869731126821222, 0.9931720237060910339),
 ( 0.7269869731126821222, 0.9931720237060910339),
 ( 1.000000000000000000, 1.000000000000000000) ) ) 
 REPRESENTATION_ITEM ( '' )  SURFACE ( )  );
#29122=CARTESIAN_POINT ( 'NONE',  ( 1.227938101723756947, -36.73927144310528092, 22.18841447410706635 ) ) ;
#29130=ORIENTED_EDGE ( 'NONE', *, *, #58378, .F. ) ;
#29133=CARTESIAN_POINT ( 'NONE',  ( 5.959547316686252039, -2.675599016784394379, -20.35048796920736081 ) ) ;
#29144=ORIENTED_EDGE ( 'NONE', *, *, #40664, .T. ) ;
#29146=CARTESIAN_POINT ( 'NONE',  ( 5.959547316686252039, 5.315863417546330183, -19.82530672674356964 ) ) ;
#29150=CARTESIAN_POINT ( 'NONE',  ( 0.9754642270333679921, -16.25787253057904991, -39.70914670678651959 ) ) ;
#29152=CARTESIAN_POINT ( 'NONE',  ( 1.154321485836934169, 36.74718014677598887, -22.16897757994436802 ) ) ;
#29154=VERTEX_POINT ( 'NONE', #18713 ) ;
#29178=CARTESIAN_POINT ( 'NONE',  ( 0.6067375320500697500, 38.42671567536892496, -28.59217831626977357 ) ) ;
#29180=CARTESIAN_POINT ( 'NONE',  ( 0.9752570700956796346, 30.50353876750672910, -30.17732761204907277 ) ) ;
#29193=ORIENTED_EDGE ( 'NONE', *, *, #6835, .F. ) ;
#29199=CARTESIAN_POINT ( 'NONE',  ( 0.5807400328401637335, -12.92266817606048335, 46.12278621143492785 ) ) ;
#29205=ORIENTED_EDGE ( 'NONE', *, *, #10253, .F. ) ;
#29206=CARTESIAN_POINT ( 'NONE',  ( 0.9730545539215883499, 25.71816799638778406, 34.34678117142565412 ) ) ;
#29207=ORIENTED_EDGE ( 'NONE', *, *, #58830, .F. ) ;
#29209=CARTESIAN_POINT ( 'NONE',  ( 1.227938101723748288, 39.32113113558966688, 17.20315230597858047 ) ) ;
#29216=ORIENTED_EDGE ( 'NONE', *, *, #48457, .F. ) ;
#29217=ORIENTED_EDGE ( 'NONE', *, *, #22567, .T. ) ;
#29218=CARTESIAN_POINT ( 'NONE',  ( 3.270143674763207553, 13.53222904135357041, -2.058141141425458454 ) ) ;
#29219=CARTESIAN_POINT ( 'NONE',  ( 1.154321713695928286, -30.92445811446669168, 29.75729669971099156 ) ) ;
#29222=EDGE_CURVE ( 'NONE', #8039, #3160, #15084, .T. ) ;
#29233=CARTESIAN_POINT ( 'NONE',  ( 4.967162193818130511, 0.000000000000000000, 0.000000000000000000 ) ) ;
#29234=CARTESIAN_POINT ( 'NONE',  ( -17.97369999999976642, -12.32233744059949210, 2.099999999999994760 ) ) ;
#29235=ORIENTED_EDGE ( 'NONE', *, *, #14476, .F. ) ;
#29242=CARTESIAN_POINT ( 'NONE',  ( 3.783198216974390515, 35.16829104054202304, -24.80909581868404956 ) ) ;
#29243=CARTESIAN_POINT ( 'NONE',  ( 0.5809828226811617480, 47.55412398569215071, -5.711058609464832792 ) ) ;
#29245=ADVANCED_FACE ( 'NONE', ( #39376 ), #57329, .F. ) ;
#29250=DIRECTION ( 'NONE',  ( 0.000000000000000000, 0.000000000000000000, 1.000000000000000000 ) ) ;
#29251=DIRECTION ( 'NONE',  ( 0.000000000000000000, 0.000000000000000000, 1.000000000000000000 ) ) ;
#29253=CARTESIAN_POINT ( 'NONE',  ( 1.227938101723748288, 36.73927144310511750, 22.18841447410732215 ) ) ;
#29258=CARTESIAN_POINT ( 'NONE',  ( 0.9730545539215883499, 6.101350888304637010, 42.47233286818619291 ) ) ;
#29277=EDGE_LOOP ( 'NONE', ( #31825, #44589, #721, #28911 ) ) ;
#29282=CARTESIAN_POINT ( 'NONE',  ( 0.9968887458511636046, -39.38692798189855182, -17.02616470386922032 ) ) ;
#29284=ADVANCED_FACE ( 'NONE', ( #34357 ), #56244, .F. ) ;
#29286=CARTESIAN_POINT ( 'NONE',  ( 1.088313998177382835, -10.35171213034662330, -41.64627086748864571 ) ) ;
#29290=CARTESIAN_POINT ( 'NONE',  ( 0.5838002273316426072, 38.08117724016846495, -29.04904228829574109 ) ) ;
#29296=CARTESIAN_POINT ( 'NONE',  ( 4.956653778116970166, 45.35992544608529187, 15.97476558431900884 ) ) ;
#29300=EDGE_CURVE ( 'NONE', #52413, #33451, #56102, .T. ) ;
#29307=CARTESIAN_POINT ( 'NONE',  ( 0.5834872094924183905, 28.97678700412181740, 38.13619618345218498 ) ) ;
#29309=CARTESIAN_POINT ( 'NONE',  ( 0.5809828226811553087, 41.74875432577648837, 23.47450554821725532 ) ) ;
#29316=CARTESIAN_POINT ( 'NONE',  ( 0.9740398440564321803, 25.79088785829030428, -34.29238484271503040 ) ) ;
#29317=CARTESIAN_POINT ( 'NONE',  ( 0.7762783648524405056, -19.15108798908280718, -43.90991295203441780 ) ) ;
#29320=CARTESIAN_POINT ( 'NONE',  ( 2.281351352603299798, 46.66131639318016511, -11.14238889600236426 ) ) ;
#29322=ORIENTED_EDGE ( 'NONE', *, *, #16894, .F. ) ;
#29324=FACE_OUTER_BOUND ( 'NONE', #45905, .T. ) ;
#29325=CARTESIAN_POINT ( 'NONE',  ( 0.5800708057587411481, -24.48933404430286842, 41.16170989303191874 ) ) ;
#29328=CARTESIAN_POINT ( 'NONE',  ( -17.42928676736936922, -12.33362675552796084, 2.032827274293960151 ) ) ;
#29330=CARTESIAN_POINT ( 'NONE',  ( 2.281448460670567613, -11.14236343022405151, 46.66132715497960248 ) ) ;
#29332=VECTOR ( 'NONE', #48866, 1000.000000000000114 ) ;
#29352=CARTESIAN_POINT ( 'NONE',  ( 4.956653778116982600, -43.37017594958069111, 20.77844580450546985 ) ) ;
#29353=ADVANCED_FACE ( 'NONE', ( #45307 ), #15467, .F. ) ;
#29354=CARTESIAN_POINT ( 'NONE',  ( -19.96574584685826537, -7.972179581716115848, 0.6786367118085059325 ) ) ;
#29356=EDGE_CURVE ( 'NONE', #22114, #4359, #60284, .T. ) ;
#29358=CARTESIAN_POINT ( 'NONE',  ( 0.9972139404380291339, -30.80335716430295889, -29.87264297738558483 ) ) ;
#29359=EDGE_CURVE ( 'NONE', #31306, #39564, #37499, .T. ) ;
#29360=CARTESIAN_POINT ( 'NONE',  ( 0.5839879327111934249, 47.47435452316582172, -6.341736898931451982 ) ) ;
#29361=( BOUNDED_SURFACE ( )  B_SPLINE_SURFACE ( 3, 1, ( 
 ( #59528, #17565 ),
 ( #36681, #16636 ),
 ( #12876, #60756 ),
 ( #17877, #37000 ) ),
 .UNSPECIFIED., .F., .F., .F. ) 
 B_SPLINE_SURFACE_WITH_KNOTS ( ( 4, 4 ),
 ( 2, 2 ),
 ( 0.000000000000000000, 1.000000000000000000 ),
 ( 0.000000000000000000, 1.000000000000000000 ),
 .UNSPECIFIED. ) 
 GEOMETRIC_REPRESENTATION_ITEM ( )  RATIONAL_B_SPLINE_SURFACE ( (
 ( 1.000000000000000000, 1.000000000000000000),
 ( 0.9953390228620291325, 0.8624445117761032620),
 ( 0.9953390228620291325, 0.8624445117761032620),
 ( 1.000000000000000000, 1.000000000000000000) ) ) 
 REPRESENTATION_ITEM ( '' )  SURFACE ( )  );
#29364=EDGE_LOOP ( 'NONE', ( #40557, #34676, #13601, #39100 ) ) ;
#29369=CARTESIAN_POINT ( 'NONE',  ( 0.7056555295713305975, -24.67549844185508334, -41.05687446835462850 ) ) ;
#29374=VECTOR ( 'NONE', #48564, 1000.000000000000227 ) ;
#29377=CARTESIAN_POINT ( 'NONE',  ( 5.860006189529234355, -36.27483683749414922, -31.78942168514599942 ) ) ;
#29382=VERTEX_POINT ( 'NONE', #52433 ) ;
#29383=ORIENTED_EDGE ( 'NONE', *, *, #2144, .T. ) ;
#29386=CARTESIAN_POINT ( 'NONE',  ( 2.526552050251862358, -41.81191169914602312, 9.948123361606700854 ) ) ;
#29387=ORIENTED_EDGE ( 'NONE', *, *, #50841, .F. ) ;
#29388=CARTESIAN_POINT ( 'NONE',  ( 4.956653778116975495, -8.845409907521238679, 47.27023054223749909 ) ) ;
#29390=CARTESIAN_POINT ( 'NONE',  ( 0.8551540677456715978, -38.56334384152412298, -28.44084013485158025 ) ) ;
#29405=AXIS2_PLACEMENT_3D ( 'NONE', #18026, #50285, #7349 ) ;
#29411=CARTESIAN_POINT ( 'NONE',  ( 0.8557997880470690211, 43.90420959842208504, -19.17299735371961944 ) ) ;
#29425=CARTESIAN_POINT ( 'NONE',  ( 0.5819845901640494645, 18.74765780149888172, -44.07435474487826355 ) ) ;
#29427=CARTESIAN_POINT ( 'NONE',  ( 4.963659409799330291, 39.92545197189578232, -20.22157859941687263 ) ) ;
#29429=CARTESIAN_POINT ( 'NONE',  ( 0.9741495583595167762, -37.35596046161881389, 21.11077839432123326 ) ) ;
#29434=CARTESIAN_POINT ( 'NONE',  ( 0.7762777257811890319, 23.17763256463769395, 41.92424087089318618 ) ) ;
#29445=ORIENTED_EDGE ( 'NONE', *, *, #54814, .F. ) ;
#29448=ADVANCED_FACE ( 'NONE', ( #27723 ), #992, .F. ) ;
#29454=CARTESIAN_POINT ( 'NONE',  ( 0.5827359174754809246, 34.12345922495658357, -33.60976280407613359 ) ) ;
#29457=ORIENTED_EDGE ( 'NONE', *, *, #56632, .T. ) ;
#29461=AXIS2_PLACEMENT_3D ( 'NONE', #20175, #34578, #730 ) ;
#29463=CARTESIAN_POINT ( 'NONE',  ( 0.5807400328401637335, -18.83234461715215247, 44.04145271122558825 ) ) ;
#29464=VERTEX_POINT ( 'NONE', #111 ) ;
#29468=CARTESIAN_POINT ( 'NONE',  ( 1.227938101723747621, 22.18841447410770940, -36.73927144310489012 ) ) ;
#29474=DIRECTION ( 'NONE',  ( -1.000000000000000000, -0.000000000000000000, -0.000000000000000000 ) ) ;
#29478=CARTESIAN_POINT ( 'NONE',  ( 0.6067375320500736358, 46.44340905096879624, -11.71046088714702904 ) ) ;
#29484=EDGE_CURVE ( 'NONE', #147, #52535, #4193, .T. ) ;
#29486=CARTESIAN_POINT ( 'NONE',  ( 0.8551540677456715978, -47.37911285756625546, 7.157691013574198458 ) ) ;
#29488=CARTESIAN_POINT ( 'NONE',  ( 0.9745511491811736926, 30.58068216140377871, -30.09905547141324433 ) ) ;
#29491=CARTESIAN_POINT ( 'NONE',  ( 5.960721111146673579, 12.50019045452716426, 16.28018152803696950 ) ) ;
#29494=CARTESIAN_POINT ( 'NONE',  ( 0.5834872094924170582, 33.70665904794288537, 34.02770606800772413 ) ) ;
#29509=ORIENTED_EDGE ( 'NONE', *, *, #30816, .T. ) ;
#29510=CARTESIAN_POINT ( 'NONE',  ( 0.5807400328401637335, 28.72484455891639854, 38.33001520688960539 ) ) ;
#29528=FACE_OUTER_BOUND ( 'NONE', #32086, .T. ) ;
#29532=( BOUNDED_SURFACE ( )  B_SPLINE_SURFACE ( 3, 1, ( 
 ( #41451, #61126 ),
 ( #22321, #42074 ),
 ( #51416, #4105 ),
 ( #60506, #3807 ) ),
 .UNSPECIFIED., .F., .F., .F. ) 
 B_SPLINE_SURFACE_WITH_KNOTS ( ( 4, 4 ),
 ( 2, 2 ),
 ( 0.000000000000000000, 1.000000000000000000 ),
 ( 0.000000000000000000, 1.000000000000000000 ),
 .UNSPECIFIED. ) 
 GEOMETRIC_REPRESENTATION_ITEM ( )  RATIONAL_B_SPLINE_SURFACE ( (
 ( 1.000000000000000000, 1.000000000000000000),
 ( 0.7269869731126817891, 0.9931720237060910339),
 ( 0.7269869731126817891, 0.9931720237060910339),
 ( 1.000000000000000000, 1.000000000000000000) ) ) 
 REPRESENTATION_ITEM ( '' )  SURFACE ( )  );
#29537=CARTESIAN_POINT ( 'NONE',  ( 5.960221823109900008, -17.77840967225713698, -10.25807604135615136 ) ) ;
#29540=AXIS2_PLACEMENT_3D ( 'NONE', #5229, #43811, #43490 ) ;
#29543=ORIENTED_EDGE ( 'NONE', *, *, #13123, .F. ) ;
#29545=LINE ( 'NONE', #15159, #54653 ) ;
#29550=EDGE_CURVE ( 'NONE', #1001, #30413, #894, .T. ) ;
#29551=( BOUNDED_SURFACE ( )  B_SPLINE_SURFACE ( 3, 1, ( 
 ( #28564, #47686 ),
 ( #32986, #18261 ),
 ( #4730, #17957 ),
 ( #52060, #13255 ) ),
 .UNSPECIFIED., .F., .F., .F. ) 
 B_SPLINE_SURFACE_WITH_KNOTS ( ( 4, 4 ),
 ( 2, 2 ),
 ( 0.000000000000000000, 1.000000000000000000 ),
 ( 0.000000000000000000, 1.000000000000000000 ),
 .UNSPECIFIED. ) 
 GEOMETRIC_REPRESENTATION_ITEM ( )  RATIONAL_B_SPLINE_SURFACE ( (
 ( 1.000000000000000000, 1.000000000000000000),
 ( 0.9732289882329797637, 0.9999525324661233672),
 ( 0.9732289882329797637, 0.9999525324661233672),
 ( 1.000000000000000000, 1.000000000000000000) ) ) 
 REPRESENTATION_ITEM ( '' )  SURFACE ( )  );
#29552=FACE_OUTER_BOUND ( 'NONE', #2302, .T. ) ;
#29553=CARTESIAN_POINT ( 'NONE',  ( 3.407937589446178528, -11.62731850632889241, 7.243367523630984017 ) ) ;
#29555=EDGE_CURVE ( 'NONE', #19642, #20940, #35278, .T. ) ;
#29568=CARTESIAN_POINT ( 'NONE',  ( 0.9745511491811738036, -26.39034508612560259, 33.83313387735780964 ) ) ;
#29570=CARTESIAN_POINT ( 'NONE',  ( 5.960221823109900008, -16.28736530777582558, -12.49086489703221936 ) ) ;
#29573=CARTESIAN_POINT ( 'NONE',  ( 5.981074661064941900, -16.27808421740017764, -12.50143471347275614 ) ) ;
#29575=ORIENTED_EDGE ( 'NONE', *, *, #54148, .F. ) ;
#29580=EDGE_CURVE ( 'NONE', #57526, #37539, #1967, .T. ) ;
#29583=DIRECTION ( 'NONE',  ( -1.000000000000000000, -0.000000000000000000, -0.000000000000000000 ) ) ;
#29586=ORIENTED_EDGE ( 'NONE', *, *, #1687, .F. ) ;
#29588=FACE_OUTER_BOUND ( 'NONE', #14447, .T. ) ;
#29596=EDGE_LOOP ( 'NONE', ( #801, #44766 ) ) ;
#29601=ORIENTED_EDGE ( 'NONE', *, *, #31336, .F. ) ;
#29604=CARTESIAN_POINT ( 'NONE',  ( 4.956653778116992370, 31.29546495791903027, -36.51451553856384180 ) ) ;
#29608=CARTESIAN_POINT ( 'NONE',  ( 0.9757892942422806692, -42.54806590760156126, -5.549787678908827182 ) ) ;
#29609=CARTESIAN_POINT ( 'NONE',  ( 0.5807400328401574052, -6.791881299635910807, 47.41494605191441281 ) ) ;
#29610=CARTESIAN_POINT ( 'NONE',  ( 0.8551540677456834771, 41.03346287276463045, -24.74404575822732255 ) ) ;
#29613=CARTESIAN_POINT ( 'NONE',  ( 0.8551540677456715978, 46.51172240253137602, -11.51835730326430962 ) ) ;
#29616=B_SPLINE_CURVE_WITH_KNOTS ( 'NONE', 3,
 ( #32864, #61027, #60707, #7468 ),
 .UNSPECIFIED., .F., .F.,
 ( 4, 4 ),
 ( 1.192622389734054877E-18, 0.004444878191957686922 ),
 .UNSPECIFIED. ) ;
#29623=DIRECTION ( 'NONE',  ( -1.000000000000000000, -0.000000000000000000, -0.000000000000000000 ) ) ;
#29625=CARTESIAN_POINT ( 'NONE',  ( 1.154321713695927398, 34.54400171733340130, -25.46626713715426149 ) ) ;
#29627=CARTESIAN_POINT ( 'NONE',  ( 0.9730545539215883499, 39.83279466599061891, -15.95224156741785393 ) ) ;
#29628=EDGE_CURVE ( 'NONE', #31436, #61473, #9074, .T. ) ;
#29632=CONICAL_SURFACE ( 'NONE', #51624, 43.08621763946400307, 1.568696531533066763 ) ;
#29638=CARTESIAN_POINT ( 'NONE',  ( 5.860006189529234355, -3.171667470662203669, -48.12869875779312423 ) ) ;
#29641=DIRECTION ( 'NONE',  ( -1.000000000000000000, -0.000000000000000000, -0.000000000000000000 ) ) ;
#29646=CARTESIAN_POINT ( 'NONE',  ( 0.9968887458511638267, 29.87314546208230226, 30.80284987750020775 ) ) ;
#29649=DIRECTION ( 'NONE',  ( 0.000000000000000000, 0.000000000000000000, 1.000000000000000000 ) ) ;
#29650=EDGE_LOOP ( 'NONE', ( #61230, #16932, #61772, #37820 ) ) ;
#29651=ORIENTED_EDGE ( 'NONE', *, *, #45996, .T. ) ;
#29652=CARTESIAN_POINT ( 'NONE',  ( 0.5832366564991512403, -12.13301812590381346, 46.33368520589910844 ) ) ;
#29667=ORIENTED_EDGE ( 'NONE', *, *, #44754, .F. ) ;
#29673=VERTEX_POINT ( 'NONE', #11708 ) ;
#29674=CONICAL_SURFACE ( 'NONE', #33733, 43.08621763946400307, 1.568696531533066763 ) ;
#29681=EDGE_CURVE ( 'NONE', #14441, #2552, #26711, .T. ) ;
#29690=CARTESIAN_POINT ( 'NONE',  ( 5.965394784446458765, 17.78272165951786832, 10.25014670152121177 ) ) ;
#29691=AXIS2_PLACEMENT_3D ( 'NONE', #20730, #35147, #54209 ) ;
#29693=ORIENTED_EDGE ( 'NONE', *, *, #47986, .T. ) ;
#29695=CARTESIAN_POINT ( 'NONE',  ( 0.5819845901640494645, -6.701564444318020897, 47.42480841519687118 ) ) ;
#29700=CARTESIAN_POINT ( 'NONE',  ( 1.227938101723748288, -42.91134962331486946, -0.8460948827229646252 ) ) ;
#29704=LINE ( 'NONE', #30321, #36842 ) ;
#29709=EDGE_CURVE ( 'NONE', #45591, #53833, #29926, .T. ) ;
#29713=FACE_OUTER_BOUND ( 'NONE', #7722, .T. ) ;
#29728=( BOUNDED_SURFACE ( )  B_SPLINE_SURFACE ( 3, 1, ( 
 ( #28852, #43288 ),
 ( #25080, #25386 ),
 ( #57957, #47975 ),
 ( #15081, #34497 ) ),
 .UNSPECIFIED., .F., .F., .F. ) 
 B_SPLINE_SURFACE_WITH_KNOTS ( ( 4, 4 ),
 ( 2, 2 ),
 ( 0.000000000000000000, 1.000000000000000000 ),
 ( 0.000000000000000000, 1.000000000000000000 ),
 .UNSPECIFIED. ) 
 GEOMETRIC_REPRESENTATION_ITEM ( )  RATIONAL_B_SPLINE_SURFACE ( (
 ( 1.000000000000000000, 1.000000000000000000),
 ( 0.9953390228620291325, 0.8624445117760984880),
 ( 0.9953390228620291325, 0.8624445117760984880),
 ( 1.000000000000000000, 1.000000000000000000) ) ) 
 REPRESENTATION_ITEM ( '' )  SURFACE ( )  );
#29746=VERTEX_POINT ( 'NONE', #26401 ) ;
#29768=VERTEX_POINT ( 'NONE', #35829 ) ;
#29769=EDGE_CURVE ( 'NONE', #30886, #18069, #35942, .T. ) ;
#29787=ORIENTED_EDGE ( 'NONE', *, *, #54100, .F. ) ;
#29792=CARTESIAN_POINT ( 'NONE',  ( 5.981074661064941900, -7.862380442164009331, -18.95903134304786519 ) ) ;
#29794=CARTESIAN_POINT ( 'NONE',  ( 0.5786265663353196143, 41.83999636203351713, -23.32245830378984408 ) ) ;
#29795=CARTESIAN_POINT ( 'NONE',  ( -15.87364305917332530, -8.000014946965743334, -0.1367906320862119773 ) ) ;
#29801=CARTESIAN_POINT ( 'NONE',  ( 3.270143674763207553, 2.058141141425593901, 13.53222904135354909 ) ) ;
#29803=B_SPLINE_CURVE_WITH_KNOTS ( 'NONE', 3,
 ( #18109, #36612, #37232, #9861 ),
 .UNSPECIFIED., .F., .F.,
 ( 4, 4 ),
 ( 0.000000000000000000, 0.004444878191956872469 ),
 .UNSPECIFIED. ) ;
#29804=DIRECTION ( 'NONE',  ( 0.000000000000000000, 0.000000000000000000, 1.000000000000000000 ) ) ;
#29806=ORIENTED_EDGE ( 'NONE', *, *, #10753, .T. ) ;
#29810=CARTESIAN_POINT ( 'NONE',  ( 1.227938101723748288, -34.55893248994524214, 25.45152231597044690 ) ) ;
#29817=ORIENTED_EDGE ( 'NONE', *, *, #32191, .F. ) ;
#29818=FACE_OUTER_BOUND ( 'NONE', #51174, .T. ) ;
#29819=VECTOR ( 'NONE', #54889, 1000.000000000000114 ) ;
#29821=VERTEX_POINT ( 'NONE', #19188 ) ;
#29828=EDGE_CURVE ( 'NONE', #9811, #53201, #37066, .T. ) ;
#29831=CARTESIAN_POINT ( 'NONE',  ( 1.227938101723757836, 39.96870412324336996, 15.63977281655856366 ) ) ;
#29834=ADVANCED_FACE ( 'NONE', ( #32981 ), #51856, .F. ) ;
#29839=CARTESIAN_POINT ( 'NONE',  ( 5.974727161628367256, -16.29297756969640076, -12.48248968439922990 ) ) ;
#29843=CARTESIAN_POINT ( 'NONE',  ( 0.6067375320500688618, -37.56348932307244581, -29.71715680108774293 ) ) ;
#29845=EDGE_CURVE ( 'NONE', #43658, #56839, #32156, .T. ) ;
#29848=CARTESIAN_POINT ( 'NONE',  ( 3.783278058412224976, 42.86118820526429829, 3.901118461246968927 ) ) ;
#29852=AXIS2_PLACEMENT_3D ( 'NONE', #15901, #48786, #11199 ) ;
#29859=CARTESIAN_POINT ( 'NONE',  ( 0.9730545539215883499, 42.47233286818625686, -6.101350888304211573 ) ) ;
#29861=B_SPLINE_CURVE_WITH_KNOTS ( 'NONE', 3,
 ( #4668, #15048, #37629, #19432 ),
 .UNSPECIFIED., .F., .F.,
 ( 4, 4 ),
 ( 1.734723475976807094E-18, 0.004050076154993000749 ),
 .UNSPECIFIED. ) ;
#29866=DIRECTION ( 'NONE',  ( -0.07439287786467650709, 0.9868880006907410074, -0.1432402660415122431 ) ) ;
#29867=AXIS2_PLACEMENT_3D ( 'NONE', #41456, #3502, #36755 ) ;
#29874=CARTESIAN_POINT ( 'NONE',  ( 0.5786265663353196143, 47.39171391660391208, 6.967625775955879064 ) ) ;
#29876=CARTESIAN_POINT ( 'NONE',  ( 0.9756354156337443406, -26.22428641656280135, 33.96210048825368233 ) ) ;
#29883=ORIENTED_EDGE ( 'NONE', *, *, #31249, .T. ) ;
#29889=VERTEX_POINT ( 'NONE', #5353 ) ;
#29891=CARTESIAN_POINT ( 'NONE',  ( 0.5800708119828333897, 34.30831427709752290, 33.42085299104031293 ) ) ;
#29892=CARTESIAN_POINT ( 'NONE',  ( 0.5837374860065634996, -41.56971235019468480, -23.79054246378012749 ) ) ;
#29894=ORIENTED_EDGE ( 'NONE', *, *, #23480, .F. ) ;
#29898=CARTESIAN_POINT ( 'NONE',  ( 5.959828726073459926, -12.49160845136047193, 16.28681682518042706 ) ) ;
#29899=CARTESIAN_POINT ( 'NONE',  ( 0.9730545539215883499, -11.59290486963477562, -41.31259007387244253 ) ) ;
#29902=EDGE_CURVE ( 'NONE', #40335, #59254, #31372, .T. ) ;
#29906=EDGE_CURVE ( 'NONE', #25113, #55904, #9730, .T. ) ;
#29908=ORIENTED_EDGE ( 'NONE', *, *, #10696, .F. ) ;
#29916=ADVANCED_FACE ( 'NONE', ( #34207 ), #58244, .F. ) ;
#29919=ORIENTED_EDGE ( 'NONE', *, *, #12964, .F. ) ;
#29921=CARTESIAN_POINT ( 'NONE',  ( 0.9752132459055864455, -42.57112816680946565, -5.369621847648042845 ) ) ;
#29922=CARTESIAN_POINT ( 'NONE',  ( 0.5807400328401574052, -5.711437504336299043, 47.55718917606841956 ) ) ;
#29923=EDGE_CURVE ( 'NONE', #34686, #35128, #16658, .T. ) ;
#29925=CARTESIAN_POINT ( 'NONE',  ( 0.9747592971366240144, -21.73404615330592549, -36.99691261380228013 ) ) ;
#29926=B_SPLINE_CURVE_WITH_KNOTS ( 'NONE', 3,
 ( #6963, #21401, #8214, #40851, #45852, #27333 ),
 .UNSPECIFIED., .F., .F.,
 ( 4, 2, 4 ),
 ( 6.256513556477135401E-18, 0.0002445244328975374024, 0.0004890488657950686248 ),
 .UNSPECIFIED. ) ;
#29930=VERTEX_POINT ( 'NONE', #35762 ) ;
#29935=CARTESIAN_POINT ( 'NONE',  ( 3.783198216974388295, -40.39102707215867127, 14.86152287314668463 ) ) ;
#29942=CARTESIAN_POINT ( 'NONE',  ( 0.5832367798473397924, 46.33367954572898384, -12.13303976268012363 ) ) ;
#29944=EDGE_LOOP ( 'NONE', ( #1953, #4160, #45052, #14119 ) ) ;
#29947=CARTESIAN_POINT ( 'NONE',  ( -4.473699999999997345, 0.000000000000000000, 0.000000000000000000 ) ) ;
#29949=CONICAL_SURFACE ( 'NONE', #18977, 43.08621763946400307, 1.568696531533066763 ) ;
#29955=CARTESIAN_POINT ( 'NONE',  ( 4.967162193818130511, 0.000000000000000000, 0.000000000000000000 ) ) ;
#29964=CARTESIAN_POINT ( 'NONE',  ( 2.281448460670567613, -28.15071835136424383, 38.84544723616133410 ) ) ;
#29966=CARTESIAN_POINT ( 'NONE',  ( 5.960721111146673579, 20.34914600876571456, 2.685391721746106963 ) ) ;
#29968=EDGE_CURVE ( 'NONE', #46035, #4359, #27716, .T. ) ;
#29970=CARTESIAN_POINT ( 'NONE',  ( 5.960221823109900008, -18.96108896995709969, -7.859839668735147278 ) ) ;
#29978=CARTESIAN_POINT ( 'NONE',  ( 4.967162193818130511, 0.000000000000000000, 0.000000000000000000 ) ) ;
#29988=ORIENTED_EDGE ( 'NONE', *, *, #35391, .F. ) ;
#29989=CARTESIAN_POINT ( 'NONE',  ( 0.5809828226811560858, -41.74875432577632495, -23.47450554821754309 ) ) ;
#29991=ADVANCED_FACE ( 'NONE', ( #35448 ), #2637, .F. ) ;
#29992=CARTESIAN_POINT ( 'NONE',  ( 3.270143674763207553, 7.080034332678427411, -11.71453292426871684 ) ) ;
#30000=CARTESIAN_POINT ( 'NONE',  ( 5.960221823109900008, -14.50993159119820852, 14.51763960716753132 ) ) ;
#30001=VERTEX_POINT ( 'NONE', #60150 ) ;
#30004=CARTESIAN_POINT ( 'NONE',  ( 0.7762777257811881437, 41.03453903600433961, 24.71864134625245057 ) ) ;
#30005=VERTEX_POINT ( 'NONE', #17259 ) ;
#30006=CARTESIAN_POINT ( 'NONE',  ( 0.5839879327111916485, 6.341736898931933375, 47.47435452316580040 ) ) ;
#30007=CARTESIAN_POINT ( 'NONE',  ( 0.5819845079324660331, -5.801222053075409946, 47.54334065046002422 ) ) ;
#30015=DIRECTION ( 'NONE',  ( 0.000000000000000000, 0.000000000000000000, 1.000000000000000000 ) ) ;
#30024=CARTESIAN_POINT ( 'NONE',  ( 0.5850706913938534814, 44.18063951072247164, -18.49682194437916039 ) ) ;
#30054=CARTESIAN_POINT ( 'NONE',  ( 0.5786265663353153954, 6.967625775955708534, 47.39171391660394761 ) ) ;
#30055=ADVANCED_FACE ( 'NONE', ( #47957 ), #37075, .F. ) ;
#30056=ORIENTED_EDGE ( 'NONE', *, *, #19810, .T. ) ;
#30062=CARTESIAN_POINT ( 'NONE',  ( 2.526464513654345545, 1.212545078562781153, 42.96196573359004134 ) ) ;
#30064=VERTEX_POINT ( 'NONE', #37003 ) ;
#30068=ADVANCED_FACE ( 'NONE', ( #14115 ), #9054, .F. ) ;
#30072=CARTESIAN_POINT ( 'NONE',  ( 0.5819845079324654780, 33.54497088780129133, -34.18710788661915245 ) ) ;
#30077=EDGE_CURVE ( 'NONE', #45338, #24773, #27885, .T. ) ;
#30082=CARTESIAN_POINT ( 'NONE',  ( 0.9747592971366227932, 33.84353661172440297, -26.37717450293392929 ) ) ;
#30085=LINE ( 'NONE', #54489, #17581 ) ;
#30088=CARTESIAN_POINT ( 'NONE',  ( -19.25527904682359548, -12.38827900997423548, -1.669286156354737427 ) ) ;
#30091=CARTESIAN_POINT ( 'NONE',  ( 4.967162193818130511, 7.970725651239789045, 42.34252806656596846 ) ) ;
#30092=CARTESIAN_POINT ( 'NONE',  ( 0.7762777257811902532, -5.369627942761314721, -47.60264404062384358 ) ) ;
#30093=SHAPE_REPRESENTATION_RELATIONSHIP ( 'NONE' , 'NONE' ,  #16880, #30252 ) ;
#30097=DIRECTION ( 'NONE',  ( 0.000000000000000000, 0.000000000000000000, 1.000000000000000000 ) ) ;
#30100=CARTESIAN_POINT ( 'NONE',  ( 3.407937589446178528, 3.987184287467786969, 13.10584870154468184 ) ) ;
#30114=DIRECTION ( 'NONE',  ( -0.07439287786467653485, -0.6957517427943121779, 0.7144194931002993965 ) ) ;
#30117=FACE_OUTER_BOUND ( 'NONE', #1565, .T. ) ;
#30123=ORIENTED_EDGE ( 'NONE', *, *, #32212, .F. ) ;
#30140=DIRECTION ( 'NONE',  ( -1.000000000000000000, -0.000000000000000000, -0.000000000000000000 ) ) ;
#30141=EDGE_CURVE ( 'NONE', #25296, #8944, #35243, .T. ) ;
#30144=B_SPLINE_CURVE_WITH_KNOTS ( 'NONE', 3,
 ( #21776, #8583, #17697, #45915, #55574, #27709 ),
 .UNSPECIFIED., .F., .F.,
 ( 4, 2, 4 ),
 ( 1.515177093957746649E-16, 0.0002445252820015210329, 0.0004890505640028906028 ),
 .UNSPECIFIED. ) ;
#30154=B_SPLINE_CURVE_WITH_KNOTS ( 'NONE', 3,
 ( #50792, #3173, #30758, #10595 ),
 .UNSPECIFIED., .F., .F.,
 ( 4, 4 ),
 ( 8.064132208641563324E-17, 0.005004741218457511680 ),
 .UNSPECIFIED. ) ;
#30157=CARTESIAN_POINT ( 'NONE',  ( 0.9730545539215883499, 39.44597740938085195, -16.88610103448514721 ) ) ;
#30174=CARTESIAN_POINT ( 'NONE',  ( 0.9722240750034576440, 29.92651530838630336, -30.74950257330989700 ) ) ;
#30175=CARTESIAN_POINT ( 'NONE',  ( 0.5819845079324659221, -41.25022834067366517, 24.34013310064380065 ) ) ;
#30182=EDGE_CURVE ( 'NONE', #58552, #13682, #25036, .T. ) ;
#30202=CARTESIAN_POINT ( 'NONE',  ( 0.6846871229502932144, 29.84551600520687131, -37.47592888575217529 ) ) ;
#30212=ORIENTED_EDGE ( 'NONE', *, *, #54598, .T. ) ;
#30220=CARTESIAN_POINT ( 'NONE',  ( 0.5809828226811617480, -38.32755012159166341, 28.72298383114474518 ) ) ;
#30223=CARTESIAN_POINT ( 'NONE',  ( 0.5832367798473397924, 44.14510605973678281, 18.58036934788090022 ) ) ;
#30227=CARTESIAN_POINT ( 'NONE',  ( 0.5850706913938534814, 23.79070617305439583, -41.56998471741203360 ) ) ;
#30235=CARTESIAN_POINT ( 'NONE',  ( 0.9968887458511664912, -39.89008038581154381, 15.81144734640172622 ) ) ;
#30240=FACE_OUTER_BOUND ( 'NONE', #34699, .T. ) ;
#30241=CARTESIAN_POINT ( 'NONE',  ( 0.5827357941260210561, -23.63272379758821629, 41.65958460246764616 ) ) ;
#30242=CARTESIAN_POINT ( 'NONE',  ( 0.5809828226811553087, -33.48000389720640868, 34.25055090842140970 ) ) ;
#30246=CARTESIAN_POINT ( 'NONE',  ( -17.04155827523767641, -12.35689285834061302, 1.886809682956876122 ) ) ;
#30248=CARTESIAN_POINT ( 'NONE',  ( 5.960721111146673579, 5.306302591836305815, 19.82781442290499996 ) ) ;
#30252=ADVANCED_BREP_SHAPE_REPRESENTATION ( '', ( #9707, #14677 ), #24677 ) ;
#30253=DIRECTION ( 'NONE',  ( -0.07836865515943411409, -0.6006129930017440888, 0.7956898808744451435 ) ) ;
#30258=CARTESIAN_POINT ( 'NONE',  ( 1.227938101723748288, 29.74462687941226235, 30.94118573761323177 ) ) ;
#30263=EDGE_LOOP ( 'NONE', ( #7502, #55022, #32398, #32968 ) ) ;
#30266=B_SPLINE_CURVE_WITH_KNOTS ( 'NONE', 3,
 ( #44996, #38756, #20550, #39368, #29625, #6105 ),
 .UNSPECIFIED., .F., .F.,
 ( 4, 2, 4 ),
 ( 0.000000000000000000, 0.0002291966416970801085, 0.0004583932833941602170 ),
 .UNSPECIFIED. ) ;
#30272=( BOUNDED_SURFACE ( )  B_SPLINE_SURFACE ( 3, 1, ( 
 ( #7196, #55434 ),
 ( #49825, #2507 ),
 ( #12557, #26024 ),
 ( #49205, #6252 ) ),
 .UNSPECIFIED., .F., .F., .F. ) 
 B_SPLINE_SURFACE_WITH_KNOTS ( ( 4, 4 ),
 ( 2, 2 ),
 ( 0.000000000000000000, 1.000000000000000000 ),
 ( 0.000000000000000000, 1.000000000000000000 ),
 .UNSPECIFIED. ) 
 GEOMETRIC_REPRESENTATION_ITEM ( )  RATIONAL_B_SPLINE_SURFACE ( (
 ( 1.000000000000000000, 1.000000000000000000),
 ( 0.9732289882329797637, 0.9999525324661233672),
 ( 0.9732289882329797637, 0.9999525324661233672),
 ( 1.000000000000000000, 1.000000000000000000) ) ) 
 REPRESENTATION_ITEM ( '' )  SURFACE ( )  );
#30283=VERTEX_POINT ( 'NONE', #11565 ) ;
#30286=ORIENTED_EDGE ( 'NONE', *, *, #39008, .F. ) ;
#30289=ORIENTED_EDGE ( 'NONE', *, *, #11452, .F. ) ;
#30291=DIRECTION ( 'NONE',  ( -1.000000000000000000, -0.000000000000000000, -0.000000000000000000 ) ) ;
#30292=CARTESIAN_POINT ( 'NONE',  ( 0.5839879882012688483, 41.47910964649828003, -23.94800997596641423 ) ) ;
#30294=B_SPLINE_CURVE_WITH_KNOTS ( 'NONE', 3,
 ( #35010, #25898, #54686, #11818, #59391, #15584 ),
 .UNSPECIFIED., .F., .F.,
 ( 4, 2, 4 ),
 ( 1.519728548185745998E-16, 0.0002445252820015179429, 0.0004890505640028839892 ),
 .UNSPECIFIED. ) ;
#30303=CARTESIAN_POINT ( 'NONE',  ( 0.5836750258453363704, -18.49664649301221786, 44.18029554260628089 ) ) ;
#30305=CARTESIAN_POINT ( 'NONE',  ( 0.5807400328401637335, -0.5448834511086642074, -47.89582301953904420 ) ) ;
#30310=CARTESIAN_POINT ( 'NONE',  ( 0.5809828226811617480, -6.791453954330657794, 47.41188724015877654 ) ) ;
#30311=CARTESIAN_POINT ( 'NONE',  ( 0.9730545539215892381, -11.59290486963536360, 41.31259007387227911 ) ) ;
#30312=B_SPLINE_CURVE_WITH_KNOTS ( 'NONE', 3,
 ( #12624, #4100, #27015, #55811 ),
 .UNSPECIFIED., .F., .F.,
 ( 4, 4 ),
 ( 0.000000000000000000, 0.005004741218457425811 ),
 .UNSPECIFIED. ) ;
#30316=CARTESIAN_POINT ( 'NONE',  ( 0.5839879327111916485, 18.41291455875303029, 44.21534283185609837 ) ) ;
#30318=CARTESIAN_POINT ( 'NONE',  ( 4.956653778116994147, 32.11725092155092653, -35.79382859084083179 ) ) ;
#30320=CARTESIAN_POINT ( 'NONE',  ( 1.227938101723748288, 34.55893248994541267, -25.45152231597022308 ) ) ;
#30321=CARTESIAN_POINT ( 'NONE',  ( 3.270143674763207553, 3.806843787665915801, 13.14781761974170671 ) ) ;
#30328=CARTESIAN_POINT ( 'NONE',  ( 0.5786265663353196143, 24.57327059187455731, -41.11783955080211683 ) ) ;
#30334=EDGE_CURVE ( 'NONE', #53833, #15433, #29803, .T. ) ;
#30335=CARTESIAN_POINT ( 'NONE',  ( 0.5807400328401637335, 47.89582301953903709, 0.5448834511091745769 ) ) ;
#30342=CARTESIAN_POINT ( 'NONE',  ( 2.281351352603293137, -45.98107981851856607, -13.68106635380611991 ) ) ;
#30353=CARTESIAN_POINT ( 'NONE',  ( 4.303969348037258058, -48.06163817123227489, 2.158280495710045876 ) ) ;
#30354=CARTESIAN_POINT ( 'NONE',  ( 0.9756950546413942771, 16.33093981194375033, -39.67916378221920581 ) ) ;
#30364=CARTESIAN_POINT ( 'NONE',  ( 0.9730545539215883499, 21.89037132892435622, 36.90443313492338717 ) ) ;
#30365=CARTESIAN_POINT ( 'NONE',  ( 5.958863334805807099, -17.77634700750921937, -10.26176968287938784 ) ) ;
#30366=EDGE_LOOP ( 'NONE', ( #16216, #29029, #53112, #5392 ) ) ;
#30374=CARTESIAN_POINT ( 'NONE',  ( 0.5819845901640485764, 34.18710267837700911, -33.54497622115095368 ) ) ;
#30383=CARTESIAN_POINT ( 'NONE',  ( 4.967162193818130511, -38.44485641567084855, 19.45289607368810181 ) ) ;
#30384=( BOUNDED_SURFACE ( )  B_SPLINE_SURFACE ( 3, 1, ( 
 ( #54059, #15882 ),
 ( #16185, #35298 ),
 ( #6738, #59379 ),
 ( #20572, #24970 ) ),
 .UNSPECIFIED., .F., .F., .F. ) 
 B_SPLINE_SURFACE_WITH_KNOTS ( ( 4, 4 ),
 ( 2, 2 ),
 ( 0.000000000000000000, 1.000000000000000000 ),
 ( 0.000000000000000000, 1.000000000000000000 ),
 .UNSPECIFIED. ) 
 GEOMETRIC_REPRESENTATION_ITEM ( )  RATIONAL_B_SPLINE_SURFACE ( (
 ( 1.000000000000000000, 1.000000000000000000),
 ( 0.7269869731126817891, 0.9931720237060910339),
 ( 0.7269869731126817891, 0.9931720237060910339),
 ( 1.000000000000000000, 1.000000000000000000) ) ) 
 REPRESENTATION_ITEM ( '' )  SURFACE ( )  );
#30402=CARTESIAN_POINT ( 'NONE',  ( 4.960156602257182357, -3.546989772329588675, -46.28683144126599558 ) ) ;
#30403=CARTESIAN_POINT ( 'NONE',  ( 0.9749527285493316819, 37.30179927241204751, -21.20640438431149732 ) ) ;
#30409=ADVANCED_FACE ( 'NONE', ( #3978 ), #45485, .F. ) ;
#30410=B_SPLINE_CURVE_WITH_KNOTS ( 'NONE', 3,
 ( #56087, #9398, #23205, #32928 ),
 .UNSPECIFIED., .F., .F.,
 ( 4, 4 ),
 ( 0.000000000000000000, 0.005004741218457409331 ),
 .UNSPECIFIED. ) ;
#30413=VERTEX_POINT ( 'NONE', #56613 ) ;
#30417=ORIENTED_EDGE ( 'NONE', *, *, #39772, .F. ) ;
#30419=CARTESIAN_POINT ( 'NONE',  ( 4.303969348037246512, -10.35452842635810455, -46.98258166031700966 ) ) ;
#30424=ORIENTED_EDGE ( 'NONE', *, *, #25117, .F. ) ;
#30425=CARTESIAN_POINT ( 'NONE',  ( 0.5800708057587371513, -33.42085258735453834, -34.30831467131393708 ) ) ;
#30429=CARTESIAN_POINT ( 'NONE',  ( 5.960221823109900008, 12.49086489703206304, 16.28736530777594993 ) ) ;
#30439=CARTESIAN_POINT ( 'NONE',  ( 1.227938101723748288, 41.66816631169206886, -10.28900963485336995 ) ) ;
#30443=CARTESIAN_POINT ( 'NONE',  ( 0.7762777257811870335, 24.71864134625287335, -41.03453903600409092 ) ) ;
#30447=FACE_OUTER_BOUND ( 'NONE', #15580, .T. ) ;
#30450=CARTESIAN_POINT ( 'NONE',  ( 0.8557997880470599172, -47.37054680076701629, -7.156447707086194043 ) ) ;
#30467=CARTESIAN_POINT ( 'NONE',  ( 3.270143674763207553, 11.02405647745170114, 8.113405361969549645 ) ) ;
#30476=CARTESIAN_POINT ( 'NONE',  ( 5.959547316686252039, 20.34955788964373014, 2.682663672454983050 ) ) ;
#30485=ORIENTED_EDGE ( 'NONE', *, *, #44117, .F. ) ;
#30491=EDGE_CURVE ( 'NONE', #37326, #18589, #55990, .T. ) ;
#30498=EDGE_LOOP ( 'NONE', ( #6362, #38834, #52892, #51001 ) ) ;
#30500=CARTESIAN_POINT ( 'NONE',  ( 0.9730545539215883499, 39.83279466599061891, -15.95224156741785393 ) ) ;
#30503=CARTESIAN_POINT ( 'NONE',  ( 0.8557997880470690211, 5.347802024197924275, -47.60865952216993691 ) ) ;
#30512=AXIS2_PLACEMENT_3D ( 'NONE', #6839, #21901, #20972 ) ;
#30521=CARTESIAN_POINT ( 'NONE',  ( 0.9756950546413942771, -30.40918718457318803, -30.27237962848467490 ) ) ;
#30522=AXIS2_PLACEMENT_3D ( 'NONE', #38404, #43414, #46036 ) ;
#30526=ORIENTED_EDGE ( 'NONE', *, *, #57454, .T. ) ;
#30527=CARTESIAN_POINT ( 'NONE',  ( 5.960221823109900008, -19.82478916873578001, 5.317678907195093174 ) ) ;
#30530=VERTEX_POINT ( 'NONE', #48681 ) ;
#30542=EDGE_CURVE ( 'NONE', #42725, #6542, #44621, .T. ) ;
#30543=CARTESIAN_POINT ( 'NONE',  ( 0.9730545539215883499, -15.95224156741799426, -39.83279466599056917 ) ) ;
#30561=CARTESIAN_POINT ( 'NONE',  ( 4.956653778116991482, -8.845409907520609849, -47.27023054223761989 ) ) ;
#30566=VERTEX_POINT ( 'NONE', #13259 ) ;
#30570=CARTESIAN_POINT ( 'NONE',  ( 0.5850706913938533704, 37.88789093229805616, 29.30134895053067368 ) ) ;
#30572=ORIENTED_EDGE ( 'NONE', *, *, #1369, .T. ) ;
#30581=B_SPLINE_CURVE_WITH_KNOTS ( 'NONE', 3,
 ( #21569, #16888, #55065, #55371 ),
 .UNSPECIFIED., .F., .F.,
 ( 4, 4 ),
 ( 6.254634441385502288E-18, 0.004050076154993000749 ),
 .UNSPECIFIED. ) ;
#30584=EDGE_LOOP ( 'NONE', ( #35363, #60102, #41669, #22003 ) ) ;
#30586=CARTESIAN_POINT ( 'NONE',  ( 0.8551540677456834771, 47.90804413217340851, -0.9122407826477434423 ) ) ;
#30590=VERTEX_POINT ( 'NONE', #35838 ) ;
#30597=CARTESIAN_POINT ( 'NONE',  ( 2.624215991343620935, 43.79392271049097474, -19.66774719432931562 ) ) ;
#30598=EDGE_CURVE ( 'NONE', #5485, #29821, #55201, .T. ) ;
#30608=CARTESIAN_POINT ( 'NONE',  ( 0.9757954354143116849, 5.207268878499845415E-15, 42.90846090505964128 ) ) ;
#30609=CARTESIAN_POINT ( 'NONE',  ( 2.624215991343608501, -40.85210347989513480, -25.21574086439748896 ) ) ;
#30611=CARTESIAN_POINT ( 'NONE',  ( 1.227938101723756947, -30.94118573761292623, -29.74462687941258210 ) ) ;
#30615=CARTESIAN_POINT ( 'NONE',  ( 5.960721111146673579, -14.51823969584109619, 14.50930005614991813 ) ) ;
#30617=ORIENTED_EDGE ( 'NONE', *, *, #33523, .F. ) ;
#30645=DIRECTION ( 'NONE',  ( 0.000000000000000000, 0.000000000000000000, 1.000000000000000000 ) ) ;
#30646=B_SPLINE_CURVE_WITH_KNOTS ( 'NONE', 3,
 ( #1305, #1009, #25435, #30752 ),
 .UNSPECIFIED., .F., .F.,
 ( 4, 4 ),
 ( 0.000000000000000000, 0.005004741218457424076 ),
 .UNSPECIFIED. ) ;
#30648=( BOUNDED_SURFACE ( )  B_SPLINE_SURFACE ( 3, 1, ( 
 ( #34034, #53105 ),
 ( #10210, #24932 ),
 ( #1097, #13451 ),
 ( #10516, #29610 ) ),
 .UNSPECIFIED., .F., .F., .F. ) 
 B_SPLINE_SURFACE_WITH_KNOTS ( ( 4, 4 ),
 ( 2, 2 ),
 ( 0.000000000000000000, 1.000000000000000000 ),
 ( 0.000000000000000000, 1.000000000000000000 ),
 .UNSPECIFIED. ) 
 GEOMETRIC_REPRESENTATION_ITEM ( )  RATIONAL_B_SPLINE_SURFACE ( (
 ( 1.000000000000000000, 1.000000000000000000),
 ( 0.7269869731126817891, 0.9931720237060910339),
 ( 0.7269869731126817891, 0.9931720237060910339),
 ( 1.000000000000000000, 1.000000000000000000) ) ) 
 REPRESENTATION_ITEM ( '' )  SURFACE ( )  );
#30655=FACE_OUTER_BOUND ( 'NONE', #1160, .T. ) ;
#30668=CARTESIAN_POINT ( 'NONE',  ( 4.303969348037258058, -2.158280495709878455, -48.06163817123227489 ) ) ;
#30670=B_SPLINE_CURVE_WITH_KNOTS ( 'NONE', 3,
 ( #49497, #15697, #6241, #48885, #34803, #44530 ),
 .UNSPECIFIED., .F., .F.,
 ( 4, 2, 4 ),
 ( 7.896833245746192927E-18, 0.0002445244328975387576, 0.0004890488657950696006 ),
 .UNSPECIFIED. ) ;
#30681=CARTESIAN_POINT ( 'NONE',  ( 0.5839879882012690704, -37.99844431214147988, -29.15719377327484807 ) ) ;
#30694=ORIENTED_EDGE ( 'NONE', *, *, #59250, .T. ) ;
#30699=CARTESIAN_POINT ( 'NONE',  ( 4.303969348037246512, -42.70173985163832953, 22.16169334783822720 ) ) ;
#30700=VERTEX_POINT ( 'NONE', #19499 ) ;
#30710=EDGE_LOOP ( 'NONE', ( #57481, #43029, #5307, #13915 ) ) ;
#30711=VECTOR ( 'NONE', #34548, 1000.000000000000114 ) ;
#30722=CARTESIAN_POINT ( 'NONE',  ( 4.303969348037258058, 42.70173985163817321, 22.16169334783852207 ) ) ;
#30723=B_SPLINE_CURVE_WITH_KNOTS ( 'NONE', 3,
 ( #10225, #9921, #9593, #4879, #43141, #32813 ),
 .UNSPECIFIED., .F., .F.,
 ( 4, 2, 4 ),
 ( 0.000000000000000000, 0.0002291966416970759885, 0.0004583932833941519770 ),
 .UNSPECIFIED. ) ;
#30729=VERTEX_POINT ( 'NONE', #57666 ) ;
#30731=CARTESIAN_POINT ( 'NONE',  ( 0.5809828226811617480, 46.11980934799338883, 12.92184523170220345 ) ) ;
#30733=ORIENTED_EDGE ( 'NONE', *, *, #54100, .T. ) ;
#30736=CARTESIAN_POINT ( 'NONE',  ( 3.270143674763207553, 4.983712007628406937, -12.74832469035447424 ) ) ;
#30752=CARTESIAN_POINT ( 'NONE',  ( 4.956653778116982600, -47.05699031914957686, 9.917440902360995736 ) ) ;
#30754=LINE ( 'NONE', #5686, #57964 ) ;
#30758=CARTESIAN_POINT ( 'NONE',  ( 4.963659409799330291, 42.53037318521015209, -13.93274247731977233 ) ) ;
#30760=CARTESIAN_POINT ( 'NONE',  ( 0.5807400328401574052, -37.66660715020846339, -29.58941477093054573 ) ) ;
#30773=CARTESIAN_POINT ( 'NONE',  ( 3.660087539127319545, 42.51124390328632785, 22.37124151181794574 ) ) ;
#30780=CARTESIAN_POINT ( 'NONE',  ( 1.154321485836934391, -33.53917069757672209, 26.77578840293023887 ) ) ;
#30781=CARTESIAN_POINT ( 'NONE',  ( 2.281448460670572498, -30.23587867650730487, -37.24544744441608657 ) ) ;
#30783=CARTESIAN_POINT ( 'NONE',  ( 5.958863334805807099, 16.28335246510367540, -12.49619391867165064 ) ) ;
#30784=DIRECTION ( 'NONE',  ( 0.07836865515943410021, -0.9179910502197358158, -0.3887811538706165138 ) ) ;
#30799=ORIENTED_EDGE ( 'NONE', *, *, #19734, .F. ) ;
#30801=AXIS2_PLACEMENT_3D ( 'NONE', #49358, #31175, #45001 ) ;
#30813=EDGE_LOOP ( 'NONE', ( #34944, #19973, #47113, #26138 ) ) ;
#30816=EDGE_CURVE ( 'NONE', #43576, #44327, #46253, .T. ) ;
#30817=CIRCLE ( 'NONE', #1787, 48.09070567114147110 ) ;
#30826=ORIENTED_EDGE ( 'NONE', *, *, #57273, .F. ) ;
#30830=DIRECTION ( 'NONE',  ( 0.000000000000000000, 0.000000000000000000, -1.000000000000000000 ) ) ;
#30835=CARTESIAN_POINT ( 'NONE',  ( 5.960721111146673579, 14.51823969584099672, -14.50930005615001583 ) ) ;
#30836=CARTESIAN_POINT ( 'NONE',  ( 0.9730545539215883499, 41.31259007387230753, 11.59290486963521971 ) ) ;
#30838=EDGE_CURVE ( 'NONE', #16591, #51919, #16273, .T. ) ;
#30842=ADVANCED_FACE ( 'NONE', ( #24488 ), #60243, .T. ) ;
#30849=VECTOR ( 'NONE', #41615, 1000.000000000000000 ) ;
#30851=CARTESIAN_POINT ( 'NONE',  ( 5.860006189529246790, -26.78264244998070609, -40.11385274514709209 ) ) ;
#30855=CARTESIAN_POINT ( 'NONE',  ( 1.227938101723748288, -15.63977281655813023, -39.96870412324352628 ) ) ;
#30858=CARTESIAN_POINT ( 'NONE',  ( 0.9730545539215883499, 42.90536227157002003, -0.5054011016614180507 ) ) ;
#30861=CARTESIAN_POINT ( 'NONE',  ( 0.5809828226811617480, -34.25055090842177208, 33.48000389720603920 ) ) ;
#30862=CARTESIAN_POINT ( 'NONE',  ( 0.5838002273316447166, 37.91535410490867264, 29.26514720557031168 ) ) ;
#30867=CARTESIAN_POINT ( 'NONE',  ( -17.42749720829281301, -12.33370093165928516, -2.032379639964776441 ) ) ;
#30881=CARTESIAN_POINT ( 'NONE',  ( 0.8551540677456834771, -41.03346287276445992, 24.74404575822760677 ) ) ;
#30886=VERTEX_POINT ( 'NONE', #44556 ) ;
#30887=FACE_OUTER_BOUND ( 'NONE', #26063, .T. ) ;
#30888=CARTESIAN_POINT ( 'NONE',  ( 5.960721111146673579, -18.96073515164543011, -7.860635756377828187 ) ) ;
#30890=ADVANCED_FACE ( 'NONE', ( #58919 ), #247, .F. ) ;
#30913=B_SPLINE_CURVE_WITH_KNOTS ( 'NONE', 3,
 ( #19602, #28676, #57776, #33706, #9564, #43420, #29290, #10193, #48101, #19922, #34316, #43110, #14911, #18996, #28364, #23671 ),
 .UNSPECIFIED., .F., .F.,
 ( 4, 3, 3, 3, 3, 4 ),
 ( 9.813676791237319219E-18, 0.0002724568934985577154, 0.0004086836638483823695, 0.0005449104342063580556, 0.0008173270854453611439, 0.001089761613562687491 ),
 .UNSPECIFIED. ) ;
#30917=CARTESIAN_POINT ( 'NONE',  ( 5.965394784446460541, 12.50653125159007395, -16.27505370423068598 ) ) ;
#30920=ORIENTED_EDGE ( 'NONE', *, *, #40202, .T. ) ;
#30930=CARTESIAN_POINT ( 'NONE',  ( 1.227938101723756947, 26.79402671879326547, 33.52879263017872091 ) ) ;
#30936=CARTESIAN_POINT ( 'NONE',  ( 1.227938101723748288, -11.92353943227977986, 41.23019537246705823 ) ) ;
#30942=VERTEX_POINT ( 'NONE', #21965 ) ;
#30944=CARTESIAN_POINT ( 'NONE',  ( 0.9968887458511642707, -42.90440775986213851, -0.6574002966412972881 ) ) ;
#30948=CARTESIAN_POINT ( 'NONE',  ( 0.5800708119828326126, -44.48635609075545005, -17.74761857127114340 ) ) ;
#30949=CARTESIAN_POINT ( 'NONE',  ( 0.5850706913938533704, 46.31100969101504461, -12.22095376871988215 ) ) ;
#30950=EDGE_LOOP ( 'NONE', ( #26217, #27231, #40508, #59953 ) ) ;
#30955=DIRECTION ( 'NONE',  ( -0.07836865515943411409, 0.9179910502197414779, -0.3887811538706032466 ) ) ;
#30956=CARTESIAN_POINT ( 'NONE',  ( 0.9730545539215883499, 42.90536227157002003, 0.5054011016614263774 ) ) ;
#30959=CARTESIAN_POINT ( 'NONE',  ( 3.660176727303405819, -47.83637937224827397, 4.399934609596405366 ) ) ;
#30974=CARTESIAN_POINT ( 'NONE',  ( 3.407937589446174087, 3.099921468255003809, 13.34359005742690485 ) ) ;
#30977=AXIS2_PLACEMENT_3D ( 'NONE', #8714, #18130, #8100 ) ;
#30979=CARTESIAN_POINT ( 'NONE',  ( 0.9757402383260939116, -39.60970160107522986, -16.49876987395769490 ) ) ;
#30980=CARTESIAN_POINT ( 'NONE',  ( 0.9722240750034578660, -25.65687433776921722, 34.39263040572782870 ) ) ;
#30987=ORIENTED_EDGE ( 'NONE', *, *, #33689, .T. ) ;
#30989=CARTESIAN_POINT ( 'NONE',  ( 0.9722240741986377666, 41.29187377038500983, 11.66659279943990946 ) ) ;
#30990=ORIENTED_EDGE ( 'NONE', *, *, #48161, .F. ) ;
#30991=DIRECTION ( 'NONE',  ( -0.07836865515943411409, -0.9608836331491561467, 0.2656332009267280969 ) ) ;
#30994=ORIENTED_EDGE ( 'NONE', *, *, #27440, .F. ) ;
#31003=CARTESIAN_POINT ( 'NONE',  ( 0.5839879327111930918, -38.05372318152033273, -29.08515285004925488 ) ) ;
#31010=CARTESIAN_POINT ( 'NONE',  ( 3.270143674763207553, -13.53222904135352778, -2.058141141425741338 ) ) ;
#31013=FACE_OUTER_BOUND ( 'NONE', #26438, .T. ) ;
#31016=( BOUNDED_SURFACE ( )  B_SPLINE_SURFACE ( 3, 1, ( 
 ( #27178, #31262 ),
 ( #59761, #13096 ),
 ( #7428, #2737 ),
 ( #26559, #3656 ) ),
 .UNSPECIFIED., .F., .F., .F. ) 
 B_SPLINE_SURFACE_WITH_KNOTS ( ( 4, 4 ),
 ( 2, 2 ),
 ( 0.000000000000000000, 1.000000000000000000 ),
 ( 0.000000000000000000, 1.000000000000000000 ),
 .UNSPECIFIED. ) 
 GEOMETRIC_REPRESENTATION_ITEM ( )  RATIONAL_B_SPLINE_SURFACE ( (
 ( 1.000000000000000000, 1.000000000000000000),
 ( 0.7269869731126817891, 0.9931720237060910339),
 ( 0.7269869731126817891, 0.9931720237060910339),
 ( 1.000000000000000000, 1.000000000000000000) ) ) 
 REPRESENTATION_ITEM ( '' )  SURFACE ( )  );
#31025=CARTESIAN_POINT ( 'NONE',  ( -18.90388840650297553, -12.35675306864543188, -1.887713692035127400 ) ) ;
#31029=VERTEX_POINT ( 'NONE', #47932 ) ;
#31031=CARTESIAN_POINT ( 'NONE',  ( 0.9757892942422837779, -34.01031843153910472, 26.16173342773525690 ) ) ;
#31036=CARTESIAN_POINT ( 'NONE',  ( 0.9740398440564311811, 21.09418882170589171, -37.36539512267997765 ) ) ;
#31044=FACE_OUTER_BOUND ( 'NONE', #59753, .T. ) ;
#31047=EDGE_CURVE ( 'NONE', #17533, #19313, #45473, .T. ) ;
#31054=CARTESIAN_POINT ( 'NONE',  ( 0.5838002273316426072, 46.22850660674022549, 12.52789267095200820 ) ) ;
#31062=FACE_OUTER_BOUND ( 'NONE', #54604, .T. ) ;
#31071=CARTESIAN_POINT ( 'NONE',  ( 0.9747592971366223491, -5.279515277919681004, 42.58247319705104417 ) ) ;
#31077=AXIS2_PLACEMENT_3D ( 'NONE', #14713, #23794, #57272 ) ;
#31081=CARTESIAN_POINT ( 'NONE',  ( 0.5786265663353196143, 46.07681357296485203, 13.09387673186351719 ) ) ;
#31084=ORIENTED_EDGE ( 'NONE', *, *, #3762, .F. ) ;
#31085=B_SPLINE_CURVE_WITH_KNOTS ( 'NONE', 3,
 ( #8139, #60743, #17864, #50317, #31219, #16508 ),
 .UNSPECIFIED., .F., .F.,
 ( 4, 2, 4 ),
 ( 1.544890704737618961E-16, 0.0002445252820015170756, 0.0004890505640028796524 ),
 .UNSPECIFIED. ) ;
#31089=EDGE_CURVE ( 'NONE', #23013, #50690, #225, .T. ) ;
#31092=CARTESIAN_POINT ( 'NONE',  ( 0.5834872094924171693, -46.20467604622292157, -12.61552836343339656 ) ) ;
#31093=CARTESIAN_POINT ( 'NONE',  ( 3.783198216974392292, -38.10565824507913391, 20.00646744835652413 ) ) ;
#31095=CARTESIAN_POINT ( 'NONE',  ( 4.963659409799329403, -42.22332985082321954, 14.83726297270265881 ) ) ;
#31097=ORIENTED_EDGE ( 'NONE', *, *, #42951, .T. ) ;
#31098=CARTESIAN_POINT ( 'NONE',  ( 5.860006189529246790, 47.30296539008823942, 9.426589201135659124 ) ) ;
#31100=CARTESIAN_POINT ( 'NONE',  ( 0.9752132459055881109, -16.20487516111980497, 39.73079175141342745 ) ) ;
#31107=CARTESIAN_POINT ( 'NONE',  ( 0.9722240741986366563, 5.023189681690755748, 42.61332881199389533 ) ) ;
#31108=CARTESIAN_POINT ( 'NONE',  ( 0.7057020205115015488, -41.89806668505397624, 23.21851350879803277 ) ) ;
#31110=CARTESIAN_POINT ( 'NONE',  ( 1.154321485836933503, 29.75729673892742255, -30.92445806269047637 ) ) ;
#31114=EDGE_CURVE ( 'NONE', #59626, #44755, #58858, .T. ) ;
#31121=CARTESIAN_POINT ( 'NONE',  ( 2.281351352603290028, -13.68106635380595293, 45.98107981851860160 ) ) ;
#31124=ORIENTED_EDGE ( 'NONE', *, *, #29555, .F. ) ;
#31126=CARTESIAN_POINT ( 'NONE',  ( 0.5807400328401637335, -12.92266817605982965, -46.12278621143511259 ) ) ;
#31132=CARTESIAN_POINT ( 'NONE',  ( 0.5836750258453351492, 47.89563095930319747, 0.1816059738418068226 ) ) ;
#31137=DIRECTION ( 'NONE',  ( -1.000000000000000000, -0.000000000000000000, -0.000000000000000000 ) ) ;
#31161=CARTESIAN_POINT ( 'NONE',  ( 1.154321713695930507, 36.74718012229653397, 22.16897764010616001 ) ) ;
#31175=DIRECTION ( 'NONE',  ( -1.000000000000000000, -0.000000000000000000, -0.000000000000000000 ) ) ;
#31177=ORIENTED_EDGE ( 'NONE', *, *, #677, .T. ) ;
#31182=B_SPLINE_CURVE_WITH_KNOTS ( 'NONE', 3,
 ( #1280, #38611, #20413, #39540, #57662, #33909 ),
 .UNSPECIFIED., .F., .F.,
 ( 4, 2, 4 ),
 ( 7.040638946443416885E-18, 0.0002445244328975364808, 0.0004890488657950659143 ),
 .UNSPECIFIED. ) ;
#31200=B_SPLINE_CURVE_WITH_KNOTS ( 'NONE', 3,
 ( #53416, #15234, #29935, #25850 ),
 .UNSPECIFIED., .F., .F.,
 ( 4, 4 ),
 ( 8.673617379884035472E-19, 0.004048833967417085622 ),
 .UNSPECIFIED. ) ;
#31216=DIRECTION ( 'NONE',  ( -1.000000000000000000, -0.000000000000000000, -0.000000000000000000 ) ) ;
#31219=CARTESIAN_POINT ( 'NONE',  ( 0.5800708057587384836, 34.30831467131400814, -33.42085258735440334 ) ) ;
#31222=CARTESIAN_POINT ( 'NONE',  ( 1.227938101723756947, 15.63977281655895979, -39.96870412324319943 ) ) ;
#31223=CARTESIAN_POINT ( 'NONE',  ( 0.5850706913938533704, 0.1816364388707057964, -47.89601588673689037 ) ) ;
#31224=B_SPLINE_CURVE_WITH_KNOTS ( 'NONE', 3,
 ( #55053, #31264, #45690, #36291 ),
 .UNSPECIFIED., .F., .F.,
 ( 4, 4 ),
 ( 1.951563910473907981E-18, 0.004444878191957666973 ),
 .UNSPECIFIED. ) ;
#31230=CARTESIAN_POINT ( 'NONE',  ( 4.956653778116975495, -26.26162724282400518, 40.28700667097671584 ) ) ;
#31235=CARTESIAN_POINT ( 'NONE',  ( 0.5832366564991534608, -18.07697797533119655, 44.35361744978930432 ) ) ;
#31239=CARTESIAN_POINT ( 'NONE',  ( 4.956653778116966613, 48.02038484091100656, 2.599733001514495712 ) ) ;
#31243=FACE_OUTER_BOUND ( 'NONE', #42897, .T. ) ;
#31247=B_SPLINE_CURVE_WITH_KNOTS ( 'NONE', 3,
 ( #56599, #37849, #18410, #37529, #9299, #56905, #51280, #32507, #55982, #3350, #23407, #50974, #42535, #36598, #46932, #47223, #13405, #51583, #41607 ),
 .UNSPECIFIED., .F., .F.,
 ( 4, 3, 3, 3, 3, 3, 4 ),
 ( 6.071532165918824830E-18, 0.0002724573126191775444, 0.0004086839781548516214, 0.0005449106435901876662, 0.0006811373090491506990, 0.0008459866663933703502, 0.001010840725717213799 ),
 .UNSPECIFIED. ) ;
#31249=EDGE_CURVE ( 'NONE', #54442, #44595, #15041, .T. ) ;
#31253=CARTESIAN_POINT ( 'NONE',  ( 0.5800708057587384836, -6.873290064481704320, 47.40012370174861900 ) ) ;
#31256=CARTESIAN_POINT ( 'NONE',  ( 2.624215991343620935, 34.92983774302966538, 32.93378783738860704 ) ) ;
#31261=VERTEX_POINT ( 'NONE', #55381 ) ;
#31262=CARTESIAN_POINT ( 'NONE',  ( 5.860006189529246790, -47.30296539008818257, -9.426589201135987750 ) ) ;
#31264=CARTESIAN_POINT ( 'NONE',  ( 2.281448460670566281, 44.80776276180771589, 17.13756432392853668 ) ) ;
#31272=CARTESIAN_POINT ( 'NONE',  ( 0.5807400328401574052, 5.711437504335963311, 47.55718917606844798 ) ) ;
#31281=CARTESIAN_POINT ( 'NONE',  ( 5.959547316686252039, 10.25972575517530139, -17.77749189599207114 ) ) ;
#31282=EDGE_CURVE ( 'NONE', #29154, #2006, #44699, .T. ) ;
#31298=( BOUNDED_SURFACE ( )  B_SPLINE_SURFACE ( 3, 1, ( 
 ( #46239, #31824 ),
 ( #3282, #22414 ),
 ( #21483, #41542 ),
 ( #36849, #40623 ) ),
 .UNSPECIFIED., .F., .F., .F. ) 
 B_SPLINE_SURFACE_WITH_KNOTS ( ( 4, 4 ),
 ( 2, 2 ),
 ( 0.000000000000000000, 1.000000000000000000 ),
 ( 0.000000000000000000, 1.000000000000000000 ),
 .UNSPECIFIED. ) 
 GEOMETRIC_REPRESENTATION_ITEM ( )  RATIONAL_B_SPLINE_SURFACE ( (
 ( 1.000000000000000000, 1.000000000000000000),
 ( 0.7269869731126821222, 0.9931720237060910339),
 ( 0.7269869731126821222, 0.9931720237060910339),
 ( 1.000000000000000000, 1.000000000000000000) ) ) 
 REPRESENTATION_ITEM ( '' )  SURFACE ( )  );
#31306=VERTEX_POINT ( 'NONE', #2762 ) ;
#31308=ORIENTED_EDGE ( 'NONE', *, *, #54942, .F. ) ;
#31309=CARTESIAN_POINT ( 'NONE',  ( 0.5836750258453355933, -37.88760409476676472, -29.30109045202428319 ) ) ;
#31311=ORIENTED_EDGE ( 'NONE', *, *, #3967, .T. ) ;
#31314=CARTESIAN_POINT ( 'NONE',  ( 0.8557997880470599172, 44.60232077416710439, -17.48760788519168941 ) ) ;
#31316=CARTESIAN_POINT ( 'NONE',  ( 4.967162193818130511, 36.06913038482799294, 23.56777426397191277 ) ) ;
#31317=ORIENTED_EDGE ( 'NONE', *, *, #54318, .F. ) ;
#31321=CARTESIAN_POINT ( 'NONE',  ( 0.5809828226811617480, -44.45562576850614533, 17.82437196699665094 ) ) ;
#31331=ADVANCED_FACE ( 'NONE', ( #6827 ), #52288, .T. ) ;
#31335=VERTEX_POINT ( 'NONE', #18739 ) ;
#31336=EDGE_CURVE ( 'NONE', #28511, #37598, #50655, .T. ) ;
#31337=CARTESIAN_POINT ( 'NONE',  ( 4.956653778116991482, 9.917440902361805755, -47.05699031914939212 ) ) ;
#31338=CARTESIAN_POINT ( 'NONE',  ( 3.660087539127316880, -32.61167949558411294, 35.27260502801121334 ) ) ;
#31339=CARTESIAN_POINT ( 'NONE',  ( 5.974727161628369032, 14.50236057684825042, 14.52429704002368993 ) ) ;
#31343=EDGE_CURVE ( 'NONE', #29821, #35268, #51299, .T. ) ;
#31347=EDGE_CURVE ( 'NONE', #36264, #32791, #35712, .T. ) ;
#31351=CARTESIAN_POINT ( 'NONE',  ( 0.5807400328401574052, 11.87003418057308402, -46.40483864045133089 ) ) ;
#31357=CARTESIAN_POINT ( 'NONE',  ( 4.956653778116991482, 8.845409907521601056, -47.27023054223744225 ) ) ;
#31363=CARTESIAN_POINT ( 'NONE',  ( 4.956653778116966613, 0.000000000000000000, 0.000000000000000000 ) ) ;
#31370=CARTESIAN_POINT ( 'NONE',  ( 2.624215991343608501, -28.09277600149193077, -38.92973006074542042 ) ) ;
#31372=B_SPLINE_CURVE_WITH_KNOTS ( 'NONE', 3,
 ( #25403, #52979, #1580, #11316 ),
 .UNSPECIFIED., .F., .F.,
 ( 4, 4 ),
 ( 3.127317220692750759E-18, 0.004050076154993002484 ),
 .UNSPECIFIED. ) ;
#31373=CARTESIAN_POINT ( 'NONE',  ( 0.9756008150404610335, -41.48296819691540804, -10.96816689273740586 ) ) ;
#31375=ORIENTED_EDGE ( 'NONE', *, *, #19531, .T. ) ;
#31376=CARTESIAN_POINT ( 'NONE',  ( 5.959547316686252039, 20.34955788964376566, -2.682663672454702830 ) ) ;
#31378=ORIENTED_EDGE ( 'NONE', *, *, #21279, .T. ) ;
#31379=CARTESIAN_POINT ( 'NONE',  ( 0.9730545539215883499, -6.101350888304943432, 42.47233286818615028 ) ) ;
#31380=ORIENTED_EDGE ( 'NONE', *, *, #34105, .T. ) ;
#31382=VECTOR ( 'NONE', #7505, 1000.000000000000114 ) ;
#31396=CARTESIAN_POINT ( 'NONE',  ( 0.9756354156337442296, -42.90827993934340157, -0.1303083999671457160 ) ) ;
#31398=CARTESIAN_POINT ( 'NONE',  ( 0.9757787079277437936, 26.08967489699762154, 34.06559579809977123 ) ) ;
#31401=CARTESIAN_POINT ( 'NONE',  ( 0.5839254288179553942, -46.24038938821425404, -12.48406597209087820 ) ) ;
#31403=EDGE_CURVE ( 'NONE', #36286, #9581, #42484, .T. ) ;
#31406=ADVANCED_FACE ( 'NONE', ( #32847 ), #11082, .F. ) ;
#31407=VERTEX_POINT ( 'NONE', #22505 ) ;
#31411=CARTESIAN_POINT ( 'NONE',  ( 0.6067375320500726366, 13.08014790719091103, -46.07640252006464010 ) ) ;
#31416=CARTESIAN_POINT ( 'NONE',  ( 3.783198216974387851, -42.41041696600773747, -7.325057189010854231 ) ) ;
#31421=CARTESIAN_POINT ( 'NONE',  ( 1.227938101723756947, 29.74462687941269223, -30.94118573761281965 ) ) ;
#31424=CARTESIAN_POINT ( 'NONE',  ( 0.9730545539215883499, 42.60426903087353878, 5.099196237955034405 ) ) ;
#31430=ORIENTED_EDGE ( 'NONE', *, *, #10680, .T. ) ;
#31436=VERTEX_POINT ( 'NONE', #53751 ) ;
#31440=B_SPLINE_CURVE_WITH_KNOTS ( 'NONE', 3,
 ( #48546, #38875, #57927, #9718 ),
 .UNSPECIFIED., .F., .F.,
 ( 4, 4 ),
 ( 8.673617379884035472E-19, 0.004444878191957692126 ),
 .UNSPECIFIED. ) ;
#31448=CARTESIAN_POINT ( 'NONE',  ( 2.624215991343620935, 47.76052319582216654, 4.864192649745549879 ) ) ;
#31454=CARTESIAN_POINT ( 'NONE',  ( 1.154321713695927398, -0.8253077511129642829, 42.90848032340448270 ) ) ;
#31455=B_SPLINE_CURVE_WITH_KNOTS ( 'NONE', 3,
 ( #33463, #5226, #48462, #5529 ),
 .UNSPECIFIED., .F., .F.,
 ( 4, 4 ),
 ( 6.254634441385500747E-18, 0.004050076154993005953 ),
 .UNSPECIFIED. ) ;
#31457=CARTESIAN_POINT ( 'NONE',  ( 0.8551540677456715978, -33.23105123575924580, 34.52115452272916940 ) ) ;
#31461=CARTESIAN_POINT ( 'NONE',  ( 2.281448460670565392, 47.71650330356587233, 4.956513608981339303 ) ) ;
#31462=VERTEX_POINT ( 'NONE', #4913 ) ;
#31472=CARTESIAN_POINT ( 'NONE',  ( 0.5800708057587400379, 33.42085258735475861, 34.30831467131368129 ) ) ;
#31474=ORIENTED_EDGE ( 'NONE', *, *, #202, .F. ) ;
#31480=CARTESIAN_POINT ( 'NONE',  ( 0.5786265663353153954, 46.07681357296503677, -13.09387673186287060 ) ) ;
#31482=CARTESIAN_POINT ( 'NONE',  ( 0.9730545539215883499, -5.099196237954599198, -42.60426903087358852 ) ) ;
#31489=CARTESIAN_POINT ( 'NONE',  ( 3.660176727303410704, -40.62966184289471983, -25.63023984566688185 ) ) ;
#31492=CARTESIAN_POINT ( 'NONE',  ( 4.967162193818129623, -38.44485641567058565, -19.45289607368863116 ) ) ;
#31498=( BOUNDED_SURFACE ( )  B_SPLINE_SURFACE ( 3, 1, ( 
 ( #41823, #18006 ),
 ( #56192, #12693 ),
 ( #27082, #23014 ),
 ( #21764, #31790 ) ),
 .UNSPECIFIED., .F., .F., .F. ) 
 B_SPLINE_SURFACE_WITH_KNOTS ( ( 4, 4 ),
 ( 2, 2 ),
 ( 0.000000000000000000, 1.000000000000000000 ),
 ( 0.000000000000000000, 1.000000000000000000 ),
 .UNSPECIFIED. ) 
 GEOMETRIC_REPRESENTATION_ITEM ( )  RATIONAL_B_SPLINE_SURFACE ( (
 ( 1.000000000000000000, 1.000000000000000000),
 ( 0.9953390228620291325, 0.8624445117760984880),
 ( 0.9953390228620291325, 0.8624445117760984880),
 ( 1.000000000000000000, 1.000000000000000000) ) ) 
 REPRESENTATION_ITEM ( '' )  SURFACE ( )  );
#31506=CARTESIAN_POINT ( 'NONE',  ( 5.981074661064941900, 17.77058762078863552, 10.26976685693829339 ) ) ;
#31508=VERTEX_POINT ( 'NONE', #29352 ) ;
#31511=DIRECTION ( 'NONE',  ( 0.000000000000000000, 0.000000000000000000, 1.000000000000000000 ) ) ;
#31516=LINE ( 'NONE', #54684, #56314 ) ;
#31538=CARTESIAN_POINT ( 'NONE',  ( 5.974727161628367256, -7.840226266082667372, 18.96851388233644897 ) ) ;
#31549=ORIENTED_EDGE ( 'NONE', *, *, #59487, .F. ) ;
#31551=EDGE_CURVE ( 'NONE', #26377, #9042, #60293, .T. ) ;
#31556=( BOUNDED_SURFACE ( )  B_SPLINE_SURFACE ( 3, 1, ( 
 ( #26309, #45442 ),
 ( #50423, #7490 ),
 ( #26615, #9666 ),
 ( #3714, #32569 ) ),
 .UNSPECIFIED., .F., .F., .F. ) 
 B_SPLINE_SURFACE_WITH_KNOTS ( ( 4, 4 ),
 ( 2, 2 ),
 ( 0.000000000000000000, 1.000000000000000000 ),
 ( 0.000000000000000000, 1.000000000000000000 ),
 .UNSPECIFIED. ) 
 GEOMETRIC_REPRESENTATION_ITEM ( )  RATIONAL_B_SPLINE_SURFACE ( (
 ( 1.000000000000000000, 1.000000000000000000),
 ( 0.7269869731126817891, 0.9931720237060910339),
 ( 0.7269869731126817891, 0.9931720237060910339),
 ( 1.000000000000000000, 1.000000000000000000) ) ) 
 REPRESENTATION_ITEM ( '' )  SURFACE ( )  );
#31570=CARTESIAN_POINT ( 'NONE',  ( 0.9740398440564311811, -30.04629765303410949, 30.63262235044618365 ) ) ;
#31571=CARTESIAN_POINT ( 'NONE',  ( 1.154321713695929175, 42.90848032340444718, 0.8253077511128138477 ) ) ;
#31574=VECTOR ( 'NONE', #21243, 1000.000000000000114 ) ;
#31579=FACE_OUTER_BOUND ( 'NONE', #13662, .T. ) ;
#31581=CARTESIAN_POINT ( 'NONE',  ( 0.9749527285493307938, -39.75066842359295549, 16.15611883305632190 ) ) ;
#31589=CARTESIAN_POINT ( 'NONE',  ( 0.8557997880470599172, 37.44587306708097429, 29.88293891557482951 ) ) ;
#31590=CARTESIAN_POINT ( 'NONE',  ( 0.8557997880470599172, -47.37054680076701629, -7.156447707086194043 ) ) ;
#31596=CARTESIAN_POINT ( 'NONE',  ( 0.5809828226811565299, 28.72298383114543796, -38.32755012159114472 ) ) ;
#31602=CARTESIAN_POINT ( 'NONE',  ( 4.960156602257182357, -30.22163187094412251, 35.23783291257160499 ) ) ;
#31606=ORIENTED_EDGE ( 'NONE', *, *, #56242, .T. ) ;
#31608=CARTESIAN_POINT ( 'NONE',  ( 5.959828726073459926, 14.51699876360180141, 14.51059719297121831 ) ) ;
#31609=CONICAL_SURFACE ( 'NONE', #7576, 43.08621763946400307, 1.568696531533066763 ) ;
#31611=CARTESIAN_POINT ( 'NONE',  ( 0.5807400328401637335, 28.72484455891696697, -38.33001520688919328 ) ) ;
#31612=ORIENTED_EDGE ( 'NONE', *, *, #22135, .T. ) ;
#31617=CARTESIAN_POINT ( 'NONE',  ( 3.407937589446178528, 10.58239600294650451, -8.699069120706665714 ) ) ;
#31618=ORIENTED_EDGE ( 'NONE', *, *, #46789, .T. ) ;
#31620=ORIENTED_EDGE ( 'NONE', *, *, #32544, .F. ) ;
#31625=VECTOR ( 'NONE', #7757, 1000.000000000000000 ) ;
#31627=CARTESIAN_POINT ( 'NONE',  ( 5.958863334805807099, -19.82657410201439063, -5.311251202228782553 ) ) ;
#31628=CARTESIAN_POINT ( 'NONE',  ( 0.5786265663353196143, 33.35675271369539274, 34.37803667029822918 ) ) ;
#31637=B_SPLINE_CURVE_WITH_KNOTS ( 'NONE', 3,
 ( #9263, #28372, #4541, #47807, #42810, #52479 ),
 .UNSPECIFIED., .F., .F.,
 ( 4, 2, 4 ),
 ( 1.511777545972668437E-16, 0.0002445252820015209787, 0.0004890505640028907112 ),
 .UNSPECIFIED. ) ;
#31648=CARTESIAN_POINT ( 'NONE',  ( 0.9745511491811738036, -34.24777528633303803, 25.84997388131846918 ) ) ;
#31656=FACE_OUTER_BOUND ( 'NONE', #55399, .T. ) ;
#31659=VECTOR ( 'NONE', #17381, 1000.000000000000227 ) ;
#31662=CARTESIAN_POINT ( 'NONE',  ( 0.5807400328401637335, -44.45848844984455184, 17.82553128098392392 ) ) ;
#31663=CARTESIAN_POINT ( 'NONE',  ( 5.959828726073459926, 19.82738831247205979, 5.308046411395318742 ) ) ;
#31666=CARTESIAN_POINT ( 'NONE',  ( 0.5819845079324661441, -29.51613512130358075, -37.72030202710103453 ) ) ;
#31675=CARTESIAN_POINT ( 'NONE',  ( 4.967162193818131399, -14.26841313271251543, -40.65506779172179108 ) ) ;
#31676=CARTESIAN_POINT ( 'NONE',  ( 2.624215991343608501, -25.21574086439734685, 40.85210347989523427 ) ) ;
#31678=EDGE_CURVE ( 'NONE', #19565, #9646, #31516, .T. ) ;
#31681=CARTESIAN_POINT ( 'NONE',  ( 5.965394784446458765, 12.50653125158985723, 16.27505370423085296 ) ) ;
#31687=EDGE_CURVE ( 'NONE', #45383, #3021, #37936, .T. ) ;
#31699=ORIENTED_EDGE ( 'NONE', *, *, #59314, .T. ) ;
#31702=B_SPLINE_CURVE_WITH_KNOTS ( 'NONE', 3,
 ( #857, #43494, #34698, #57856, #14984, #19070 ),
 .UNSPECIFIED., .F., .F.,
 ( 4, 2, 4 ),
 ( 1.528339392293451082E-16, 0.0002445252820015200571, 0.0004890505640028873502 ),
 .UNSPECIFIED. ) ;
#31714=FACE_OUTER_BOUND ( 'NONE', #55794, .T. ) ;
#31716=CARTESIAN_POINT ( 'NONE',  ( 5.860006189529234355, -31.81514841426733042, -36.25227510158496358 ) ) ;
#31723=CARTESIAN_POINT ( 'NONE',  ( 0.9756354156337464500, -16.54067710771387922, 39.59221474545856978 ) ) ;
#31727=B_SPLINE_CURVE_WITH_KNOTS ( 'NONE', 3,
 ( #25780, #39912, #27323, #31100, #2261, #12318, #41452, #16700, #26395, #60822, #3195, #31723, #46151, #40525, #50814, #17017, #51417, #7581, #36134 ),
 .UNSPECIFIED., .F., .F.,
 ( 4, 3, 3, 3, 3, 3, 4 ),
 ( 3.469446951953614189E-18, 0.0002724573126191747797, 0.0004086839781548505372, 0.0005449106435901899430, 0.0006811373090491522168, 0.0008459866663933644955, 0.001010840725717214884 ),
 .UNSPECIFIED. ) ;
#31728=EDGE_CURVE ( 'NONE', #33861, #39282, #7943, .T. ) ;
#31738=CARTESIAN_POINT ( 'NONE',  ( 0.9972139404380304661, 42.62325912566431185, 4.947665363828915197 ) ) ;
#31741=VECTOR ( 'NONE', #49171, 1000.000000000000000 ) ;
#31746=ORIENTED_EDGE ( 'NONE', *, *, #48242, .T. ) ;
#31759=( BOUNDED_SURFACE ( )  B_SPLINE_SURFACE ( 3, 1, ( 
 ( #53063, #5435 ),
 ( #24573, #27930 ),
 ( #32954, #23526 ),
 ( #61112, #50263 ) ),
 .UNSPECIFIED., .F., .F., .F. ) 
 B_SPLINE_SURFACE_WITH_KNOTS ( ( 4, 4 ),
 ( 2, 2 ),
 ( 0.000000000000000000, 1.000000000000000000 ),
 ( 0.000000000000000000, 1.000000000000000000 ),
 .UNSPECIFIED. ) 
 GEOMETRIC_REPRESENTATION_ITEM ( )  RATIONAL_B_SPLINE_SURFACE ( (
 ( 1.000000000000000000, 1.000000000000000000),
 ( 0.9732289882329797637, 0.9999525324661233672),
 ( 0.9732289882329797637, 0.9999525324661233672),
 ( 1.000000000000000000, 1.000000000000000000) ) ) 
 REPRESENTATION_ITEM ( '' )  SURFACE ( )  );
#31761=ORIENTED_EDGE ( 'NONE', *, *, #9635, .T. ) ;
#31762=ORIENTED_EDGE ( 'NONE', *, *, #57273, .T. ) ;
#31763=CARTESIAN_POINT ( 'NONE',  ( 0.5819845079324652559, 47.89381220525411464, -0.4540594263154777988 ) ) ;
#31765=EDGE_CURVE ( 'NONE', #5485, #17533, #8622, .T. ) ;
#31766=FACE_OUTER_BOUND ( 'NONE', #52689, .T. ) ;
#31770=ORIENTED_EDGE ( 'NONE', *, *, #60144, .T. ) ;
#31771=CARTESIAN_POINT ( 'NONE',  ( 5.974727161628369032, -20.34732802718245281, -2.694421823322846965 ) ) ;
#31772=DIRECTION ( 'NONE',  ( 0.000000000000000000, 0.000000000000000000, 1.000000000000000000 ) ) ;
#31773=EDGE_CURVE ( 'NONE', #24092, #26757, #20713, .T. ) ;
#31777=CARTESIAN_POINT ( 'NONE',  ( 0.5786265663353196143, -41.11783955080221631, -24.57327059187441520 ) ) ;
#31786=CARTESIAN_POINT ( 'NONE',  ( 0.9754402186311939005, -30.47320128434239805, -30.20795797590429999 ) ) ;
#31789=VERTEX_POINT ( 'NONE', #61846 ) ;
#31790=CARTESIAN_POINT ( 'NONE',  ( 0.5807400328401637335, -18.83234461715150942, -44.04145271122585115 ) ) ;
#31797=AXIS2_PLACEMENT_3D ( 'NONE', #51337, #13157, #41664 ) ;
#31805=B_SPLINE_CURVE_WITH_KNOTS ( 'NONE', 3,
 ( #61208, #42754, #43373, #4490, #9216, #33658 ),
 .UNSPECIFIED., .F., .F.,
 ( 4, 2, 4 ),
 ( 8.148123767742043513E-18, 0.0002291978881530196295, 0.0004583957763060310733 ),
 .UNSPECIFIED. ) ;
#31806=CARTESIAN_POINT ( 'NONE',  ( 0.5809828226811553087, -6.791453954330003207, -47.41188724015886180 ) ) ;
#31807=CARTESIAN_POINT ( 'NONE',  ( 4.967162193818130511, -8.839793687085512275, 42.16965968614191240 ) ) ;
#31810=EDGE_LOOP ( 'NONE', ( #28452, #41811, #3701, #43762 ) ) ;
#31812=CARTESIAN_POINT ( 'NONE',  ( -17.83651567053104969, -12.32233744059949387, -2.099999999999997868 ) ) ;
#31813=LINE ( 'NONE', #12716, #38417 ) ;
#31815=CARTESIAN_POINT ( 'NONE',  ( 0.5809828226811617480, -44.45562576850614533, 17.82437196699665094 ) ) ;
#31822=VECTOR ( 'NONE', #17253, 1000.000000000000227 ) ;
#31824=CARTESIAN_POINT ( 'NONE',  ( 0.8551540677456739292, 11.51835730326480345, 46.51172240253124812 ) ) ;
#31825=ORIENTED_EDGE ( 'NONE', *, *, #57631, .F. ) ;
#31828=CARTESIAN_POINT ( 'NONE',  ( 4.303969348037258058, -42.70173985163801689, -22.16169334783882050 ) ) ;
#31835=VERTEX_POINT ( 'NONE', #5454 ) ;
#31839=EDGE_CURVE ( 'NONE', #11505, #46408, #24591, .T. ) ;
#31857=EDGE_CURVE ( 'NONE', #25296, #44894, #2714, .T. ) ;
#31858=ORIENTED_EDGE ( 'NONE', *, *, #25432, .F. ) ;
#31861=CARTESIAN_POINT ( 'NONE',  ( 0.5827359174754830340, 41.29633904010511714, 24.26188383263383130 ) ) ;
#31885=EDGE_CURVE ( 'NONE', #26419, #39143, #16164, .T. ) ;
#31889=CARTESIAN_POINT ( 'NONE',  ( 0.8551540677456715978, 19.17641535420913002, -43.91216198251520098 ) ) ;
#31894=CARTESIAN_POINT ( 'NONE',  ( 5.965394784446460541, -12.50653125159019474, 16.27505370423059716 ) ) ;
#31898=CARTESIAN_POINT ( 'NONE',  ( 0.9745511491811745808, -39.77127619790150703, 16.10518088436892725 ) ) ;
#31908=VERTEX_POINT ( 'NONE', #22949 ) ;
#31916=CARTESIAN_POINT ( 'NONE',  ( 0.8551540677456715978, -34.52115452272952467, 33.23105123575887632 ) ) ;
#31918=ORIENTED_EDGE ( 'NONE', *, *, #27036, .F. ) ;
#31921=CARTESIAN_POINT ( 'NONE',  ( 4.956653778116966613, 48.02038484091100656, 2.599733001514495712 ) ) ;
#31922=VECTOR ( 'NONE', #41112, 1000.000000000000114 ) ;
#31923=CARTESIAN_POINT ( 'NONE',  ( 0.8557997880470690211, -44.60232077416674201, -17.48760788519264153 ) ) ;
#31926=DIRECTION ( 'NONE',  ( -1.000000000000000000, -0.000000000000000000, -0.000000000000000000 ) ) ;
#31930=EDGE_CURVE ( 'NONE', #61413, #11680, #13965, .T. ) ;
#31944=CARTESIAN_POINT ( 'NONE',  ( 5.960221823109900008, -14.51763960716768409, -14.50993159119805931 ) ) ;
#31946=CARTESIAN_POINT ( 'NONE',  ( 4.960156602257182357, -38.31207700265973415, 26.21519897043416236 ) ) ;
#31950=EDGE_LOOP ( 'NONE', ( #22431, #34715, #23736, #36492 ) ) ;
#31965=CARTESIAN_POINT ( 'NONE',  ( 1.227938101723756947, -0.8460948827222184443, -42.91134962331487657 ) ) ;
#31972=CARTESIAN_POINT ( 'NONE',  ( -48.95476116535499500, 0.000000000000000000, 0.000000000000000000 ) ) ;
#31974=CARTESIAN_POINT ( 'NONE',  ( 1.227938101723748288, -17.20315230597871903, 39.32113113558960293 ) ) ;
#31979=B_SPLINE_CURVE_WITH_KNOTS ( 'NONE', 3,
 ( #56446, #8849, #19194, #52362, #9455, #23876 ),
 .UNSPECIFIED., .F., .F.,
 ( 4, 2, 4 ),
 ( 9.543442895606953578E-18, 0.0002291978881530156180, 0.0004583957763060216950 ),
 .UNSPECIFIED. ) ;
#31980=FACE_OUTER_BOUND ( 'NONE', #49564, .T. ) ;
#31988=CARTESIAN_POINT ( 'NONE',  ( 0.5832366564991503521, 46.33368520589916528, 12.13301812590366247 ) ) ;
#32010=ORIENTED_EDGE ( 'NONE', *, *, #22204, .T. ) ;
#32022=CARTESIAN_POINT ( 'NONE',  ( 0.9752132459055870006, -42.90780255730422255, 0.2329632697542413367 ) ) ;
#32023=ORIENTED_EDGE ( 'NONE', *, *, #22606, .F. ) ;
#32026=EDGE_LOOP ( 'NONE', ( #10012, #46442, #60191, #5411 ) ) ;
#32034=EDGE_LOOP ( 'NONE', ( #48438, #8471, #42058, #28506 ) ) ;
#32038=EDGE_CURVE ( 'NONE', #49001, #39397, #8713, .T. ) ;
#32040=LINE ( 'NONE', #42076, #15787 ) ;
#32051=CARTESIAN_POINT ( 'NONE',  ( 0.5807400328401637335, -11.87003418057209636, -46.40483864045158668 ) ) ;
#32056=CARTESIAN_POINT ( 'NONE',  ( 5.960721111146673579, 10.26825948882926021, -17.77250458025982027 ) ) ;
#32063=EDGE_LOOP ( 'NONE', ( #49535, #3905, #42425, #46984 ) ) ;
#32065=CARTESIAN_POINT ( 'NONE',  ( 4.956653778116966613, 0.000000000000000000, 0.000000000000000000 ) ) ;
#32067=EDGE_CURVE ( 'NONE', #6622, #56918, #55375, .T. ) ;
#32075=VERTEX_POINT ( 'NONE', #7340 ) ;
#32078=CARTESIAN_POINT ( 'NONE',  ( 3.407937589446178528, 11.14158115674373484, 7.970324840161996605 ) ) ;
#32079=CARTESIAN_POINT ( 'NONE',  ( 0.9758171775293928984, -41.44488232057073418, 11.11125068417978135 ) ) ;
#32081=CARTESIAN_POINT ( 'NONE',  ( 5.960721111146673579, -20.34914600876573587, -2.685391721745965299 ) ) ;
#32086=EDGE_LOOP ( 'NONE', ( #52526, #1114, #42280, #8636 ) ) ;
#32087=ORIENTED_EDGE ( 'NONE', *, *, #29580, .F. ) ;
#32088=CARTESIAN_POINT ( 'NONE',  ( 1.088908134280559104, -29.78762923589991019, 30.89124834763379113 ) ) ;
#32090=CARTESIAN_POINT ( 'NONE',  ( 0.5819845079324659221, 44.07435181061364204, -18.74766465427176598 ) ) ;
#32091=CARTESIAN_POINT ( 'NONE',  ( 0.9722240750034545353, 16.95645446544487456, 39.41582016107707176 ) ) ;
#32096=DIRECTION ( 'NONE',  ( -0.07439287786467650709, 0.3693942911085772440, -0.9262902123089734596 ) ) ;
#32100=ORIENTED_EDGE ( 'NONE', *, *, #54625, .F. ) ;
#32103=CARTESIAN_POINT ( 'NONE',  ( 0.9757787079277443487, 30.31292661677494493, 30.36877398309911769 ) ) ;
#32104=CARTESIAN_POINT ( 'NONE',  ( 1.227938101723748288, 33.52879263017863565, 26.79402671879338271 ) ) ;
#32113=CARTESIAN_POINT ( 'NONE',  ( 0.9752570700956806338, 42.90785210525868365, 0.2306661201222729995 ) ) ;
#32114=CARTESIAN_POINT ( 'NONE',  ( 0.9758171775293909000, -5.606549717953911660, -42.54062484958063095 ) ) ;
#32122=CARTESIAN_POINT ( 'NONE',  ( 0.5786265663353153954, -41.83999636203303396, -23.32245830379073226 ) ) ;
#32137=CARTESIAN_POINT ( 'NONE',  ( 0.6067099128993189705, -37.56352526808326786, 29.71710940500716447 ) ) ;
#32150=CARTESIAN_POINT ( 'NONE',  ( 5.960221823109900008, -20.34928172836728777, -2.684531185214347193 ) ) ;
#32152=B_SPLINE_CURVE_WITH_KNOTS ( 'NONE', 3,
 ( #14772, #10683, #39837, #48577 ),
 .UNSPECIFIED., .F., .F.,
 ( 4, 4 ),
 ( 1.084202172485504434E-19, 0.004444878191957696463 ),
 .UNSPECIFIED. ) ;
#32156=B_SPLINE_CURVE_WITH_KNOTS ( 'NONE', 3,
 ( #20717, #44550, #58278, #48293, #19488, #44241, #39857, #53893, #38605, #11019, #5043, #15408, #15722, #43937, #20108, #29795, #25099, #38925, #58911, #58585, #34828, #48908, #39535, #5957, #33903, #39228, #16025, #14790, #54195, #43309 ),
 .UNSPECIFIED., .F., .F.,
 ( 4, 2, 2, 2, 2, 2, 2, 2, 2, 2, 2, 2, 2, 2, 4 ),
 ( 0.000000000000000000, 0.0004121561524868821188, 0.0008243123049737642377, 0.001236468457460646302, 0.001648624609947528042, 0.002472936914921291304, 0.002885093067408174561, 0.003297249219895058252, 0.003709405372381941943, 0.004121561524868825634, 0.004945873829842592148, 0.005358029982329475839, 0.005770186134816359530, 0.006182342287303243221, 0.006594498439790126912 ),
 .UNSPECIFIED. ) ;
#32175=CARTESIAN_POINT ( 'NONE',  ( 4.963659409799330291, 44.68724496494571241, 2.450325214228553428 ) ) ;
#32183=CARTESIAN_POINT ( 'NONE',  ( -20.00694009185712119, -12.48893006068259837, 0.5428783724460725102 ) ) ;
#32191=EDGE_CURVE ( 'NONE', #24422, #22241, #31805, .T. ) ;
#32194=ADVANCED_FACE ( 'NONE', ( #61814 ), #33048, .F. ) ;
#32196=CARTESIAN_POINT ( 'NONE',  ( 0.5809828226811565299, 28.72298383114543796, -38.32755012159114472 ) ) ;
#32197=CARTESIAN_POINT ( 'NONE',  ( 5.965394784446458765, -2.693446924985486657, -20.34787558161485777 ) ) ;
#32199=B_SPLINE_CURVE_WITH_KNOTS ( 'NONE', 3,
 ( #37444, #8590, #18021, #51815 ),
 .UNSPECIFIED., .F., .F.,
 ( 4, 4 ),
 ( 3.252606517456513302E-19, 0.004444878191957676514 ),
 .UNSPECIFIED. ) ;
#32200=CARTESIAN_POINT ( 'NONE',  ( 5.959828726073459926, -10.26672511661743670, -17.77343634131838002 ) ) ;
#32207=FACE_OUTER_BOUND ( 'NONE', #35640, .T. ) ;
#32211=CARTESIAN_POINT ( 'NONE',  ( 5.860006189529246790, -21.31760477694550460, -43.26650951066891793 ) ) ;
#32212=EDGE_CURVE ( 'NONE', #28122, #47245, #14617, .T. ) ;
#32217=EDGE_CURVE ( 'NONE', #36286, #31306, #410, .T. ) ;
#32222=CARTESIAN_POINT ( 'NONE',  ( 1.154321713695932727, -29.75729669971086722, -30.92445811446677340 ) ) ;
#32228=CARTESIAN_POINT ( 'NONE',  ( 4.967162193818130511, 42.96271701169388990, -3.259922920617310371 ) ) ;
#32233=CARTESIAN_POINT ( 'NONE',  ( 1.227938101723756947, 39.32113113558990847, -17.20315230597801914 ) ) ;
#32241=VECTOR ( 'NONE', #34142, 1000.000000000000000 ) ;
#32252=B_SPLINE_CURVE_WITH_KNOTS ( 'NONE', 3,
 ( #57170, #14304, #24300, #29921, #52487, #9900, #58100, #29608, #39046, #42816, #33410, #10828, #475, #48115, #38421, #29002, #44066, #43435, #34031 ),
 .UNSPECIFIED., .F., .F.,
 ( 4, 3, 3, 3, 3, 3, 4 ),
 ( 5.204170427930421283E-18, 0.0002724573126191775444, 0.0004086839781548478809, 0.0005449106435901823536, 0.0006811373090491453864, 0.0008459866663933667723, 0.001010840725717211197 ),
 .UNSPECIFIED. ) ;
#32254=DIRECTION ( 'NONE',  ( 0.07836865515943411409, 0.9873352307081162405, 0.1379401902675667646 ) ) ;
#32256=CARTESIAN_POINT ( 'NONE',  ( 0.9730545539215883499, 11.59290486963506517, 41.31259007387235727 ) ) ;
#32261=CARTESIAN_POINT ( 'NONE',  ( 0.9730545539215883499, 11.59290486963565137, -41.31259007387218674 ) ) ;
#32268=CARTESIAN_POINT ( 'NONE',  ( 0.5827357941260213892, 47.53228940613941234, 5.891356987507786691 ) ) ;
#32271=CARTESIAN_POINT ( 'NONE',  ( 0.9758171775293921213, -34.03798695362329596, 26.12572690811900600 ) ) ;
#32273=B_SPLINE_CURVE_WITH_KNOTS ( 'NONE', 3,
 ( #6993, #12058, #16738, #16424 ),
 .UNSPECIFIED., .F., .F.,
 ( 4, 4 ),
 ( 2.909219710836648185E-18, 0.004050076154993001616 ),
 .UNSPECIFIED. ) ;
#32281=ADVANCED_FACE ( 'NONE', ( #49513 ), #30272, .F. ) ;
#32283=CARTESIAN_POINT ( 'NONE',  ( 0.5839879882012665169, 6.251648354650867212, -47.48621496524027208 ) ) ;
#32289=CARTESIAN_POINT ( 'NONE',  ( 2.281448460670571166, -43.80196084514292210, 19.56578495220155389 ) ) ;
#32291=CARTESIAN_POINT ( 'NONE',  ( 0.8557997880470697982, 34.51495345639548873, 33.22501220301912639 ) ) ;
#32300=VERTEX_POINT ( 'NONE', #1889 ) ;
#32301=CARTESIAN_POINT ( 'NONE',  ( 5.981074661064941900, -19.82752479807530932, 5.303881226583333941 ) ) ;
#32304=CARTESIAN_POINT ( 'NONE',  ( 4.967162193818130511, -40.93989340068600313, -13.42934394584206359 ) ) ;
#32307=ORIENTED_EDGE ( 'NONE', *, *, #29968, .F. ) ;
#32310=EDGE_LOOP ( 'NONE', ( #16654, #2841, #2495, #15624 ) ) ;
#32325=CARTESIAN_POINT ( 'NONE',  ( 4.960156602257184133, 20.99019478193049792, 41.40608197274642066 ) ) ;
#32328=VECTOR ( 'NONE', #56002, 1000.000000000000114 ) ;
#32336=CARTESIAN_POINT ( 'NONE',  ( 0.8557997880470697982, 24.73961900479251952, 41.02602466100786671 ) ) ;
#32338=EDGE_CURVE ( 'NONE', #10841, #10038, #56406, .T. ) ;
#32347=B_SPLINE_CURVE_WITH_KNOTS ( 'NONE', 3,
 ( #19413, #32902, #9069, #38530 ),
 .UNSPECIFIED., .F., .F.,
 ( 4, 4 ),
 ( 1.962615573354718958E-17, 0.005004741218457442291 ),
 .UNSPECIFIED. ) ;
#32359=CARTESIAN_POINT ( 'NONE',  ( 0.9754642270333697684, 37.07163437210445522, 21.60621846558649040 ) ) ;
#32366=ORIENTED_EDGE ( 'NONE', *, *, #51654, .T. ) ;
#32368=CARTESIAN_POINT ( 'NONE',  ( 0.5839254288179560604, 23.86932519546729381, 41.52446060675833195 ) ) ;
#32369=CARTESIAN_POINT ( 'NONE',  ( 0.8557997880470697982, 37.44587306708137930, -29.88293891557432858 ) ) ;
#32378=CARTESIAN_POINT ( 'NONE',  ( 0.9757787079277443487, -11.06737752163067334, -41.45659305953932972 ) ) ;
#32380=CARTESIAN_POINT ( 'NONE',  ( 0.9741495583595178864, -41.54695848110004874, 10.72301204857641643 ) ) ;
#32383=EDGE_CURVE ( 'NONE', #3369, #42030, #60139, .T. ) ;
#32387=B_SPLINE_CURVE_WITH_KNOTS ( 'NONE', 3,
 ( #22173, #56593, #26868, #13711 ),
 .UNSPECIFIED., .F., .F.,
 ( 4, 4 ),
 ( 4.336808689942017736E-19, 0.004444878191957683453 ),
 .UNSPECIFIED. ) ;
#32391=B_SPLINE_CURVE_WITH_KNOTS ( 'NONE', 3,
 ( #47728, #23918, #43048, #85 ),
 .UNSPECIFIED., .F., .F.,
 ( 4, 4 ),
 ( 5.485677294651095664E-18, 0.004050076154992997279 ),
 .UNSPECIFIED. ) ;
#32397=CARTESIAN_POINT ( 'NONE',  ( 1.227938101723756947, -29.74462687941247552, 30.94118573761302926 ) ) ;
#32398=ORIENTED_EDGE ( 'NONE', *, *, #22407, .T. ) ;
#32409=CARTESIAN_POINT ( 'NONE',  ( 4.967162193818130511, 0.000000000000000000, 0.000000000000000000 ) ) ;
#32411=CARTESIAN_POINT ( 'NONE',  ( 0.9756354156337445627, 30.24859376089824536, 30.43287766742259493 ) ) ;
#32414=ORIENTED_EDGE ( 'NONE', *, *, #45557, .T. ) ;
#32416=CARTESIAN_POINT ( 'NONE',  ( 5.958863334805807099, -10.26176968287932745, -17.77634700750925134 ) ) ;
#32430=CARTESIAN_POINT ( 'NONE',  ( 4.963659409799332067, 40.34793212403996421, -19.36487359954654508 ) ) ;
#32444=CARTESIAN_POINT ( 'NONE',  ( 5.965394784446460541, -5.326334832595787994, 19.82223131420045092 ) ) ;
#32445=VERTEX_POINT ( 'NONE', #41995 ) ;
#32451=CARTESIAN_POINT ( 'NONE',  ( 0.9752570700956822991, 41.38610171411352212, 11.32817567195924902 ) ) ;
#32455=CARTESIAN_POINT ( 'NONE',  ( 0.8551540677456715978, 47.61725548905990735, 5.348818140991062009 ) ) ;
#32458=AXIS2_PLACEMENT_3D ( 'NONE', #21610, #17844, #40750 ) ;
#32460=ORIENTED_EDGE ( 'NONE', *, *, #30838, .T. ) ;
#32461=EDGE_CURVE ( 'NONE', #40550, #35241, #55323, .T. ) ;
#32471=CIRCLE ( 'NONE', #5430, 48.09070567114147110 ) ;
#32474=CARTESIAN_POINT ( 'NONE',  ( 0.9756950546413931669, 0.09673755062796540738, 42.90834738653779823 ) ) ;
#32477=EDGE_CURVE ( 'NONE', #21542, #3021, #23471, .T. ) ;
#32479=CARTESIAN_POINT ( 'NONE',  ( 0.8551540677456739292, 29.88829867897867842, -37.45266983663464799 ) ) ;
#32482=CARTESIAN_POINT ( 'NONE',  ( 4.967162193818130511, 35.57684288742009215, -24.30453456948074376 ) ) ;
#32485=ORIENTED_EDGE ( 'NONE', *, *, #57022, .T. ) ;
#32497=CARTESIAN_POINT ( 'NONE',  ( 4.967162193818131399, 42.16965968614193372, 8.839793687085363061 ) ) ;
#32507=CARTESIAN_POINT ( 'NONE',  ( 0.9757892942422833338, 5.549787678908993271, -42.54806590760148310 ) ) ;
#32509=CARTESIAN_POINT ( 'NONE',  ( 5.959547316686252039, -10.26589671991350983, -17.77392908783930636 ) ) ;
#32511=CARTESIAN_POINT ( 'NONE',  ( 0.5836750258453337059, -47.89563095930320458, -0.1816059738421414715 ) ) ;
#32515=CARTESIAN_POINT ( 'NONE',  ( 0.6846871229502899947, 41.05093867799220675, -24.69859318104445833 ) ) ;
#32524=AXIS2_PLACEMENT_3D ( 'NONE', #5693, #24841, #16362 ) ;
#32529=CARTESIAN_POINT ( 'NONE',  ( 4.956653778117001252, 47.27023054223765541, -8.845409907520457082 ) ) ;
#32542=ORIENTED_EDGE ( 'NONE', *, *, #35946, .F. ) ;
#32544=EDGE_CURVE ( 'NONE', #10228, #28932, #15328, .T. ) ;
#32550=CARTESIAN_POINT ( 'NONE',  ( 0.5838002273316420521, -29.26514720557047156, 37.91535410490859448 ) ) ;
#32552=CARTESIAN_POINT ( 'NONE',  ( 0.9752570700956790795, 21.25416333281098957, 37.27462300504085135 ) ) ;
#32556=ORIENTED_EDGE ( 'NONE', *, *, #49452, .F. ) ;
#32562=CARTESIAN_POINT ( 'NONE',  ( 0.6846871229502932144, 47.60345020167359564, -5.395516691086709393 ) ) ;
#32563=CARTESIAN_POINT ( 'NONE',  ( 0.5839879327111914264, 29.22928252017514339, 37.94312859586424480 ) ) ;
#32566=CARTESIAN_POINT ( 'NONE',  ( 5.960721111146673579, 16.28787783074210438, 12.49016043756476790 ) ) ;
#32568=CARTESIAN_POINT ( 'NONE',  ( 0.9757892942422822236, 11.15510465569001575, 41.43309903783659109 ) ) ;
#32569=CARTESIAN_POINT ( 'NONE',  ( 0.8551540677456834771, -5.348818140991232539, 47.61725548905988603 ) ) ;
#32570=CARTESIAN_POINT ( 'NONE',  ( 0.9730545539215883499, 21.89037132892487847, -36.90443313492307453 ) ) ;
#32572=EDGE_LOOP ( 'NONE', ( #54057, #41425, #24305, #33382 ) ) ;
#32576=CARTESIAN_POINT ( 'NONE',  ( 2.624215991343608501, 13.78323291683847351, -45.98641578154015974 ) ) ;
#32579=( BOUNDED_SURFACE ( )  B_SPLINE_SURFACE ( 3, 1, ( 
 ( #4000, #60705 ),
 ( #31608, #4303 ),
 ( #13434, #3690 ),
 ( #42566, #46046 ) ),
 .UNSPECIFIED., .F., .F., .F. ) 
 B_SPLINE_SURFACE_WITH_KNOTS ( ( 4, 4 ),
 ( 2, 2 ),
 ( 0.000000000000000000, 1.000000000000000000 ),
 ( 0.000000000000000000, 1.000000000000000000 ),
 .UNSPECIFIED. ) 
 GEOMETRIC_REPRESENTATION_ITEM ( )  RATIONAL_B_SPLINE_SURFACE ( (
 ( 1.000000000000000000, 1.000000000000000000),
 ( 0.9953390228620291325, 0.8624445117761032620),
 ( 0.9953390228620291325, 0.8624445117761032620),
 ( 1.000000000000000000, 1.000000000000000000) ) ) 
 REPRESENTATION_ITEM ( '' )  SURFACE ( )  );
#32589=CARTESIAN_POINT ( 'NONE',  ( 4.956653778116991482, -21.75875759808677046, -42.88673967249153662 ) ) ;
#32599=CARTESIAN_POINT ( 'NONE',  ( 0.8557997880470690211, -43.90420959842193582, 19.17299735371994629 ) ) ;
#32601=CARTESIAN_POINT ( 'NONE',  ( 0.5839879327111922036, 46.28746210677714146, 12.30864801674728604 ) ) ;
#32610=LINE ( 'NONE', #23204, #8041 ) ;
#32614=ORIENTED_EDGE ( 'NONE', *, *, #54814, .T. ) ;
#32615=AXIS2_PLACEMENT_3D ( 'NONE', #31972, #41385, #22874 ) ;
#32628=ORIENTED_EDGE ( 'NONE', *, *, #19420, .F. ) ;
#32629=CARTESIAN_POINT ( 'NONE',  ( 0.9749527285493303497, -16.15611883305616203, -39.75066842359304076 ) ) ;
#32635=CARTESIAN_POINT ( 'NONE',  ( 0.6846871229502899947, 13.23224427737829245, 46.04462816497493094 ) ) ;
#32637=DIRECTION ( 'NONE',  ( -1.000000000000000000, -0.000000000000000000, -0.000000000000000000 ) ) ;
#32645=CARTESIAN_POINT ( 'NONE',  ( 4.967162193818130511, -28.74031574030035685, 32.10009971360062764 ) ) ;
#32649=ORIENTED_EDGE ( 'NONE', *, *, #33170, .F. ) ;
#32651=CIRCLE ( 'NONE', #40675, 43.08621763946400307 ) ;
#32652=CARTESIAN_POINT ( 'NONE',  ( 5.960221823109900008, 17.77840967225720448, -10.25807604135603235 ) ) ;
#32654=CARTESIAN_POINT ( 'NONE',  ( 0.5837374860065642768, -44.31936661703457503, -18.16107481025645498 ) ) ;
#32656=B_SPLINE_CURVE_WITH_KNOTS ( 'NONE', 3,
 ( #5768, #44058, #1086, #27066, #31454, #7631 ),
 .UNSPECIFIED., .F., .F.,
 ( 4, 2, 4 ),
 ( 0.000000000000000000, 0.0002291966416970791327, 0.0004583932833941582654 ),
 .UNSPECIFIED. ) ;
#32659=EDGE_CURVE ( 'NONE', #22415, #5939, #20592, .T. ) ;
#32664=CARTESIAN_POINT ( 'NONE',  ( 5.960221823109900008, 19.82761049839341894, -5.307149561567879203 ) ) ;
#32666=CARTESIAN_POINT ( 'NONE',  ( 1.227938101723756947, 33.52879263017899092, -26.79402671879293507 ) ) ;
#32667=CARTESIAN_POINT ( 'NONE',  ( 2.281351352603289584, -1.314116150903787084, 47.95523304704244083 ) ) ;
#32673=CARTESIAN_POINT ( 'NONE',  ( 1.154321485836935279, 11.90271791109313071, 41.23280395520811226 ) ) ;
#32674=CARTESIAN_POINT ( 'NONE',  ( 0.9758171775293918992, 39.64453667157746253, 16.41489794146139758 ) ) ;
#32680=ORIENTED_EDGE ( 'NONE', *, *, #40265, .F. ) ;
#32681=CARTESIAN_POINT ( 'NONE',  ( 0.5809828226811617480, -34.25055090842177208, 33.48000389720603920 ) ) ;
#32693=ORIENTED_EDGE ( 'NONE', *, *, #55429, .T. ) ;
#32704=ORIENTED_EDGE ( 'NONE', *, *, #32868, .F. ) ;
#32710=LINE ( 'NONE', #51792, #12667 ) ;
#32723=ORIENTED_EDGE ( 'NONE', *, *, #33216, .F. ) ;
#32725=CARTESIAN_POINT ( 'NONE',  ( 5.960721111146673579, 18.96557324978276071, 7.848955554238579602 ) ) ;
#32726=CARTESIAN_POINT ( 'NONE',  ( 4.963659409799332067, 36.94443854030220109, 25.25989740981512099 ) ) ;
#32733=CARTESIAN_POINT ( 'NONE',  ( 0.9754642270333693244, 42.90808635884410194, 0.1757168848620660473 ) ) ;
#32735=CARTESIAN_POINT ( 'NONE',  ( 4.963659409799328515, -9.199077662859210136, 43.79875484948445319 ) ) ;
#32736=AXIS2_PLACEMENT_3D ( 'NONE', #28829, #35097, #47951 ) ;
#32738=CARTESIAN_POINT ( 'NONE',  ( 0.5809828226811617480, -6.791453954330657794, 47.41188724015877654 ) ) ;
#32743=CARTESIAN_POINT ( 'NONE',  ( 4.956653778116992370, 21.75875759808766929, -42.88673967249108188 ) ) ;
#32748=EDGE_CURVE ( 'NONE', #12007, #448, #12283, .T. ) ;
#32749=DIRECTION ( 'NONE',  ( -1.000000000000000000, -0.000000000000000000, -0.000000000000000000 ) ) ;
#32758=CARTESIAN_POINT ( 'NONE',  ( 1.088908134280556661, -42.90644581410504799, 0.7803765577540302534 ) ) ;
#32760=CARTESIAN_POINT ( 'NONE',  ( 0.7057020205114954425, 17.55108080125446435, 44.57024707370717209 ) ) ;
#32765=CONICAL_SURFACE ( 'NONE', #3698, 43.08621763946400307, 1.568696531533066763 ) ;
#32768=CARTESIAN_POINT ( 'NONE',  ( 0.9749527285493307938, 41.37154756071291928, 11.38116287125068204 ) ) ;
#32770=AXIS2_PLACEMENT_3D ( 'NONE', #52442, #32749, #18966 ) ;
#32771=DIRECTION ( 'NONE',  ( -1.000000000000000000, -0.000000000000000000, -0.000000000000000000 ) ) ;
#32774=EDGE_CURVE ( 'NONE', #44156, #23013, #33252, .T. ) ;
#32777=EDGE_CURVE ( 'NONE', #27088, #57237, #28675, .T. ) ;
#32780=EDGE_LOOP ( 'NONE', ( #60138, #21419, #46043, #21771 ) ) ;
#32781=CARTESIAN_POINT ( 'NONE',  ( 4.967162193818130511, 13.42934394584164082, 40.93989340068615945 ) ) ;
#32782=CARTESIAN_POINT ( 'NONE',  ( 4.967162193818130511, 0.000000000000000000, 0.000000000000000000 ) ) ;
#32789=CARTESIAN_POINT ( 'NONE',  ( 0.9968887458511642707, 15.81144734640186833, 39.89008038581149407 ) ) ;
#32791=VERTEX_POINT ( 'NONE', #36595 ) ;
#32792=VERTEX_POINT ( 'NONE', #32196 ) ;
#32806=CARTESIAN_POINT ( 'NONE',  ( 0.5809828226811617480, -0.5448590168535863976, 47.89273459658653564 ) ) ;
#32813=CARTESIAN_POINT ( 'NONE',  ( 1.227938101723748288, 26.79402671879374864, -33.52879263017835143 ) ) ;
#32824=CARTESIAN_POINT ( 'NONE',  ( 0.8551540677456739292, 5.348818140990903025, 47.61725548905992156 ) ) ;
#32846=ORIENTED_EDGE ( 'NONE', *, *, #56242, .F. ) ;
#32847=FACE_OUTER_BOUND ( 'NONE', #38076, .T. ) ;
#32851=CARTESIAN_POINT ( 'NONE',  ( -20.05974703543239457, -7.996306382744656993, -0.2778595553339769930 ) ) ;
#32854=CARTESIAN_POINT ( 'NONE',  ( 1.227938101723756947, -11.92353943227920610, -41.23019537246722876 ) ) ;
#32856=ORIENTED_EDGE ( 'NONE', *, *, #61189, .T. ) ;
#32862=CARTESIAN_POINT ( 'NONE',  ( 4.956653778116988818, -45.35992544608517818, -15.97476558431931082 ) ) ;
#32863=ORIENTED_EDGE ( 'NONE', *, *, #13734, .T. ) ;
#32864=CARTESIAN_POINT ( 'NONE',  ( 0.8557997880470697982, -41.93815086860240626, -23.15977007032367041 ) ) ;
#32865=DIRECTION ( 'NONE',  ( 0.000000000000000000, 0.000000000000000000, 1.000000000000000000 ) ) ;
#32868=EDGE_CURVE ( 'NONE', #14241, #58875, #51857, .T. ) ;
#32877=CARTESIAN_POINT ( 'NONE',  ( 0.9730545539215883499, -42.47233286818612896, -6.101350888305089093 ) ) ;
#32881=CARTESIAN_POINT ( 'NONE',  ( 0.8557997880470697982, 46.50333260518559086, 11.51622788066474534 ) ) ;
#32884=CARTESIAN_POINT ( 'NONE',  ( 0.9749527285493296835, 0.2856147164664618043, -42.90750796893249941 ) ) ;
#32887=EDGE_LOOP ( 'NONE', ( #3039, #49319, #50355, #53490 ) ) ;
#32889=ORIENTED_EDGE ( 'NONE', *, *, #12606, .F. ) ;
#32893=DIRECTION ( 'NONE',  ( 0.07836865515943412797, 0.4916162952473433490, 0.8672783706145211768 ) ) ;
#32899=CARTESIAN_POINT ( 'NONE',  ( 4.956653778116968390, 48.02038484091101367, -2.599733001514498376 ) ) ;
#32900=EDGE_CURVE ( 'NONE', #46035, #49237, #33748, .T. ) ;
#32902=CARTESIAN_POINT ( 'NONE',  ( 4.960156602257181468, 34.56254177294268004, 30.99165383632775672 ) ) ;
#32903=ORIENTED_EDGE ( 'NONE', *, *, #25759, .F. ) ;
#32905=CARTESIAN_POINT ( 'NONE',  ( 5.960721111146673579, -20.35079619394244332, -2.672857320903232470 ) ) ;
#32911=CARTESIAN_POINT ( 'NONE',  ( 0.5819845901640506858, -12.83441129068565445, 46.14435291605025924 ) ) ;
#32912=CARTESIAN_POINT ( 'NONE',  ( 0.8551540677456715978, -46.03951182599418246, -13.28067116677250503 ) ) ;
#32917=ORIENTED_EDGE ( 'NONE', *, *, #10696, .T. ) ;
#32918=VECTOR ( 'NONE', #32096, 1000.000000000000114 ) ;
#32926=ORIENTED_EDGE ( 'NONE', *, *, #16407, .F. ) ;
#32928=CARTESIAN_POINT ( 'NONE',  ( 4.956653778116990594, 2.599733001515011743, -48.02038484091096393 ) ) ;
#32934=ORIENTED_EDGE ( 'NONE', *, *, #6009, .T. ) ;
#32953=CARTESIAN_POINT ( 'NONE',  ( 0.5832367798473377940, -33.67436043247238331, -34.05962365606854547 ) ) ;
#32954=CARTESIAN_POINT ( 'NONE',  ( 5.958863334805807099, 12.49619391867160445, 16.28335246510371448 ) ) ;
#32958=AXIS2_PLACEMENT_3D ( 'NONE', #35392, #924, #25660 ) ;
#32965=CARTESIAN_POINT ( 'NONE',  ( 1.227938101723747621, -20.72293514920724533, -37.58536632582800507 ) ) ;
#32968=ORIENTED_EDGE ( 'NONE', *, *, #31347, .F. ) ;
#32970=CARTESIAN_POINT ( 'NONE',  ( 0.5786265663353153954, 38.43785771743204549, 28.58414684753499557 ) ) ;
#32971=( BOUNDED_SURFACE ( )  B_SPLINE_SURFACE ( 3, 1, ( 
 ( #18846, #61403 ),
 ( #58175, #9417 ),
 ( #20007, #15300 ),
 ( #24685, #29377 ) ),
 .UNSPECIFIED., .F., .F., .F. ) 
 B_SPLINE_SURFACE_WITH_KNOTS ( ( 4, 4 ),
 ( 2, 2 ),
 ( 0.000000000000000000, 1.000000000000000000 ),
 ( 0.000000000000000000, 1.000000000000000000 ),
 .UNSPECIFIED. ) 
 GEOMETRIC_REPRESENTATION_ITEM ( )  RATIONAL_B_SPLINE_SURFACE ( (
 ( 1.000000000000000000, 1.000000000000000000),
 ( 0.7269869731126821222, 0.9931720237060910339),
 ( 0.7269869731126821222, 0.9931720237060910339),
 ( 1.000000000000000000, 1.000000000000000000) ) ) 
 REPRESENTATION_ITEM ( '' )  SURFACE ( )  );
#32975=CARTESIAN_POINT ( 'NONE',  ( 3.407937589446178528, -6.447869442558249453, 12.08659953757606864 ) ) ;
#32976=CARTESIAN_POINT ( 'NONE',  ( 0.5832366564991501301, -46.19265750221180156, 12.65934068133968360 ) ) ;
#32978=LINE ( 'NONE', #48292, #12866 ) ;
#32981=FACE_OUTER_BOUND ( 'NONE', #60796, .T. ) ;
#32983=CARTESIAN_POINT ( 'NONE',  ( 0.9756008150404602564, 30.24019526051588258, -30.44122083654187705 ) ) ;
#32986=CARTESIAN_POINT ( 'NONE',  ( 5.958863334805807099, -7.853699934219767975, -18.96369761673816967 ) ) ;
#32991=CARTESIAN_POINT ( 'NONE',  ( 0.9740398440564321803, 39.79907313245131917, 16.03656236596764373 ) ) ;
#32993=EDGE_CURVE ( 'NONE', #61588, #28220, #49640, .T. ) ;
#32994=CARTESIAN_POINT ( 'NONE',  ( 4.956653778116966613, 0.000000000000000000, 0.000000000000000000 ) ) ;
#32999=CARTESIAN_POINT ( 'NONE',  ( 0.5834872094924158370, -34.02770606800785202, 33.70665904794278589 ) ) ;
#33007=CARTESIAN_POINT ( 'NONE',  ( 5.959547316686252039, 7.858107265727477753, 18.96183906913546480 ) ) ;
#33013=CARTESIAN_POINT ( 'NONE',  ( 0.9730545539215883499, 11.59290486963565137, -41.31259007387218674 ) ) ;
#33017=CARTESIAN_POINT ( 'NONE',  ( 4.303969348037258058, 25.89994482339369952, 40.54345935592787953 ) ) ;
#33024=VECTOR ( 'NONE', #22402, 1000.000000000000114 ) ;
#33028=CARTESIAN_POINT ( 'NONE',  ( 0.9736507210033062965, -0.4504567742783994189, 42.90603603725247694 ) ) ;
#33031=ORIENTED_EDGE ( 'NONE', *, *, #44663, .T. ) ;
#33032=DIRECTION ( 'NONE',  ( 0.000000000000000000, 0.000000000000000000, 1.000000000000000000 ) ) ;
#33036=CARTESIAN_POINT ( 'NONE',  ( 4.956653778116980824, -40.28700667097698584, 26.26162724282358951 ) ) ;
#33037=CARTESIAN_POINT ( 'NONE',  ( 0.9754402186311945666, 30.47320128434260766, 30.20795797590407972 ) ) ;
#33044=CARTESIAN_POINT ( 'NONE',  ( 0.9722240750034545353, -16.95645446544459034, -39.41582016107722097 ) ) ;
#33048=( BOUNDED_SURFACE ( )  B_SPLINE_SURFACE ( 3, 1, ( 
 ( #4184, #28324 ),
 ( #18329, #18949 ),
 ( #23627, #38070 ),
 ( #4800, #33357 ) ),
 .UNSPECIFIED., .F., .F., .F. ) 
 B_SPLINE_SURFACE_WITH_KNOTS ( ( 4, 4 ),
 ( 2, 2 ),
 ( 0.000000000000000000, 1.000000000000000000 ),
 ( 0.000000000000000000, 1.000000000000000000 ),
 .UNSPECIFIED. ) 
 GEOMETRIC_REPRESENTATION_ITEM ( )  RATIONAL_B_SPLINE_SURFACE ( (
 ( 1.000000000000000000, 1.000000000000000000),
 ( 0.7269869731126817891, 0.9931720237060910339),
 ( 0.7269869731126817891, 0.9931720237060910339),
 ( 1.000000000000000000, 1.000000000000000000) ) ) 
 REPRESENTATION_ITEM ( '' )  SURFACE ( )  );
#33055=CARTESIAN_POINT ( 'NONE',  ( 0.5807400328401574052, -23.47602859900685601, -41.75144119563910294 ) ) ;
#33058=EDGE_CURVE ( 'NONE', #21453, #35725, #47442, .T. ) ;
#33064=CARTESIAN_POINT ( 'NONE',  ( 5.960721111146673579, 0.006321279846536711350, 20.52557019979492026 ) ) ;
#33082=LINE ( 'NONE', #51527, #5009 ) ;
#33084=ORIENTED_EDGE ( 'NONE', *, *, #44635, .F. ) ;
#33085=CARTESIAN_POINT ( 'NONE',  ( 0.9757787079277433495, 41.43615150473016229, 11.14366644276425333 ) ) ;
#33087=CARTESIAN_POINT ( 'NONE',  ( 1.227938101723756947, -34.55893248994489397, -25.45152231597092651 ) ) ;
#33100=CARTESIAN_POINT ( 'NONE',  ( -17.97369999999976642, 0.000000000000000000, -1.381000053334577907E-15 ) ) ;
#33101=ORIENTED_EDGE ( 'NONE', *, *, #57332, .F. ) ;
#33108=DIRECTION ( 'NONE',  ( -0.000000000000000000, 1.000000000000000000, -0.000000000000000000 ) ) ;
#33109=ORIENTED_EDGE ( 'NONE', *, *, #55588, .F. ) ;
#33114=CARTESIAN_POINT ( 'NONE',  ( 0.5839880159502339740, -47.48028790449882308, -6.296669079378655276 ) ) ;
#33116=CARTESIAN_POINT ( 'NONE',  ( 0.9736507210033066295, 26.47691119766837531, -33.76542629919376992 ) ) ;
#33125=EDGE_CURVE ( 'NONE', #6666, #21601, #22036, .T. ) ;
#33130=CARTESIAN_POINT ( 'NONE',  ( 0.5839879882104919151, -5.421203860810959572E-16, -47.89596766822081975 ) ) ;
#33131=CARTESIAN_POINT ( 'NONE',  ( 5.965394784446460541, 5.298374383010361122, 19.82972329408687884 ) ) ;
#33138=B_SPLINE_CURVE_WITH_KNOTS ( 'NONE', 3,
 ( #56605, #42239, #38157, #33445, #14339, #9611 ),
 .UNSPECIFIED., .F., .F.,
 ( 4, 2, 4 ),
 ( 0.000000000000000000, 0.0002291966416970781027, 0.0004583932833941562054 ),
 .UNSPECIFIED. ) ;
#33145=EDGE_CURVE ( 'NONE', #31335, #38495, #20471, .T. ) ;
#33154=CARTESIAN_POINT ( 'NONE',  ( 0.9972139404380286898, -11.74016833743892008, -41.27214627875022046 ) ) ;
#33159=B_SPLINE_CURVE_WITH_KNOTS ( 'NONE', 3,
 ( #17949, #42081, #61132, #18253, #37364, #55554 ),
 .UNSPECIFIED., .F., .F.,
 ( 4, 2, 4 ),
 ( 3.471140604459641645E-18, 0.0002291966416970821143, 0.0004583932833941607591 ),
 .UNSPECIFIED. ) ;
#33165=EDGE_LOOP ( 'NONE', ( #38053, #9468, #12937, #35027, #53873, #9318, #16728, #8971, #6618, #5984, #48605, #22040, #8580, #22345, #9511, #23509, #51440, #56937, #46990, #12579, #31606, #25004, #46436, #45812, #40659, #30056, #50359, #46796, #28763, #48181, #49480, #12314, #13533, #53689, #60872, #26765, #34636, #2023, #58304, #39810, #29806, #52934, #3963, #53018, #58218, #21842, #39103, #22289, #34687, #34432, #44837, #41509, #22287, #24561, #21682, #6307, #34258, #46426, #37886, #61026, #5310, #56471, #25676, #51895, #3009, #3644, #55228, #15701, #42195, #10582, #3165, #19459, #21072, #53125, #28977, #47173, #57463, #6836, #31177, #9822, #12164, #44105, #53790, #54419, #57148, #57951, #27128, #3449, #4192, #31770, #26834, #26606, #33536, #39243, #17443, #2060, #34622, #22851, #56768, #51328, #40203, #59191, #36979, #8689, #15431, #53553, #53991, #34127, #31762, #4706, #44964, #61365, #2457, #23319, #56769, #20875, #54383, #24511, #29383, #15050, #30572, #19986, #124, #15913, #49870, #55645, #16309, #23893, #2884, #57276, #12590, #34265, #59183, #1670, #37274, #35165, #20314, #4615, #24128, #28704, #41971, #61875, #49503, #37406, #49295, #50910, #19898, #27133 ) ) ;
#33167=CARTESIAN_POINT ( 'NONE',  ( 0.5819845901640484653, -29.51612926147643279, 37.72030663501146819 ) ) ;
#33170=EDGE_CURVE ( 'NONE', #60259, #461, #31813, .T. ) ;
#33171=ORIENTED_EDGE ( 'NONE', *, *, #53666, .F. ) ;
#33173=EDGE_CURVE ( 'NONE', #14400, #3122, #16397, .T. ) ;
#33176=CARTESIAN_POINT ( 'NONE',  ( 0.5807400328401637335, -28.72484455891667565, 38.33001520688940644 ) ) ;
#33178=EDGE_CURVE ( 'NONE', #14690, #1876, #6339, .T. ) ;
#33180=CARTESIAN_POINT ( 'NONE',  ( 1.088313998177379505, -42.43756598879024722, -6.373602917100628318 ) ) ;
#33189=ORIENTED_EDGE ( 'NONE', *, *, #52756, .T. ) ;
#33192=CONICAL_SURFACE ( 'NONE', #12186, 43.08621763946400307, 1.568696531533066763 ) ;
#33194=CARTESIAN_POINT ( 'NONE',  ( 5.960721111146673579, -19.82781442290494311, -5.306302591836510985 ) ) ;
#33197=CARTESIAN_POINT ( 'NONE',  ( 1.227938101723756947, 33.52879263017899092, -26.79402671879293507 ) ) ;
#33209=CARTESIAN_POINT ( 'NONE',  ( 0.6067099128993264090, -34.36589933408221498, -33.36330296770427850 ) ) ;
#33210=ORIENTED_EDGE ( 'NONE', *, *, #46906, .T. ) ;
#33216=EDGE_CURVE ( 'NONE', #21472, #28471, #14259, .T. ) ;
#33228=CARTESIAN_POINT ( 'NONE',  ( 0.5809828226811617480, 41.74875432577682233, -23.47450554821666202 ) ) ;
#33230=VECTOR ( 'NONE', #28558, 1000.000000000000114 ) ;
#33235=CARTESIAN_POINT ( 'NONE',  ( 5.965394784446460541, -19.82972329408689305, 5.298374383010291844 ) ) ;
#33249=EDGE_CURVE ( 'NONE', #29382, #3160, #27394, .T. ) ;
#33250=CARTESIAN_POINT ( 'NONE',  ( 5.860006189529234355, -40.09484204000618490, 26.81109398084693396 ) ) ;
#33252=B_SPLINE_CURVE_WITH_KNOTS ( 'NONE', 3,
 ( #3348, #47221, #46930, #46303 ),
 .UNSPECIFIED., .F., .F.,
 ( 4, 4 ),
 ( 5.969062235490920269E-17, 0.005004741218457481322 ),
 .UNSPECIFIED. ) ;
#33256=EDGE_CURVE ( 'NONE', #33762, #44988, #7017, .T. ) ;
#33257=CARTESIAN_POINT ( 'NONE',  ( 0.9756008150404599233, -16.55159915785250035, -39.58764833544695705 ) ) ;
#33270=ORIENTED_EDGE ( 'NONE', *, *, #33256, .T. ) ;
#33276=ORIENTED_EDGE ( 'NONE', *, *, #38868, .T. ) ;
#33278=CARTESIAN_POINT ( 'NONE',  ( 0.5807400328401637335, 29.58941477093015493, 37.66660715020876893 ) ) ;
#33279=FACE_OUTER_BOUND ( 'NONE', #27009, .T. ) ;
#33285=CARTESIAN_POINT ( 'NONE',  ( 0.5800708119828335008, 33.42085299104068952, -34.30831427709716763 ) ) ;
#33286=CARTESIAN_POINT ( 'NONE',  ( 3.407937589446174087, 4.815089211105057387, 12.82481284928205234 ) ) ;
#33291=CARTESIAN_POINT ( 'NONE',  ( 0.9968887458511651589, -34.43855515351788910, 25.59699785741774392 ) ) ;
#33295=CARTESIAN_POINT ( 'NONE',  ( 0.9730545539215883499, -36.90443313492315980, -21.89037132892475057 ) ) ;
#33299=VERTEX_POINT ( 'NONE', #44315 ) ;
#33303=ORIENTED_EDGE ( 'NONE', *, *, #28036, .T. ) ;
#33304=CARTESIAN_POINT ( 'NONE',  ( 0.5839254288179541730, -33.93171296845864049, 33.80331890503256176 ) ) ;
#33307=ORIENTED_EDGE ( 'NONE', *, *, #12776, .T. ) ;
#33311=CARTESIAN_POINT ( 'NONE',  ( 5.958863334805807099, 7.853699934219627643, 18.96369761673823007 ) ) ;
#33312=LINE ( 'NONE', #28584, #9963 ) ;
#33313=ORIENTED_EDGE ( 'NONE', *, *, #61913, .T. ) ;
#33314=EDGE_LOOP ( 'NONE', ( #39253, #14912, #44205, #58348 ) ) ;
#33315=CARTESIAN_POINT ( 'NONE',  ( 0.5834872094924180574, -12.17696997821490434, -46.32218741137609186 ) ) ;
#33332=VERTEX_POINT ( 'NONE', #5726 ) ;
#33343=CARTESIAN_POINT ( 'NONE',  ( 0.8557997880470606944, 47.37054680076706603, 7.156447707085862753 ) ) ;
#33348=CARTESIAN_POINT ( 'NONE',  ( 3.660087539127307554, -4.399983418616474573, 47.83637163185230889 ) ) ;
#33353=CARTESIAN_POINT ( 'NONE',  ( 2.281448460670576939, 43.80196084514306420, -19.56578495220123060 ) ) ;
#33356=CARTESIAN_POINT ( 'NONE',  ( 0.9740398440564302929, -42.48528956276141599, 6.011466167923952497 ) ) ;
#33357=CARTESIAN_POINT ( 'NONE',  ( 0.8551540677456834771, -23.16399837394575911, 41.94570365541195400 ) ) ;
#33358=CARTESIAN_POINT ( 'NONE',  ( 0.7762777257811898091, 0.8897018348892672401, -47.89627391089018005 ) ) ;
#33360=CARTESIAN_POINT ( 'NONE',  ( 5.860006189529234355, -47.30964106197851038, -9.393028332205226150 ) ) ;
#33364=CARTESIAN_POINT ( 'NONE',  ( 5.960221823109900008, -10.26751639438380259, 17.77295928189537833 ) ) ;
#33371=CARTESIAN_POINT ( 'NONE',  ( 4.967162193818130511, 0.000000000000000000, 0.000000000000000000 ) ) ;
#33375=CARTESIAN_POINT ( 'NONE',  ( 2.624215991343608501, 1.411420423866143414, -47.98682984381859740 ) ) ;
#33376=CARTESIAN_POINT ( 'NONE',  ( 4.960156602257182357, 3.546989772329889767, 46.28683144126594584 ) ) ;
#33381=CARTESIAN_POINT ( 'NONE',  ( 5.981074661064941900, -5.320466518161074632, 19.82308078259081796 ) ) ;
#33382=ORIENTED_EDGE ( 'NONE', *, *, #59393, .T. ) ;
#33388=ORIENTED_EDGE ( 'NONE', *, *, #15430, .F. ) ;
#33390=CARTESIAN_POINT ( 'NONE',  ( 0.5807400328401637335, -17.82553128098375339, -44.45848844984462289 ) ) ;
#33403=EDGE_CURVE ( 'NONE', #56700, #22536, #40571, .T. ) ;
#33405=CARTESIAN_POINT ( 'NONE',  ( 4.960156602257181468, -14.43621227656559824, 44.12083041402459571 ) ) ;
#33410=CARTESIAN_POINT ( 'NONE',  ( 0.9757402383260936896, -42.53022961222599463, -5.684842778069664426 ) ) ;
#33414=CARTESIAN_POINT ( 'NONE',  ( 0.8557997880470690211, 41.93815086860257679, 23.15977007032337553 ) ) ;
#33423=CARTESIAN_POINT ( 'NONE',  ( 0.9758171775293924544, 26.11633498242675699, -34.04519363167607082 ) ) ;
#33424=B_SPLINE_CURVE_WITH_KNOTS ( 'NONE', 3,
 ( #31590, #54758, #26263, #35073, #21890, #21265 ),
 .UNSPECIFIED., .F., .F.,
 ( 4, 2, 4 ),
 ( 1.520533924285649780E-16, 0.0002445252820015233640, 0.0004890505640028946143 ),
 .UNSPECIFIED. ) ;
#33427=CARTESIAN_POINT ( 'NONE',  ( 0.5819845079324649229, -18.74766465427192585, -44.07435181061359941 ) ) ;
#33432=ORIENTED_EDGE ( 'NONE', *, *, #12606, .T. ) ;
#33434=CARTESIAN_POINT ( 'NONE',  ( 0.7762777257811878107, -24.71864134625259268, 41.03453903600424724 ) ) ;
#33439=CARTESIAN_POINT ( 'NONE',  ( 1.227938101723756947, 34.55893248994507161, 25.45152231597068848 ) ) ;
#33445=CARTESIAN_POINT ( 'NONE',  ( 1.088313998177381503, -41.64627086748864571, 10.35171213034677962 ) ) ;
#33449=CARTESIAN_POINT ( 'NONE',  ( 0.5850706913938534814, -46.21698775168654549, 12.57184842332001296 ) ) ;
#33450=DIRECTION ( 'NONE',  ( -1.000000000000000000, -0.000000000000000000, -0.000000000000000000 ) ) ;
#33451=VERTEX_POINT ( 'NONE', #37067 ) ;
#33455=B_SPLINE_CURVE_WITH_KNOTS ( 'NONE', 3,
 ( #19160, #52020, #38270, #4085 ),
 .UNSPECIFIED., .F., .F.,
 ( 4, 4 ),
 ( 2.168404344971008868E-19, 0.004048833967417087357 ),
 .UNSPECIFIED. ) ;
#33456=VECTOR ( 'NONE', #9862, 1000.000000000000227 ) ;
#33458=CARTESIAN_POINT ( 'NONE',  ( 0.9747592971366234593, 42.49794971112902431, -5.921534893733704230 ) ) ;
#33463=CARTESIAN_POINT ( 'NONE',  ( 4.967162193818130511, -7.970725651239513709, -42.34252806656601820 ) ) ;
#33468=CARTESIAN_POINT ( 'NONE',  ( 1.154321485836933947, -20.73950273457868931, 37.57248783354764754 ) ) ;
#33472=VERTEX_POINT ( 'NONE', #55207 ) ;
#33473=CARTESIAN_POINT ( 'NONE',  ( 0.8557997880470690211, -29.88293891557446003, -37.44587306708127983 ) ) ;
#33493=CARTESIAN_POINT ( 'NONE',  ( 0.9752132459055858904, 34.18286753639641518, 25.93579301218368371 ) ) ;
#33502=CARTESIAN_POINT ( 'NONE',  ( 1.227938101723748288, 17.20315230597897482, -39.32113113558949635 ) ) ;
#33505=LINE ( 'NONE', #13166, #14596 ) ;
#33506=FACE_OUTER_BOUND ( 'NONE', #20555, .T. ) ;
#33508=ORIENTED_EDGE ( 'NONE', *, *, #11314, .F. ) ;
#33523=EDGE_CURVE ( 'NONE', #22531, #50798, #18934, .T. ) ;
#33526=EDGE_CURVE ( 'NONE', #12115, #3984, #15148, .T. ) ;
#33531=CARTESIAN_POINT ( 'NONE',  ( 3.783198216974388739, -39.06945274417380176, -18.05208553945188754 ) ) ;
#33533=CARTESIAN_POINT ( 'NONE',  ( 0.5809828226811544205, 17.82437196699742188, -44.45562576850583270 ) ) ;
#33536=ORIENTED_EDGE ( 'NONE', *, *, #45283, .T. ) ;
#33537=CARTESIAN_POINT ( 'NONE',  ( 0.9747592971366226822, -36.99691261380223750, 21.73404615330606759 ) ) ;
#33543=CARTESIAN_POINT ( 'NONE',  ( 5.960221823109900008, -2.673723662181196392, -20.35070456576733733 ) ) ;
#33551=VERTEX_POINT ( 'NONE', #9146 ) ;
#33560=CARTESIAN_POINT ( 'NONE',  ( 1.227938101723756947, 42.91134962331487657, -0.8460948827226678626 ) ) ;
#33570=CARTESIAN_POINT ( 'NONE',  ( 0.5809828226811544205, 47.55412398569205834, 5.711058609465488267 ) ) ;
#33579=VERTEX_POINT ( 'NONE', #38303 ) ;
#33589=CARTESIAN_POINT ( 'NONE',  ( 5.974727161628367256, -0.01551142186635440928, -20.52494643607030156 ) ) ;
#33598=ADVANCED_FACE ( 'NONE', ( #27956 ), #22389, .T. ) ;
#33599=( BOUNDED_SURFACE ( )  B_SPLINE_SURFACE ( 3, 1, ( 
 ( #12335, #55835 ),
 ( #12957, #21099 ),
 ( #60218, #21407 ),
 ( #45857, #50828 ) ),
 .UNSPECIFIED., .F., .F., .F. ) 
 B_SPLINE_SURFACE_WITH_KNOTS ( ( 4, 4 ),
 ( 2, 2 ),
 ( 0.000000000000000000, 1.000000000000000000 ),
 ( 0.000000000000000000, 1.000000000000000000 ),
 .UNSPECIFIED. ) 
 GEOMETRIC_REPRESENTATION_ITEM ( )  RATIONAL_B_SPLINE_SURFACE ( (
 ( 1.000000000000000000, 1.000000000000000000),
 ( 0.7269869731126821222, 0.9931720237060910339),
 ( 0.7269869731126821222, 0.9931720237060910339),
 ( 1.000000000000000000, 1.000000000000000000) ) ) 
 REPRESENTATION_ITEM ( '' )  SURFACE ( )  );
#33607=DIRECTION ( 'NONE',  ( 0.07439287786467665975, 0.9597484305373172875, 0.2708295585865166943 ) ) ;
#33609=CARTESIAN_POINT ( 'NONE',  ( 0.9741495583595187746, 5.208308905148107293, 42.59115242362807408 ) ) ;
#33617=CARTESIAN_POINT ( 'NONE',  ( 4.967162193818130511, 0.000000000000000000, 0.000000000000000000 ) ) ;
#33621=ORIENTED_EDGE ( 'NONE', *, *, #29828, .F. ) ;
#33622=CARTESIAN_POINT ( 'NONE',  ( 0.5809828226811617480, -41.20389530892290253, -24.41822904836968178 ) ) ;
#33635=DIRECTION ( 'NONE',  ( 0.07836865515943411409, -0.6131273243286340380, 0.7860872967108117892 ) ) ;
#33636=CARTESIAN_POINT ( 'NONE',  ( 0.9754642270333683252, -0.1757168848622158996, 42.90808635884411615 ) ) ;
#33653=DIRECTION ( 'NONE',  ( -1.000000000000000000, -0.000000000000000000, -0.000000000000000000 ) ) ;
#33658=CARTESIAN_POINT ( 'NONE',  ( 0.9730545539215883499, -21.89037132892409687, -36.90443313492354349 ) ) ;
#33664=CARTESIAN_POINT ( 'NONE',  ( 3.407937589446174087, -6.447869442558080699, -12.08659953757615568 ) ) ;
#33666=ADVANCED_FACE ( 'NONE', ( #13874 ), #56618, .F. ) ;
#33670=CARTESIAN_POINT ( 'NONE',  ( 0.5827357941260215002, -41.29633147056626541, 24.26189667804985461 ) ) ;
#33673=EDGE_CURVE ( 'NONE', #27525, #10594, #43938, .T. ) ;
#33687=CARTESIAN_POINT ( 'NONE',  ( 0.8557997880470690211, -38.55640757422419540, -28.43566216845010075 ) ) ;
#33689=EDGE_CURVE ( 'NONE', #61163, #37784, #26405, .T. ) ;
#33695=B_SPLINE_CURVE_WITH_KNOTS ( 'NONE', 3,
 ( #765, #35227, #59005, #28973 ),
 .UNSPECIFIED., .F., .F.,
 ( 4, 4 ),
 ( 1.301042606982605321E-18, 0.004048833967417087357 ),
 .UNSPECIFIED. ) ;
#33696=VERTEX_POINT ( 'NONE', #19803 ) ;
#33700=CIRCLE ( 'NONE', #35715, 42.88844316795388778 ) ;
#33701=CARTESIAN_POINT ( 'NONE',  ( 0.6846871229502932144, -17.53234844287709038, -44.58493949244024890 ) ) ;
#33704=DIRECTION ( 'NONE',  ( 0.000000000000000000, 0.000000000000000000, 1.000000000000000000 ) ) ;
#33706=CARTESIAN_POINT ( 'NONE',  ( 0.5832367798473380160, 38.16362489683130121, -28.94059862654955495 ) ) ;
#33709=CARTESIAN_POINT ( 'NONE',  ( 0.5809828226811560858, -11.86925843957200222, 46.40184912890835278 ) ) ;
#33717=ORIENTED_EDGE ( 'NONE', *, *, #11123, .F. ) ;
#33718=CARTESIAN_POINT ( 'NONE',  ( 5.974727161628367256, 19.82959049719567801, 5.297264154381005063 ) ) ;
#33724=ORIENTED_EDGE ( 'NONE', *, *, #15018, .F. ) ;
#33725=CARTESIAN_POINT ( 'NONE',  ( 4.956653778116970166, 36.51451553856417576, 31.29546495791861460 ) ) ;
#33733=AXIS2_PLACEMENT_3D ( 'NONE', #14212, #55311, #46807 ) ;
#33737=CARTESIAN_POINT ( 'NONE',  ( 0.5827359174754822568, -17.99288944686860248, -44.38786494726115706 ) ) ;
#33738=DIRECTION ( 'NONE',  ( -1.000000000000000000, -0.000000000000000000, -0.000000000000000000 ) ) ;
#33741=LINE ( 'NONE', #23098, #769 ) ;
#33743=CARTESIAN_POINT ( 'NONE',  ( 0.9758171775293909000, 39.64000636436386316, -16.42583507057825187 ) ) ;
#33746=ORIENTED_EDGE ( 'NONE', *, *, #14938, .F. ) ;
#33748=LINE ( 'NONE', #9602, #57327 ) ;
#33753=CARTESIAN_POINT ( 'NONE',  ( 0.5827359174754810356, -47.89462060834306811, -0.3632382226755718757 ) ) ;
#33755=CARTESIAN_POINT ( 'NONE',  ( 0.9730545539215892381, -10.61654491617593266, 41.57420493492382008 ) ) ;
#33756=EDGE_CURVE ( 'NONE', #24624, #8570, #35138, .T. ) ;
#33757=FACE_OUTER_BOUND ( 'NONE', #28274, .T. ) ;
#33760=EDGE_CURVE ( 'NONE', #355, #13139, #39139, .T. ) ;
#33762=VERTEX_POINT ( 'NONE', #15409 ) ;
#33763=ORIENTED_EDGE ( 'NONE', *, *, #11426, .F. ) ;
#33764=CARTESIAN_POINT ( 'NONE',  ( 5.974727161628369032, -10.27590650342049550, 17.76736931401842412 ) ) ;
#33766=CARTESIAN_POINT ( 'NONE',  ( 2.624215991343608501, 7.662883702705343580, -47.39206852872448650 ) ) ;
#33781=CARTESIAN_POINT ( 'NONE',  ( 0.5809828226811553087, 47.41188724015889022, -6.791453954329836229 ) ) ;
#33785=CARTESIAN_POINT ( 'NONE',  ( 0.5809828226811617480, 28.72298383114487663, 38.32755012159156394 ) ) ;
#33792=CARTESIAN_POINT ( 'NONE',  ( 4.967162193818130511, 38.83676580803767564, 18.65818244221271627 ) ) ;
#33801=ORIENTED_EDGE ( 'NONE', *, *, #11743, .T. ) ;
#33808=CARTESIAN_POINT ( 'NONE',  ( 0.9757402383260946888, 0.08489923450698490248, -42.90839848328081274 ) ) ;
#33812=ORIENTED_EDGE ( 'NONE', *, *, #33837, .F. ) ;
#33824=CARTESIAN_POINT ( 'NONE',  ( 0.9747592971366239034, -21.17324310849259916, 37.32069240268765498 ) ) ;
#33825=CARTESIAN_POINT ( 'NONE',  ( 0.7762777257811885878, 7.133808567472943452, -47.37038525518526910 ) ) ;
#33827=LINE ( 'NONE', #43539, #7837 ) ;
#33830=CARTESIAN_POINT ( 'NONE',  ( 0.6067099128993220791, 43.97493306231487509, -18.98236771638412179 ) ) ;
#33835=B_SPLINE_CURVE_WITH_KNOTS ( 'NONE', 3,
 ( #58521, #15653, #30342, #23879 ),
 .UNSPECIFIED., .F., .F.,
 ( 4, 4 ),
 ( 0.000000000000000000, 0.004446090762761371190 ),
 .UNSPECIFIED. ) ;
#33837=EDGE_CURVE ( 'NONE', #2091, #8650, #7693, .T. ) ;
#33840=B_SPLINE_CURVE_WITH_KNOTS ( 'NONE', 3,
 ( #11466, #44392, #53722, #50281 ),
 .UNSPECIFIED., .F., .F.,
 ( 4, 4 ),
 ( 0.000000000000000000, 0.004444878191957665238 ),
 .UNSPECIFIED. ) ;
#33841=ORIENTED_EDGE ( 'NONE', *, *, #57631, .T. ) ;
#33847=CARTESIAN_POINT ( 'NONE',  ( 4.956653778116966613, 0.000000000000000000, 0.000000000000000000 ) ) ;
#33861=VERTEX_POINT ( 'NONE', #12264 ) ;
#33863=ORIENTED_EDGE ( 'NONE', *, *, #30334, .F. ) ;
#33869=CARTESIAN_POINT ( 'NONE',  ( 0.5837374860065638327, 0.1816420316515440225, 47.89569815517036488 ) ) ;
#33892=VERTEX_POINT ( 'NONE', #18727 ) ;
#33895=CARTESIAN_POINT ( 'NONE',  ( 2.624215991343608501, 25.21574086439763107, -40.85210347989505664 ) ) ;
#33901=CARTESIAN_POINT ( 'NONE',  ( 3.407937589446174087, -8.699069120706843350, 10.58239600294635885 ) ) ;
#33902=CIRCLE ( 'NONE', #49893, 42.88844316795388778 ) ;
#33903=CARTESIAN_POINT ( 'NONE',  ( -17.04189967907673520, -7.774469338339614843, -1.886945943481975085 ) ) ;
#33909=CARTESIAN_POINT ( 'NONE',  ( 0.8557997880470697982, 44.60232077416686991, 17.48760788519232889 ) ) ;
#33914=VERTEX_POINT ( 'NONE', #60151 ) ;
#33915=CARTESIAN_POINT ( 'NONE',  ( 0.5809828226811565299, 28.72298383114543796, -38.32755012159114472 ) ) ;
#33930=CARTESIAN_POINT ( 'NONE',  ( 1.227938101723756947, -41.66816631169184859, -10.28900963485423858 ) ) ;
#33935=ORIENTED_EDGE ( 'NONE', *, *, #29628, .T. ) ;
#33938=VERTEX_POINT ( 'NONE', #23726 ) ;
#33947=EDGE_CURVE ( 'NONE', #28202, #37398, #27011, .T. ) ;
#33958=EDGE_CURVE ( 'NONE', #16449, #22415, #44425, .T. ) ;
#33959=CARTESIAN_POINT ( 'NONE',  ( 3.783198216974394956, -20.00646744835639268, -38.10565824507919785 ) ) ;
#33966=CARTESIAN_POINT ( 'NONE',  ( 0.7762777257811885878, 13.25585385760172130, -46.03397617421214960 ) ) ;
#33978=ADVANCED_FACE ( 'NONE', ( #10246 ), #7014, .F. ) ;
#33989=AXIS2_PLACEMENT_3D ( 'NONE', #33617, #5982, #52694 ) ;
#33991=CARTESIAN_POINT ( 'NONE',  ( 0.9758171775293941197, -11.09981579996835421, 41.44794628856071483 ) ) ;
#33995=ORIENTED_EDGE ( 'NONE', *, *, #9619, .F. ) ;
#33997=CARTESIAN_POINT ( 'NONE',  ( 0.5809828226811617480, 17.82437196699680726, 44.45562576850608139 ) ) ;
#34000=EDGE_CURVE ( 'NONE', #56250, #25196, #38774, .T. ) ;
#34001=ORIENTED_EDGE ( 'NONE', *, *, #31839, .F. ) ;
#34004=CARTESIAN_POINT ( 'NONE',  ( 4.967162193818130511, 40.93989340068610261, 13.42934394584178648 ) ) ;
#34009=CARTESIAN_POINT ( 'NONE',  ( 4.960156602257181468, -44.12083041402475203, 14.43621227656513284 ) ) ;
#34026=EDGE_CURVE ( 'NONE', #54823, #49884, #12826, .T. ) ;
#34031=CARTESIAN_POINT ( 'NONE',  ( 0.9730545539215883499, -42.47233286818612896, -6.101350888305089093 ) ) ;
#34034=CARTESIAN_POINT ( 'NONE',  ( 5.981074661064941900, -17.77917279944639262, 10.25489689131099702 ) ) ;
#34054=CARTESIAN_POINT ( 'NONE',  ( 0.5837374860065644988, -23.79054246377998538, 41.56971235019474875 ) ) ;
#34071=DIRECTION ( 'NONE',  ( 0.000000000000000000, 0.000000000000000000, 1.000000000000000000 ) ) ;
#34076=CARTESIAN_POINT ( 'NONE',  ( -48.95476116535499500, 1.530808498934191127E-15, 12.50000000000000000 ) ) ;
#34090=CARTESIAN_POINT ( 'NONE',  ( 1.154321485836934169, -30.92445806269057940, -29.75729673892731597 ) ) ;
#34099=CARTESIAN_POINT ( 'NONE',  ( 0.5800708119828337228, -24.48933355903736242, -41.16171018093183420 ) ) ;
#34102=CARTESIAN_POINT ( 'NONE',  ( 0.5827357941260206120, -37.77622264066033608, 29.44458568814497212 ) ) ;
#34105=EDGE_CURVE ( 'NONE', #22050, #34186, #53182, .T. ) ;
#34111=CARTESIAN_POINT ( 'NONE',  ( 0.5809828226811617480, -47.41188724015875522, -6.791453954330822107 ) ) ;
#34118=LINE ( 'NONE', #25306, #23787 ) ;
#34126=CARTESIAN_POINT ( 'NONE',  ( 0.9722240750034587542, -26.58024222649022406, -33.68410530487897603 ) ) ;
#34127=ORIENTED_EDGE ( 'NONE', *, *, #1408, .T. ) ;
#34134=FACE_OUTER_BOUND ( 'NONE', #7493, .T. ) ;
#34142=DIRECTION ( 'NONE',  ( 0.07439287786467665975, -0.8569499480574984673, -0.5100024374914908787 ) ) ;
#34145=( BOUNDED_SURFACE ( )  B_SPLINE_SURFACE ( 3, 1, ( 
 ( #25355, #44493 ),
 ( #49776, #11902 ),
 ( #1522, #20663 ),
 ( #25659, #58850 ) ),
 .UNSPECIFIED., .F., .F., .F. ) 
 B_SPLINE_SURFACE_WITH_KNOTS ( ( 4, 4 ),
 ( 2, 2 ),
 ( 0.000000000000000000, 1.000000000000000000 ),
 ( 0.000000000000000000, 1.000000000000000000 ),
 .UNSPECIFIED. ) 
 GEOMETRIC_REPRESENTATION_ITEM ( )  RATIONAL_B_SPLINE_SURFACE ( (
 ( 1.000000000000000000, 1.000000000000000000),
 ( 0.7269869731126817891, 0.9931720237060910339),
 ( 0.7269869731126817891, 0.9931720237060910339),
 ( 1.000000000000000000, 1.000000000000000000) ) ) 
 REPRESENTATION_ITEM ( '' )  SURFACE ( )  );
#34147=ORIENTED_EDGE ( 'NONE', *, *, #42824, .T. ) ;
#34150=CARTESIAN_POINT ( 'NONE',  ( 0.5838002273316428292, 18.45474575185574295, -44.19779719735679180 ) ) ;
#34154=CARTESIAN_POINT ( 'NONE',  ( 0.9752132459055851132, -37.04276540031525400, 21.65565338840803022 ) ) ;
#34159=CARTESIAN_POINT ( 'NONE',  ( 0.9968887458511644928, -41.27232779986113798, -11.73947777183265018 ) ) ;
#34163=CARTESIAN_POINT ( 'NONE',  ( 0.5809828226811626362, 29.58751527316234231, -37.66417181417519799 ) ) ;
#34166=CARTESIAN_POINT ( 'NONE',  ( 5.959547316686252039, -17.77749189599210311, -10.25972575517523744 ) ) ;
#34169=B_SPLINE_CURVE_WITH_KNOTS ( 'NONE', 3,
 ( #57724, #33966, #53040, #31411, #45841, #12021 ),
 .UNSPECIFIED., .F., .F.,
 ( 4, 2, 4 ),
 ( 1.506943126379255764E-16, 0.0002445252820015211413, 0.0004890505640028915786 ),
 .UNSPECIFIED. ) ;
#34172=EDGE_CURVE ( 'NONE', #9042, #60259, #7569, .T. ) ;
#34173=CARTESIAN_POINT ( 'NONE',  ( 1.154321713695928953, 22.16897764010656502, -36.74718012229632791 ) ) ;
#34186=VERTEX_POINT ( 'NONE', #22106 ) ;
#34188=ORIENTED_EDGE ( 'NONE', *, *, #53744, .T. ) ;
#34189=CARTESIAN_POINT ( 'NONE',  ( 3.783198216974388739, -36.37893817280271236, -22.99723434398829980 ) ) ;
#34195=CARTESIAN_POINT ( 'NONE',  ( 0.8557997880470606944, -13.27832040216671317, 46.03118133706021808 ) ) ;
#34201=CARTESIAN_POINT ( 'NONE',  ( 0.5809828226811617480, -5.711058609464997105, -47.55412398569212939 ) ) ;
#34206=CARTESIAN_POINT ( 'NONE',  ( 0.9968887458511647148, -42.62316256128687542, 4.948372828380621868 ) ) ;
#34207=FACE_OUTER_BOUND ( 'NONE', #50649, .T. ) ;
#34209=CARTESIAN_POINT ( 'NONE',  ( 0.9752132459055834479, 30.17566824627289890, -30.50512806189381010 ) ) ;
#34213=CARTESIAN_POINT ( 'NONE',  ( 0.5807400328401637335, -28.72484455891615696, -38.33001520688979724 ) ) ;
#34221=DIRECTION ( 'NONE',  ( -1.000000000000000000, -0.000000000000000000, -0.000000000000000000 ) ) ;
#34223=ORIENTED_EDGE ( 'NONE', *, *, #33170, .T. ) ;
#34227=PRODUCT_DEFINITION_CONTEXT ( 'detailed design', #36008, 'design' ) ;
#34232=B_SPLINE_CURVE_WITH_KNOTS ( 'NONE', 3,
 ( #1200, #20332, #53807, #44470 ),
 .UNSPECIFIED., .F., .F.,
 ( 4, 4 ),
 ( 0.000000000000000000, 0.004048833967417087357 ),
 .UNSPECIFIED. ) ;
#34237=ORIENTED_EDGE ( 'NONE', *, *, #33145, .F. ) ;
#34238=CARTESIAN_POINT ( 'NONE',  ( 4.967162193818130511, 42.34252806656603241, -7.970725651239366272 ) ) ;
#34241=CARTESIAN_POINT ( 'NONE',  ( 5.965394784446460541, -10.25014670152102880, -17.78272165951797490 ) ) ;
#34243=ORIENTED_EDGE ( 'NONE', *, *, #48947, .F. ) ;
#34258=ORIENTED_EDGE ( 'NONE', *, *, #30598, .T. ) ;
#34261=CARTESIAN_POINT ( 'NONE',  ( 2.526552050251864134, 1.212569781798530588, -42.96196914573629755 ) ) ;
#34265=ORIENTED_EDGE ( 'NONE', *, *, #33125, .T. ) ;
#34267=CARTESIAN_POINT ( 'NONE',  ( 0.5809828226811626362, -12.92184523170236510, 46.11980934799335330 ) ) ;
#34271=CARTESIAN_POINT ( 'NONE',  ( 1.227938101723756947, 6.439911493064564674, 42.43379953535188065 ) ) ;
#34273=CARTESIAN_POINT ( 'NONE',  ( 0.5807400328401574052, -29.58941477093041428, 37.66660715020855577 ) ) ;
#34275=CARTESIAN_POINT ( 'NONE',  ( 0.8551540677456739292, -47.37911285756614888, -7.157691013574849492 ) ) ;
#34277=CARTESIAN_POINT ( 'NONE',  ( 0.9730545539215883499, -0.5054011016609686324, -42.90536227157002713 ) ) ;
#34278=EDGE_LOOP ( 'NONE', ( #58163, #53429, #14361, #25621 ) ) ;
#34291=ORIENTED_EDGE ( 'NONE', *, *, #38868, .F. ) ;
#34297=ORIENTED_EDGE ( 'NONE', *, *, #48568, .F. ) ;
#34310=CARTESIAN_POINT ( 'NONE',  ( 4.956653778116975495, -20.77844580450591394, 43.37017594958047084 ) ) ;
#34312=CARTESIAN_POINT ( 'NONE',  ( 2.281448460670567613, 13.68109378871710469, 45.98107640562100329 ) ) ;
#34316=CARTESIAN_POINT ( 'NONE',  ( 0.5839879327111915375, 37.94312859586454323, -29.22928252017475970 ) ) ;
#34320=CARTESIAN_POINT ( 'NONE',  ( 1.227938101723748288, 11.92353943228006585, -41.23019537246697297 ) ) ;
#34330=CARTESIAN_POINT ( 'NONE',  ( 4.967162193818130511, -28.74031574029989855, -32.10009971360102554 ) ) ;
#34331=B_SPLINE_CURVE_WITH_KNOTS ( 'NONE', 3,
 ( #37330, #7313, #13212, #11750, #42646, #27607 ),
 .UNSPECIFIED., .F., .F.,
 ( 4, 2, 4 ),
 ( 7.040638946443416885E-18, 0.0002445244328975362097, 0.0004890488657950653722 ),
 .UNSPECIFIED. ) ;
#34334=( BOUNDED_SURFACE ( )  B_SPLINE_SURFACE ( 3, 1, ( 
 ( #57898, #61363 ),
 ( #584, #23476 ),
 ( #47919, #19718 ),
 ( #38844, #47292 ) ),
 .UNSPECIFIED., .F., .F., .F. ) 
 B_SPLINE_SURFACE_WITH_KNOTS ( ( 4, 4 ),
 ( 2, 2 ),
 ( 0.000000000000000000, 1.000000000000000000 ),
 ( 0.000000000000000000, 1.000000000000000000 ),
 .UNSPECIFIED. ) 
 GEOMETRIC_REPRESENTATION_ITEM ( )  RATIONAL_B_SPLINE_SURFACE ( (
 ( 1.000000000000000000, 1.000000000000000000),
 ( 0.7269869731126821222, 0.9931720237060910339),
 ( 0.7269869731126821222, 0.9931720237060910339),
 ( 1.000000000000000000, 1.000000000000000000) ) ) 
 REPRESENTATION_ITEM ( '' )  SURFACE ( )  );
#34335=DIRECTION ( 'NONE',  ( -0.07836865515943411409, -0.9893941468723549404, -0.1223011693452953769 ) ) ;
#34340=VERTEX_POINT ( 'NONE', #18973 ) ;
#34343=CARTESIAN_POINT ( 'NONE',  ( 2.624215991343608501, 47.76052319582223049, -4.864192649744909502 ) ) ;
#34350=DIRECTION ( 'NONE',  ( 1.000000000000000000, 0.000000000000000000, 0.000000000000000000 ) ) ;
#34352=CARTESIAN_POINT ( 'NONE',  ( 0.9757402383260935785, 39.67468066200785870, -16.34189654378392120 ) ) ;
#34355=ORIENTED_EDGE ( 'NONE', *, *, #41951, .F. ) ;
#34357=FACE_OUTER_BOUND ( 'NONE', #46495, .T. ) ;
#34361=AXIS2_PLACEMENT_3D ( 'NONE', #44405, #10552, #29649 ) ;
#34367=CARTESIAN_POINT ( 'NONE',  ( 4.967162193818130511, 38.44485641567099776, -19.45289607368781759 ) ) ;
#34371=CARTESIAN_POINT ( 'NONE',  ( 0.5839880159502356394, -12.44022138820718126, 46.25220722086343272 ) ) ;
#34373=CARTESIAN_POINT ( 'NONE',  ( 0.5807400328401574052, 38.33001520688949881, 28.72484455891654420 ) ) ;
#34374=ADVANCED_FACE ( 'NONE', ( #57753 ), #37995, .F. ) ;
#34376=DIRECTION ( 'NONE',  ( 0.000000000000000000, 0.000000000000000000, 1.000000000000000000 ) ) ;
#34382=EDGE_CURVE ( 'NONE', #10602, #20520, #38089, .T. ) ;
#34383=B_SPLINE_CURVE_WITH_KNOTS ( 'NONE', 3,
 ( #38878, #57931, #48549, #4998 ),
 .UNSPECIFIED., .F., .F.,
 ( 4, 4 ),
 ( 1.028564492747080581E-18, 0.004444878191957681718 ),
 .UNSPECIFIED. ) ;
#34386=ORIENTED_EDGE ( 'NONE', *, *, #20922, .T. ) ;
#34394=EDGE_CURVE ( 'NONE', #29077, #7813, #46463, .T. ) ;
#34409=EDGE_LOOP ( 'NONE', ( #58078, #18841, #33303, #18059 ) ) ;
#34410=CARTESIAN_POINT ( 'NONE',  ( 5.959828726073459926, -14.51059719297126627, 14.51699876360174812 ) ) ;
#34412=CARTESIAN_POINT ( 'NONE',  ( 4.956653778116949738, -36.51451553856396970, -31.29546495791881000 ) ) ;
#34416=CARTESIAN_POINT ( 'NONE',  ( 0.5809828226811617480, 5.711058609465307967, 47.55412398569209387 ) ) ;
#34417=CARTESIAN_POINT ( 'NONE',  ( 0.5834872094924170582, -6.476680342366908150, 47.45604551759235079 ) ) ;
#34421=B_SPLINE_CURVE_WITH_KNOTS ( 'NONE', 3,
 ( #17321, #24098, #42921, #14407 ),
 .UNSPECIFIED., .F., .F.,
 ( 4, 4 ),
 ( 0.000000000000000000, 0.004446090762761357312 ),
 .UNSPECIFIED. ) ;
#34422=ORIENTED_EDGE ( 'NONE', *, *, #15470, .F. ) ;
#34425=ADVANCED_FACE ( 'NONE', ( #6974 ), #49121, .F. ) ;
#34428=DIRECTION ( 'NONE',  ( 0.000000000000000000, 0.000000000000000000, 1.000000000000000000 ) ) ;
#34429=LINE ( 'NONE', #53798, #55803 ) ;
#34432=ORIENTED_EDGE ( 'NONE', *, *, #33058, .T. ) ;
#34449=CARTESIAN_POINT ( 'NONE',  ( 5.959828726073459926, 20.52560994243598813, -0.004526594003165452379 ) ) ;
#34451=EDGE_LOOP ( 'NONE', ( #8395, #10905, #45145, #56459 ) ) ;
#34462=CARTESIAN_POINT ( 'NONE',  ( 0.9730545539215883499, 15.95224156741883270, -39.83279466599022811 ) ) ;
#34478=ORIENTED_EDGE ( 'NONE', *, *, #2961, .F. ) ;
#34491=EDGE_LOOP ( 'NONE', ( #40016, #200, #54920, #43421 ) ) ;
#34493=B_SPLINE_CURVE_WITH_KNOTS ( 'NONE', 3,
 ( #57920, #14972, #7454, #54142, #16903, #59469 ),
 .UNSPECIFIED., .F., .F.,
 ( 4, 2, 4 ),
 ( 3.529906531158615134E-18, 0.0002445244328975414139, 0.0004890488657950793584 ),
 .UNSPECIFIED. ) ;
#34494=ORIENTED_EDGE ( 'NONE', *, *, #38642, .F. ) ;
#34497=CARTESIAN_POINT ( 'NONE',  ( 0.5807400328401637335, 0.5448834511089987176, 47.89582301953903709 ) ) ;
#34506=CARTESIAN_POINT ( 'NONE',  ( 0.5827357941260211671, -44.10984861950467462, 18.66407988912473925 ) ) ;
#34512=CARTESIAN_POINT ( 'NONE',  ( 5.860006189529234355, -3.137522369585849624, 48.13093674595583593 ) ) ;
#34513=DIRECTION ( 'NONE',  ( -1.000000000000000000, -0.000000000000000000, -0.000000000000000000 ) ) ;
#34518=LINE ( 'NONE', #29801, #42681 ) ;
#34521=EDGE_CURVE ( 'NONE', #27525, #20977, #9092, .T. ) ;
#34522=CARTESIAN_POINT ( 'NONE',  ( 0.5839254288179537289, 33.80331890503270387, 33.93171296845855522 ) ) ;
#34525=CARTESIAN_POINT ( 'NONE',  ( 0.5839879882012687373, 29.15719377327500439, -37.99844431214138041 ) ) ;
#34529=EDGE_CURVE ( 'NONE', #6221, #55702, #13565, .T. ) ;
#34530=ORIENTED_EDGE ( 'NONE', *, *, #3288, .F. ) ;
#34548=DIRECTION ( 'NONE',  ( -0.07836865515943411409, -0.007886984708650450482, -0.9968932487286225053 ) ) ;
#34578=DIRECTION ( 'NONE',  ( -1.000000000000000000, -0.000000000000000000, -0.000000000000000000 ) ) ;
#34579=CARTESIAN_POINT ( 'NONE',  ( 2.624215991343620935, -34.92983774302943090, -32.93378783738885573 ) ) ;
#34583=( BOUNDED_SURFACE ( )  B_SPLINE_SURFACE ( 3, 1, ( 
 ( #40046, #25594 ),
 ( #50321, #10898 ),
 ( #20900, #15902 ),
 ( #11201, #55012 ) ),
 .UNSPECIFIED., .F., .F., .F. ) 
 B_SPLINE_SURFACE_WITH_KNOTS ( ( 4, 4 ),
 ( 2, 2 ),
 ( 0.000000000000000000, 1.000000000000000000 ),
 ( 0.000000000000000000, 1.000000000000000000 ),
 .UNSPECIFIED. ) 
 GEOMETRIC_REPRESENTATION_ITEM ( )  RATIONAL_B_SPLINE_SURFACE ( (
 ( 1.000000000000000000, 1.000000000000000000),
 ( 0.7269869731126817891, 0.9931720237060910339),
 ( 0.7269869731126817891, 0.9931720237060910339),
 ( 1.000000000000000000, 1.000000000000000000) ) ) 
 REPRESENTATION_ITEM ( '' )  SURFACE ( )  );
#34585=ORIENTED_EDGE ( 'NONE', *, *, #39217, .F. ) ;
#34593=CARTESIAN_POINT ( 'NONE',  ( 1.154321485836933725, 6.418927614506086954, 42.43366804742919385 ) ) ;
#34594=FACE_OUTER_BOUND ( 'NONE', #14050, .T. ) ;
#34604=EDGE_CURVE ( 'NONE', #23510, #47692, #59908, .T. ) ;
#34606=VERTEX_POINT ( 'NONE', #14801 ) ;
#34609=CARTESIAN_POINT ( 'NONE',  ( 0.5836750258453369256, -41.38803015411989605, -24.10509086647793353 ) ) ;
#34613=DIRECTION ( 'NONE',  ( 0.000000000000000000, 0.000000000000000000, 1.000000000000000000 ) ) ;
#34622=ORIENTED_EDGE ( 'NONE', *, *, #40922, .T. ) ;
#34633=CARTESIAN_POINT ( 'NONE',  ( 4.956653778116966613, 0.000000000000000000, 0.000000000000000000 ) ) ;
#34636=ORIENTED_EDGE ( 'NONE', *, *, #1739, .T. ) ;
#34637=CARTESIAN_POINT ( 'NONE',  ( 0.5800708057587392608, -46.42229836006543309, 11.78915002112706212 ) ) ;
#34641=CARTESIAN_POINT ( 'NONE',  ( 0.5827359174754822568, 24.26188383263427184, -41.29633904010488266 ) ) ;
#34643=CARTESIAN_POINT ( 'NONE',  ( 3.407937589446174087, -10.00592723328967715, 9.356405769959017960 ) ) ;
#34644=CARTESIAN_POINT ( 'NONE',  ( 5.981074661064941900, -20.34795181394750685, 2.687517936919654016 ) ) ;
#34648=CARTESIAN_POINT ( 'NONE',  ( 0.7056555295713298204, 5.417452459790411012, -47.59410019435323136 ) ) ;
#34656=FACE_OUTER_BOUND ( 'NONE', #53530, .T. ) ;
#34664=CARTESIAN_POINT ( 'NONE',  ( 5.965394784446458765, 2.693446924985354318, 20.34787558161487908 ) ) ;
#34674=FACE_OUTER_BOUND ( 'NONE', #57263, .T. ) ;
#34675=ORIENTED_EDGE ( 'NONE', *, *, #10604, .F. ) ;
#34676=ORIENTED_EDGE ( 'NONE', *, *, #3949, .F. ) ;
#34678=CARTESIAN_POINT ( 'NONE',  ( 5.965394784446460541, 20.34787558161483645, 2.693446924985696267 ) ) ;
#34686=VERTEX_POINT ( 'NONE', #37694 ) ;
#34687=ORIENTED_EDGE ( 'NONE', *, *, #3335, .T. ) ;
#34691=CARTESIAN_POINT ( 'NONE',  ( 2.624215991343620935, -17.05978231157435943, 44.87417713512083139 ) ) ;
#34697=( BOUNDED_SURFACE ( )  B_SPLINE_SURFACE ( 3, 1, ( 
 ( #24971, #34373 ),
 ( #44110, #6429 ),
 ( #20880, #30570 ),
 ( #1436, #59380 ) ),
 .UNSPECIFIED., .F., .F., .F. ) 
 B_SPLINE_SURFACE_WITH_KNOTS ( ( 4, 4 ),
 ( 2, 2 ),
 ( 0.000000000000000000, 1.000000000000000000 ),
 ( 0.000000000000000000, 1.000000000000000000 ),
 .UNSPECIFIED. ) 
 GEOMETRIC_REPRESENTATION_ITEM ( )  RATIONAL_B_SPLINE_SURFACE ( (
 ( 1.000000000000000000, 1.000000000000000000),
 ( 0.9732289882329797637, 0.9999525324661233672),
 ( 0.9732289882329797637, 0.9999525324661233672),
 ( 1.000000000000000000, 1.000000000000000000) ) ) 
 REPRESENTATION_ITEM ( '' )  SURFACE ( )  );
#34698=CARTESIAN_POINT ( 'NONE',  ( 0.7057020205114994393, -44.57024707370723604, 17.55108080125430448 ) ) ;
#34699=EDGE_LOOP ( 'NONE', ( #6467, #10480, #29883, #6351 ) ) ;
#34705=CARTESIAN_POINT ( 'NONE',  ( 0.5800708119828335008, -41.78924007434309118, -23.40241990038080999 ) ) ;
#34710=CARTESIAN_POINT ( 'NONE',  ( 4.967162193818130511, -43.02067033766017801, -2.375726030843023029 ) ) ;
#34713=CARTESIAN_POINT ( 'NONE',  ( 3.407937589446174087, 0.4592810312473891710, -13.69123696618923880 ) ) ;
#34715=ORIENTED_EDGE ( 'NONE', *, *, #34929, .F. ) ;
#34723=CARTESIAN_POINT ( 'NONE',  ( 1.227938101723748288, -39.32113113558953899, -17.20315230597885758 ) ) ;
#34725=CARTESIAN_POINT ( 'NONE',  ( 0.5827359174754822568, 5.891371786504956631, 47.53228759166450601 ) ) ;
#34730=VECTOR ( 'NONE', #1202, 1000.000000000000000 ) ;
#34741=CARTESIAN_POINT ( 'NONE',  ( 4.967162193818130511, -42.96271701169388280, 3.259922920617591924 ) ) ;
#34753=CIRCLE ( 'NONE', #15744, 48.09070567114147110 ) ;
#34763=CARTESIAN_POINT ( 'NONE',  ( 0.5819845079324660331, 17.90867223323947144, -44.42187385013345136 ) ) ;
#34781=CARTESIAN_POINT ( 'NONE',  ( 2.624215991343608501, 28.09277600149218657, 38.92973006074523568 ) ) ;
#34783=LINE ( 'NONE', #38565, #31741 ) ;
#34784=FACE_OUTER_BOUND ( 'NONE', #40148, .T. ) ;
#34788=CARTESIAN_POINT ( 'NONE',  ( 4.956653778116893783, -15.97476558431863758, -45.35992544608534160 ) ) ;
#34792=CARTESIAN_POINT ( 'NONE',  ( 1.227938101723756947, -20.72293514920776758, 37.58536632582772086 ) ) ;
#34800=CARTESIAN_POINT ( 'NONE',  ( 0.5839880159502324197, -44.26747004398431073, 18.28706857028357291 ) ) ;
#34803=CARTESIAN_POINT ( 'NONE',  ( 0.7762783648524383961, 47.37038525648369358, -7.133808749408959038 ) ) ;
#34805=ORIENTED_EDGE ( 'NONE', *, *, #33760, .T. ) ;
#34806=CARTESIAN_POINT ( 'NONE',  ( 0.9740398440564311811, 33.78760696452741286, -26.44872719679335660 ) ) ;
#34812=CARTESIAN_POINT ( 'NONE',  ( 0.5809828226811553087, -47.89273459658654275, 0.5448590168530708100 ) ) ;
#34814=CARTESIAN_POINT ( 'NONE',  ( -19.03272015457537947, -12.36519495213270936, 1.833918244462691804 ) ) ;
#34816=EDGE_CURVE ( 'NONE', #20940, #5144, #44303, .T. ) ;
#34817=CONICAL_SURFACE ( 'NONE', #56825, 43.08621763946400307, 1.568696531533066763 ) ;
#34827=CARTESIAN_POINT ( 'NONE',  ( 1.088313998177380837, -42.64115081428568743, 4.827222641555085403 ) ) ;
#34828=CARTESIAN_POINT ( 'NONE',  ( -16.29483284318931879, -7.897602733921581297, -1.291116304381162649 ) ) ;
#34830=CARTESIAN_POINT ( 'NONE',  ( 0.9968887458511658251, -37.48500720268744857, 20.88287852258433475 ) ) ;
#34831=CARTESIAN_POINT ( 'NONE',  ( 0.8551540677456715978, 46.51172240253119838, 11.51835730326495977 ) ) ;
#34834=CARTESIAN_POINT ( 'NONE',  ( 0.5819845901640501307, 33.54497622115130895, 34.18710267837666095 ) ) ;
#34841=CARTESIAN_POINT ( 'NONE',  ( 3.783198216974387851, -35.16829104054189514, 24.80909581868430180 ) ) ;
#34843=CARTESIAN_POINT ( 'NONE',  ( 0.9757787079277435716, 5.561523338227147839, 42.54650880470565255 ) ) ;
#34844=DIRECTION ( 'NONE',  ( -1.000000000000000000, -0.000000000000000000, -0.000000000000000000 ) ) ;
#34848=FACE_OUTER_BOUND ( 'NONE', #34491, .T. ) ;
#34853=ORIENTED_EDGE ( 'NONE', *, *, #39006, .F. ) ;
#34858=ORIENTED_EDGE ( 'NONE', *, *, #16839, .F. ) ;
#34866=CARTESIAN_POINT ( 'NONE',  ( 0.6067375320500725255, 24.55990317723916050, -41.12099578548227896 ) ) ;
#34872=B_SPLINE_CURVE_WITH_KNOTS ( 'NONE', 3,
 ( #35251, #24921, #54308, #11431 ),
 .UNSPECIFIED., .F., .F.,
 ( 4, 4 ),
 ( 1.734723475976807094E-18, 0.004444878191957671310 ),
 .UNSPECIFIED. ) ;
#34883=EDGE_CURVE ( 'NONE', #35798, #9554, #35304, .T. ) ;
#34885=VERTEX_POINT ( 'NONE', #20623 ) ;
#34886=VERTEX_POINT ( 'NONE', #50053 ) ;
#34888=ADVANCED_FACE ( 'NONE', ( #26233 ), #40369, .F. ) ;
#34900=EDGE_CURVE ( 'NONE', #47955, #14355, #35973, .T. ) ;
#34913=CARTESIAN_POINT ( 'NONE',  ( 0.9749527285493305717, -11.38116287125083304, 41.37154756071290507 ) ) ;
#34928=ORIENTED_EDGE ( 'NONE', *, *, #3532, .T. ) ;
#34929=EDGE_CURVE ( 'NONE', #59165, #27464, #37404, .T. ) ;
#34930=CARTESIAN_POINT ( 'NONE',  ( 0.9730545539215883499, 42.90536227157002003, -0.5054011016614180507 ) ) ;
#34943=AXIS2_PLACEMENT_3D ( 'NONE', #13532, #32637, #51721 ) ;
#34944=ORIENTED_EDGE ( 'NONE', *, *, #10021, .F. ) ;
#34949=ORIENTED_EDGE ( 'NONE', *, *, #14391, .F. ) ;
#34950=CARTESIAN_POINT ( 'NONE',  ( 5.960721111146673579, 19.82781442290490403, 5.306302591836648652 ) ) ;
#34952=CARTESIAN_POINT ( 'NONE',  ( 0.8557997880470599172, -41.02602466100761802, -24.73961900479294584 ) ) ;
#34971=CIRCLE ( 'NONE', #15961, 48.09070567114147110 ) ;
#34973=CARTESIAN_POINT ( 'NONE',  ( -4.473700000000000010, 0.000000000000000000, 0.000000000000000000 ) ) ;
#34978=DIRECTION ( 'NONE',  ( -1.000000000000000000, -0.000000000000000000, -0.000000000000000000 ) ) ;
#34983=CARTESIAN_POINT ( 'NONE',  ( -17.29576878204978385, -12.34032024113386328, 1.992322322936505241 ) ) ;
#34995=EDGE_LOOP ( 'NONE', ( #18765, #9642, #33841, #12594 ) ) ;
#34997=CARTESIAN_POINT ( 'NONE',  ( 0.8551540677456715978, -37.45266983663517379, 29.88829867897801051 ) ) ;
#35001=CARTESIAN_POINT ( 'NONE',  ( 0.9722240750034576440, 0.5819398758580140996, 42.90442369954360657 ) ) ;
#35004=B_SPLINE_CURVE_WITH_KNOTS ( 'NONE', 3,
 ( #14659, #20280, #58449, #843, #48766, #43171 ),
 .UNSPECIFIED., .F., .F.,
 ( 4, 2, 4 ),
 ( 4.907736672678014827E-18, 0.0002291966416970822227, 0.0004583932833941595664 ),
 .UNSPECIFIED. ) ;
#35008=CARTESIAN_POINT ( 'NONE',  ( 0.8557997880470690211, -43.90420959842193582, 19.17299735371994629 ) ) ;
#35010=CARTESIAN_POINT ( 'NONE',  ( 0.8557997880470599172, 41.93815086860288943, -23.15977007032279289 ) ) ;
#35017=CARTESIAN_POINT ( 'NONE',  ( 2.624215991343620935, 13.78323291683783758, 45.98641578154036580 ) ) ;
#35020=B_SPLINE_CURVE_WITH_KNOTS ( 'NONE', 3,
 ( #3424, #22560, #35755, #36064, #46377, #26325, #41684, #31031, #32271, #36369, #45460, #51352, #3126, #55435, #22256, #31648, #26950, #41378, #12250 ),
 .UNSPECIFIED., .F., .F.,
 ( 4, 3, 3, 3, 3, 3, 4 ),
 ( 9.813676791237319219E-18, 0.0002724573126191738581, 0.0004086839781548484772, 0.0005449106435901825704, 0.0006811373090491529758, 0.0008459866663933752291, 0.001010840725717212282 ),
 .UNSPECIFIED. ) ;
#35027=ORIENTED_EDGE ( 'NONE', *, *, #6143, .T. ) ;
#35030=ORIENTED_EDGE ( 'NONE', *, *, #21230, .F. ) ;
#35031=CARTESIAN_POINT ( 'NONE',  ( 4.956653778116975495, -14.93973939759918323, 45.71126949320244393 ) ) ;
#35036=DIRECTION ( 'NONE',  ( 0.07439287786467664587, -0.9161872986448699185, -0.3937848822959399420 ) ) ;
#35038=CARTESIAN_POINT ( 'NONE',  ( 0.9741495583595176644, 33.79932324264184729, 26.43366215195271351 ) ) ;
#35040=CARTESIAN_POINT ( 'NONE',  ( 0.5819845079324663661, 6.701571823032717923, 47.42480735454289231 ) ) ;
#35044=ORIENTED_EDGE ( 'NONE', *, *, #25341, .F. ) ;
#35048=CARTESIAN_POINT ( 'NONE',  ( 2.281448460670571610, -25.11570011049342455, -40.87338159040662333 ) ) ;
#35055=CARTESIAN_POINT ( 'NONE',  ( 0.7056555295713294873, 7.085402321211779153, 47.37451042924655553 ) ) ;
#35061=CARTESIAN_POINT ( 'NONE',  ( 0.5809828226811548646, -47.41188724015884048, 6.791453954330148868 ) ) ;
#35067=CARTESIAN_POINT ( 'NONE',  ( 5.960721111146673579, -20.52557019979492026, 0.006321279846751705171 ) ) ;
#35073=CARTESIAN_POINT ( 'NONE',  ( 0.6067375320500714153, -47.38951440911012014, -6.954068056451214730 ) ) ;
#35076=DIRECTION ( 'NONE',  ( 0.000000000000000000, 0.000000000000000000, 1.000000000000000000 ) ) ;
#35079=CARTESIAN_POINT ( 'NONE',  ( 0.8551540677456834771, -47.37911285756625546, 7.157691013574193128 ) ) ;
#35083=EDGE_CURVE ( 'NONE', #55130, #23728, #58321, .T. ) ;
#35088=ORIENTED_EDGE ( 'NONE', *, *, #29079, .F. ) ;
#35089=LINE ( 'NONE', #41561, #58010 ) ;
#35093=CARTESIAN_POINT ( 'NONE',  ( 5.965394784446460541, -0.01447339372467435804, 20.52536205633085231 ) ) ;
#35097=DIRECTION ( 'NONE',  ( -1.000000000000000000, -0.000000000000000000, -0.000000000000000000 ) ) ;
#35099=EDGE_LOOP ( 'NONE', ( #46555, #61661, #59802, #33101 ) ) ;
#35103=CARTESIAN_POINT ( 'NONE',  ( 0.5850706913938533704, -12.57184842332050145, 46.21698775168641760 ) ) ;
#35112=EDGE_CURVE ( 'NONE', #56726, #41729, #30723, .T. ) ;
#35120=CIRCLE ( 'NONE', #31077, 48.09070567114147110 ) ;
#35128=VERTEX_POINT ( 'NONE', #42521 ) ;
#35131=CARTESIAN_POINT ( 'NONE',  ( 1.227938101723748288, 33.52879263017863565, 26.79402671879338271 ) ) ;
#35135=CARTESIAN_POINT ( 'NONE',  ( 4.967162193818130511, -3.259922920617460029, -42.96271701169388280 ) ) ;
#35138=LINE ( 'NONE', #48596, #15420 ) ;
#35146=LINE ( 'NONE', #1591, #465 ) ;
#35147=DIRECTION ( 'NONE',  ( -1.000000000000000000, -0.000000000000000000, -0.000000000000000000 ) ) ;
#35150=CARTESIAN_POINT ( 'NONE',  ( 5.974727161628367256, 5.327229920347150482, 19.82156119440447384 ) ) ;
#35151=CARTESIAN_POINT ( 'NONE',  ( 0.9730545539215883499, -5.099196237955184507, 42.60426903087352457 ) ) ;
#35165=ORIENTED_EDGE ( 'NONE', *, *, #25283, .T. ) ;
#35167=ORIENTED_EDGE ( 'NONE', *, *, #44909, .F. ) ;
#35169=DIRECTION ( 'NONE',  ( 0.07439287786467665975, 0.8701500408883677817, -0.4871392060437993443 ) ) ;
#35174=( BOUNDED_SURFACE ( )  B_SPLINE_SURFACE ( 3, 1, ( 
 ( #46017, #60075 ),
 ( #50667, #23410 ),
 ( #8998, #60993 ),
 ( #42238, #61600 ) ),
 .UNSPECIFIED., .F., .F., .F. ) 
 B_SPLINE_SURFACE_WITH_KNOTS ( ( 4, 4 ),
 ( 2, 2 ),
 ( 0.000000000000000000, 1.000000000000000000 ),
 ( 0.000000000000000000, 1.000000000000000000 ),
 .UNSPECIFIED. ) 
 GEOMETRIC_REPRESENTATION_ITEM ( )  RATIONAL_B_SPLINE_SURFACE ( (
 ( 1.000000000000000000, 1.000000000000000000),
 ( 0.9953390228620291325, 0.8624445117760984880),
 ( 0.9953390228620291325, 0.8624445117760984880),
 ( 1.000000000000000000, 1.000000000000000000) ) ) 
 REPRESENTATION_ITEM ( '' )  SURFACE ( )  );
#35176=ADVANCED_FACE ( 'NONE', ( #37263 ), #61904, .F. ) ;
#35182=VERTEX_POINT ( 'NONE', #9348 ) ;
#35190=CARTESIAN_POINT ( 'NONE',  ( 4.967162193818130511, -38.44485641567084855, 19.45289607368810181 ) ) ;
#35195=CARTESIAN_POINT ( 'NONE',  ( 5.974727161628369032, 16.27409205901359002, 12.50710176110013272 ) ) ;
#35204=FACE_OUTER_BOUND ( 'NONE', #3106, .T. ) ;
#35217=CARTESIAN_POINT ( 'NONE',  ( 2.624215991343620935, 44.87417713512088824, 17.05978231157419955 ) ) ;
#35219=CARTESIAN_POINT ( 'NONE',  ( 4.303969348037258058, 39.44373910178610032, 27.54579249306222977 ) ) ;
#35226=VERTEX_POINT ( 'NONE', #47575 ) ;
#35227=CARTESIAN_POINT ( 'NONE',  ( 2.526552050251863246, 40.15571433620807795, -15.32056541070799405 ) ) ;
#35228=CARTESIAN_POINT ( 'NONE',  ( 0.8557997880470599172, 24.73961900479308440, -41.02602466100753276 ) ) ;
#35233=EDGE_LOOP ( 'NONE', ( #49734, #2374, #46125, #26456 ) ) ;
#35237=CARTESIAN_POINT ( 'NONE',  ( 0.8557997880470697982, -47.60865952216995822, -5.347802024197736870 ) ) ;
#35239=CARTESIAN_POINT ( 'NONE',  ( 3.783278058412225864, 42.41041238787303769, -7.325100730113862646 ) ) ;
#35240=ADVANCED_FACE ( 'NONE', ( #4942 ), #5906, .F. ) ;
#35241=VERTEX_POINT ( 'NONE', #4010 ) ;
#35242=CARTESIAN_POINT ( 'NONE',  ( 0.8557997880470697982, 13.27832040216639520, 46.03118133706031045 ) ) ;
#35243=CIRCLE ( 'NONE', #58226, 48.09070567114147110 ) ;
#35246=VECTOR ( 'NONE', #21501, 1000.000000000000227 ) ;
#35251=CARTESIAN_POINT ( 'NONE',  ( 0.8557997880470690211, 19.17299735372009550, 43.90420959842187187 ) ) ;
#35254=CARTESIAN_POINT ( 'NONE',  ( 0.5819845901640493535, 44.42187107932970491, -17.90867915372005115 ) ) ;
#35255=CARTESIAN_POINT ( 'NONE',  ( 5.974727161628369032, 14.52429704002363486, -14.50236057684829838 ) ) ;
#35257=CARTESIAN_POINT ( 'NONE',  ( 0.5827359174754813687, 12.74690115177672567, -46.16863801597752115 ) ) ;
#35263=CARTESIAN_POINT ( 'NONE',  ( 0.8557997880470606944, -46.50333260518566902, 11.51622788066442027 ) ) ;
#35264=CARTESIAN_POINT ( 'NONE',  ( 0.5809828226811617480, 28.72298383114487663, 38.32755012159156394 ) ) ;
#35265=ORIENTED_EDGE ( 'NONE', *, *, #3741, .T. ) ;
#35268=VERTEX_POINT ( 'NONE', #13768 ) ;
#35270=CARTESIAN_POINT ( 'NONE',  ( 4.960156602257184133, -41.85906677498947204, -20.07163247083191493 ) ) ;
#35274=CARTESIAN_POINT ( 'NONE',  ( 0.5836750258453352602, 46.31062999473601138, -12.22088356912678186 ) ) ;
#35276=FACE_BOUND ( 'NONE', #50962, .T. ) ;
#35278=B_SPLINE_CURVE_WITH_KNOTS ( 'NONE', 3,
 ( #49586, #6642, #39608, #38995, #58051, #44012 ),
 .UNSPECIFIED., .F., .F.,
 ( 4, 2, 4 ),
 ( 1.480053515295545178E-16, 0.0002445252820015214124, 0.0004890505640028948312 ),
 .UNSPECIFIED. ) ;
#35284=CARTESIAN_POINT ( 'NONE',  ( 1.154321713695927620, -17.18284946700656945, 39.32643513900325871 ) ) ;
#35287=AXIS2_PLACEMENT_3D ( 'NONE', #47616, #42936, #35076 ) ;
#35298=CARTESIAN_POINT ( 'NONE',  ( 4.303969348037258058, 32.45857549159350697, -35.51084504003163289 ) ) ;
#35302=CARTESIAN_POINT ( 'NONE',  ( 0.6846871229502899947, 44.58493949244006416, 17.53234844287758065 ) ) ;
#35304=B_SPLINE_CURVE_WITH_KNOTS ( 'NONE', 3,
 ( #35666, #54729, #30944, #44461, #1488, #29700 ),
 .UNSPECIFIED., .F., .F.,
 ( 4, 2, 4 ),
 ( 1.084202172485504434E-19, 0.0002291966416970792682, 0.0004583932833941584280 ),
 .UNSPECIFIED. ) ;
#35306=ORIENTED_EDGE ( 'NONE', *, *, #40471, .F. ) ;
#35318=ORIENTED_EDGE ( 'NONE', *, *, #47265, .F. ) ;
#35320=CARTESIAN_POINT ( 'NONE',  ( 0.8557997880470599172, 41.02602466100778145, 24.73961900479265807 ) ) ;
#35322=( BOUNDED_SURFACE ( )  B_SPLINE_SURFACE ( 3, 1, ( 
 ( #7045, #16174 ),
 ( #11791, #59061 ),
 ( #16796, #59994 ),
 ( #40929, #36215 ) ),
 .UNSPECIFIED., .F., .F., .F. ) 
 B_SPLINE_SURFACE_WITH_KNOTS ( ( 4, 4 ),
 ( 2, 2 ),
 ( 0.000000000000000000, 1.000000000000000000 ),
 ( 0.000000000000000000, 1.000000000000000000 ),
 .UNSPECIFIED. ) 
 GEOMETRIC_REPRESENTATION_ITEM ( )  RATIONAL_B_SPLINE_SURFACE ( (
 ( 1.000000000000000000, 1.000000000000000000),
 ( 0.9732289882329797637, 0.9999525324661233672),
 ( 0.9732289882329797637, 0.9999525324661233672),
 ( 1.000000000000000000, 1.000000000000000000) ) ) 
 REPRESENTATION_ITEM ( '' )  SURFACE ( )  );
#35331=EDGE_CURVE ( 'NONE', #35962, #9258, #9151, .T. ) ;
#35347=CARTESIAN_POINT ( 'NONE',  ( 4.960156602257182357, -8.553784487773192780, 45.62767441207047625 ) ) ;
#35348=CARTESIAN_POINT ( 'NONE',  ( 0.5809828226811617480, 11.86925843957166471, 46.40184912890843805 ) ) ;
#35352=AXIS2_PLACEMENT_3D ( 'NONE', #23347, #19580, #20491 ) ;
#35356=CARTESIAN_POINT ( 'NONE',  ( 0.5836750258453348161, 18.16108240858346790, 44.31929073742199421 ) ) ;
#35363=ORIENTED_EDGE ( 'NONE', *, *, #2673, .F. ) ;
#35370=CARTESIAN_POINT ( 'NONE',  ( 5.959547316686252039, -18.96456592444106448, 7.851524054666073837 ) ) ;
#35377=CARTESIAN_POINT ( 'NONE',  ( -4.473699999999999122, 0.000000000000000000, 0.000000000000000000 ) ) ;
#35382=CARTESIAN_POINT ( 'NONE',  ( 0.5807400328401637335, -24.41979442053199634, 41.20655774452961850 ) ) ;
#35387=CARTESIAN_POINT ( 'NONE',  ( 0.9747592971366227932, -39.76507150545822356, -16.12077520819492804 ) ) ;
#35391=EDGE_CURVE ( 'NONE', #7563, #28286, #10592, .T. ) ;
#35392=CARTESIAN_POINT ( 'NONE',  ( 4.967162193818130511, 0.000000000000000000, 0.000000000000000000 ) ) ;
#35400=B_SPLINE_CURVE_WITH_KNOTS ( 'NONE', 3,
 ( #7404, #40667, #1475, #11521, #49724, #54092 ),
 .UNSPECIFIED., .F., .F.,
 ( 4, 2, 4 ),
 ( 3.471140604459641645E-18, 0.0002291966416970819787, 0.0004583932833941604880 ),
 .UNSPECIFIED. ) ;
#35403=CARTESIAN_POINT ( 'NONE',  ( 5.965394784446458765, 12.48356622107676728, -16.29267539192330361 ) ) ;
#35418=CARTESIAN_POINT ( 'NONE',  ( 0.6846871229502932144, 17.53234844287741723, 44.58493949244010679 ) ) ;
#35419=ORIENTED_EDGE ( 'NONE', *, *, #17167, .T. ) ;
#35420=CARTESIAN_POINT ( 'NONE',  ( 0.5807400328401637335, 12.92266817606015294, 46.12278621143501312 ) ) ;
#35426=ORIENTED_EDGE ( 'NONE', *, *, #28979, .F. ) ;
#35427=B_SPLINE_CURVE_WITH_KNOTS ( 'NONE', 3,
 ( #61472, #61176, #9801, #18597 ),
 .UNSPECIFIED., .F., .F.,
 ( 4, 4 ),
 ( 2.168404344971008868E-19, 0.004444878191957678248 ),
 .UNSPECIFIED. ) ;
#35430=CARTESIAN_POINT ( 'NONE',  ( 5.974727161628367256, 17.76736931401860531, -10.27590650342018996 ) ) ;
#35431=VERTEX_POINT ( 'NONE', #35031 ) ;
#35440=CARTESIAN_POINT ( 'NONE',  ( 4.960156602257181468, 9.558288641082377524, -45.42786611289300680 ) ) ;
#35447=CARTESIAN_POINT ( 'NONE',  ( 4.956653778116975495, 8.845409907520915382, 47.27023054223757015 ) ) ;
#35448=FACE_OUTER_BOUND ( 'NONE', #56079, .T. ) ;
#35450=CARTESIAN_POINT ( 'NONE',  ( 5.959547316686252039, 18.96183906913543282, -7.858107265727552360 ) ) ;
#35451=CARTESIAN_POINT ( 'NONE',  ( 2.624215991343620935, 42.26352390376096935, 22.77108897942150634 ) ) ;
#35452=CARTESIAN_POINT ( 'NONE',  ( 3.660176727303397382, 36.93665184075219798, 30.71420464230583036 ) ) ;
#35457=CARTESIAN_POINT ( 'NONE',  ( 4.960156602257180580, -8.553784487772583489, -45.62767441207059704 ) ) ;
#35482=ORIENTED_EDGE ( 'NONE', *, *, #4837, .F. ) ;
#35485=ORIENTED_EDGE ( 'NONE', *, *, #5352, .F. ) ;
#35488=CARTESIAN_POINT ( 'NONE',  ( 0.5807400328401574052, 34.25275203086281550, -33.48217046439075517 ) ) ;
#35494=CARTESIAN_POINT ( 'NONE',  ( 0.8557997880470599172, 24.73961900479308440, -41.02602466100753276 ) ) ;
#35499=CARTESIAN_POINT ( 'NONE',  ( 2.526552050251860582, -37.81244156771004583, 20.43086833796944290 ) ) ;
#35501=CARTESIAN_POINT ( 'NONE',  ( 2.281448460670564504, 42.18752512472242699, 22.83953674062028227 ) ) ;
#35505=CARTESIAN_POINT ( 'NONE',  ( 5.965394784446460541, -19.82223131420050422, -5.326334832595580160 ) ) ;
#35509=CARTESIAN_POINT ( 'NONE',  ( 4.956653778116991482, -31.29546495791826644, -36.51451553856450971 ) ) ;
#35510=EDGE_CURVE ( 'NONE', #33332, #57526, #20208, .T. ) ;
#35512=FACE_OUTER_BOUND ( 'NONE', #32887, .T. ) ;
#35514=LINE ( 'NONE', #30467, #16232 ) ;
#35517=CARTESIAN_POINT ( 'NONE',  ( 0.5850706913938534814, 33.99603398296591195, 33.73916126769462664 ) ) ;
#35518=CIRCLE ( 'NONE', #26504, 43.08621763946400307 ) ;
#35522=AXIS2_PLACEMENT_3D ( 'NONE', #32409, #55565, #8265 ) ;
#35523=CARTESIAN_POINT ( 'NONE',  ( 0.8557997880470697982, -37.44587306708118035, 29.88293891557457371 ) ) ;
#35534=CARTESIAN_POINT ( 'NONE',  ( 2.281448460670572942, -19.56578495220138336, -43.80196084514300736 ) ) ;
#35536=ORIENTED_EDGE ( 'NONE', *, *, #45229, .F. ) ;
#35546=( BOUNDED_SURFACE ( )  B_SPLINE_SURFACE ( 3, 1, ( 
 ( #17310, #36427 ),
 ( #55495, #50805 ),
 ( #27014, #27938 ),
 ( #42365, #13539 ) ),
 .UNSPECIFIED., .F., .F., .F. ) 
 B_SPLINE_SURFACE_WITH_KNOTS ( ( 4, 4 ),
 ( 2, 2 ),
 ( 0.000000000000000000, 1.000000000000000000 ),
 ( 0.000000000000000000, 1.000000000000000000 ),
 .UNSPECIFIED. ) 
 GEOMETRIC_REPRESENTATION_ITEM ( )  RATIONAL_B_SPLINE_SURFACE ( (
 ( 1.000000000000000000, 1.000000000000000000),
 ( 0.9953390228620291325, 0.8624445117761032620),
 ( 0.9953390228620291325, 0.8624445117761032620),
 ( 1.000000000000000000, 1.000000000000000000) ) ) 
 REPRESENTATION_ITEM ( '' )  SURFACE ( )  );
#35548=CARTESIAN_POINT ( 'NONE',  ( 0.8557997880470690211, 7.156447707085701104, 47.37054680076709445 ) ) ;
#35552=B_SPLINE_CURVE_WITH_KNOTS ( 'NONE', 3,
 ( #58642, #53948, #44912, #1949 ),
 .UNSPECIFIED., .F., .F.,
 ( 4, 4 ),
 ( 0.000000000000000000, 0.004048833967417085622 ),
 .UNSPECIFIED. ) ;
#35556=VECTOR ( 'NONE', #4911, 1000.000000000000114 ) ;
#35558=VERTEX_POINT ( 'NONE', #23686 ) ;
#35563=B_SPLINE_CURVE_WITH_KNOTS ( 'NONE', 3,
 ( #12098, #45603, #46225, #55273, #45303, #21164, #30862, #49660, #40608, #12397, #36207, #60589, #41525, #59986, #6718, #11783 ),
 .UNSPECIFIED., .F., .F.,
 ( 4, 3, 3, 3, 3, 4 ),
 ( 1.250973872328959318E-17, 0.0002724568934985464397, 0.0004086836638483691965, 0.0005449104342063506830, 0.0008173270854453626617, 0.001089761613562683371 ),
 .UNSPECIFIED. ) ;
#35565=CARTESIAN_POINT ( 'NONE',  ( 4.967162193818130511, -28.74031574029989855, -32.10009971360102554 ) ) ;
#35573=CARTESIAN_POINT ( 'NONE',  ( 0.9758171775293923433, -21.45936886481769079, -37.15687890897639534 ) ) ;
#35580=ORIENTED_EDGE ( 'NONE', *, *, #54437, .T. ) ;
#35588=CARTESIAN_POINT ( 'NONE',  ( 4.967162193818130511, 0.000000000000000000, 0.000000000000000000 ) ) ;
#35589=CARTESIAN_POINT ( 'NONE',  ( 0.5838002273316427182, 46.29900743592995127, -12.26477999444020028 ) ) ;
#35619=ORIENTED_EDGE ( 'NONE', *, *, #20415, .F. ) ;
#35630=ORIENTED_EDGE ( 'NONE', *, *, #33689, .F. ) ;
#35633=ORIENTED_EDGE ( 'NONE', *, *, #8843, .F. ) ;
#35640=EDGE_LOOP ( 'NONE', ( #38735, #43320, #15963, #43644 ) ) ;
#35644=CARTESIAN_POINT ( 'NONE',  ( 5.960721111146673579, -18.96557324978293124, 7.848955554238177257 ) ) ;
#35653=CARTESIAN_POINT ( 'NONE',  ( 5.959547316686252039, -0.003562808153049117858, 20.52562247508876681 ) ) ;
#35666=CARTESIAN_POINT ( 'NONE',  ( 0.9730545539215883499, -42.90536227157002003, -0.5054011016617259155 ) ) ;
#35680=CARTESIAN_POINT ( 'NONE',  ( 0.5786265663353196143, 43.97352617418616205, 18.99608782658049932 ) ) ;
#35682=B_SPLINE_CURVE_WITH_KNOTS ( 'NONE', 3,
 ( #37508, #48348, #14846, #13384 ),
 .UNSPECIFIED., .F., .F.,
 ( 4, 4 ),
 ( 7.505561329662603978E-17, 0.005004741218457486526 ),
 .UNSPECIFIED. ) ;
#35686=CARTESIAN_POINT ( 'NONE',  ( 0.9972139404380291339, -42.62325912566429054, -4.947665363829212737 ) ) ;
#35687=CARTESIAN_POINT ( 'NONE',  ( 3.407937589446178528, -13.34359005742687110, -3.099921468255143253 ) ) ;
#35691=EDGE_CURVE ( 'NONE', #59165, #59626, #13687, .T. ) ;
#35696=CARTESIAN_POINT ( 'NONE',  ( 5.960221823109900008, 10.25807604135621531, -17.77840967225710145 ) ) ;
#35702=CARTESIAN_POINT ( 'NONE',  ( 0.9745511491811753579, -25.84997388131836260, -34.24777528633308066 ) ) ;
#35712=B_SPLINE_CURVE_WITH_KNOTS ( 'NONE', 3,
 ( #18427, #46633, #47551, #42255, #32222, #57218 ),
 .UNSPECIFIED., .F., .F.,
 ( 4, 2, 4 ),
 ( 7.770031522344853663E-18, 0.0002291966416970820058, 0.0004583932833941562054 ),
 .UNSPECIFIED. ) ;
#35714=VERTEX_POINT ( 'NONE', #48719 ) ;
#35715=AXIS2_PLACEMENT_3D ( 'NONE', #21339, #49841, #40469 ) ;
#35716=LINE ( 'NONE', #20674, #24855 ) ;
#35721=CARTESIAN_POINT ( 'NONE',  ( 5.965394784446458765, 14.50338846149133154, -14.52385693118987575 ) ) ;
#35725=VERTEX_POINT ( 'NONE', #34952 ) ;
#35728=ORIENTED_EDGE ( 'NONE', *, *, #38471, .F. ) ;
#35729=ORIENTED_EDGE ( 'NONE', *, *, #43504, .T. ) ;
#35730=CARTESIAN_POINT ( 'NONE',  ( 0.9740398440564311811, -0.4145941695170031194, -42.90647580953696405 ) ) ;
#35732=CARTESIAN_POINT ( 'NONE',  ( 3.660176727303416477, 45.06760739764710877, -16.63097650367919655 ) ) ;
#35740=CARTESIAN_POINT ( 'NONE',  ( 0.9736507210033049642, 34.31386771842698380, -25.76216842460662448 ) ) ;
#35742=CARTESIAN_POINT ( 'NONE',  ( 5.960721111146673579, 17.77250458025991975, -10.26825948882907191 ) ) ;
#35753=CIRCLE ( 'NONE', #13698, 48.09070567114147110 ) ;
#35755=CARTESIAN_POINT ( 'NONE',  ( 0.9747592971366217940, -33.84353661172422534, 26.37717450293414956 ) ) ;
#35756=CARTESIAN_POINT ( 'NONE',  ( 5.965394784446458765, -7.868087674480825022, -18.95742317323941961 ) ) ;
#35758=CARTESIAN_POINT ( 'NONE',  ( 0.9752132459055865565, 21.25214916889643035, -37.27572867006939106 ) ) ;
#35762=CARTESIAN_POINT ( 'NONE',  ( 4.956653778116960396, -3.690426056930336429, 47.94889704119049867 ) ) ;
#35764=ADVANCED_FACE ( 'NONE', ( #19306 ), #21494, .F. ) ;
#35765=B_SPLINE_CURVE_WITH_KNOTS ( 'NONE', 3,
 ( #59921, #7921, #54903, #31738, #16714, #31424 ),
 .UNSPECIFIED., .F., .F.,
 ( 4, 2, 4 ),
 ( 8.848046324741092137E-18, 0.0002291978881530159703, 0.0004583957763060231044 ),
 .UNSPECIFIED. ) ;
#35766=CARTESIAN_POINT ( 'NONE',  ( 5.960221823109900008, -19.82478916873571606, -5.317678907195369398 ) ) ;
#35767=CARTESIAN_POINT ( 'NONE',  ( 2.281351352603290472, 37.24546109640818514, 30.23585463601389023 ) ) ;
#35776=CARTESIAN_POINT ( 'NONE',  ( 4.967162193818130511, 18.65818244221310351, -38.83676580803746958 ) ) ;
#35782=CARTESIAN_POINT ( 'NONE',  ( 0.9757892942422830007, -41.45966865212799490, -11.05594550521687935 ) ) ;
#35784=ORIENTED_EDGE ( 'NONE', *, *, #47538, .F. ) ;
#35798=VERTEX_POINT ( 'NONE', #15224 ) ;
#35802=CARTESIAN_POINT ( 'NONE',  ( 5.958863334805807099, 16.28483817244722687, 12.49425770716493211 ) ) ;
#35808=DIRECTION ( 'NONE',  ( -1.000000000000000000, -0.000000000000000000, -0.000000000000000000 ) ) ;
#35810=CARTESIAN_POINT ( 'NONE',  ( 0.5827357941260201679, -46.35666768646128588, -12.04516435546850772 ) ) ;
#35817=ORIENTED_EDGE ( 'NONE', *, *, #29222, .F. ) ;
#35821=LINE ( 'NONE', #26704, #29819 ) ;
#35829=CARTESIAN_POINT ( 'NONE',  ( 4.967162193818130511, -14.26841313271309808, 40.65506779172159924 ) ) ;
#35830=CARTESIAN_POINT ( 'NONE',  ( 0.8557997880470599172, -41.93815086860273311, 23.15977007032308421 ) ) ;
#35835=CARTESIAN_POINT ( 'NONE',  ( 2.526464513654346433, 4.405490210169002552, -42.75268905308551126 ) ) ;
#35838=CARTESIAN_POINT ( 'NONE',  ( 0.8557997880470606944, 29.88293891557523807, -37.44587306708065455 ) ) ;
#35842=ORIENTED_EDGE ( 'NONE', *, *, #52467, .F. ) ;
#35850=CARTESIAN_POINT ( 'NONE',  ( 4.967162193818130511, 0.000000000000000000, 0.000000000000000000 ) ) ;
#35853=CARTESIAN_POINT ( 'NONE',  ( 0.5832367798473397924, 47.89515946578896433, 0.2724222379462135080 ) ) ;
#35854=CARTESIAN_POINT ( 'NONE',  ( 5.959547316686252039, -18.96183906913538308, -7.858107265727685586 ) ) ;
#35859=EDGE_CURVE ( 'NONE', #39947, #9360, #54016, .T. ) ;
#35866=CARTESIAN_POINT ( 'NONE',  ( 1.088313998177379949, 0.7798619649927278630, -42.90642884828984194 ) ) ;
#35873=VERTEX_POINT ( 'NONE', #55182 ) ;
#35874=CARTESIAN_POINT ( 'NONE',  ( 0.9749527285493317930, -30.13822974582791403, -30.54214995146802281 ) ) ;
#35879=CARTESIAN_POINT ( 'NONE',  ( 0.5850706913938533704, -47.89601588673689037, -0.1816364388705385968 ) ) ;
#35888=CARTESIAN_POINT ( 'NONE',  ( 5.959547316686252039, -10.25972575517517704, -17.77749189599214219 ) ) ;
#35894=CARTESIAN_POINT ( 'NONE',  ( 0.9747592971366254577, 42.90728926179866676, -0.3237797888856475126 ) ) ;
#35897=CARTESIAN_POINT ( 'NONE',  ( 4.956653778116992370, 27.17045123668527751, -39.67974989265010777 ) ) ;
#35901=VECTOR ( 'NONE', #17958, 1000.000000000000000 ) ;
#35902=CARTESIAN_POINT ( 'NONE',  ( 0.8557997880470697982, 11.51622788066522851, -46.50333260518546297 ) ) ;
#35918=CARTESIAN_POINT ( 'NONE',  ( 2.281351352603296689, -11.14238889600251703, -46.66131639318008695 ) ) ;
#35920=CARTESIAN_POINT ( 'NONE',  ( 5.974727161628369032, 17.76736931401846320, 10.27590650342043510 ) ) ;
#35922=B_SPLINE_CURVE_WITH_KNOTS ( 'NONE', 3,
 ( #53978, #6349, #15799, #44027, #11103, #1661 ),
 .UNSPECIFIED., .F., .F.,
 ( 4, 2, 4 ),
 ( 1.267774990240505488E-17, 0.0002445244328975401671, 0.0004890488657950676490 ),
 .UNSPECIFIED. ) ;
#35925=CARTESIAN_POINT ( 'NONE',  ( 0.5839880159502346402, -47.49213420504720773, 6.206687493267523337 ) ) ;
#35930=AXIS2_PLACEMENT_3D ( 'NONE', #15477, #14872, #29250 ) ;
#35942=B_SPLINE_CURVE_WITH_KNOTS ( 'NONE', 3,
 ( #54898, #31107, #50822, #45535, #21710, #51427 ),
 .UNSPECIFIED., .F., .F.,
 ( 4, 2, 4 ),
 ( 0.000000000000000000, 0.0002291966416970797290, 0.0004583932833941594580 ),
 .UNSPECIFIED. ) ;
#35944=CARTESIAN_POINT ( 'NONE',  ( 0.9757402383260946888, 41.46830379850868553, -11.02350435907860948 ) ) ;
#35946=EDGE_CURVE ( 'NONE', #21513, #43532, #61219, .T. ) ;
#35954=CARTESIAN_POINT ( 'NONE',  ( 0.9968887458511649369, 42.62316256128691805, -4.948372828380340316 ) ) ;
#35960=CARTESIAN_POINT ( 'NONE',  ( 1.154321485836935279, -15.65787964449893011, 39.95809831208273266 ) ) ;
#35962=VERTEX_POINT ( 'NONE', #42974 ) ;
#35963=CARTESIAN_POINT ( 'NONE',  ( 0.5839254288179560604, -18.41284501069709023, 44.21529885210824062 ) ) ;
#35965=CARTESIAN_POINT ( 'NONE',  ( 0.6846871229502899947, -0.8641397935256196483, -47.90045233486065968 ) ) ;
#35970=LINE ( 'NONE', #55339, #45808 ) ;
#35973=B_SPLINE_CURVE_WITH_KNOTS ( 'NONE', 3,
 ( #44159, #39442, #18087, #45676 ),
 .UNSPECIFIED., .F., .F.,
 ( 4, 4 ),
 ( 0.000000000000000000, 0.005004741218457424944 ),
 .UNSPECIFIED. ) ;
#35974=( BOUNDED_SURFACE ( )  B_SPLINE_SURFACE ( 3, 1, ( 
 ( #36750, #23544 ),
 ( #32652, #42673 ),
 ( #51735, #46450 ),
 ( #42371, #27948 ) ),
 .UNSPECIFIED., .F., .F., .F. ) 
 B_SPLINE_SURFACE_WITH_KNOTS ( ( 4, 4 ),
 ( 2, 2 ),
 ( 0.000000000000000000, 1.000000000000000000 ),
 ( 0.000000000000000000, 1.000000000000000000 ),
 .UNSPECIFIED. ) 
 GEOMETRIC_REPRESENTATION_ITEM ( )  RATIONAL_B_SPLINE_SURFACE ( (
 ( 1.000000000000000000, 1.000000000000000000),
 ( 0.9953390228620291325, 0.8624445117760984880),
 ( 0.9953390228620291325, 0.8624445117760984880),
 ( 1.000000000000000000, 1.000000000000000000) ) ) 
 REPRESENTATION_ITEM ( '' )  SURFACE ( )  );
#35977=CARTESIAN_POINT ( 'NONE',  ( 0.6846871229502932144, -46.49193983736599023, 11.56285438919616126 ) ) ;
#35979=CARTESIAN_POINT ( 'NONE',  ( 1.227938101723756947, -0.8460948827222184443, -42.91134962331487657 ) ) ;
#35987=FACE_OUTER_BOUND ( 'NONE', #54994, .T. ) ;
#35993=LINE ( 'NONE', #7753, #60088 ) ;
#35999=CARTESIAN_POINT ( 'NONE',  ( 0.5850706913938533704, 6.071602062250609499, 47.50996714391784792 ) ) ;
#36001=CARTESIAN_POINT ( 'NONE',  ( 4.303969348037258058, -20.38638383586087954, -43.57722561725979915 ) ) ;
#36002=DIRECTION ( 'NONE',  ( 0.000000000000000000, 0.000000000000000000, 1.000000000000000000 ) ) ;
#36007=DIRECTION ( 'NONE',  ( -1.000000000000000000, -0.000000000000000000, -0.000000000000000000 ) ) ;
#36008=APPLICATION_CONTEXT ( 'automotive_design' ) ;
#36010=DIRECTION ( 'NONE',  ( 0.07439287786467664587, -0.2453289374370136722, -0.9665813013808186582 ) ) ;
#36013=CARTESIAN_POINT ( 'NONE',  ( 5.974727161628369032, 20.35137732084676188, -2.663664384318572331 ) ) ;
#36014=CARTESIAN_POINT ( 'NONE',  ( 0.6067099128993250767, 28.59222530349279268, -38.42667919752372541 ) ) ;
#36015=CARTESIAN_POINT ( 'NONE',  ( 0.9752132459055878888, 39.55248938404437098, -16.63533515462534851 ) ) ;
#36019=EDGE_CURVE ( 'NONE', #36850, #10364, #39628, .T. ) ;
#36023=ADVANCED_FACE ( 'NONE', ( #13531 ), #38351, .F. ) ;
#36040=VERTEX_POINT ( 'NONE', #11290 ) ;
#36045=CARTESIAN_POINT ( 'NONE',  ( 5.959547316686252039, -19.82530672674358385, -5.315863417546260905 ) ) ;
#36049=CARTESIAN_POINT ( 'NONE',  ( 5.960721111146673579, 19.82454228767745974, -5.318514366754729217 ) ) ;
#36053=CARTESIAN_POINT ( 'NONE',  ( 0.9758171775293912331, 34.03798695362348781, -26.12572690811879284 ) ) ;
#36054=DIRECTION ( 'NONE',  ( 0.07439287786467665975, -0.2708295585865200805, 0.9597484305373162883 ) ) ;
#36060=ORIENTED_EDGE ( 'NONE', *, *, #12102, .F. ) ;
#36064=CARTESIAN_POINT ( 'NONE',  ( 0.9752132459055842251, -33.89922943039196923, 26.30543738863332948 ) ) ;
#36065=CARTESIAN_POINT ( 'NONE',  ( 5.860006189529246790, 47.30964106197871644, -9.393028332204265141 ) ) ;
#36070=EDGE_CURVE ( 'NONE', #59493, #30942, #44526, .T. ) ;
#36077=CARTESIAN_POINT ( 'NONE',  ( 0.6846871229502899947, -47.37786444808398301, 7.109010606687220957 ) ) ;
#36087=CARTESIAN_POINT ( 'NONE',  ( 0.6067375320500690838, 44.51755737952380798, -17.67235760802216404 ) ) ;
#36089=CARTESIAN_POINT ( 'NONE',  ( 1.227938101723756947, -42.65467462194914816, -4.762198645644879491 ) ) ;
#36096=CARTESIAN_POINT ( 'NONE',  ( 0.9757402383260943557, -41.42435672089860788, -11.18751708556354352 ) ) ;
#36098=ORIENTED_EDGE ( 'NONE', *, *, #51654, .F. ) ;
#36099=CIRCLE ( 'NONE', #13059, 43.08621763946400307 ) ;
#36100=CARTESIAN_POINT ( 'NONE',  ( 5.960721111146673579, 12.49016043756449434, 16.28787783074231399 ) ) ;
#36104=CARTESIAN_POINT ( 'NONE',  ( 0.9736507210033064075, -6.046964561328232790, 42.48017254354721217 ) ) ;
#36105=EDGE_LOOP ( 'NONE', ( #39175, #2315, #23900, #38335 ) ) ;
#36110=CARTESIAN_POINT ( 'NONE',  ( 0.9749527285493309048, 16.15611883305644980, 39.75066842359289154 ) ) ;
#36112=LINE ( 'NONE', #46737, #61445 ) ;
#36116=CARTESIAN_POINT ( 'NONE',  ( 0.8557997880470690211, -46.50333260518550560, -11.51622788066506686 ) ) ;
#36120=ORIENTED_EDGE ( 'NONE', *, *, #50773, .F. ) ;
#36126=CARTESIAN_POINT ( 'NONE',  ( 0.8557997880470690211, 33.22501220301949587, -34.51495345639514767 ) ) ;
#36127=CARTESIAN_POINT ( 'NONE',  ( 4.967162193818130511, -32.68434214048149045, -28.07411493385329138 ) ) ;
#36132=CARTESIAN_POINT ( 'NONE',  ( 5.974727161628369032, -19.82156119440441699, -5.327229920347356540 ) ) ;
#36134=CARTESIAN_POINT ( 'NONE',  ( 0.9730545539215892381, -16.88610103448586131, 39.44597740938055352 ) ) ;
#36136=EDGE_CURVE ( 'NONE', #19642, #57673, #59192, .T. ) ;
#36154=CARTESIAN_POINT ( 'NONE',  ( 0.8557997880470606944, -46.50333260518566902, 11.51622788066442027 ) ) ;
#36156=CARTESIAN_POINT ( 'NONE',  ( 1.227938101723756947, 30.94118573761312874, 29.74462687941236538 ) ) ;
#36161=( BOUNDED_SURFACE ( )  B_SPLINE_SURFACE ( 3, 1, ( 
 ( #26326, #36065 ),
 ( #21632, #6026 ),
 ( #1040, #39601 ),
 ( #48977, #12559 ) ),
 .UNSPECIFIED., .F., .F., .F. ) 
 B_SPLINE_SURFACE_WITH_KNOTS ( ( 4, 4 ),
 ( 2, 2 ),
 ( 0.000000000000000000, 1.000000000000000000 ),
 ( 0.000000000000000000, 1.000000000000000000 ),
 .UNSPECIFIED. ) 
 GEOMETRIC_REPRESENTATION_ITEM ( )  RATIONAL_B_SPLINE_SURFACE ( (
 ( 1.000000000000000000, 1.000000000000000000),
 ( 0.7269869731126817891, 0.9931720237060910339),
 ( 0.7269869731126817891, 0.9931720237060910339),
 ( 1.000000000000000000, 1.000000000000000000) ) ) 
 REPRESENTATION_ITEM ( '' )  SURFACE ( )  );
#36163=EDGE_LOOP ( 'NONE', ( #54018, #48021, #1326, #28187 ) ) ;
#36165=CARTESIAN_POINT ( 'NONE',  ( 0.5839879327111910934, 47.89596760851024015, -0.09083573661728495952 ) ) ;
#36175=ORIENTED_EDGE ( 'NONE', *, *, #35510, .T. ) ;
#36176=EDGE_LOOP ( 'NONE', ( #11693, #13503, #44150, #55404 ) ) ;
#36201=CARTESIAN_POINT ( 'NONE',  ( 5.960221823109900008, -19.82761049839345446, 5.307149561567740648 ) ) ;
#36207=CARTESIAN_POINT ( 'NONE',  ( 0.5839879327111926477, 38.05372318152053168, 29.08515285004899198 ) ) ;
#36208=CARTESIAN_POINT ( 'NONE',  ( 3.660176727303408484, -47.34518114598553495, -8.130955556894974734 ) ) ;
#36211=CARTESIAN_POINT ( 'NONE',  ( -17.69715666991890046, -12.32470354188516737, -2.086247415145098483 ) ) ;
#36215=CARTESIAN_POINT ( 'NONE',  ( 0.5807400328401574052, 41.75144119563918821, -23.47602859900671035 ) ) ;
#36222=EDGE_CURVE ( 'NONE', #22677, #21167, #58765, .T. ) ;
#36224=CARTESIAN_POINT ( 'NONE',  ( 4.967162193818130511, 38.44485641567099776, -19.45289607368781759 ) ) ;
#36228=FACE_OUTER_BOUND ( 'NONE', #28399, .T. ) ;
#36231=CARTESIAN_POINT ( 'NONE',  ( 5.958863334805807099, 5.313608583996244583, 19.82594244347354717 ) ) ;
#36236=ORIENTED_EDGE ( 'NONE', *, *, #8600, .F. ) ;
#36244=ADVANCED_FACE ( 'NONE', ( #31013 ), #46765, .F. ) ;
#36248=CARTESIAN_POINT ( 'NONE',  ( 4.956653778116975495, -39.67974989265057673, 27.17045123668458828 ) ) ;
#36251=CARTESIAN_POINT ( 'NONE',  ( 1.154321485836933503, 15.65787964449918235, -39.95809831208263319 ) ) ;
#36252=LINE ( 'NONE', #12437, #43565 ) ;
#36255=CARTESIAN_POINT ( 'NONE',  ( 4.967162193818130511, -13.42934394584192148, 40.93989340068605998 ) ) ;
#36256=CARTESIAN_POINT ( 'NONE',  ( 1.227938101723756947, 25.45152231597106507, -34.55893248994479450 ) ) ;
#36257=CARTESIAN_POINT ( 'NONE',  ( 5.965394784446460541, -18.96850062921640401, 7.841344330024606180 ) ) ;
#36258=ADVANCED_FACE ( 'NONE', ( #16613 ), #31556, .F. ) ;
#36264=VERTEX_POINT ( 'NONE', #38206 ) ;
#36267=CARTESIAN_POINT ( 'NONE',  ( 1.088908134280554219, 26.73890361625913314, 33.56490895818176767 ) ) ;
#36282=CARTESIAN_POINT ( 'NONE',  ( 0.5807400328401574052, 46.40483864045162221, -11.87003418057194715 ) ) ;
#36283=ORIENTED_EDGE ( 'NONE', *, *, #33760, .F. ) ;
#36286=VERTEX_POINT ( 'NONE', #28774 ) ;
#36289=CARTESIAN_POINT ( 'NONE',  ( 0.9747592971366223491, -30.11108831501858418, 30.56898208368264136 ) ) ;
#36291=CARTESIAN_POINT ( 'NONE',  ( 4.956653778116970166, 45.35992544608529187, 15.97476558431900884 ) ) ;
#36303=CARTESIAN_POINT ( 'NONE',  ( 5.959547316686252039, 7.851524054666414010, -18.96456592444092593 ) ) ;
#36307=CARTESIAN_POINT ( 'NONE',  ( 2.624215991343608501, 22.77108897942136423, 42.26352390376104751 ) ) ;
#36311=CARTESIAN_POINT ( 'NONE',  ( 0.7057020205115011047, 37.48480537461333739, 29.82342581815218807 ) ) ;
#36314=VERTEX_POINT ( 'NONE', #46986 ) ;
#36318=CARTESIAN_POINT ( 'NONE',  ( 0.9747592971366239034, -26.37717450293403587, -33.84353661172428929 ) ) ;
#36326=CARTESIAN_POINT ( 'NONE',  ( 4.956653778116981712, -42.88673967249145846, 21.75875759808692322 ) ) ;
#36327=ORIENTED_EDGE ( 'NONE', *, *, #32212, .T. ) ;
#36334=CARTESIAN_POINT ( 'NONE',  ( 5.959547316686252039, -12.49803383497762255, 16.28190225198596863 ) ) ;
#36347=ORIENTED_EDGE ( 'NONE', *, *, #43607, .F. ) ;
#36350=CARTESIAN_POINT ( 'NONE',  ( 2.281351352603296245, 44.80774876812585461, -17.13758816714702249 ) ) ;
#36351=CARTESIAN_POINT ( 'NONE',  ( 0.5850706913938534814, 46.31100969101487408, 12.22095376872053230 ) ) ;
#36354=CARTESIAN_POINT ( 'NONE',  ( 0.9741495583595177754, 10.72301204857656565, 41.54695848110000611 ) ) ;
#36363=ORIENTED_EDGE ( 'NONE', *, *, #9784, .T. ) ;
#36368=DIRECTION ( 'NONE',  ( 0.07836865515943411409, 0.007886984708664454904, -0.9968932487286223942 ) ) ;
#36369=CARTESIAN_POINT ( 'NONE',  ( 0.9757787079277446818, -34.06559579809986360, 26.08967489699748299 ) ) ;
#36378=EDGE_CURVE ( 'NONE', #54442, #56211, #42503, .T. ) ;
#36379=CARTESIAN_POINT ( 'NONE',  ( 1.227938101723748288, 36.73927144310511750, 22.18841447410732215 ) ) ;
#36389=EDGE_CURVE ( 'NONE', #1853, #57497, #28789, .T. ) ;
#36391=CARTESIAN_POINT ( 'NONE',  ( 0.5837374860065649429, -29.30115996485969276, -37.88763545422905565 ) ) ;
#36395=DIRECTION ( 'NONE',  ( -0.07439287786467650709, -0.9903339163990665384, -0.1170659376278938568 ) ) ;
#36397=CARTESIAN_POINT ( 'NONE',  ( 1.227938101723748288, -15.63977281655813023, -39.96870412324352628 ) ) ;
#36402=CARTESIAN_POINT ( 'NONE',  ( 0.9758171775293917882, -41.44794628856068641, -11.09981579996850520 ) ) ;
#36409=VERTEX_POINT ( 'NONE', #1794 ) ;
#36413=EDGE_CURVE ( 'NONE', #20940, #42745, #34118, .T. ) ;
#36419=ORIENTED_EDGE ( 'NONE', *, *, #7189, .T. ) ;
#36422=ORIENTED_EDGE ( 'NONE', *, *, #57953, .F. ) ;
#36423=CARTESIAN_POINT ( 'NONE',  ( 0.9747592971366245695, -42.90728926179867386, 0.3237797888853479189 ) ) ;
#36426=EDGE_LOOP ( 'NONE', ( #54593, #54455, #59929, #54397 ) ) ;
#36427=CARTESIAN_POINT ( 'NONE',  ( 0.5807400328401637335, -6.791881299635922353, 47.41494605191441281 ) ) ;
#36430=DIRECTION ( 'NONE',  ( -1.000000000000000000, -0.000000000000000000, -0.000000000000000000 ) ) ;
#36431=( BOUNDED_SURFACE ( )  B_SPLINE_SURFACE ( 3, 1, ( 
 ( #36478, #55235 ),
 ( #31771, #36791 ),
 ( #12062, #31448 ),
 ( #32081, #49942 ) ),
 .UNSPECIFIED., .F., .F., .F. ) 
 B_SPLINE_SURFACE_WITH_KNOTS ( ( 4, 4 ),
 ( 2, 2 ),
 ( 0.000000000000000000, 1.000000000000000000 ),
 ( 0.000000000000000000, 1.000000000000000000 ),
 .UNSPECIFIED. ) 
 GEOMETRIC_REPRESENTATION_ITEM ( )  RATIONAL_B_SPLINE_SURFACE ( (
 ( 1.000000000000000000, 1.000000000000000000),
 ( 0.7269869731126817891, 0.9931720237060910339),
 ( 0.7269869731126817891, 0.9931720237060910339),
 ( 1.000000000000000000, 1.000000000000000000) ) ) 
 REPRESENTATION_ITEM ( '' )  SURFACE ( )  );
#36432=EDGE_LOOP ( 'NONE', ( #30123, #16440, #11274, #37831 ) ) ;
#36434=CARTESIAN_POINT ( 'NONE',  ( 4.956653778116966613, 0.000000000000000000, 0.000000000000000000 ) ) ;
#36438=B_SPLINE_CURVE_WITH_KNOTS ( 'NONE', 3,
 ( #23159, #29085, #239, #19389, #51957, #28773 ),
 .UNSPECIFIED., .F., .F.,
 ( 4, 2, 4 ),
 ( 1.512800854419661994E-16, 0.0002445252820015211956, 0.0004890505640028910365 ),
 .UNSPECIFIED. ) ;
#36439=EDGE_CURVE ( 'NONE', #27464, #61276, #5060, .T. ) ;
#36441=DIRECTION ( 'NONE',  ( -0.07836865515943411409, 0.7956898808744471419, 0.6006129930017412022 ) ) ;
#36442=EDGE_CURVE ( 'NONE', #45486, #5687, #44152, .T. ) ;
#36449=CARTESIAN_POINT ( 'NONE',  ( 0.9972139404380304661, 29.87264297738568075, -30.80335716430286652 ) ) ;
#36453=CARTESIAN_POINT ( 'NONE',  ( 2.526464513654345545, 9.948146339971810193, -41.81190200959790104 ) ) ;
#36454=( BOUNDED_SURFACE ( )  B_SPLINE_SURFACE ( 3, 1, ( 
 ( #20151, #16067 ),
 ( #39268, #58318 ),
 ( #29839, #6003 ),
 ( #58632, #11063 ) ),
 .UNSPECIFIED., .F., .F., .F. ) 
 B_SPLINE_SURFACE_WITH_KNOTS ( ( 4, 4 ),
 ( 2, 2 ),
 ( 0.000000000000000000, 1.000000000000000000 ),
 ( 0.000000000000000000, 1.000000000000000000 ),
 .UNSPECIFIED. ) 
 GEOMETRIC_REPRESENTATION_ITEM ( )  RATIONAL_B_SPLINE_SURFACE ( (
 ( 1.000000000000000000, 1.000000000000000000),
 ( 0.7269869731126821222, 0.9931720237060910339),
 ( 0.7269869731126821222, 0.9931720237060910339),
 ( 1.000000000000000000, 1.000000000000000000) ) ) 
 REPRESENTATION_ITEM ( '' )  SURFACE ( )  );
#36456=CARTESIAN_POINT ( 'NONE',  ( 0.5800708057587382616, -44.00606528161371500, -18.90714313908705435 ) ) ;
#36458=CARTESIAN_POINT ( 'NONE',  ( 0.5809828226811553087, -37.66417181417572380, 29.58751527316164953 ) ) ;
#36460=EDGE_LOOP ( 'NONE', ( #55699, #58681, #33724, #4886 ) ) ;
#36465=DIRECTION ( 'NONE',  ( -1.000000000000000000, -0.000000000000000000, -0.000000000000000000 ) ) ;
#36466=VERTEX_POINT ( 'NONE', #41284 ) ;
#36476=CARTESIAN_POINT ( 'NONE',  ( 0.9740398440564311811, -41.33716823241940119, 11.50548031350427181 ) ) ;
#36478=CARTESIAN_POINT ( 'NONE',  ( 5.981074661064941900, -20.34795181394747132, -2.687517936919926687 ) ) ;
#36481=ADVANCED_FACE ( 'NONE', ( #31243 ), #10340, .F. ) ;
#36484=B_SPLINE_CURVE_WITH_KNOTS ( 'NONE', 3,
 ( #13652, #18042, #18656, #28347 ),
 .UNSPECIFIED., .F., .F.,
 ( 4, 4 ),
 ( 0.000000000000000000, 0.004446090762761349506 ),
 .UNSPECIFIED. ) ;
#36491=CARTESIAN_POINT ( 'NONE',  ( 0.5819845079324649229, 11.95724301473572204, -46.37938935563219189 ) ) ;
#36492=ORIENTED_EDGE ( 'NONE', *, *, #50107, .F. ) ;
#36511=CARTESIAN_POINT ( 'NONE',  ( 0.9757787079277449038, 42.90844198810271592, 0.03949005143916181626 ) ) ;
#36512=DIRECTION ( 'NONE',  ( 0.000000000000000000, 0.000000000000000000, 1.000000000000000000 ) ) ;
#36514=EDGE_CURVE ( 'NONE', #33861, #17001, #45069, .T. ) ;
#36518=EDGE_CURVE ( 'NONE', #817, #12427, #45369, .T. ) ;
#36521=CARTESIAN_POINT ( 'NONE',  ( 0.7762783648524380631, -0.8897020150994838783, -47.89627393592492410 ) ) ;
#36525=CARTESIAN_POINT ( 'NONE',  ( 5.959828726073459926, 20.34941966491239285, -2.683617577144171928 ) ) ;
#36528=( BOUNDED_SURFACE ( )  B_SPLINE_SURFACE ( 3, 1, ( 
 ( #16554, #59135 ),
 ( #16245, #30328 ),
 ( #49748, #45691 ),
 ( #41305, #25950 ) ),
 .UNSPECIFIED., .F., .F., .F. ) 
 B_SPLINE_SURFACE_WITH_KNOTS ( ( 4, 4 ),
 ( 2, 2 ),
 ( 0.000000000000000000, 1.000000000000000000 ),
 ( 0.000000000000000000, 1.000000000000000000 ),
 .UNSPECIFIED. ) 
 GEOMETRIC_REPRESENTATION_ITEM ( )  RATIONAL_B_SPLINE_SURFACE ( (
 ( 1.000000000000000000, 1.000000000000000000),
 ( 0.9953390228620291325, 0.8624445117761032620),
 ( 0.9953390228620291325, 0.8624445117761032620),
 ( 1.000000000000000000, 1.000000000000000000) ) ) 
 REPRESENTATION_ITEM ( '' )  SURFACE ( )  );
#36529=AXIS2_PLACEMENT_3D ( 'NONE', #36540, #55298, #12121 ) ;
#36532=CARTESIAN_POINT ( 'NONE',  ( 0.5809828226811617480, -46.11980934799329646, -12.92184523170252497 ) ) ;
#36537=CARTESIAN_POINT ( 'NONE',  ( 3.783198216974389627, 41.09147814699341694, 12.79806054635149160 ) ) ;
#36540=CARTESIAN_POINT ( 'NONE',  ( -4.473699999999999122, 0.000000000000000000, 0.000000000000000000 ) ) ;
#36545=( GEOMETRIC_REPRESENTATION_CONTEXT ( 3 ) GLOBAL_UNCERTAINTY_ASSIGNED_CONTEXT ( ( #46178 ) ) GLOBAL_UNIT_ASSIGNED_CONTEXT ( ( #18785, #57567, #13783 ) ) REPRESENTATION_CONTEXT ( 'NONE', 'WORKASPACE' ) );
#36546=CARTESIAN_POINT ( 'NONE',  ( 0.9756354156337477823, 41.41248945940456849, 11.23134828980288624 ) ) ;
#36552=FACE_OUTER_BOUND ( 'NONE', #43737, .T. ) ;
#36554=EDGE_CURVE ( 'NONE', #25968, #17303, #39515, .T. ) ;
#36566=EDGE_CURVE ( 'NONE', #5033, #44660, #35970, .T. ) ;
#36568=CARTESIAN_POINT ( 'NONE',  ( 0.5819845079324652559, 41.70428776698897622, 23.55367910461011505 ) ) ;
#36570=CARTESIAN_POINT ( 'NONE',  ( 0.9722240750034599754, -15.88116978453009409, 39.86121765932393401 ) ) ;
#36576=ORIENTED_EDGE ( 'NONE', *, *, #35083, .T. ) ;
#36578=CARTESIAN_POINT ( 'NONE',  ( 5.960721111146673579, -20.52557019979492026, 0.006321279846751705171 ) ) ;
#36593=EDGE_CURVE ( 'NONE', #45511, #13813, #22464, .T. ) ;
#36595=CARTESIAN_POINT ( 'NONE',  ( 1.227938101723748288, -29.74462687941204209, -30.94118573761343782 ) ) ;
#36598=CARTESIAN_POINT ( 'NONE',  ( 0.9752570700956786354, 5.829291291129283792, -42.51066151201238341 ) ) ;
#36600=CARTESIAN_POINT ( 'NONE',  ( 5.960721111146673579, -12.50019045452750355, 16.28018152803671370 ) ) ;
#36603=ADVANCED_FACE ( 'NONE', ( #16533 ), #40742, .F. ) ;
#36606=CARTESIAN_POINT ( 'NONE',  ( 5.958863334805807099, 14.51469124124459675, 14.51296551801808121 ) ) ;
#36607=DIRECTION ( 'NONE',  ( 0.000000000000000000, 0.000000000000000000, 1.000000000000000000 ) ) ;
#36612=CARTESIAN_POINT ( 'NONE',  ( 2.281448460670310929, 1.314143534315831419, 47.95523685111403012 ) ) ;
#36619=DIRECTION ( 'NONE',  ( 0.07836865515943411409, -0.6006129930017385377, -0.7956898808744492513 ) ) ;
#36620=CARTESIAN_POINT ( 'NONE',  ( 0.9754642270333685472, -39.57465882553916003, -16.58255499746116968 ) ) ;
#36622=EDGE_LOOP ( 'NONE', ( #10750, #59955, #17173, #27993 ) ) ;
#36627=ORIENTED_EDGE ( 'NONE', *, *, #45845, .T. ) ;
#36630=CARTESIAN_POINT ( 'NONE',  ( 4.960156602257182357, 38.88108289790896066, -25.36362146861343803 ) ) ;
#36636=CARTESIAN_POINT ( 'NONE',  ( 0.9757402383260949108, 21.38067434779580012, 37.20221273948016005 ) ) ;
#36645=ORIENTED_EDGE ( 'NONE', *, *, #43706, .F. ) ;
#36648=CARTESIAN_POINT ( 'NONE',  ( 0.9756008150404597012, -0.1421465479999864390, -42.90824081423206593 ) ) ;
#36649=CARTESIAN_POINT ( 'NONE',  ( 4.956653778116966613, 0.000000000000000000, 0.000000000000000000 ) ) ;
#36652=CARTESIAN_POINT ( 'NONE',  ( 0.5850706913938533704, 46.21698775168644602, 12.57184842332033980 ) ) ;
#36654=VERTEX_POINT ( 'NONE', #51262 ) ;
#36668=CARTESIAN_POINT ( 'NONE',  ( 4.956653778116949738, 45.71126949320249366, 14.93973939759898606 ) ) ;
#36675=EDGE_CURVE ( 'NONE', #53786, #14355, #17658, .T. ) ;
#36676=CARTESIAN_POINT ( 'NONE',  ( 3.270143674763207553, -13.14781761974166585, -3.806843787666058798 ) ) ;
#36679=CARTESIAN_POINT ( 'NONE',  ( 5.960221823109900008, -16.28072933292556357, 12.49951306783062144 ) ) ;
#36681=CARTESIAN_POINT ( 'NONE',  ( 5.959828726073459926, -2.674641840416323912, 20.35060134307029855 ) ) ;
#36685=CARTESIAN_POINT ( 'NONE',  ( 0.5807400328401637335, -47.41494605191447675, 6.791881299635417868 ) ) ;
#36694=CARTESIAN_POINT ( 'NONE',  ( 0.5839254288179548391, -29.08514953649795487, -38.05364096126348272 ) ) ;
#36695=VECTOR ( 'NONE', #20959, 1000.000000000000000 ) ;
#36698=CARTESIAN_POINT ( 'NONE',  ( 0.5850706913938533704, -41.38834827854191190, -24.10530971368332231 ) ) ;
#36702=B_SPLINE_CURVE_WITH_KNOTS ( 'NONE', 3,
 ( #8932, #37783, #28043, #47163 ),
 .UNSPECIFIED., .F., .F.,
 ( 4, 4 ),
 ( 0.000000000000000000, 0.004446090762761125727 ),
 .UNSPECIFIED. ) ;
#36713=ORIENTED_EDGE ( 'NONE', *, *, #29709, .F. ) ;
#36716=ORIENTED_EDGE ( 'NONE', *, *, #2527, .T. ) ;
#36722=CARTESIAN_POINT ( 'NONE',  ( 0.9758171775293918992, 16.42583507057867465, 39.64000636436365710 ) ) ;
#36742=DIRECTION ( 'NONE',  ( -1.000000000000000000, -0.000000000000000000, -0.000000000000000000 ) ) ;
#36750=CARTESIAN_POINT ( 'NONE',  ( 5.960721111146673579, 17.77882586010667154, -10.25731071096564051 ) ) ;
#36753=CARTESIAN_POINT ( 'NONE',  ( 0.5800708057587390387, 6.873290064482054262, -47.40012370174857637 ) ) ;
#36755=DIRECTION ( 'NONE',  ( 0.000000000000000000, 0.000000000000000000, 1.000000000000000000 ) ) ;
#36774=CARTESIAN_POINT ( 'NONE',  ( 4.956653778116966613, 0.000000000000000000, 0.000000000000000000 ) ) ;
#36782=B_SPLINE_CURVE_WITH_KNOTS ( 'NONE', 3,
 ( #2533, #41104, #11647, #36087, #11974, #22277 ),
 .UNSPECIFIED., .F., .F.,
 ( 4, 2, 4 ),
 ( 1.516581828351926341E-16, 0.0002445252820015211413, 0.0004890505640028906028 ),
 .UNSPECIFIED. ) ;
#36788=LINE ( 'NONE', #32078, #55932 ) ;
#36790=EDGE_LOOP ( 'NONE', ( #59316, #16360, #57124, #42653 ) ) ;
#36791=CARTESIAN_POINT ( 'NONE',  ( 4.303969348037258058, 47.93217632892348234, 4.133486515473467016 ) ) ;
#36807=CARTESIAN_POINT ( 'NONE',  ( 0.5809828226811565299, -23.47450554821739743, 41.74875432577639600 ) ) ;
#36815=CARTESIAN_POINT ( 'NONE',  ( 0.9749527285493310158, 30.13822974582813430, 30.54214995146782741 ) ) ;
#36819=ORIENTED_EDGE ( 'NONE', *, *, #27547, .F. ) ;
#36829=( BOUNDED_SURFACE ( )  B_SPLINE_SURFACE ( 3, 1, ( 
 ( #31506, #60930 ),
 ( #35920, #31828 ),
 ( #26184, #41546 ),
 ( #2368, #50300 ) ),
 .UNSPECIFIED., .F., .F., .F. ) 
 B_SPLINE_SURFACE_WITH_KNOTS ( ( 4, 4 ),
 ( 2, 2 ),
 ( 0.000000000000000000, 1.000000000000000000 ),
 ( 0.000000000000000000, 1.000000000000000000 ),
 .UNSPECIFIED. ) 
 GEOMETRIC_REPRESENTATION_ITEM ( )  RATIONAL_B_SPLINE_SURFACE ( (
 ( 1.000000000000000000, 1.000000000000000000),
 ( 0.7269869731126817891, 0.9931720237060910339),
 ( 0.7269869731126817891, 0.9931720237060910339),
 ( 1.000000000000000000, 1.000000000000000000) ) ) 
 REPRESENTATION_ITEM ( '' )  SURFACE ( )  );
#36830=DIRECTION ( 'NONE',  ( -1.000000000000000000, -0.000000000000000000, -0.000000000000000000 ) ) ;
#36838=CARTESIAN_POINT ( 'NONE',  ( 4.967162193818130511, 0.000000000000000000, 0.000000000000000000 ) ) ;
#36842=VECTOR ( 'NONE', #6484, 1000.000000000000114 ) ;
#36845=CARTESIAN_POINT ( 'NONE',  ( 2.526552050251863690, 4.405466163647298039, 42.75269566045968617 ) ) ;
#36849=CARTESIAN_POINT ( 'NONE',  ( 5.981074661064941900, -5.320466518160800184, -19.82308078259089612 ) ) ;
#36850=VERTEX_POINT ( 'NONE', #55573 ) ;
#36851=VERTEX_POINT ( 'NONE', #7335 ) ;
#36853=CARTESIAN_POINT ( 'NONE',  ( 3.407937589446174087, -13.63405474014709462, 1.331713209622455985 ) ) ;
#36858=CARTESIAN_POINT ( 'NONE',  ( 0.9730545539215883499, 39.44597740938085195, -16.88610103448514721 ) ) ;
#36860=VERTEX_POINT ( 'NONE', #16157 ) ;
#36873=CARTESIAN_POINT ( 'NONE',  ( 5.960721111146673579, 20.35079619394242201, 2.672857320903374578 ) ) ;
#36874=VECTOR ( 'NONE', #22262, 1000.000000000000114 ) ;
#36880=CARTESIAN_POINT ( 'NONE',  ( 4.967162193818130511, 0.000000000000000000, 0.000000000000000000 ) ) ;
#36883=CARTESIAN_POINT ( 'NONE',  ( 5.981074661064941900, -7.846517100474943440, 18.96560215432003815 ) ) ;
#36884=CARTESIAN_POINT ( 'NONE',  ( 0.5839254288179568375, 41.43367229384582373, 24.02657516616520539 ) ) ;
#36889=ORIENTED_EDGE ( 'NONE', *, *, #50407, .T. ) ;
#36892=EDGE_CURVE ( 'NONE', #19313, #49122, #49911, .T. ) ;
#36903=CARTESIAN_POINT ( 'NONE',  ( -19.96574511507958150, -12.48220789061827496, -0.6787824490278846490 ) ) ;
#36904=( BOUNDED_SURFACE ( )  B_SPLINE_SURFACE ( 3, 1, ( 
 ( #27057, #28280 ),
 ( #33311, #61167 ),
 ( #57076, #14208 ),
 ( #33007, #13275 ) ),
 .UNSPECIFIED., .F., .F., .F. ) 
 B_SPLINE_SURFACE_WITH_KNOTS ( ( 4, 4 ),
 ( 2, 2 ),
 ( 0.000000000000000000, 1.000000000000000000 ),
 ( 0.000000000000000000, 1.000000000000000000 ),
 .UNSPECIFIED. ) 
 GEOMETRIC_REPRESENTATION_ITEM ( )  RATIONAL_B_SPLINE_SURFACE ( (
 ( 1.000000000000000000, 1.000000000000000000),
 ( 0.9732289882329797637, 0.9999525324661233672),
 ( 0.9732289882329797637, 0.9999525324661233672),
 ( 1.000000000000000000, 1.000000000000000000) ) ) 
 REPRESENTATION_ITEM ( '' )  SURFACE ( )  );
#36917=CARTESIAN_POINT ( 'NONE',  ( 1.154321713695928286, 41.66001467525155277, -10.30834583266686977 ) ) ;
#36918=CARTESIAN_POINT ( 'NONE',  ( 0.6846871229502932144, 23.20185915381556185, 41.91507847151805777 ) ) ;
#36923=B_SPLINE_CURVE_WITH_KNOTS ( 'NONE', 3,
 ( #59431, #21543, #40371, #60059 ),
 .UNSPECIFIED., .F., .F.,
 ( 4, 4 ),
 ( 0.000000000000000000, 0.004446090762761356445 ),
 .UNSPECIFIED. ) ;
#36925=CARTESIAN_POINT ( 'NONE',  ( 0.9741495583595167762, -39.79188455996729346, 16.05424148287313102 ) ) ;
#36933=CARTESIAN_POINT ( 'NONE',  ( 3.270143674763207553, -11.98875605389974908, -6.605065939546945764 ) ) ;
#36937=ORIENTED_EDGE ( 'NONE', *, *, #29828, .T. ) ;
#36938=CARTESIAN_POINT ( 'NONE',  ( 2.281448460670576939, 47.37344300043622525, -7.562315317391275826 ) ) ;
#36943=FACE_OUTER_BOUND ( 'NONE', #59260, .T. ) ;
#36949=CARTESIAN_POINT ( 'NONE',  ( 0.5832366564991497970, -0.2724446024274073119, -47.89515933308369000 ) ) ;
#36954=CARTESIAN_POINT ( 'NONE',  ( 0.5827357941260201679, -28.86820951701459492, 38.21849163199665611 ) ) ;
#36955=EDGE_CURVE ( 'NONE', #37400, #37022, #29057, .T. ) ;
#36959=ORIENTED_EDGE ( 'NONE', *, *, #24836, .F. ) ;
#36962=EDGE_CURVE ( 'NONE', #3984, #47332, #13621, .T. ) ;
#36969=CARTESIAN_POINT ( 'NONE',  ( 4.956653778116971942, 35.79382859084115864, 32.11725092155054995 ) ) ;
#36976=CARTESIAN_POINT ( 'NONE',  ( 4.303969348037246512, -46.98258166031697414, 10.35452842635826975 ) ) ;
#36979=ORIENTED_EDGE ( 'NONE', *, *, #47122, .T. ) ;
#36984=CARTESIAN_POINT ( 'NONE',  ( 0.8557997880470606944, 43.90420959842181503, 19.17299735372024827 ) ) ;
#36991=CARTESIAN_POINT ( 'NONE',  ( 4.963659409799330291, -19.36487359954670140, -40.34793212403990736 ) ) ;
#36992=B_SPLINE_CURVE_WITH_KNOTS ( 'NONE', 3,
 ( #33087, #42487, #28360, #48396, #52159, #5456 ),
 .UNSPECIFIED., .F., .F.,
 ( 4, 2, 4 ),
 ( 7.757919228897728493E-18, 0.0002291978881530151843, 0.0004583957763060226166 ),
 .UNSPECIFIED. ) ;
#36997=VERTEX_POINT ( 'NONE', #18944 ) ;
#37000=CARTESIAN_POINT ( 'NONE',  ( 0.8551540677456715978, 7.157691013575044892, -47.37911285756612756 ) ) ;
#37002=CARTESIAN_POINT ( 'NONE',  ( 0.5850706913938533704, 29.30134895053109645, -37.88789093229775062 ) ) ;
#37003=CARTESIAN_POINT ( 'NONE',  ( 4.956653778116990594, -26.26162724282345096, -40.28700667097706400 ) ) ;
#37009=EDGE_CURVE ( 'NONE', #54002, #31835, #40182, .T. ) ;
#37015=B_SPLINE_CURVE_WITH_KNOTS ( 'NONE', 3,
 ( #22910, #27914, #9407, #23511, #42040, #22600, #4073, #52315, #46727, #28512, #42961, #9102, #23212, #8796, #57016, #18516 ),
 .UNSPECIFIED., .F., .F.,
 ( 4, 3, 3, 3, 3, 4 ),
 ( 1.127622383284612036E-17, 0.0002724568934985555470, 0.0004086836638483797675, 0.0005449104342063609829, 0.0008173270854453709017, 0.001089761613562690743 ),
 .UNSPECIFIED. ) ;
#37020=CARTESIAN_POINT ( 'NONE',  ( 0.5809828226811553087, 46.11980934799357357, -12.92184523170154620 ) ) ;
#37022=VERTEX_POINT ( 'NONE', #22698 ) ;
#37037=B_SPLINE_CURVE_WITH_KNOTS ( 'NONE', 3,
 ( #30383, #20390, #49814, #59198 ),
 .UNSPECIFIED., .F., .F.,
 ( 4, 4 ),
 ( 0.000000000000000000, 0.005004741218457418872 ),
 .UNSPECIFIED. ) ;
#37047=EDGE_CURVE ( 'NONE', #52648, #38360, #40958, .T. ) ;
#37049=CARTESIAN_POINT ( 'NONE',  ( 5.860006189529246790, -31.78942168514539546, -36.27483683749468923 ) ) ;
#37057=CARTESIAN_POINT ( 'NONE',  ( 1.088908134280555107, 41.64642044161488599, 10.35121946298427709 ) ) ;
#37059=CARTESIAN_POINT ( 'NONE',  ( 2.281448460670572054, -13.68109378871678139, -45.98107640562109566 ) ) ;
#37063=CARTESIAN_POINT ( 'NONE',  ( 4.956653778116966613, 0.000000000000000000, 0.000000000000000000 ) ) ;
#37064=CARTESIAN_POINT ( 'NONE',  ( 0.5834872094924168362, -46.32218741137608475, 12.17696997821507132 ) ) ;
#37066=LINE ( 'NONE', #33286, #33230 ) ;
#37067=CARTESIAN_POINT ( 'NONE',  ( -17.97369999999976642, -12.32233744059949210, -2.099999999999997424 ) ) ;
#37069=CARTESIAN_POINT ( 'NONE',  ( 1.154321485836935057, 33.53917069757689973, -26.77578840293002216 ) ) ;
#37072=CARTESIAN_POINT ( 'NONE',  ( 0.9747592971366230152, 37.32069240268771892, 21.17324310849245705 ) ) ;
#37074=EDGE_CURVE ( 'NONE', #56714, #52535, #14754, .T. ) ;
#37075=( BOUNDED_SURFACE ( )  B_SPLINE_SURFACE ( 3, 1, ( 
 ( #38235, #47298 ),
 ( #13487, #51057 ),
 ( #46700, #17880 ),
 ( #27267, #23483 ) ),
 .UNSPECIFIED., .F., .F., .F. ) 
 B_SPLINE_SURFACE_WITH_KNOTS ( ( 4, 4 ),
 ( 2, 2 ),
 ( 0.000000000000000000, 1.000000000000000000 ),
 ( 0.000000000000000000, 1.000000000000000000 ),
 .UNSPECIFIED. ) 
 GEOMETRIC_REPRESENTATION_ITEM ( )  RATIONAL_B_SPLINE_SURFACE ( (
 ( 1.000000000000000000, 1.000000000000000000),
 ( 0.7269869731126817891, 0.9931720237060910339),
 ( 0.7269869731126817891, 0.9931720237060910339),
 ( 1.000000000000000000, 1.000000000000000000) ) ) 
 REPRESENTATION_ITEM ( '' )  SURFACE ( )  );
#37076=CARTESIAN_POINT ( 'NONE',  ( 0.6846871229502899947, 34.48177377577836467, 33.25969555998755567 ) ) ;
#37077=EDGE_CURVE ( 'NONE', #56211, #60, #29545, .T. ) ;
#37079=CARTESIAN_POINT ( 'NONE',  ( 1.088908134280559326, 11.85879120571506284, 41.24246781061821565 ) ) ;
#37081=CARTESIAN_POINT ( 'NONE',  ( 0.9756008150404611445, 39.69644259322205926, 16.28894658522346361 ) ) ;
#37088=CARTESIAN_POINT ( 'NONE',  ( 5.959547316686252039, 19.82530672674354832, 5.315863417546399461 ) ) ;
#37092=CARTESIAN_POINT ( 'NONE',  ( 0.9972139404380295780, 4.947665363829381491, -42.62325912566426211 ) ) ;
#37093=( BOUNDED_SURFACE ( )  B_SPLINE_SURFACE ( 3, 1, ( 
 ( #47779, #9239 ),
 ( #28348, #23049 ),
 ( #56230, #19277 ),
 ( #14275, #5138 ) ),
 .UNSPECIFIED., .F., .F., .F. ) 
 B_SPLINE_SURFACE_WITH_KNOTS ( ( 4, 4 ),
 ( 2, 2 ),
 ( 0.000000000000000000, 1.000000000000000000 ),
 ( 0.000000000000000000, 1.000000000000000000 ),
 .UNSPECIFIED. ) 
 GEOMETRIC_REPRESENTATION_ITEM ( )  RATIONAL_B_SPLINE_SURFACE ( (
 ( 1.000000000000000000, 1.000000000000000000),
 ( 0.7269869731126821222, 0.9931720237060910339),
 ( 0.7269869731126821222, 0.9931720237060910339),
 ( 1.000000000000000000, 1.000000000000000000) ) ) 
 REPRESENTATION_ITEM ( '' )  SURFACE ( )  );
#37107=B_SPLINE_CURVE_WITH_KNOTS ( 'NONE', 3,
 ( #41412, #16344, #16662, #2847, #59865, #31373, #11655, #35782, #36402, #50172, #36096, #41111, #45803, #22284, #60170, #50469, #55775, #26665, #7229 ),
 .UNSPECIFIED., .F., .F.,
 ( 4, 3, 3, 3, 3, 3, 4 ),
 ( 1.040890552917501732E-17, 0.0002724573126191767855, 0.0004086839781548530308, 0.0005449106435901854978, 0.0006811373090491518916, 0.0008459866663933626523, 0.001010840725717205343 ),
 .UNSPECIFIED. ) ;
#37109=ORIENTED_EDGE ( 'NONE', *, *, #42718, .F. ) ;
#37111=CARTESIAN_POINT ( 'NONE',  ( 5.960221823109900008, 17.77840967225706592, 10.25807604135628104 ) ) ;
#37113=CARTESIAN_POINT ( 'NONE',  ( 0.9722240750034555345, 20.94823713380391439, -37.44729079646473480 ) ) ;
#37120=CARTESIAN_POINT ( 'NONE',  ( 0.9730545539215883499, -29.98130006528840141, -30.69604515769682251 ) ) ;
#37127=CARTESIAN_POINT ( 'NONE',  ( 2.526552050251864134, 33.34585601411865952, 27.11558601691277204 ) ) ;
#37142=EDGE_LOOP ( 'NONE', ( #44849, #20349, #33801, #25993 ) ) ;
#37143=CARTESIAN_POINT ( 'NONE',  ( -16.69237839429539605, -12.38826022272751359, -1.669401441924114993 ) ) ;
#37144=CARTESIAN_POINT ( 'NONE',  ( 4.956653778116999476, 43.37017594958085454, -20.77844580450516077 ) ) ;
#37154=EDGE_CURVE ( 'NONE', #59171, #49382, #34169, .T. ) ;
#37155=LINE ( 'NONE', #23650, #39381 ) ;
#37157=ORIENTED_EDGE ( 'NONE', *, *, #52462, .F. ) ;
#37166=ORIENTED_EDGE ( 'NONE', *, *, #17908, .T. ) ;
#37180=ORIENTED_EDGE ( 'NONE', *, *, #36518, .T. ) ;
#37188=CARTESIAN_POINT ( 'NONE',  ( 0.5809828226811553087, 41.74875432577648837, 23.47450554821725532 ) ) ;
#37194=ORIENTED_EDGE ( 'NONE', *, *, #6121, .F. ) ;
#37205=CARTESIAN_POINT ( 'NONE',  ( 0.5839254288179558383, -18.24509008251443376, -44.28478521851638305 ) ) ;
#37209=CARTESIAN_POINT ( 'NONE',  ( 0.5807400328401574052, 46.12278621143515522, -12.92266817605966445 ) ) ;
#37211=CARTESIAN_POINT ( 'NONE',  ( 0.5809828226811565299, -17.82437196699712700, 44.45562576850595349 ) ) ;
#37232=CARTESIAN_POINT ( 'NONE',  ( 3.660087539126834599, 1.881558488211524383, 48.00143792263125420 ) ) ;
#37239=CARTESIAN_POINT ( 'NONE',  ( 0.9756008150404608115, 10.96816689273754442, -41.48296819691537252 ) ) ;
#37240=ADVANCED_FACE ( 'NONE', ( #8830 ), #45130, .F. ) ;
#37243=CARTESIAN_POINT ( 'NONE',  ( -18.90529782703537975, -7.774448652089772871, -1.887028486091764101 ) ) ;
#37245=ADVANCED_FACE ( 'NONE', ( #56739 ), #29532, .F. ) ;
#37248=EDGE_LOOP ( 'NONE', ( #7498, #10674, #41885, #10182 ) ) ;
#37251=CARTESIAN_POINT ( 'NONE',  ( 0.5839879882104919151, -5.421203860810959572E-16, -47.89596766822081975 ) ) ;
#37254=CARTESIAN_POINT ( 'NONE',  ( 5.959828726073459926, -12.49879082830580579, 16.28130559351243178 ) ) ;
#37256=ORIENTED_EDGE ( 'NONE', *, *, #52275, .F. ) ;
#37263=FACE_OUTER_BOUND ( 'NONE', #32310, .T. ) ;
#37268=ORIENTED_EDGE ( 'NONE', *, *, #43607, .T. ) ;
#37271=CARTESIAN_POINT ( 'NONE',  ( 0.5809828226811617480, 28.72298383114487663, 38.32755012159156394 ) ) ;
#37274=ORIENTED_EDGE ( 'NONE', *, *, #37047, .T. ) ;
#37277=CARTESIAN_POINT ( 'NONE',  ( 0.5263152470540364281, 0.000000000000000000, 0.000000000000000000 ) ) ;
#37282=CARTESIAN_POINT ( 'NONE',  ( 0.8551540677456739292, 13.28067116677265957, -46.03951182599413983 ) ) ;
#37286=CARTESIAN_POINT ( 'NONE',  ( 4.960156602257184133, 44.12083041402459571, 14.43621227656543304 ) ) ;
#37295=ADVANCED_FACE ( 'NONE', ( #22946 ), #35974, .F. ) ;
#37296=CARTESIAN_POINT ( 'NONE',  ( 5.959547316686252039, -12.49238070347988483, 16.28624005235077732 ) ) ;
#37297=CARTESIAN_POINT ( 'NONE',  ( 5.959547316686252039, -7.858107265727872992, 18.96183906913529782 ) ) ;
#37316=CARTESIAN_POINT ( 'NONE',  ( 4.960156602257182357, -2.524999074837246837, -46.35381625054459676 ) ) ;
#37322=EDGE_LOOP ( 'NONE', ( #25150, #37910, #22658, #13223 ) ) ;
#37326=VERTEX_POINT ( 'NONE', #58818 ) ;
#37329=CARTESIAN_POINT ( 'NONE',  ( 0.5839879882104920261, 5.827794150371782279E-15, 47.89596766822081264 ) ) ;
#37330=CARTESIAN_POINT ( 'NONE',  ( 0.5809828226811553087, 12.92184523170202937, 46.11980934799343856 ) ) ;
#37339=CARTESIAN_POINT ( 'NONE',  ( 0.5834872094924158370, -33.70665904794267220, -34.02770606800797282 ) ) ;
#37355=ORIENTED_EDGE ( 'NONE', *, *, #32777, .F. ) ;
#37360=CARTESIAN_POINT ( 'NONE',  ( 0.5839879882012674051, -44.25011577017258446, -18.32896541547120250 ) ) ;
#37364=CARTESIAN_POINT ( 'NONE',  ( 1.154321713695927176, 39.95809834491024759, -15.65787958845375449 ) ) ;
#37365=EDGE_CURVE ( 'NONE', #59890, #22653, #28937, .T. ) ;
#37366=CARTESIAN_POINT ( 'NONE',  ( 0.8557997880470606944, -24.73961900479280374, 41.02602466100771039 ) ) ;
#37373=CARTESIAN_POINT ( 'NONE',  ( 0.5809828226811553087, 24.41822904836923058, 41.20389530892317254 ) ) ;
#37376=CARTESIAN_POINT ( 'NONE',  ( 0.8551540677456715978, 34.52115452272929730, 33.23105123575911790 ) ) ;
#37379=CARTESIAN_POINT ( 'NONE',  ( 0.9747592971366246806, 39.76507150545830171, 16.12077520819463672 ) ) ;
#37383=CARTESIAN_POINT ( 'NONE',  ( 3.270143674763207553, 1.514386915940791445, -13.60381564321232695 ) ) ;
#37387=EDGE_LOOP ( 'NONE', ( #44431, #14461, #22318, #12771 ) ) ;
#37393=ORIENTED_EDGE ( 'NONE', *, *, #20936, .T. ) ;
#37394=CARTESIAN_POINT ( 'NONE',  ( 0.9741495583595169983, -10.72301204857627255, -41.54695848110009848 ) ) ;
#37398=VERTEX_POINT ( 'NONE', #10619 ) ;
#37399=CARTESIAN_POINT ( 'NONE',  ( 0.5832366564991503521, -12.65934068133952195, -46.19265750221184419 ) ) ;
#37400=VERTEX_POINT ( 'NONE', #49431 ) ;
#37401=CARTESIAN_POINT ( 'NONE',  ( 2.526552050251863246, 31.23611603144905402, -29.52128340070568413 ) ) ;
#37404=B_SPLINE_CURVE_WITH_KNOTS ( 'NONE', 3,
 ( #46599, #17778, #2728, #27472, #31253, #60060 ),
 .UNSPECIFIED., .F., .F.,
 ( 4, 2, 4 ),
 ( 1.518576772339270681E-16, 0.0002445252820015215208, 0.0004890505640028912533 ),
 .UNSPECIFIED. ) ;
#37406=ORIENTED_EDGE ( 'NONE', *, *, #52338, .T. ) ;
#37424=ORIENTED_EDGE ( 'NONE', *, *, #58120, .T. ) ;
#37436=B_SPLINE_CURVE_WITH_KNOTS ( 'NONE', 3,
 ( #58848, #21272, #11899, #40405 ),
 .UNSPECIFIED., .F., .F.,
 ( 4, 4 ),
 ( 1.843143693225357538E-18, 0.004444878191957690391 ),
 .UNSPECIFIED. ) ;
#37439=CARTESIAN_POINT ( 'NONE',  ( 0.9730545539215883499, -42.60426903087357431, 5.099196237954729760 ) ) ;
#37442=CARTESIAN_POINT ( 'NONE',  ( 0.9745511491811756910, 42.90705396078542577, 0.3405614984922070154 ) ) ;
#37443=LINE ( 'NONE', #106, #59794 ) ;
#37444=CARTESIAN_POINT ( 'NONE',  ( 0.8557997880470697982, -37.44587306708118035, 29.88293891557457371 ) ) ;
#37448=ORIENTED_EDGE ( 'NONE', *, *, #10328, .F. ) ;
#37449=ADVANCED_FACE ( 'NONE', ( #17171 ), #57883, .F. ) ;
#37451=CARTESIAN_POINT ( 'NONE',  ( 4.967162193818130511, 38.83676580803792433, -18.65818244221215849 ) ) ;
#37459=EDGE_CURVE ( 'NONE', #147, #22861, #6441, .T. ) ;
#37462=CARTESIAN_POINT ( 'NONE',  ( 1.227938101723748288, -6.439911493064859549, 42.43379953535183802 ) ) ;
#37475=CARTESIAN_POINT ( 'NONE',  ( 0.9757892942422807803, 41.45966865212812280, 11.05594550521658981 ) ) ;
#37482=CARTESIAN_POINT ( 'NONE',  ( 0.9736507210033054083, 41.56063510425045848, -10.66979144439325644 ) ) ;
#37486=VERTEX_POINT ( 'NONE', #7425 ) ;
#37499=B_SPLINE_CURVE_WITH_KNOTS ( 'NONE', 3,
 ( #7666, #51201, #8283, #60911, #50284, #35902 ),
 .UNSPECIFIED., .F., .F.,
 ( 4, 2, 4 ),
 ( 7.040638946443416885E-18, 0.0002445244328975375650, 0.0004890488657950680827 ),
 .UNSPECIFIED. ) ;
#37500=ORIENTED_EDGE ( 'NONE', *, *, #10926, .F. ) ;
#37504=CARTESIAN_POINT ( 'NONE',  ( 0.9730545539215883499, -5.099196237954599198, -42.60426903087358852 ) ) ;
#37508=CARTESIAN_POINT ( 'NONE',  ( 4.956653778116990594, -26.26162724282345096, -40.28700667097706400 ) ) ;
#37516=CARTESIAN_POINT ( 'NONE',  ( 4.967162193818130511, 8.839793687085803597, -42.16965968614184135 ) ) ;
#37528=CARTESIAN_POINT ( 'NONE',  ( 5.960721111146673579, -2.685391721745896909, -20.34914600876574298 ) ) ;
#37529=CARTESIAN_POINT ( 'NONE',  ( 0.9752132459055862235, 5.369621847648212487, -42.57112816680945855 ) ) ;
#37535=CARTESIAN_POINT ( 'NONE',  ( 5.959547316686252039, -17.77749189599224877, 10.25972575517499052 ) ) ;
#37539=VERTEX_POINT ( 'NONE', #37211 ) ;
#37540=CIRCLE ( 'NONE', #54475, 48.09070567114147110 ) ;
#37542=CARTESIAN_POINT ( 'NONE',  ( 0.5807400328401637335, -44.45848844984429604, -17.82553128098455275 ) ) ;
#37543=CARTESIAN_POINT ( 'NONE',  ( 0.8551540677456715978, 47.90804413217340851, -0.9122407826477486603 ) ) ;
#37551=CARTESIAN_POINT ( 'NONE',  ( 3.660087539127338641, 47.34518630204121337, -8.130906407639580280 ) ) ;
#37553=CARTESIAN_POINT ( 'NONE',  ( 4.956653778116960396, -3.690426056930336429, 47.94889704119049867 ) ) ;
#37558=ORIENTED_EDGE ( 'NONE', *, *, #35859, .T. ) ;
#37559=( BOUNDED_SURFACE ( )  B_SPLINE_SURFACE ( 3, 1, ( 
 ( #51594, #22803 ),
 ( #40705, #36307 ),
 ( #17802, #56302 ),
 ( #55993, #22495 ) ),
 .UNSPECIFIED., .F., .F., .F. ) 
 B_SPLINE_SURFACE_WITH_KNOTS ( ( 4, 4 ),
 ( 2, 2 ),
 ( 0.000000000000000000, 1.000000000000000000 ),
 ( 0.000000000000000000, 1.000000000000000000 ),
 .UNSPECIFIED. ) 
 GEOMETRIC_REPRESENTATION_ITEM ( )  RATIONAL_B_SPLINE_SURFACE ( (
 ( 1.000000000000000000, 1.000000000000000000),
 ( 0.7269869731126821222, 0.9931720237060910339),
 ( 0.7269869731126821222, 0.9931720237060910339),
 ( 1.000000000000000000, 1.000000000000000000) ) ) 
 REPRESENTATION_ITEM ( '' )  SURFACE ( )  );
#37564=ORIENTED_EDGE ( 'NONE', *, *, #58973, .T. ) ;
#37565=CARTESIAN_POINT ( 'NONE',  ( 0.5827359174754824789, -29.44457394064646749, 37.77623182210385977 ) ) ;
#37566=CARTESIAN_POINT ( 'NONE',  ( 0.9741495583595165542, 21.11077839432136827, 37.35596046161874995 ) ) ;
#37573=ORIENTED_EDGE ( 'NONE', *, *, #24836, .T. ) ;
#37575=ORIENTED_EDGE ( 'NONE', *, *, #53744, .F. ) ;
#37582=CARTESIAN_POINT ( 'NONE',  ( 0.9756354156337461170, 33.96210048825376049, 26.22428641656263437 ) ) ;
#37583=CARTESIAN_POINT ( 'NONE',  ( 0.5807400328401637335, -37.66660715020845629, -29.58941477093055639 ) ) ;
#37595=CARTESIAN_POINT ( 'NONE',  ( 4.956653778116975495, -36.51451553856441024, 31.29546495791839078 ) ) ;
#37598=VERTEX_POINT ( 'NONE', #1117 ) ;
#37605=CARTESIAN_POINT ( 'NONE',  ( 0.7762783648524402835, -34.49689442177322718, -33.23866576554873831 ) ) ;
#37619=ORIENTED_EDGE ( 'NONE', *, *, #32067, .T. ) ;
#37620=B_SPLINE_CURVE_WITH_KNOTS ( 'NONE', 3,
 ( #5334, #43603, #19786, #41076 ),
 .UNSPECIFIED., .F., .F.,
 ( 4, 4 ),
 ( 0.000000000000000000, 0.004446090762761369455 ),
 .UNSPECIFIED. ) ;
#37621=CARTESIAN_POINT ( 'NONE',  ( 0.5809828226811553087, 47.89273459658653564, -0.5448590168534052092 ) ) ;
#37624=CARTESIAN_POINT ( 'NONE',  ( 0.7056555295713312637, 34.46100226633736696, 33.27140645154206311 ) ) ;
#37625=DIRECTION ( 'NONE',  ( 0.9990097760809872884, 0.000000000000000000, -0.04449120468829269315 ) ) ;
#37626=ORIENTED_EDGE ( 'NONE', *, *, #52913, .T. ) ;
#37629=CARTESIAN_POINT ( 'NONE',  ( 2.526464513654346433, 17.56107808841309037, 39.22765990515326706 ) ) ;
#37643=EDGE_LOOP ( 'NONE', ( #51082, #52319 ) ) ;
#37651=CARTESIAN_POINT ( 'NONE',  ( 0.9740398440564311811, -16.80263250099859462, -39.48175649279251331 ) ) ;
#37653=FACE_OUTER_BOUND ( 'NONE', #61264, .T. ) ;
#37656=ADVANCED_FACE ( 'NONE', ( #39999, #29324 ), #11161, .F. ) ;
#37661=ORIENTED_EDGE ( 'NONE', *, *, #57668, .F. ) ;
#37670=ORIENTED_EDGE ( 'NONE', *, *, #31857, .T. ) ;
#37676=CARTESIAN_POINT ( 'NONE',  ( 0.5832367798473389042, -44.14510605973666202, -18.58036934788121997 ) ) ;
#37681=CARTESIAN_POINT ( 'NONE',  ( 0.5832367798473385712, -46.33367954572892700, 12.13303976268045048 ) ) ;
#37683=CARTESIAN_POINT ( 'NONE',  ( 4.956653778116975495, -26.26162724282400518, 40.28700667097671584 ) ) ;
#37686=DIRECTION ( 'NONE',  ( 0.9990097760809872884, 0.000000000000000000, -0.04449120468829285274 ) ) ;
#37688=CARTESIAN_POINT ( 'NONE',  ( 0.9756354156337465611, 37.09450626018210073, 21.56699035436949430 ) ) ;
#37691=CARTESIAN_POINT ( 'NONE',  ( 0.5807400328401637335, -23.47602859900744221, 41.75144119563879030 ) ) ;
#37694=CARTESIAN_POINT ( 'NONE',  ( 0.9730545539215883499, 15.95224156741883270, -39.83279466599022811 ) ) ;
#37695=CARTESIAN_POINT ( 'NONE',  ( 0.9736507210033062965, 39.46762617149634167, 16.83559693395279311 ) ) ;
#37698=CARTESIAN_POINT ( 'NONE',  ( 0.5834872094924163921, 23.75111410077710161, 41.59216540884673208 ) ) ;
#37705=VERTEX_POINT ( 'NONE', #30242 ) ;
#37706=ORIENTED_EDGE ( 'NONE', *, *, #25209, .F. ) ;
#37710=( BOUNDED_SURFACE ( )  B_SPLINE_SURFACE ( 3, 1, ( 
 ( #61073, #13185 ),
 ( #31663, #9081 ),
 ( #27887, #3745 ),
 ( #4047, #32912 ) ),
 .UNSPECIFIED., .F., .F., .F. ) 
 B_SPLINE_SURFACE_WITH_KNOTS ( ( 4, 4 ),
 ( 2, 2 ),
 ( 0.000000000000000000, 1.000000000000000000 ),
 ( 0.000000000000000000, 1.000000000000000000 ),
 .UNSPECIFIED. ) 
 GEOMETRIC_REPRESENTATION_ITEM ( )  RATIONAL_B_SPLINE_SURFACE ( (
 ( 1.000000000000000000, 1.000000000000000000),
 ( 0.9953390228620291325, 0.8624445117761032620),
 ( 0.9953390228620291325, 0.8624445117761032620),
 ( 1.000000000000000000, 1.000000000000000000) ) ) 
 REPRESENTATION_ITEM ( '' )  SURFACE ( )  );
#37716=ORIENTED_EDGE ( 'NONE', *, *, #21522, .F. ) ;
#37727=EDGE_CURVE ( 'NONE', #23289, #33299, #11464, .T. ) ;
#37735=CARTESIAN_POINT ( 'NONE',  ( 5.960721111146673579, 2.672857320903031741, 20.35079619394246819 ) ) ;
#37739=( BOUNDED_SURFACE ( )  B_SPLINE_SURFACE ( 3, 1, ( 
 ( #7069, #26196 ),
 ( #59703, #44720 ),
 ( #11496, #34691 ),
 ( #16821, #49087 ) ),
 .UNSPECIFIED., .F., .F., .F. ) 
 B_SPLINE_SURFACE_WITH_KNOTS ( ( 4, 4 ),
 ( 2, 2 ),
 ( 0.000000000000000000, 1.000000000000000000 ),
 ( 0.000000000000000000, 1.000000000000000000 ),
 .UNSPECIFIED. ) 
 GEOMETRIC_REPRESENTATION_ITEM ( )  RATIONAL_B_SPLINE_SURFACE ( (
 ( 1.000000000000000000, 1.000000000000000000),
 ( 0.7269869731126817891, 0.9931720237060910339),
 ( 0.7269869731126817891, 0.9931720237060910339),
 ( 1.000000000000000000, 1.000000000000000000) ) ) 
 REPRESENTATION_ITEM ( '' )  SURFACE ( )  );
#37744=EDGE_CURVE ( 'NONE', #56250, #44331, #35563, .T. ) ;
#37751=ORIENTED_EDGE ( 'NONE', *, *, #18964, .T. ) ;
#37752=ORIENTED_EDGE ( 'NONE', *, *, #5312, .T. ) ;
#37762=CYLINDRICAL_SURFACE ( 'NONE', #24788, 12.50000000000000000 ) ;
#37768=VECTOR ( 'NONE', #48042, 1000.000000000000114 ) ;
#37776=B_SPLINE_CURVE_WITH_KNOTS ( 'NONE', 3,
 ( #48876, #16293, #40140, #34792 ),
 .UNSPECIFIED., .F., .F.,
 ( 4, 4 ),
 ( 8.673617379884035472E-19, 0.004050076154992999014 ),
 .UNSPECIFIED. ) ;
#37782=CARTESIAN_POINT ( 'NONE',  ( 5.974727161628367256, 0.01551142186621108643, 20.52494643607030156 ) ) ;
#37783=CARTESIAN_POINT ( 'NONE',  ( 3.660176727303303679, 32.61164548483971259, 35.27264088192871583 ) ) ;
#37784=VERTEX_POINT ( 'NONE', #45924 ) ;
#37788=CARTESIAN_POINT ( 'NONE',  ( 5.860006189529246790, 9.426589201136151175, -47.30296539008815415 ) ) ;
#37798=EDGE_CURVE ( 'NONE', #22653, #28122, #51290, .T. ) ;
#37808=CARTESIAN_POINT ( 'NONE',  ( 0.8557997880470697982, -17.48760788519248521, 44.60232077416680596 ) ) ;
#37811=ORIENTED_EDGE ( 'NONE', *, *, #4494, .F. ) ;
#37820=ORIENTED_EDGE ( 'NONE', *, *, #42224, .T. ) ;
#37825=( BOUNDED_SURFACE ( )  B_SPLINE_SURFACE ( 3, 1, ( 
 ( #1340, #39294 ),
 ( #20476, #35517 ),
 ( #6332, #25469 ),
 ( #54575, #10463 ) ),
 .UNSPECIFIED., .F., .F., .F. ) 
 B_SPLINE_SURFACE_WITH_KNOTS ( ( 4, 4 ),
 ( 2, 2 ),
 ( 0.000000000000000000, 1.000000000000000000 ),
 ( 0.000000000000000000, 1.000000000000000000 ),
 .UNSPECIFIED. ) 
 GEOMETRIC_REPRESENTATION_ITEM ( )  RATIONAL_B_SPLINE_SURFACE ( (
 ( 1.000000000000000000, 1.000000000000000000),
 ( 0.9732289882329797637, 0.9999525324661233672),
 ( 0.9732289882329797637, 0.9999525324661233672),
 ( 1.000000000000000000, 1.000000000000000000) ) ) 
 REPRESENTATION_ITEM ( '' )  SURFACE ( )  );
#37831=ORIENTED_EDGE ( 'NONE', *, *, #56123, .F. ) ;
#37835=VECTOR ( 'NONE', #39292, 1000.000000000000114 ) ;
#37838=CARTESIAN_POINT ( 'NONE',  ( 4.956653778116970166, 47.94889704119054130, 3.690426056930153464 ) ) ;
#37844=CARTESIAN_POINT ( 'NONE',  ( 0.5809828226811617480, -24.41822904836953612, 41.20389530892298779 ) ) ;
#37847=CARTESIAN_POINT ( 'NONE',  ( 0.5838002273316430513, 0.1361971433784746333, -47.89576566046785899 ) ) ;
#37848=CARTESIAN_POINT ( 'NONE',  ( 4.303969348037258058, -14.52400616872337302, -45.86537346639072865 ) ) ;
#37849=CARTESIAN_POINT ( 'NONE',  ( 0.9740398440564312921, 5.189371650077472253, -42.59352035928881719 ) ) ;
#37850=CARTESIAN_POINT ( 'NONE',  ( 4.967162193818130511, 42.96271701169385437, 3.259922920617894793 ) ) ;
#37864=CARTESIAN_POINT ( 'NONE',  ( 0.5809828226811617480, 34.25055090842200656, -33.48000389720580472 ) ) ;
#37867=CARTESIAN_POINT ( 'NONE',  ( 0.9752132459055858904, 10.88033124649678740, -41.50604997043402022 ) ) ;
#37871=CARTESIAN_POINT ( 'NONE',  ( -19.64296139440948252, -7.897528540900530025, -1.281472113053201856 ) ) ;
#37875=CARTESIAN_POINT ( 'NONE',  ( 1.154321713695931839, -25.46626713715435741, -34.54400171733326630 ) ) ;
#37886=ORIENTED_EDGE ( 'NONE', *, *, #56024, .T. ) ;
#37891=B_SPLINE_CURVE_WITH_KNOTS ( 'NONE', 3,
 ( #18011, #18321, #4180, #13620 ),
 .UNSPECIFIED., .F., .F.,
 ( 4, 4 ),
 ( 0.000000000000000000, 0.005004741218457419739 ),
 .UNSPECIFIED. ) ;
#37894=ORIENTED_EDGE ( 'NONE', *, *, #45283, .F. ) ;
#37910=ORIENTED_EDGE ( 'NONE', *, *, #41124, .T. ) ;
#37911=CARTESIAN_POINT ( 'NONE',  ( 0.9968887458511670463, 17.02616470386932690, -39.38692798189845945 ) ) ;
#37912=CARTESIAN_POINT ( 'NONE',  ( 4.303969348037246512, 45.86537346639057944, 14.52400616872384909 ) ) ;
#37918=VECTOR ( 'NONE', #4722, 1000.000000000000114 ) ;
#37926=ORIENTED_EDGE ( 'NONE', *, *, #44754, .T. ) ;
#37927=CARTESIAN_POINT ( 'NONE',  ( 5.960721111146673579, 0.006321279846820317821, -20.52557019979492026 ) ) ;
#37932=DIRECTION ( 'NONE',  ( 0.07439287786467664587, 0.3937848822959431616, -0.9161872986448684753 ) ) ;
#37934=EDGE_CURVE ( 'NONE', #47555, #24092, #58703, .T. ) ;
#37936=B_SPLINE_CURVE_WITH_KNOTS ( 'NONE', 3,
 ( #21499, #54996, #26503, #45633, #41250, #35008 ),
 .UNSPECIFIED., .F., .F.,
 ( 4, 2, 4 ),
 ( 3.529906531158615134E-18, 0.0002445244328975384866, 0.0004890488657950735037 ),
 .UNSPECIFIED. ) ;
#37943=CARTESIAN_POINT ( 'NONE',  ( 0.9722240750034584211, -39.86121765932388428, -15.88116978453023620 ) ) ;
#37944=CARTESIAN_POINT ( 'NONE',  ( 5.958863334805807099, 17.77512673691304812, 10.26388325355093833 ) ) ;
#37952=CARTESIAN_POINT ( 'NONE',  ( 4.303969348037258058, 45.86537346639077839, -14.52400616872321493 ) ) ;
#37958=VECTOR ( 'NONE', #48902, 1000.000000000000114 ) ;
#37965=CARTESIAN_POINT ( 'NONE',  ( 0.5807400328401637335, -47.89582301953904420, 0.5448834511088314070 ) ) ;
#37973=CARTESIAN_POINT ( 'NONE',  ( 5.960221823109900008, -7.849768660536430076, -18.96526051813977531 ) ) ;
#37976=CARTESIAN_POINT ( 'NONE',  ( 0.5809828226811617480, -33.48000389720591841, -34.25055090842189287 ) ) ;
#37979=CARTESIAN_POINT ( 'NONE',  ( 0.6067099128993237445, 47.57459301987705658, 5.548253864790559930 ) ) ;
#37990=AXIS2_PLACEMENT_3D ( 'NONE', #36434, #12630, #3193 ) ;
#37992=CARTESIAN_POINT ( 'NONE',  ( 3.407937589446178528, -2.242416846335508307, -13.51415833181190429 ) ) ;
#37995=( BOUNDED_SURFACE ( )  B_SPLINE_SURFACE ( 3, 1, ( 
 ( #18650, #4819 ),
 ( #56837, #33375 ),
 ( #37782, #14887 ),
 ( #23959, #13967 ) ),
 .UNSPECIFIED., .F., .F., .F. ) 
 B_SPLINE_SURFACE_WITH_KNOTS ( ( 4, 4 ),
 ( 2, 2 ),
 ( 0.000000000000000000, 1.000000000000000000 ),
 ( 0.000000000000000000, 1.000000000000000000 ),
 .UNSPECIFIED. ) 
 GEOMETRIC_REPRESENTATION_ITEM ( )  RATIONAL_B_SPLINE_SURFACE ( (
 ( 1.000000000000000000, 1.000000000000000000),
 ( 0.7269869731126821222, 0.9931720237060910339),
 ( 0.7269869731126821222, 0.9931720237060910339),
 ( 1.000000000000000000, 1.000000000000000000) ) ) 
 REPRESENTATION_ITEM ( '' )  SURFACE ( )  );
#38002=CARTESIAN_POINT ( 'NONE',  ( 5.959828726073459926, 19.82738831247213440, -5.308046411395043407 ) ) ;
#38005=DIRECTION ( 'NONE',  ( -1.000000000000000000, -0.000000000000000000, -0.000000000000000000 ) ) ;
#38006=CARTESIAN_POINT ( 'NONE',  ( 3.407937589446178528, 12.08659953757608818, 6.447869442558206821 ) ) ;
#38007=B_SPLINE_CURVE_WITH_KNOTS ( 'NONE', 3,
 ( #33013, #71, #13910, #24203, #52085, #61174 ),
 .UNSPECIFIED., .F., .F.,
 ( 4, 2, 4 ),
 ( 0.000000000000000000, 0.0002291966416970780756, 0.0004583932833941561512 ),
 .UNSPECIFIED. ) ;
#38008=EDGE_CURVE ( 'NONE', #53492, #8960, #26399, .T. ) ;
#38010=CARTESIAN_POINT ( 'NONE',  ( 0.9757402383260936896, -37.11731350497343840, -21.52772413548522223 ) ) ;
#38020=CARTESIAN_POINT ( 'NONE',  ( 4.963659409799332067, 25.25989740981550113, -36.94443854030191687 ) ) ;
#38031=B_SPLINE_CURVE_WITH_KNOTS ( 'NONE', 3,
 ( #48900, #30092, #10389, #5950, #25712, #34201 ),
 .UNSPECIFIED., .F., .F.,
 ( 4, 2, 4 ),
 ( 1.506204625983992411E-16, 0.0002445252820015209245, 0.0004890505640028912533 ),
 .UNSPECIFIED. ) ;
#38048=VERTEX_POINT ( 'NONE', #1860 ) ;
#38050=CARTESIAN_POINT ( 'NONE',  ( 0.9730545539215883499, 36.90443313492330901, 21.89037132892449478 ) ) ;
#38053=ORIENTED_EDGE ( 'NONE', *, *, #11377, .F. ) ;
#38060=DIRECTION ( 'NONE',  ( 0.000000000000000000, 0.000000000000000000, 1.000000000000000000 ) ) ;
#38069=CARTESIAN_POINT ( 'NONE',  ( 0.9752570700956801897, -42.57087745267993739, 5.371905812151998028 ) ) ;
#38070=CARTESIAN_POINT ( 'NONE',  ( 2.624215991343620935, -22.77108897942165910, 42.26352390376089829 ) ) ;
#38075=CARTESIAN_POINT ( 'NONE',  ( 0.5850706913938533704, 12.22095376872036532, 46.31100969101492382 ) ) ;
#38076=EDGE_LOOP ( 'NONE', ( #16170, #309, #54174, #27623 ) ) ;
#38080=CARTESIAN_POINT ( 'NONE',  ( 3.783198216974383854, 24.80909581868442615, 35.16829104054179567 ) ) ;
#38082=CARTESIAN_POINT ( 'NONE',  ( 4.967162193818130511, 2.375726030843182457, -43.02067033766016380 ) ) ;
#38083=CARTESIAN_POINT ( 'NONE',  ( 0.9972139404380321315, -39.38665787682673880, 17.02682566833171052 ) ) ;
#38087=CARTESIAN_POINT ( 'NONE',  ( 0.5839880159502324197, 12.35255585954184276, 46.27569712847341066 ) ) ;
#38088=EDGE_CURVE ( 'NONE', #21206, #60545, #43582, .T. ) ;
#38089=LINE ( 'NONE', #52760, #33456 ) ;
#38093=AXIS2_PLACEMENT_3D ( 'NONE', #16807, #50299, #14843 ) ;
#38097=EDGE_CURVE ( 'NONE', #25828, #18062, #43001, .T. ) ;
#38100=CARTESIAN_POINT ( 'NONE',  ( 0.5809828226811553087, 37.66417181417592275, -29.58751527316140795 ) ) ;
#38101=CARTESIAN_POINT ( 'NONE',  ( 2.281448460670575606, 28.15071835136453515, -38.84544723616112805 ) ) ;
#38104=VERTEX_POINT ( 'NONE', #39818 ) ;
#38105=CARTESIAN_POINT ( 'NONE',  ( 3.407937589446178528, -8.699069120706699465, -10.58239600294647609 ) ) ;
#38106=CARTESIAN_POINT ( 'NONE',  ( 5.959828726073459926, 7.858992891709871031, 18.96145866559674786 ) ) ;
#38109=ADVANCED_FACE ( 'NONE', ( #25682 ), #22774, .F. ) ;
#38116=EDGE_LOOP ( 'NONE', ( #19759, #22397, #37180, #26181 ) ) ;
#38122=VERTEX_POINT ( 'NONE', #15375 ) ;
#38124=CARTESIAN_POINT ( 'NONE',  ( 0.9730545539215883499, 10.61654491617622398, -41.57420493492374192 ) ) ;
#38126=VECTOR ( 'NONE', #40528, 1000.000000000000114 ) ;
#38128=CARTESIAN_POINT ( 'NONE',  ( 4.956653778116990594, 2.599733001515011743, -48.02038484091096393 ) ) ;
#38129=ORIENTED_EDGE ( 'NONE', *, *, #9772, .F. ) ;
#38136=CARTESIAN_POINT ( 'NONE',  ( 0.9757787079277450148, 26.15233402543316288, -34.01751575780794923 ) ) ;
#38141=FACE_OUTER_BOUND ( 'NONE', #28225, .T. ) ;
#38144=CARTESIAN_POINT ( 'NONE',  ( 0.8557997880470599172, -44.60232077416698360, 17.48760788519201981 ) ) ;
#38145=ORIENTED_EDGE ( 'NONE', *, *, #12902, .F. ) ;
#38149=CARTESIAN_POINT ( 'NONE',  ( 0.6067099128993241886, 38.42667919752404515, 28.59222530349236990 ) ) ;
#38157=CARTESIAN_POINT ( 'NONE',  ( 0.9968887458511649369, -41.61262323391479612, 10.46947792236080410 ) ) ;
#38165=CARTESIAN_POINT ( 'NONE',  ( 5.960221823109900008, -20.52559243573973546, -0.005450390361650292448 ) ) ;
#38168=CARTESIAN_POINT ( 'NONE',  ( 0.9757787079277434605, 42.54650880470572361, -5.561523338226725954 ) ) ;
#38173=CARTESIAN_POINT ( 'NONE',  ( 4.303969348037258058, -45.22910199346963367, -16.39840148505139794 ) ) ;
#38176=ORIENTED_EDGE ( 'NONE', *, *, #60144, .F. ) ;
#38177=EDGE_CURVE ( 'NONE', #20273, #722, #11588, .T. ) ;
#38179=DIRECTION ( 'NONE',  ( 0.000000000000000000, 0.000000000000000000, 1.000000000000000000 ) ) ;
#38190=CARTESIAN_POINT ( 'NONE',  ( 0.5809828226811617480, -38.32755012159166341, 28.72298383114474518 ) ) ;
#38194=EDGE_LOOP ( 'NONE', ( #17963, #3163, #43563, #807 ) ) ;
#38202=CARTESIAN_POINT ( 'NONE',  ( 5.959828726073459926, 16.28681682518047324, 12.49160845136040621 ) ) ;
#38204=CARTESIAN_POINT ( 'NONE',  ( 0.9745511491811736926, 0.3405614984926567113, -42.90705396078546130 ) ) ;
#38206=CARTESIAN_POINT ( 'NONE',  ( 0.9730545539215883499, -29.98130006528840141, -30.69604515769682251 ) ) ;
#38211=ORIENTED_EDGE ( 'NONE', *, *, #10325, .F. ) ;
#38219=EDGE_CURVE ( 'NONE', #54223, #61565, #1138, .T. ) ;
#38235=CARTESIAN_POINT ( 'NONE',  ( 5.981074661064941900, -7.846517100474690309, -18.96560215432014118 ) ) ;
#38240=CARTESIAN_POINT ( 'NONE',  ( 2.526464513654344657, -31.23609615087156754, -29.52129845577965028 ) ) ;
#38241=CARTESIAN_POINT ( 'NONE',  ( 0.5839880159502340851, 18.37091806000297112, -44.23273844814446676 ) ) ;
#38245=CARTESIAN_POINT ( 'NONE',  ( 4.963659409799330291, -2.450325214228700865, 44.68724496494572662 ) ) ;
#38247=EDGE_CURVE ( 'NONE', #17579, #42439, #39227, .T. ) ;
#38249=CARTESIAN_POINT ( 'NONE',  ( 0.8557997880470599172, -7.156447707086029730, 47.37054680076704472 ) ) ;
#38269=CARTESIAN_POINT ( 'NONE',  ( 0.9756950546413934999, -16.50968749804410862, -39.60512406639365679 ) ) ;
#38270=CARTESIAN_POINT ( 'NONE',  ( 3.783198216974386963, -42.86118135813610763, 3.901161703631905731 ) ) ;
#38283=ORIENTED_EDGE ( 'NONE', *, *, #43272, .F. ) ;
#38294=CARTESIAN_POINT ( 'NONE',  ( 0.5786265663353153954, 24.57327059187398177, 41.11783955080247921 ) ) ;
#38296=FACE_OUTER_BOUND ( 'NONE', #13898, .T. ) ;
#38302=CARTESIAN_POINT ( 'NONE',  ( 0.8551540677456739292, -0.9122407826479072002, 47.90804413217340851 ) ) ;
#38303=CARTESIAN_POINT ( 'NONE',  ( 0.9730545539215883499, 33.73144377768594637, -26.52009130076736554 ) ) ;
#38310=CARTESIAN_POINT ( 'NONE',  ( 3.407937589446178528, -12.82481284928200260, -4.815089211105192391 ) ) ;
#38315=DIRECTION ( 'NONE',  ( -0.07836865515943411409, -0.2503967164834531856, 0.9649662368512210708 ) ) ;
#38317=CARTESIAN_POINT ( 'NONE',  ( 3.783198216974391404, 9.462293521184873768, 41.98529422752520901 ) ) ;
#38319=VERTEX_POINT ( 'NONE', #16667 ) ;
#38321=EDGE_CURVE ( 'NONE', #45266, #28142, #48968, .T. ) ;
#38335=ORIENTED_EDGE ( 'NONE', *, *, #17889, .F. ) ;
#38336=CARTESIAN_POINT ( 'NONE',  ( 5.974727161628369032, -10.24903993264996949, -17.78288073588499074 ) ) ;
#38341=ORIENTED_EDGE ( 'NONE', *, *, #44605, .T. ) ;
#38343=CARTESIAN_POINT ( 'NONE',  ( 1.154321485836934169, -41.23280395520815489, 11.90271791109298505 ) ) ;
#38350=EDGE_CURVE ( 'NONE', #44883, #30283, #26673, .T. ) ;
#38351=( BOUNDED_SURFACE ( )  B_SPLINE_SURFACE ( 3, 1, ( 
 ( #28227, #47343 ),
 ( #27929, #32635 ),
 ( #23525, #18855 ),
 ( #9424, #35420 ) ),
 .UNSPECIFIED., .F., .F., .F. ) 
 B_SPLINE_SURFACE_WITH_KNOTS ( ( 4, 4 ),
 ( 2, 2 ),
 ( 0.000000000000000000, 1.000000000000000000 ),
 ( 0.000000000000000000, 1.000000000000000000 ),
 .UNSPECIFIED. ) 
 GEOMETRIC_REPRESENTATION_ITEM ( )  RATIONAL_B_SPLINE_SURFACE ( (
 ( 1.000000000000000000, 1.000000000000000000),
 ( 0.9953390228620291325, 0.8624445117760984880),
 ( 0.9953390228620291325, 0.8624445117760984880),
 ( 1.000000000000000000, 1.000000000000000000) ) ) 
 REPRESENTATION_ITEM ( '' )  SURFACE ( )  );
#38359=EDGE_CURVE ( 'NONE', #35182, #5228, #37015, .T. ) ;
#38360=VERTEX_POINT ( 'NONE', #28211 ) ;
#38369=( BOUNDED_SURFACE ( )  B_SPLINE_SURFACE ( 3, 1, ( 
 ( #10710, #34213 ),
 ( #1585, #20721 ),
 ( #5963, #43315 ),
 ( #29491, #25105 ) ),
 .UNSPECIFIED., .F., .F., .F. ) 
 B_SPLINE_SURFACE_WITH_KNOTS ( ( 4, 4 ),
 ( 2, 2 ),
 ( 0.000000000000000000, 1.000000000000000000 ),
 ( 0.000000000000000000, 1.000000000000000000 ),
 .UNSPECIFIED. ) 
 GEOMETRIC_REPRESENTATION_ITEM ( )  RATIONAL_B_SPLINE_SURFACE ( (
 ( 1.000000000000000000, 1.000000000000000000),
 ( 0.9953390228620291325, 0.8624445117761032620),
 ( 0.9953390228620291325, 0.8624445117761032620),
 ( 1.000000000000000000, 1.000000000000000000) ) ) 
 REPRESENTATION_ITEM ( '' )  SURFACE ( )  );
#38371=CARTESIAN_POINT ( 'NONE',  ( 0.9968887458511649369, 20.88287852258444843, 37.48500720268736330 ) ) ;
#38386=APPLICATION_CONTEXT ( 'automotive_design' ) ;
#38387=CARTESIAN_POINT ( 'NONE',  ( 0.9757787079277466802, -11.14366644276439544, 41.43615150473007702 ) ) ;
#38389=CARTESIAN_POINT ( 'NONE',  ( 0.9722240750034577550, -36.86535092060692875, 21.95618656573991245 ) ) ;
#38393=CARTESIAN_POINT ( 'NONE',  ( 0.5809828226811553087, -37.66417181417572380, 29.58751527316164953 ) ) ;
#38399=CARTESIAN_POINT ( 'NONE',  ( 0.5819845079324659221, -41.70428776698881279, -23.55367910461039926 ) ) ;
#38404=CARTESIAN_POINT ( 'NONE',  ( -4.473699999999997345, 0.000000000000000000, 0.000000000000000000 ) ) ;
#38408=CARTESIAN_POINT ( 'NONE',  ( 0.5809828226811553087, 0.5448590168532381206, 47.89273459658653564 ) ) ;
#38417=VECTOR ( 'NONE', #3893, 1000.000000000000000 ) ;
#38418=ORIENTED_EDGE ( 'NONE', *, *, #61226, .F. ) ;
#38421=CARTESIAN_POINT ( 'NONE',  ( 0.9749527285493311268, -42.50314808877157446, -5.883724875809550170 ) ) ;
#38425=ORIENTED_EDGE ( 'NONE', *, *, #3941, .T. ) ;
#38428=ORIENTED_EDGE ( 'NONE', *, *, #37934, .T. ) ;
#38430=CARTESIAN_POINT ( 'NONE',  ( 4.963659409799330291, 36.94443854030254215, -25.25989740981460230 ) ) ;
#38436=B_SPLINE_CURVE_WITH_KNOTS ( 'NONE', 3,
 ( #31806, #50892, #13021, #51195, #8277, #27398 ),
 .UNSPECIFIED., .F., .F.,
 ( 4, 2, 4 ),
 ( 6.149443329761889321E-18, 0.0002445244328975373482, 0.0004890488657950686248 ),
 .UNSPECIFIED. ) ;
#38439=CARTESIAN_POINT ( 'NONE',  ( 0.5809828226811553087, -18.83114015454665946, -44.03860873105715967 ) ) ;
#38447=ORIENTED_EDGE ( 'NONE', *, *, #3941, .F. ) ;
#38449=CARTESIAN_POINT ( 'NONE',  ( 0.7762783648524370639, 38.54028518467420383, 28.45155609988340828 ) ) ;
#38459=CARTESIAN_POINT ( 'NONE',  ( 5.959547316686252039, 19.82530672674362293, -5.315863417546125014 ) ) ;
#38460=LINE ( 'NONE', #52842, #52845 ) ;
#38464=FACE_OUTER_BOUND ( 'NONE', #15422, .T. ) ;
#38466=CARTESIAN_POINT ( 'NONE',  ( 1.088908134280556661, 30.89124834763388350, 29.78762923589977873 ) ) ;
#38467=CARTESIAN_POINT ( 'NONE',  ( 5.958863334805807099, -20.34989385289155450, -2.680345151634541789 ) ) ;
#38471=EDGE_CURVE ( 'NONE', #35962, #36314, #57929, .T. ) ;
#38472=VECTOR ( 'NONE', #34335, 1000.000000000000114 ) ;
#38475=CARTESIAN_POINT ( 'NONE',  ( 0.8557997880470606944, -33.22501220301877112, -34.51495345639583689 ) ) ;
#38480=CARTESIAN_POINT ( 'NONE',  ( 0.9722240750034588652, -20.94823713380363017, 37.44729079646484848 ) ) ;
#38482=EDGE_CURVE ( 'NONE', #15844, #22653, #58550, .T. ) ;
#38495=VERTEX_POINT ( 'NONE', #19442 ) ;
#38500=ADVANCED_FACE ( 'NONE', ( #58237 ), #49704, .T. ) ;
#38511=EDGE_CURVE ( 'NONE', #23911, #25935, #34783, .T. ) ;
#38513=CARTESIAN_POINT ( 'NONE',  ( 1.088313998177384834, 17.14007796983287335, -39.34193117255236416 ) ) ;
#38515=FACE_OUTER_BOUND ( 'NONE', #19325, .T. ) ;
#38518=CARTESIAN_POINT ( 'NONE',  ( 1.088908134280555107, -26.73890361625891643, -33.56490895818192399 ) ) ;
#38522=AXIS2_PLACEMENT_3D ( 'NONE', #59617, #17648, #16725 ) ;
#38530=CARTESIAN_POINT ( 'NONE',  ( 4.967162193818129623, 32.10009971360071290, 28.74031574030022540 ) ) ;
#38535=CARTESIAN_POINT ( 'NONE',  ( 5.958863334805807099, 17.77512673691319023, -10.26388325355069142 ) ) ;
#38544=CARTESIAN_POINT ( 'NONE',  ( 4.967162193818129623, -32.10009971360051395, -28.74031574030045633 ) ) ;
#38547=CARTESIAN_POINT ( 'NONE',  ( 4.956653778116997699, 42.88673967249161478, -21.75875759808661059 ) ) ;
#38558=CARTESIAN_POINT ( 'NONE',  ( 5.960721111146673579, -2.672857320903164524, -20.35079619394245043 ) ) ;
#38565=CARTESIAN_POINT ( 'NONE',  ( 3.407937589446178528, -0.4592810312471026224, -13.69123696618924946 ) ) ;
#38570=EDGE_LOOP ( 'NONE', ( #32649, #8301, #38648, #60986 ) ) ;
#38576=CARTESIAN_POINT ( 'NONE',  ( 0.9972139404380309102, 36.82725283858638221, -22.02214929131103105 ) ) ;
#38580=CARTESIAN_POINT ( 'NONE',  ( 0.5809828226811556418, 44.45562576850601744, 17.82437196699697424 ) ) ;
#38581=DIRECTION ( 'NONE',  ( -0.07439287786467653485, -0.7144194931002968429, -0.6957517427943147315 ) ) ;
#38583=CARTESIAN_POINT ( 'NONE',  ( 0.5786265663353196143, -18.99608782658064854, 43.97352617418609100 ) ) ;
#38586=CARTESIAN_POINT ( 'NONE',  ( 1.227938101723748288, 17.20315230597897482, -39.32113113558949635 ) ) ;
#38590=DIRECTION ( 'NONE',  ( -0.07439287786467652097, 0.01320009283086247091, 0.9971416435352943308 ) ) ;
#38597=CARTESIAN_POINT ( 'NONE',  ( 0.5834872094924171693, -44.16273175734627898, -18.53852119651611829 ) ) ;
#38599=CARTESIAN_POINT ( 'NONE',  ( 3.660176727303411592, 1.881607889988430760, -48.00143922595152901 ) ) ;
#38605=CARTESIAN_POINT ( 'NONE',  ( -16.58482686117664784, -7.842831842844969259, 1.581017821500569243 ) ) ;
#38610=CARTESIAN_POINT ( 'NONE',  ( 1.227938101723748288, 33.52879263017863565, 26.79402671879338271 ) ) ;
#38611=CARTESIAN_POINT ( 'NONE',  ( 0.5800708119828345000, 44.48635609075557085, 17.74761857127083431 ) ) ;
#38612=CARTESIAN_POINT ( 'NONE',  ( 0.5839879882012675161, -23.94800997596656700, -41.47910964649822319 ) ) ;
#38615=CARTESIAN_POINT ( 'NONE',  ( 1.088908134280551998, 34.51503525510850778, 25.50067491870050418 ) ) ;
#38617=CARTESIAN_POINT ( 'NONE',  ( 0.5838002273316442725, 29.26514720557072380, -37.91535410490837421 ) ) ;
#38621=ADVANCED_FACE ( 'NONE', ( #41046 ), #41634, .F. ) ;
#38622=CARTESIAN_POINT ( 'NONE',  ( 0.9730545539215883499, 5.099196237954877198, 42.60426903087355299 ) ) ;
#38627=EDGE_LOOP ( 'NONE', ( #40160, #5465, #47033, #20650 ) ) ;
#38641=CARTESIAN_POINT ( 'NONE',  ( 4.960156602257181468, 45.42786611289310628, 9.558288641081908565 ) ) ;
#38642=EDGE_CURVE ( 'NONE', #12689, #29464, #11468, .T. ) ;
#38644=ORIENTED_EDGE ( 'NONE', *, *, #28089, .F. ) ;
#38648=ORIENTED_EDGE ( 'NONE', *, *, #31551, .F. ) ;
#38651=CARTESIAN_POINT ( 'NONE',  ( 5.965394784446460541, 2.664747781315840225, 20.35165389555759319 ) ) ;
#38653=B_SPLINE_CURVE_WITH_KNOTS ( 'NONE', 3,
 ( #18943, #97, #51807, #51490 ),
 .UNSPECIFIED., .F., .F.,
 ( 4, 4 ),
 ( 8.673617379884035472E-19, 0.004048833967417086489 ),
 .UNSPECIFIED. ) ;
#38657=B_SPLINE_CURVE_WITH_KNOTS ( 'NONE', 3,
 ( #4605, #9335, #28438, #23750, #16207, #25287 ),
 .UNSPECIFIED., .F., .F.,
 ( 4, 2, 4 ),
 ( 8.985151752445514084E-18, 0.0002291978881530159432, 0.0004583957763060229418 ),
 .UNSPECIFIED. ) ;
#38683=DIRECTION ( 'NONE',  ( -0.07836865515943411409, -0.3742079063794971905, 0.9240274869783773326 ) ) ;
#38687=FACE_OUTER_BOUND ( 'NONE', #40573, .T. ) ;
#38691=CARTESIAN_POINT ( 'NONE',  ( 0.9740398440564312921, -25.79088785829005204, 34.29238484271522225 ) ) ;
#38693=CARTESIAN_POINT ( 'NONE',  ( 4.956653778116994147, 32.11725092155092653, -35.79382859084083179 ) ) ;
#38704=ORIENTED_EDGE ( 'NONE', *, *, #61584, .F. ) ;
#38705=CARTESIAN_POINT ( 'NONE',  ( 3.783198216974387851, 22.99723434398843480, -36.37893817280263420 ) ) ;
#38712=CARTESIAN_POINT ( 'NONE',  ( 0.9745511491811759130, -39.51062171155246716, -16.73445648040612355 ) ) ;
#38714=DIRECTION ( 'NONE',  ( -0.07439287786467650709, -0.6174937095821653177, -0.7830499462674573863 ) ) ;
#38717=CARTESIAN_POINT ( 'NONE',  ( 1.227938101723748288, 10.28900963485380693, 41.66816631169195517 ) ) ;
#38728=CARTESIAN_POINT ( 'NONE',  ( 1.154321713695928286, 42.43366804783615720, 6.418927679455782354 ) ) ;
#38729=VERTEX_POINT ( 'NONE', #42571 ) ;
#38735=ORIENTED_EDGE ( 'NONE', *, *, #19061, .T. ) ;
#38740=CARTESIAN_POINT ( 'NONE',  ( 0.5839879882012674051, 29.15724166963650177, 37.99840755997057329 ) ) ;
#38750=CARTESIAN_POINT ( 'NONE',  ( 0.9757892942422826676, 26.08029006934586747, -34.07281211842300195 ) ) ;
#38756=CARTESIAN_POINT ( 'NONE',  ( 0.9722240741986377666, 34.39263045016090103, -25.65687427836869716 ) ) ;
#38758=CARTESIAN_POINT ( 'NONE',  ( 0.5839880159502337520, -23.98728323041079946, 41.45643525694599418 ) ) ;
#38762=ORIENTED_EDGE ( 'NONE', *, *, #4837, .T. ) ;
#38767=B_SPLINE_CURVE_WITH_KNOTS ( 'NONE', 3,
 ( #7211, #16325, #50753, #11638 ),
 .UNSPECIFIED., .F., .F.,
 ( 4, 4 ),
 ( 2.168404344971008868E-19, 0.004048833967417087357 ),
 .UNSPECIFIED. ) ;
#38768=FACE_OUTER_BOUND ( 'NONE', #30950, .T. ) ;
#38769=CARTESIAN_POINT ( 'NONE',  ( 3.270143674763207553, -8.113405361969586949, 11.02405647745167272 ) ) ;
#38774=LINE ( 'NONE', #15263, #8423 ) ;
#38784=B_SPLINE_CURVE_WITH_KNOTS ( 'NONE', 3,
 ( #33709, #8959, #43112, #23982, #19606, #149 ),
 .UNSPECIFIED., .F., .F.,
 ( 4, 2, 4 ),
 ( 5.275955480050202716E-18, 0.0002445244328975379987, 0.0004890488657950707932 ),
 .UNSPECIFIED. ) ;
#38797=VERTEX_POINT ( 'NONE', #53472 ) ;
#38808=DIRECTION ( 'NONE',  ( -0.07836865515943411409, -0.8593913859058586180, 0.5052769534812658891 ) ) ;
#38816=CONICAL_SURFACE ( 'NONE', #12791, 43.08621763946400307, 1.568696531533066763 ) ;
#38820=CARTESIAN_POINT ( 'NONE',  ( 0.9730545539215883499, 25.71816799638778406, 34.34678117142565412 ) ) ;
#38825=ORIENTED_EDGE ( 'NONE', *, *, #29902, .T. ) ;
#38833=CARTESIAN_POINT ( 'NONE',  ( 0.8551540677456715978, -29.88829867897840131, 37.45266983663486116 ) ) ;
#38834=ORIENTED_EDGE ( 'NONE', *, *, #14591, .F. ) ;
#38835=B_SPLINE_CURVE_WITH_KNOTS ( 'NONE', 3,
 ( #3063, #50673, #59778, #41934 ),
 .UNSPECIFIED., .F., .F.,
 ( 4, 4 ),
 ( 8.673617379884035472E-19, 0.004050076154993000749 ),
 .UNSPECIFIED. ) ;
#38844=CARTESIAN_POINT ( 'NONE',  ( 5.981074661064941900, 18.95903134304789361, -7.862380442163942718 ) ) ;
#38849=CARTESIAN_POINT ( 'NONE',  ( 0.6846871229502932144, 47.90045233486063836, 0.8641397935261219132 ) ) ;
#38855=CARTESIAN_POINT ( 'NONE',  ( 5.960221823109900008, 20.52559243573973546, -0.005450390361510015769 ) ) ;
#38861=CARTESIAN_POINT ( 'NONE',  ( 0.7057020205115015488, 47.37450661940669505, 7.085441699093776968 ) ) ;
#38868=EDGE_CURVE ( 'NONE', #15318, #25828, #222, .T. ) ;
#38872=CARTESIAN_POINT ( 'NONE',  ( 4.967162193818130511, -40.93989340068619498, 13.42934394584149871 ) ) ;
#38875=CARTESIAN_POINT ( 'NONE',  ( 2.281448460670575162, 37.24544744441619315, -30.23587867650717698 ) ) ;
#38878=CARTESIAN_POINT ( 'NONE',  ( 0.8557997880470697982, -47.89938907511594834, 0.9121262075944505110 ) ) ;
#38882=ORIENTED_EDGE ( 'NONE', *, *, #12148, .T. ) ;
#38888=CARTESIAN_POINT ( 'NONE',  ( 3.783278058412224087, 43.00370293663097954, -1.726763838446331523 ) ) ;
#38889=EDGE_LOOP ( 'NONE', ( #57470, #3904, #48585, #34297 ) ) ;
#38894=CARTESIAN_POINT ( 'NONE',  ( 5.959828726073459926, -7.858992891710012252, -18.96145866559668747 ) ) ;
#38901=B_SPLINE_CURVE_WITH_KNOTS ( 'NONE', 3,
 ( #31921, #50696, #27833, #27213 ),
 .UNSPECIFIED., .F., .F.,
 ( 4, 4 ),
 ( 0.000000000000000000, 0.004446090762761349506 ),
 .UNSPECIFIED. ) ;
#38905=FACE_OUTER_BOUND ( 'NONE', #58451, .T. ) ;
#38917=EDGE_CURVE ( 'NONE', #58012, #53765, #22669, .T. ) ;
#38918=CARTESIAN_POINT ( 'NONE',  ( 5.959547316686252039, -17.77392908783926728, -10.26589671991357022 ) ) ;
#38925=CARTESIAN_POINT ( 'NONE',  ( -15.94139450991274209, -7.982454930101551049, -0.5465034650385233173 ) ) ;
#38943=ORIENTED_EDGE ( 'NONE', *, *, #44713, .F. ) ;
#38946=ORIENTED_EDGE ( 'NONE', *, *, #49452, .T. ) ;
#38949=VERTEX_POINT ( 'NONE', #45050 ) ;
#38953=CARTESIAN_POINT ( 'NONE',  ( 0.9722240741986383217, 39.41582013185147559, 16.95645453362478960 ) ) ;
#38958=VECTOR ( 'NONE', #357, 1000.000000000000114 ) ;
#38959=CARTESIAN_POINT ( 'NONE',  ( 0.9736507210033056303, -33.76542629919387650, -26.47691119766824741 ) ) ;
#38960=ORIENTED_EDGE ( 'NONE', *, *, #50077, .F. ) ;
#38961=ORIENTED_EDGE ( 'NONE', *, *, #32900, .F. ) ;
#38971=CARTESIAN_POINT ( 'NONE',  ( 5.981074661064941900, -17.77917279944625051, -10.25489689131124216 ) ) ;
#38976=ORIENTED_EDGE ( 'NONE', *, *, #40830, .F. ) ;
#38977=CARTESIAN_POINT ( 'NONE',  ( 5.960721111146673579, 16.28018152803675633, 12.50019045452743782 ) ) ;
#38978=CARTESIAN_POINT ( 'NONE',  ( 0.7057020205115038802, -13.20843872046520673, 46.04437542275042006 ) ) ;
#38982=CARTESIAN_POINT ( 'NONE',  ( 4.967162193818130511, 7.970725651239789045, 42.34252806656596846 ) ) ;
#38983=EDGE_CURVE ( 'NONE', #2858, #52304, #51834, .T. ) ;
#38992=CARTESIAN_POINT ( 'NONE',  ( 4.967162193818130511, -2.375726030842277403, -43.02067033766020643 ) ) ;
#38993=EDGE_LOOP ( 'NONE', ( #58962, #12450, #36889, #48315 ) ) ;
#38994=EDGE_CURVE ( 'NONE', #59424, #36040, #20445, .T. ) ;
#38995=CARTESIAN_POINT ( 'NONE',  ( 0.6067375320500716374, -28.59217831626991213, -38.42671567536882549 ) ) ;
#38996=CARTESIAN_POINT ( 'NONE',  ( 0.8557997880470690211, 23.15977007032381607, -41.93815086860232810 ) ) ;
#39003=CARTESIAN_POINT ( 'NONE',  ( 5.959547316686252039, -2.682663672455063431, 20.34955788964371948 ) ) ;
#39006=EDGE_CURVE ( 'NONE', #5333, #12545, #45105, .T. ) ;
#39007=CARTESIAN_POINT ( 'NONE',  ( 0.9730545539215892381, -10.61654491617593266, 41.57420493492382008 ) ) ;
#39008=EDGE_CURVE ( 'NONE', #22114, #49237, #54774, .T. ) ;
#39011=CARTESIAN_POINT ( 'NONE',  ( 0.9730545539215883499, -30.69604515769629316, -29.98130006528894498 ) ) ;
#39021=CARTESIAN_POINT ( 'NONE',  ( 0.5839879882012689594, -41.47913983251933701, -23.94795769224428739 ) ) ;
#39023=ORIENTED_EDGE ( 'NONE', *, *, #46686, .F. ) ;
#39034=CARTESIAN_POINT ( 'NONE',  ( 0.9756008150404590351, 42.55970871350812956, 5.459718823765672191 ) ) ;
#39046=CARTESIAN_POINT ( 'NONE',  ( 0.9758171775293911221, -42.54217005300507992, -5.594812732687539203 ) ) ;
#39049=EDGE_LOOP ( 'NONE', ( #8807, #56163, #55721, #40722 ) ) ;
#39053=CARTESIAN_POINT ( 'NONE',  ( 0.5832366564991493529, 23.71163571971582229, -41.61464700196751210 ) ) ;
#39056=DIRECTION ( 'NONE',  ( -1.000000000000000000, -0.000000000000000000, -0.000000000000000000 ) ) ;
#39057=EDGE_CURVE ( 'NONE', #20008, #25113, #16745, .T. ) ;
#39061=CARTESIAN_POINT ( 'NONE',  ( 0.7056555295713272669, -19.10539864320367798, -43.92642606846697362 ) ) ;
#39076=CARTESIAN_POINT ( 'NONE',  ( -15.92917370011572409, -12.49037116071005116, 0.5520084180848008337 ) ) ;
#39083=CARTESIAN_POINT ( 'NONE',  ( 0.8557997880470697982, -7.156447707085392018, -47.37054680076713709 ) ) ;
#39085=CARTESIAN_POINT ( 'NONE',  ( 5.959547316686252039, 19.82715097195162457, -5.308980600728250288 ) ) ;
#39087=EDGE_LOOP ( 'NONE', ( #6081, #38129, #57209, #37575 ) ) ;
#39088=CARTESIAN_POINT ( 'NONE',  ( 3.660087539127319101, -27.72868323267833901, 39.22752134874908592 ) ) ;
#39092=CARTESIAN_POINT ( 'NONE',  ( 0.5850706913938533704, 47.46255051844953954, 6.431767090162980871 ) ) ;
#39099=CARTESIAN_POINT ( 'NONE',  ( 4.956653778116990594, -32.11725092155016625, -35.79382859084151391 ) ) ;
#39100=ORIENTED_EDGE ( 'NONE', *, *, #1344, .F. ) ;
#39102=CARTESIAN_POINT ( 'NONE',  ( 0.5819845079324661441, 47.42480735454296337, -6.701571823032242747 ) ) ;
#39103=ORIENTED_EDGE ( 'NONE', *, *, #55163, .T. ) ;
#39115=CARTESIAN_POINT ( 'NONE',  ( 1.227938101723756947, 33.52879263017899092, -26.79402671879293507 ) ) ;
#39123=CARTESIAN_POINT ( 'NONE',  ( 5.959547316686252039, -14.51128755440551465, 14.51632612601503602 ) ) ;
#39130=CARTESIAN_POINT ( 'NONE',  ( 0.5839879882012706247, -6.251648354650508388, 47.48621496524026497 ) ) ;
#39137=CARTESIAN_POINT ( 'NONE',  ( 0.5834872094924171693, 18.11905305011518763, 44.33648115256904987 ) ) ;
#39138=CARTESIAN_POINT ( 'NONE',  ( 4.960156602257180580, 30.99165383632812976, -34.56254177294235319 ) ) ;
#39139=B_SPLINE_CURVE_WITH_KNOTS ( 'NONE', 3,
 ( #58279, #43620, #5650, #21028 ),
 .UNSPECIFIED., .F., .F.,
 ( 4, 4 ),
 ( 0.000000000000000000, 0.004444878191957700800 ),
 .UNSPECIFIED. ) ;
#39141=DIRECTION ( 'NONE',  ( -1.000000000000000000, -0.000000000000000000, -0.000000000000000000 ) ) ;
#39143=VERTEX_POINT ( 'NONE', #29604 ) ;
#39149=CARTESIAN_POINT ( 'NONE',  ( 0.8557997880470599172, -38.55640757422458620, 28.43566216844957140 ) ) ;
#39151=CARTESIAN_POINT ( 'NONE',  ( 5.959828726073459926, -2.683617577144532973, 20.34941966491234311 ) ) ;
#39160=CARTESIAN_POINT ( 'NONE',  ( 3.407937589446174087, 11.62731850632884090, 7.243367523631064842 ) ) ;
#39163=LINE ( 'NONE', #23806, #1636 ) ;
#39164=ORIENTED_EDGE ( 'NONE', *, *, #39057, .T. ) ;
#39166=FACE_OUTER_BOUND ( 'NONE', #27379, .T. ) ;
#39170=CARTESIAN_POINT ( 'NONE',  ( 3.783198216974388739, 39.06945274417391545, 18.05208553945161043 ) ) ;
#39175=ORIENTED_EDGE ( 'NONE', *, *, #60177, .F. ) ;
#39181=ADVANCED_FACE ( 'NONE', ( #23988 ), #8749, .T. ) ;
#39182=CARTESIAN_POINT ( 'NONE',  ( 4.956653778116959508, -15.97476558431919180, 45.35992544608522792 ) ) ;
#39189=CARTESIAN_POINT ( 'NONE',  ( 4.967162193818131399, -38.83676580803778933, 18.65818244221244981 ) ) ;
#39200=LINE ( 'NONE', #26003, #18697 ) ;
#39205=VERTEX_POINT ( 'NONE', #4542 ) ;
#39209=CARTESIAN_POINT ( 'NONE',  ( 1.227938101723748288, -34.55893248994524214, 25.45152231597044690 ) ) ;
#39215=CARTESIAN_POINT ( 'NONE',  ( 4.963659409799330291, -25.25989740981525244, 36.94443854030213004 ) ) ;
#39217=EDGE_CURVE ( 'NONE', #50690, #21453, #10755, .T. ) ;
#39223=CARTESIAN_POINT ( 'NONE',  ( 3.270143674763207553, 12.53844339339242531, -5.490410281242639634 ) ) ;
#39226=CARTESIAN_POINT ( 'NONE',  ( 4.967162193818130511, 0.000000000000000000, 0.000000000000000000 ) ) ;
#39227=B_SPLINE_CURVE_WITH_KNOTS ( 'NONE', 3,
 ( #29206, #19833, #58941, #39254, #15747, #11345 ),
 .UNSPECIFIED., .F., .F.,
 ( 4, 2, 4 ),
 ( 9.828040028768063295E-18, 0.0002291966416970815722, 0.0004583932833941532781 ),
 .UNSPECIFIED. ) ;
#39228=CARTESIAN_POINT ( 'NONE',  ( -17.29528526743291295, -7.748184832854354553, -1.992127074845276402 ) ) ;
#39235=DIRECTION ( 'NONE',  ( -0.07836865515943411409, 0.1379401902675563285, 0.9873352307081176837 ) ) ;
#39237=CARTESIAN_POINT ( 'NONE',  ( 3.783278058412225864, 29.18720354295088981, -31.62921638229637722 ) ) ;
#39239=VERTEX_POINT ( 'NONE', #54312 ) ;
#39243=ORIENTED_EDGE ( 'NONE', *, *, #28910, .T. ) ;
#39246=ORIENTED_EDGE ( 'NONE', *, *, #28989, .F. ) ;
#39249=FACE_OUTER_BOUND ( 'NONE', #53106, .T. ) ;
#39251=CARTESIAN_POINT ( 'NONE',  ( 0.9722240750034568668, 25.65687433776948012, -34.39263040572760843 ) ) ;
#39252=ORIENTED_EDGE ( 'NONE', *, *, #61563, .F. ) ;
#39253=ORIENTED_EDGE ( 'NONE', *, *, #27751, .F. ) ;
#39254=CARTESIAN_POINT ( 'NONE',  ( 1.088313998177382169, 25.50107284445311606, 34.51470853099723968 ) ) ;
#39268=CARTESIAN_POINT ( 'NONE',  ( 5.965394784446458765, -16.29267539192334624, -12.48356622107671221 ) ) ;
#39277=CARTESIAN_POINT ( 'NONE',  ( 0.5807400328401637335, -34.25275203086212628, -33.48217046439146571 ) ) ;
#39282=VERTEX_POINT ( 'NONE', #30836 ) ;
#39292=DIRECTION ( 'NONE',  ( -0.07439287786467650709, -0.8569499480575021311, 0.5100024374914848835 ) ) ;
#39294=CARTESIAN_POINT ( 'NONE',  ( 0.5807400328401574052, 34.25275203086236075, 33.48217046439123834 ) ) ;
#39297=CARTESIAN_POINT ( 'NONE',  ( 0.7056555295713283771, -41.05687446835452903, 24.67549844185522545 ) ) ;
#39302=CARTESIAN_POINT ( 'NONE',  ( 0.5809828226811617480, -41.74875432577665890, 23.47450554821694979 ) ) ;
#39304=CARTESIAN_POINT ( 'NONE',  ( 0.5807400328401637335, 37.66660715020866235, 29.58941477093028993 ) ) ;
#39309=ORIENTED_EDGE ( 'NONE', *, *, #36413, .T. ) ;
#39317=CARTESIAN_POINT ( 'NONE',  ( 5.960721111146673579, 5.306302591836305815, 19.82781442290499996 ) ) ;
#39325=CARTESIAN_POINT ( 'NONE',  ( 4.967162193818130511, 42.34252806656603241, -7.970725651239366272 ) ) ;
#39327=CARTESIAN_POINT ( 'NONE',  ( 2.281448460670572942, 4.956513608981858887, -47.71650330356582259 ) ) ;
#39340=CARTESIAN_POINT ( 'NONE',  ( 3.783278058412225864, 20.00643011788508119, -38.10568111914483325 ) ) ;
#39344=ORIENTED_EDGE ( 'NONE', *, *, #3485, .F. ) ;
#39346=DIRECTION ( 'NONE',  ( 0.000000000000000000, 0.000000000000000000, 1.000000000000000000 ) ) ;
#39350=CARTESIAN_POINT ( 'NONE',  ( 5.958863334805807099, -10.26388325355099695, 17.77512673691301259 ) ) ;
#39354=CARTESIAN_POINT ( 'NONE',  ( 0.5839879327111923146, 23.86931774877355750, -41.52454255611482381 ) ) ;
#39366=CARTESIAN_POINT ( 'NONE',  ( 0.8557997880470690211, 5.347802024197924275, -47.60865952216993691 ) ) ;
#39368=CARTESIAN_POINT ( 'NONE',  ( 1.088313998177377950, 34.51470853099749547, -25.50107284445278921 ) ) ;
#39370=CARTESIAN_POINT ( 'NONE',  ( 0.9756950546413922787, 39.60512406639371363, -16.50968749804397717 ) ) ;
#39376=FACE_OUTER_BOUND ( 'NONE', #38570, .T. ) ;
#39381=VECTOR ( 'NONE', #56225, 1000.000000000000114 ) ;
#39385=LINE ( 'NONE', #58745, #24892 ) ;
#39387=DIRECTION ( 'NONE',  ( 0.07439287786467665975, -0.7830499462674513911, -0.6174937095821728672 ) ) ;
#39390=ORIENTED_EDGE ( 'NONE', *, *, #11045, .F. ) ;
#39393=CARTESIAN_POINT ( 'NONE',  ( 5.974727161628369032, 20.34732802718243860, 2.694421823322989074 ) ) ;
#39397=VERTEX_POINT ( 'NONE', #57706 ) ;
#39406=FACE_OUTER_BOUND ( 'NONE', #4702, .T. ) ;
#39417=ADVANCED_FACE ( 'NONE', ( #29528 ), #27673, .T. ) ;
#39420=CARTESIAN_POINT ( 'NONE',  ( 2.526464513654346877, 33.34586834545809353, -27.11556434133515125 ) ) ;
#39435=ORIENTED_EDGE ( 'NONE', *, *, #11314, .T. ) ;
#39442=CARTESIAN_POINT ( 'NONE',  ( 4.963659409799330291, 13.93274247732079374, -42.53037318520974708 ) ) ;
#39443=CARTESIAN_POINT ( 'NONE',  ( 1.227938101723748288, 39.32113113558966688, 17.20315230597858047 ) ) ;
#39454=CARTESIAN_POINT ( 'NONE',  ( 3.407937589446178528, 8.699069120706768743, 10.58239600294641747 ) ) ;
#39473=CARTESIAN_POINT ( 'NONE',  ( 0.5837374860065642768, 18.16107481025659354, -44.31936661703453240 ) ) ;
#39476=ORIENTED_EDGE ( 'NONE', *, *, #38321, .T. ) ;
#39477=CARTESIAN_POINT ( 'NONE',  ( 0.9756354156337461170, -37.22481466014910723, 21.34128958497367279 ) ) ;
#39485=EDGE_CURVE ( 'NONE', #29768, #33332, #32391, .T. ) ;
#39486=CARTESIAN_POINT ( 'NONE',  ( 0.7057020205115056566, 23.21851350879818554, 41.89806668505389098 ) ) ;
#39487=VERTEX_POINT ( 'NONE', #28605 ) ;
#39489=EDGE_CURVE ( 'NONE', #27511, #33696, #21179, .T. ) ;
#39491=ORIENTED_EDGE ( 'NONE', *, *, #58541, .F. ) ;
#39503=ORIENTED_EDGE ( 'NONE', *, *, #15430, .T. ) ;
#39511=CARTESIAN_POINT ( 'NONE',  ( 3.270143674763207553, 6.605065939546987508, -11.98875605389972421 ) ) ;
#39515=B_SPLINE_CURVE_WITH_KNOTS ( 'NONE', 3,
 ( #26855, #3333, #25932, #26542, #22161, #30936 ),
 .UNSPECIFIED., .F., .F.,
 ( 4, 2, 4 ),
 ( 3.476216610979977084E-18, 0.0002291966416970788345, 0.0004583932833941541996 ),
 .UNSPECIFIED. ) ;
#39521=ORIENTED_EDGE ( 'NONE', *, *, #1552, .F. ) ;
#39529=CARTESIAN_POINT ( 'NONE',  ( 2.281351352603296245, 1.314116150904124369, -47.95523304704244794 ) ) ;
#39534=CARTESIAN_POINT ( 'NONE',  ( 4.956653778116994147, 32.11725092155092653, -35.79382859084083179 ) ) ;
#39535=CARTESIAN_POINT ( 'NONE',  ( -16.69190930225257929, -7.824346355838889266, -1.669031402509471240 ) ) ;
#39540=CARTESIAN_POINT ( 'NONE',  ( 0.7056555295713315967, 44.57023068418428835, 17.55111680842054511 ) ) ;
#39544=ORIENTED_EDGE ( 'NONE', *, *, #35510, .F. ) ;
#39556=CARTESIAN_POINT ( 'NONE',  ( 5.959828726073459926, 16.28130559351264495, -12.49879082830551269 ) ) ;
#39559=FACE_OUTER_BOUND ( 'NONE', #38194, .T. ) ;
#39564=VERTEX_POINT ( 'NONE', #22232 ) ;
#39566=CARTESIAN_POINT ( 'NONE',  ( 4.967162193818130511, -18.65818244221228284, -38.83676580803786749 ) ) ;
#39570=( BOUNDED_SURFACE ( )  B_SPLINE_SURFACE ( 3, 1, ( 
 ( #14345, #28116 ),
 ( #33764, #19052 ),
 ( #57838, #47857 ),
 ( #42546, #9007 ) ),
 .UNSPECIFIED., .F., .F., .F. ) 
 B_SPLINE_SURFACE_WITH_KNOTS ( ( 4, 4 ),
 ( 2, 2 ),
 ( 0.000000000000000000, 1.000000000000000000 ),
 ( 0.000000000000000000, 1.000000000000000000 ),
 .UNSPECIFIED. ) 
 GEOMETRIC_REPRESENTATION_ITEM ( )  RATIONAL_B_SPLINE_SURFACE ( (
 ( 1.000000000000000000, 1.000000000000000000),
 ( 0.7269869731126817891, 0.9931720237060910339),
 ( 0.7269869731126817891, 0.9931720237060910339),
 ( 1.000000000000000000, 1.000000000000000000) ) ) 
 REPRESENTATION_ITEM ( '' )  SURFACE ( )  );
#39571=CARTESIAN_POINT ( 'NONE',  ( 3.270143674763207553, 11.71453292426878967, 7.080034332678304843 ) ) ;
#39597=VECTOR ( 'NONE', #5634, 1000.000000000000114 ) ;
#39598=CARTESIAN_POINT ( 'NONE',  ( 0.9722240750034584211, -33.68410530487889076, 26.58024222649031643 ) ) ;
#39601=CARTESIAN_POINT ( 'NONE',  ( 2.624215991343620935, 47.39206852872467834, -7.662883702704190725 ) ) ;
#39602=CARTESIAN_POINT ( 'NONE',  ( 1.154321713695928064, 37.57248787340968477, -20.73950268329786439 ) ) ;
#39608=CARTESIAN_POINT ( 'NONE',  ( 0.7057020205115022149, -28.48867101281799563, -38.50899875908083203 ) ) ;
#39612=CARTESIAN_POINT ( 'NONE',  ( 0.5839879327111930918, -41.43370681949794943, 24.02664985973689582 ) ) ;
#39613=CARTESIAN_POINT ( 'NONE',  ( 5.960221823109900008, -20.35070456576733022, -2.673723662181264782 ) ) ;
#39614=LINE ( 'NONE', #5434, #41905 ) ;
#39615=CARTESIAN_POINT ( 'NONE',  ( 4.967162193818130511, -28.07411493385318124, 32.68434214048159703 ) ) ;
#39624=ORIENTED_EDGE ( 'NONE', *, *, #56900, .F. ) ;
#39628=B_SPLINE_CURVE_WITH_KNOTS ( 'NONE', 3,
 ( #37976, #4389, #13849, #32953, #37339, #61410, #5326, #635, #28845, #47966, #24143, #24455, #8816, #43593, #56723, #9121 ),
 .UNSPECIFIED., .F., .F.,
 ( 4, 3, 3, 3, 3, 4 ),
 ( 9.813676791237319219E-18, 0.0002724568934985570649, 0.0004086836638483829116, 0.0005449104342063630429, 0.0008173270854453619028, 0.001089761613562694647 ),
 .UNSPECIFIED. ) ;
#39633=EDGE_CURVE ( 'NONE', #46967, #47555, #10046, .T. ) ;
#39634=CARTESIAN_POINT ( 'NONE',  ( 4.956653778116987041, -47.94889704119048446, -3.690426056930470988 ) ) ;
#39641=B_SPLINE_CURVE_WITH_KNOTS ( 'NONE', 3,
 ( #8278, #56206, #12708, #27399, #23028, #13022 ),
 .UNSPECIFIED., .F., .F.,
 ( 4, 2, 4 ),
 ( 3.471140604459641645E-18, 0.0002291966416970775606, 0.0004583932833941516518 ),
 .UNSPECIFIED. ) ;
#39644=( BOUNDED_SURFACE ( )  B_SPLINE_SURFACE ( 3, 1, ( 
 ( #3355, #50070 ),
 ( #55365, #2747 ),
 ( #36606, #12187 ),
 ( #51286, #21566 ) ),
 .UNSPECIFIED., .F., .F., .F. ) 
 B_SPLINE_SURFACE_WITH_KNOTS ( ( 4, 4 ),
 ( 2, 2 ),
 ( 0.000000000000000000, 1.000000000000000000 ),
 ( 0.000000000000000000, 1.000000000000000000 ),
 .UNSPECIFIED. ) 
 GEOMETRIC_REPRESENTATION_ITEM ( )  RATIONAL_B_SPLINE_SURFACE ( (
 ( 1.000000000000000000, 1.000000000000000000),
 ( 0.9732289882329797637, 0.9999525324661233672),
 ( 0.9732289882329797637, 0.9999525324661233672),
 ( 1.000000000000000000, 1.000000000000000000) ) ) 
 REPRESENTATION_ITEM ( '' )  SURFACE ( )  );
#39647=AXIS2_PLACEMENT_3D ( 'NONE', #9003, #60367, #36607 ) ;
#39653=CARTESIAN_POINT ( 'NONE',  ( 5.965394784446460541, 14.52385693119002852, -14.50338846149118233 ) ) ;
#39663=CARTESIAN_POINT ( 'NONE',  ( 0.5807400328401637335, 46.40483864045162221, -11.87003418057193826 ) ) ;
#39666=DIRECTION ( 'NONE',  ( -1.000000000000000000, -0.000000000000000000, -0.000000000000000000 ) ) ;
#39668=ORIENTED_EDGE ( 'NONE', *, *, #21903, .T. ) ;
#39669=LINE ( 'NONE', #34643, #5860 ) ;
#39671=CARTESIAN_POINT ( 'NONE',  ( 4.303969348037246512, 47.93217632892353919, -4.133486515472823974 ) ) ;
#39689=CARTESIAN_POINT ( 'NONE',  ( 0.8557997880470697982, -11.51622788066490166, 46.50333260518556244 ) ) ;
#39696=LINE ( 'NONE', #58746, #48705 ) ;
#39699=CARTESIAN_POINT ( 'NONE',  ( 4.960156602257177028, 20.07163247083200019, -41.85906677498932993 ) ) ;
#39703=CARTESIAN_POINT ( 'NONE',  ( 0.5809828226811560858, -11.86925843957200222, 46.40184912890835278 ) ) ;
#39708=CARTESIAN_POINT ( 'NONE',  ( 0.5809828226811617480, 24.41822904836982389, -41.20389530892281726 ) ) ;
#39710=ORIENTED_EDGE ( 'NONE', *, *, #19382, .T. ) ;
#39711=ORIENTED_EDGE ( 'NONE', *, *, #12320, .F. ) ;
#39712=CARTESIAN_POINT ( 'NONE',  ( 4.963659409799330291, 33.33129552235126880, -29.86601237216371985 ) ) ;
#39719=EDGE_CURVE ( 'NONE', #9930, #57761, #48197, .T. ) ;
#39720=CARTESIAN_POINT ( 'NONE',  ( 5.960721111146673579, -20.52557019979492026, -0.006321279846748652925 ) ) ;
#39732=CARTESIAN_POINT ( 'NONE',  ( 0.5834872094924170582, 41.59216540884697366, -23.75111410077667529 ) ) ;
#39741=CARTESIAN_POINT ( 'NONE',  ( 0.5807400328401637335, 12.92266817606080487, -46.12278621143483548 ) ) ;
#39743=CARTESIAN_POINT ( 'NONE',  ( 2.281351352603276261, -37.24546109640797908, -30.23585463601414602 ) ) ;
#39745=CIRCLE ( 'NONE', #48700, 48.09070567114147110 ) ;
#39746=( BOUNDED_SURFACE ( )  B_SPLINE_SURFACE ( 3, 1, ( 
 ( #18716, #14030 ),
 ( #52203, #37848 ),
 ( #33131, #19961 ),
 ( #30248, #57821 ) ),
 .UNSPECIFIED., .F., .F., .F. ) 
 B_SPLINE_SURFACE_WITH_KNOTS ( ( 4, 4 ),
 ( 2, 2 ),
 ( 0.000000000000000000, 1.000000000000000000 ),
 ( 0.000000000000000000, 1.000000000000000000 ),
 .UNSPECIFIED. ) 
 GEOMETRIC_REPRESENTATION_ITEM ( )  RATIONAL_B_SPLINE_SURFACE ( (
 ( 1.000000000000000000, 1.000000000000000000),
 ( 0.7269869731126817891, 0.9931720237060910339),
 ( 0.7269869731126817891, 0.9931720237060910339),
 ( 1.000000000000000000, 1.000000000000000000) ) ) 
 REPRESENTATION_ITEM ( '' )  SURFACE ( )  );
#39749=CARTESIAN_POINT ( 'NONE',  ( 3.660176727303399158, 22.37119938028490296, 42.51126973288290145 ) ) ;
#39757=CARTESIAN_POINT ( 'NONE',  ( 0.5827359174754822568, 17.99288944686893643, 44.38786494726102205 ) ) ;
#39758=CARTESIAN_POINT ( 'NONE',  ( 5.959547316686252039, 19.82530672674362293, -5.315863417546125014 ) ) ;
#39760=CARTESIAN_POINT ( 'NONE',  ( 0.9722240750034586432, -0.5819398758577144504, -42.90442369954358526 ) ) ;
#39765=ORIENTED_EDGE ( 'NONE', *, *, #10617, .F. ) ;
#39772=EDGE_CURVE ( 'NONE', #3804, #995, #42139, .T. ) ;
#39780=DIRECTION ( 'NONE',  ( 0.000000000000000000, 0.000000000000000000, -1.000000000000000000 ) ) ;
#39788=B_SPLINE_CURVE_WITH_KNOTS ( 'NONE', 3,
 ( #11108, #44034, #44330, #53983 ),
 .UNSPECIFIED., .F., .F.,
 ( 4, 4 ),
 ( 3.127317220692750759E-18, 0.004050076154992999014 ),
 .UNSPECIFIED. ) ;
#39790=FACE_OUTER_BOUND ( 'NONE', #32026, .T. ) ;
#39791=B_SPLINE_CURVE_WITH_KNOTS ( 'NONE', 3,
 ( #32599, #32289, #51370, #51685 ),
 .UNSPECIFIED., .F., .F.,
 ( 4, 4 ),
 ( 1.084202172485504434E-19, 0.004444878191957680851 ),
 .UNSPECIFIED. ) ;
#39795=EDGE_CURVE ( 'NONE', #23158, #47724, #44146, .T. ) ;
#39797=CARTESIAN_POINT ( 'NONE',  ( 0.9757402383260940226, -26.05362288587344821, -34.09320464257837102 ) ) ;
#39804=DIRECTION ( 'NONE',  ( 0.07836865515943411409, -0.7956898808744553575, 0.6006129930017304330 ) ) ;
#39810=ORIENTED_EDGE ( 'NONE', *, *, #36019, .T. ) ;
#39811=VERTEX_POINT ( 'NONE', #34111 ) ;
#39818=CARTESIAN_POINT ( 'NONE',  ( 4.956653778116475451, 47.27023054223744225, 8.845409907520236814 ) ) ;
#39835=ORIENTED_EDGE ( 'NONE', *, *, #56096, .F. ) ;
#39836=CARTESIAN_POINT ( 'NONE',  ( 0.9754402186311939005, 33.92707563620680133, -26.26956909363283543 ) ) ;
#39837=CARTESIAN_POINT ( 'NONE',  ( 3.660087539127335976, 40.62968541507479614, -25.63019641081286082 ) ) ;
#39842=CARTESIAN_POINT ( 'NONE',  ( -18.65399042163502941, -12.34045889288082343, 1.991456727128138926 ) ) ;
#39856=EDGE_CURVE ( 'NONE', #21001, #2809, #18262, .T. ) ;
#39857=CARTESIAN_POINT ( 'NONE',  ( -16.91999570892151539, -7.790225163110376272, 1.821671769791115558 ) ) ;
#39862=CARTESIAN_POINT ( 'NONE',  ( 0.5832367798473389042, 33.67436043247259647, 34.05962365606829678 ) ) ;
#39881=ORIENTED_EDGE ( 'NONE', *, *, #22081, .F. ) ;
#39882=CARTESIAN_POINT ( 'NONE',  ( 3.783278058412226752, -41.98530666033908432, -9.462251542474252375 ) ) ;
#39885=CARTESIAN_POINT ( 'NONE',  ( 0.9730545539215883499, 5.099196237955498923, -42.60426903087348194 ) ) ;
#39889=DIRECTION ( 'NONE',  ( 0.07439287786467665975, 0.9262902123089796769, -0.3693942911085615899 ) ) ;
#39891=ORIENTED_EDGE ( 'NONE', *, *, #61049, .T. ) ;
#39898=ORIENTED_EDGE ( 'NONE', *, *, #31728, .F. ) ;
#39905=CARTESIAN_POINT ( 'NONE',  ( 4.967162193818129623, -40.65506779172174845, 14.26841313271267886 ) ) ;
#39909=VERTEX_POINT ( 'NONE', #30608 ) ;
#39912=CARTESIAN_POINT ( 'NONE',  ( 0.9740398440564319582, -16.03656236596777873, 39.79907313245126232 ) ) ;
#39920=CARTESIAN_POINT ( 'NONE',  ( 0.5807400328401574052, -44.45848844984429604, -17.82553128098455630 ) ) ;
#39932=CARTESIAN_POINT ( 'NONE',  ( 0.8551540677456715978, 47.37911285756620572, 7.157691013574528860 ) ) ;
#39934=CARTESIAN_POINT ( 'NONE',  ( 0.9749527285493297946, -26.34702925571524545, 33.86694354778348526 ) ) ;
#39941=ORIENTED_EDGE ( 'NONE', *, *, #28205, .F. ) ;
#39947=VERTEX_POINT ( 'NONE', #21223 ) ;
#39954=CARTESIAN_POINT ( 'NONE',  ( 3.407937589446174087, -3.099921468254910106, -13.34359005742692617 ) ) ;
#39963=ADVANCED_FACE ( 'NONE', ( #16528 ), #8067, .F. ) ;
#39973=CARTESIAN_POINT ( 'NONE',  ( 0.5836750258453368145, 44.31929073742215763, -18.16108240858296696 ) ) ;
#39981=ORIENTED_EDGE ( 'NONE', *, *, #9824, .F. ) ;
#39985=CARTESIAN_POINT ( 'NONE',  ( 0.7057020205114996614, 33.27137945725718282, 34.46103118762803064 ) ) ;
#39993=CIRCLE ( 'NONE', #32958, 43.08621763946400307 ) ;
#39998=EDGE_CURVE ( 'NONE', #51084, #45511, #15273, .T. ) ;
#39999=FACE_BOUND ( 'NONE', #37643, .T. ) ;
#40002=EDGE_CURVE ( 'NONE', #38122, #20520, #244, .T. ) ;
#40005=CARTESIAN_POINT ( 'NONE',  ( 0.5800708119828332787, -13.00144522946626324, -46.09746484493492602 ) ) ;
#40007=CARTESIAN_POINT ( 'NONE',  ( 5.959828726073459926, 19.82504517499705443, 5.316791119501156793 ) ) ;
#40013=CARTESIAN_POINT ( 'NONE',  ( 3.270143674763207553, 3.806843787666105428, -13.14781761974165164 ) ) ;
#40016=ORIENTED_EDGE ( 'NONE', *, *, #19477, .F. ) ;
#40024=ORIENTED_EDGE ( 'NONE', *, *, #31728, .T. ) ;
#40026=CARTESIAN_POINT ( 'NONE',  ( 0.5809828226811548646, -47.41188724015884048, 6.791453954330148868 ) ) ;
#40028=( BOUNDED_SURFACE ( )  B_SPLINE_SURFACE ( 3, 1, ( 
 ( #57588, #20047 ),
 ( #34449, #53522 ),
 ( #38855, #49148 ),
 ( #29114, #15036 ) ),
 .UNSPECIFIED., .F., .F., .F. ) 
 B_SPLINE_SURFACE_WITH_KNOTS ( ( 4, 4 ),
 ( 2, 2 ),
 ( 0.000000000000000000, 1.000000000000000000 ),
 ( 0.000000000000000000, 1.000000000000000000 ),
 .UNSPECIFIED. ) 
 GEOMETRIC_REPRESENTATION_ITEM ( )  RATIONAL_B_SPLINE_SURFACE ( (
 ( 1.000000000000000000, 1.000000000000000000),
 ( 0.9953390228620291325, 0.8624445117761032620),
 ( 0.9953390228620291325, 0.8624445117761032620),
 ( 1.000000000000000000, 1.000000000000000000) ) ) 
 REPRESENTATION_ITEM ( '' )  SURFACE ( )  );
#40029=EDGE_LOOP ( 'NONE', ( #45649, #9392, #58201, #3528 ) ) ;
#40035=B_SPLINE_CURVE_WITH_KNOTS ( 'NONE', 3,
 ( #55755, #17881, #13184, #42010, #17261, #51675, #3744, #18185, #27571, #32283, #13488, #61072, #50452, #40786, #50751, #8447 ),
 .UNSPECIFIED., .F., .F.,
 ( 4, 3, 3, 3, 3, 4 ),
 ( 1.127622383284612036E-17, 0.0002724568934985560891, 0.0004086836638483819901, 0.0005449104342063619587, 0.0008173270854453694922, 0.001089761613562688575 ),
 .UNSPECIFIED. ) ;
#40042=CARTESIAN_POINT ( 'NONE',  ( 0.9752132459055868896, 41.38545930839060816, -11.33038172416108935 ) ) ;
#40046=CARTESIAN_POINT ( 'NONE',  ( 5.981074661064941900, 19.82752479807527379, -5.303881226583471609 ) ) ;
#40047=ORIENTED_EDGE ( 'NONE', *, *, #41124, .F. ) ;
#40050=CARTESIAN_POINT ( 'NONE',  ( 0.5819845079324655890, 41.25022834067384281, -24.34013310064351998 ) ) ;
#40059=ORIENTED_EDGE ( 'NONE', *, *, #21148, .T. ) ;
#40060=CARTESIAN_POINT ( 'NONE',  ( 5.959828726073459926, -5.308046411395388020, 19.82738831247204203 ) ) ;
#40062=ORIENTED_EDGE ( 'NONE', *, *, #31857, .F. ) ;
#40069=CARTESIAN_POINT ( 'NONE',  ( 0.5832367798473389042, -6.521664418777500138, 47.44985149964048077 ) ) ;
#40073=CARTESIAN_POINT ( 'NONE',  ( 0.5819845079324649229, 18.74766465427224915, 44.07435181061346441 ) ) ;
#40077=LINE ( 'NONE', #42150, #31574 ) ;
#40079=EDGE_LOOP ( 'NONE', ( #40411, #60133, #38960, #23378 ) ) ;
#40093=CARTESIAN_POINT ( 'NONE',  ( 0.5800708119828329457, -5.628966929618073323, 47.56394195701285810 ) ) ;
#40094=CARTESIAN_POINT ( 'NONE',  ( 5.960221823109900008, -20.52559243573973546, 0.005450390361653345561 ) ) ;
#40102=CARTESIAN_POINT ( 'NONE',  ( 4.967162193818130511, -42.96271701169384016, -3.259922920618186115 ) ) ;
#40107=AXIS2_PLACEMENT_3D ( 'NONE', #49562, #35808, #17007 ) ;
#40116=ORIENTED_EDGE ( 'NONE', *, *, #11455, .F. ) ;
#40128=( BOUNDED_SURFACE ( )  B_SPLINE_SURFACE ( 3, 1, ( 
 ( #54550, #6619 ),
 ( #53625, #25446 ),
 ( #26076, #11681 ),
 ( #6942, #54872 ) ),
 .UNSPECIFIED., .F., .F., .F. ) 
 B_SPLINE_SURFACE_WITH_KNOTS ( ( 4, 4 ),
 ( 2, 2 ),
 ( 0.000000000000000000, 1.000000000000000000 ),
 ( 0.000000000000000000, 1.000000000000000000 ),
 .UNSPECIFIED. ) 
 GEOMETRIC_REPRESENTATION_ITEM ( )  RATIONAL_B_SPLINE_SURFACE ( (
 ( 1.000000000000000000, 1.000000000000000000),
 ( 0.9732289882329797637, 0.9999525324661233672),
 ( 0.9732289882329797637, 0.9999525324661233672),
 ( 1.000000000000000000, 1.000000000000000000) ) ) 
 REPRESENTATION_ITEM ( '' )  SURFACE ( )  );
#40134=ORIENTED_EDGE ( 'NONE', *, *, #52235, .T. ) ;
#40140=CARTESIAN_POINT ( 'NONE',  ( 2.526464513654346433, -20.43088802552588490, 37.81242626108687688 ) ) ;
#40148=EDGE_LOOP ( 'NONE', ( #43258, #4364, #55473, #34949 ) ) ;
#40151=CARTESIAN_POINT ( 'NONE',  ( 5.860006189529234355, -43.25137511473265306, 21.34829429597452588 ) ) ;
#40152=VERTEX_POINT ( 'NONE', #5784 ) ;
#40155=CARTESIAN_POINT ( 'NONE',  ( 3.270143674763207553, -1.514386915940690415, 13.60381564321233583 ) ) ;
#40160=ORIENTED_EDGE ( 'NONE', *, *, #36518, .F. ) ;
#40167=CARTESIAN_POINT ( 'NONE',  ( 0.9741495583595179975, 37.35596046161894890, -21.11077839432095971 ) ) ;
#40172=EDGE_CURVE ( 'NONE', #40335, #47955, #43665, .T. ) ;
#40173=CARTESIAN_POINT ( 'NONE',  ( 0.5837374860065636106, 33.99581326751435029, 33.73893264285563021 ) ) ;
#40177=CARTESIAN_POINT ( 'NONE',  ( 3.270143674763207553, -1.514386915940500788, -13.60381564321235892 ) ) ;
#40180=CARTESIAN_POINT ( 'NONE',  ( 5.981074661064941900, 5.320466518160661629, 19.82308078259092810 ) ) ;
#40181=CARTESIAN_POINT ( 'NONE',  ( 4.956653778116966613, 0.000000000000000000, 0.000000000000000000 ) ) ;
#40182=B_SPLINE_CURVE_WITH_KNOTS ( 'NONE', 3,
 ( #56812, #42442, #3257, #47434 ),
 .UNSPECIFIED., .F., .F.,
 ( 4, 4 ),
 ( 1.551583845779545699E-17, 0.005004741218457433617 ),
 .UNSPECIFIED. ) ;
#40186=DIRECTION ( 'NONE',  ( -1.000000000000000000, -0.000000000000000000, -0.000000000000000000 ) ) ;
#40200=( BOUNDED_SURFACE ( )  B_SPLINE_SURFACE ( 3, 1, ( 
 ( #43934, #58276 ),
 ( #11017, #29794 ),
 ( #53579, #1271 ),
 ( #1895, #25098 ) ),
 .UNSPECIFIED., .F., .F., .F. ) 
 B_SPLINE_SURFACE_WITH_KNOTS ( ( 4, 4 ),
 ( 2, 2 ),
 ( 0.000000000000000000, 1.000000000000000000 ),
 ( 0.000000000000000000, 1.000000000000000000 ),
 .UNSPECIFIED. ) 
 GEOMETRIC_REPRESENTATION_ITEM ( )  RATIONAL_B_SPLINE_SURFACE ( (
 ( 1.000000000000000000, 1.000000000000000000),
 ( 0.9953390228620291325, 0.8624445117761032620),
 ( 0.9953390228620291325, 0.8624445117761032620),
 ( 1.000000000000000000, 1.000000000000000000) ) ) 
 REPRESENTATION_ITEM ( '' )  SURFACE ( )  );
#40202=EDGE_CURVE ( 'NONE', #39143, #30590, #133, .T. ) ;
#40203=ORIENTED_EDGE ( 'NONE', *, *, #33403, .T. ) ;
#40209=CARTESIAN_POINT ( 'NONE',  ( 4.956653778116966613, 0.000000000000000000, 0.000000000000000000 ) ) ;
#40212=B_SPLINE_CURVE_WITH_KNOTS ( 'NONE', 3,
 ( #22334, #49592, #35835, #44933 ),
 .UNSPECIFIED., .F., .F.,
 ( 4, 4 ),
 ( 9.697399036122160616E-19, 0.004050076154993000749 ),
 .UNSPECIFIED. ) ;
#40213=ORIENTED_EDGE ( 'NONE', *, *, #58612, .F. ) ;
#40214=CARTESIAN_POINT ( 'NONE',  ( 0.5800708057587401489, -37.61306623599821108, -29.65250565429482776 ) ) ;
#40219=FACE_OUTER_BOUND ( 'NONE', #59842, .T. ) ;
#40229=VECTOR ( 'NONE', #15302, 1000.000000000000114 ) ;
#40231=B_SPLINE_CURVE_WITH_KNOTS ( 'NONE', 3,
 ( #51924, #9013, #28120, #52851 ),
 .UNSPECIFIED., .F., .F.,
 ( 4, 4 ),
 ( 2.602085213965210642E-18, 0.004050076154993001616 ),
 .UNSPECIFIED. ) ;
#40233=CARTESIAN_POINT ( 'NONE',  ( 4.967162193818130511, -13.42934394584192148, 40.93989340068605998 ) ) ;
#40235=CARTESIAN_POINT ( 'NONE',  ( 3.270143674763207553, -12.74832469035448668, -4.983712007628368745 ) ) ;
#40236=FACE_OUTER_BOUND ( 'NONE', #32063, .T. ) ;
#40240=B_SPLINE_CURVE_WITH_KNOTS ( 'NONE', 3,
 ( #24141, #29152, #19457, #38576, #52329, #23841 ),
 .UNSPECIFIED., .F., .F.,
 ( 4, 2, 4 ),
 ( 9.745765416140531346E-18, 0.0002291978881530162956, 0.0004583957763060228334 ),
 .UNSPECIFIED. ) ;
#40245=EDGE_CURVE ( 'NONE', #49095, #14998, #6115, .T. ) ;
#40259=ORIENTED_EDGE ( 'NONE', *, *, #43455, .T. ) ;
#40260=EDGE_LOOP ( 'NONE', ( #33508, #54159, #56765, #51724 ) ) ;
#40261=DIRECTION ( 'NONE',  ( 0.07439287786467665975, 0.2453289374370069276, 0.9665813013808205456 ) ) ;
#40265=EDGE_CURVE ( 'NONE', #45486, #43576, #10711, .T. ) ;
#40267=VECTOR ( 'NONE', #20342, 1000.000000000000114 ) ;
#40283=CARTESIAN_POINT ( 'NONE',  ( 0.5839879327111926477, 12.30864801674776565, -46.28746210677699224 ) ) ;
#40284=ORIENTED_EDGE ( 'NONE', *, *, #50773, .T. ) ;
#40287=CARTESIAN_POINT ( 'NONE',  ( 0.9740398440564311811, -21.81228698783116116, -36.95080095316296109 ) ) ;
#40288=ORIENTED_EDGE ( 'NONE', *, *, #32900, .T. ) ;
#40303=CARTESIAN_POINT ( 'NONE',  ( 0.9757892942422827787, -5.651566539685542345, -42.53466646637867399 ) ) ;
#40308=CARTESIAN_POINT ( 'NONE',  ( 3.783198216974387851, 42.41041696600780142, 7.325057189010560244 ) ) ;
#40324=FACE_OUTER_BOUND ( 'NONE', #40260, .T. ) ;
#40333=CARTESIAN_POINT ( 'NONE',  ( 0.9730545539215883499, -41.57420493492377744, -10.61654491617608009 ) ) ;
#40335=VERTEX_POINT ( 'NONE', #17690 ) ;
#40336=CARTESIAN_POINT ( 'NONE',  ( 5.960221823109900008, -0.005450390361581681532, -20.52559243573973546 ) ) ;
#40351=VECTOR ( 'NONE', #42185, 1000.000000000000114 ) ;
#40353=CARTESIAN_POINT ( 'NONE',  ( 0.8557997880470690211, -33.22501220301925429, 34.51495345639537504 ) ) ;
#40358=CARTESIAN_POINT ( 'NONE',  ( 0.5839879882012706247, -18.32896541547101421, 44.25011577017261288 ) ) ;
#40359=EDGE_LOOP ( 'NONE', ( #2837, #46596, #26895, #43669 ) ) ;
#40362=CARTESIAN_POINT ( 'NONE',  ( 4.956653778116975495, -8.845409907521238679, 47.27023054223749909 ) ) ;
#40364=CARTESIAN_POINT ( 'NONE',  ( 0.5832366564991519065, 6.521686574606105680, 47.44984844891988018 ) ) ;
#40365=EDGE_CURVE ( 'NONE', #25700, #31789, #20359, .T. ) ;
#40369=( BOUNDED_SURFACE ( )  B_SPLINE_SURFACE ( 3, 1, ( 
 ( #39758, #2419 ),
 ( #21544, #40681 ),
 ( #1188, #35977 ),
 ( #55041, #48816 ) ),
 .UNSPECIFIED., .F., .F., .F. ) 
 B_SPLINE_SURFACE_WITH_KNOTS ( ( 4, 4 ),
 ( 2, 2 ),
 ( 0.000000000000000000, 1.000000000000000000 ),
 ( 0.000000000000000000, 1.000000000000000000 ),
 .UNSPECIFIED. ) 
 GEOMETRIC_REPRESENTATION_ITEM ( )  RATIONAL_B_SPLINE_SURFACE ( (
 ( 1.000000000000000000, 1.000000000000000000),
 ( 0.9953390228620291325, 0.8624445117761032620),
 ( 0.9953390228620291325, 0.8624445117761032620),
 ( 1.000000000000000000, 1.000000000000000000) ) ) 
 REPRESENTATION_ITEM ( '' )  SURFACE ( )  );
#40371=CARTESIAN_POINT ( 'NONE',  ( 2.281351352603290028, 17.13758816714750211, 44.80774876812563434 ) ) ;
#40374=CARTESIAN_POINT ( 'NONE',  ( 1.088908134280557105, -0.7803765577538801512, -42.90644581410506930 ) ) ;
#40375=CARTESIAN_POINT ( 'NONE',  ( 4.303969348037258058, 35.51084504003198106, 32.45857549159314459 ) ) ;
#40378=CARTESIAN_POINT ( 'NONE',  ( 0.5809828226811617480, -23.47450554821680413, -41.74875432577673706 ) ) ;
#40385=CARTESIAN_POINT ( 'NONE',  ( 5.860006189529234355, 43.26650951066869766, 21.31760477694597711 ) ) ;
#40390=CARTESIAN_POINT ( 'NONE',  ( 0.9736507210033060744, -39.81239086052226384, 16.00326134587904292 ) ) ;
#40398=EDGE_CURVE ( 'NONE', #61473, #23542, #22382, .T. ) ;
#40403=CARTESIAN_POINT ( 'NONE',  ( 0.9741495583595175534, -25.80610403442885570, -34.28086552274318421 ) ) ;
#40405=CARTESIAN_POINT ( 'NONE',  ( 4.956653778116992370, 15.97476558431944937, -45.35992544608513555 ) ) ;
#40406=EDGE_LOOP ( 'NONE', ( #56312, #17066, #5391, #19223 ) ) ;
#40407=CARTESIAN_POINT ( 'NONE',  ( 4.956653778116975495, -31.29546495791875316, 36.51451553856407628 ) ) ;
#40408=CARTESIAN_POINT ( 'NONE',  ( 0.9740398440564311811, 16.03656236596804163, -39.79907313245115574 ) ) ;
#40411=ORIENTED_EDGE ( 'NONE', *, *, #19531, .F. ) ;
#40415=CARTESIAN_POINT ( 'NONE',  ( 4.967162193818130511, -32.68434214048189546, 28.07411493385282242 ) ) ;
#40417=ORIENTED_EDGE ( 'NONE', *, *, #61226, .T. ) ;
#40419=EDGE_CURVE ( 'NONE', #52535, #1876, #9938, .T. ) ;
#40423=ORIENTED_EDGE ( 'NONE', *, *, #58497, .F. ) ;
#40425=ORIENTED_EDGE ( 'NONE', *, *, #40491, .T. ) ;
#40441=AXIS2_PLACEMENT_3D ( 'NONE', #49213, #34513, #20110 ) ;
#40458=B_SPLINE_CURVE_WITH_KNOTS ( 'NONE', 3,
 ( #32854, #53681, #10812, #33154, #52229, #29899 ),
 .UNSPECIFIED., .F., .F.,
 ( 4, 2, 4 ),
 ( 1.015220885719448790E-17, 0.0002291978881530158890, 0.0004583957763060215866 ),
 .UNSPECIFIED. ) ;
#40459=CARTESIAN_POINT ( 'NONE',  ( 5.974727161628367256, -7.868887636447487566, -18.95664195401514007 ) ) ;
#40460=ORIENTED_EDGE ( 'NONE', *, *, #48464, .F. ) ;
#40464=CARTESIAN_POINT ( 'NONE',  ( 5.959828726073459926, 20.35060134307034829, -2.674641840415962868 ) ) ;
#40465=CARTESIAN_POINT ( 'NONE',  ( 4.956653778116975495, 15.97476558431885252, 45.35992544608534160 ) ) ;
#40468=CARTESIAN_POINT ( 'NONE',  ( 5.959828726073459926, -19.82504517499708996, -5.316791119501019125 ) ) ;
#40469=DIRECTION ( 'NONE',  ( 0.000000000000000000, 0.000000000000000000, 1.000000000000000000 ) ) ;
#40471=EDGE_CURVE ( 'NONE', #47638, #46904, #43560, .T. ) ;
#40476=CARTESIAN_POINT ( 'NONE',  ( 0.5834872094924179464, 46.20467604622299262, 12.61552836343307327 ) ) ;
#40480=CARTESIAN_POINT ( 'NONE',  ( 1.088908134280555329, -4.826714665689156192, 42.64123480278976075 ) ) ;
#40491=EDGE_CURVE ( 'NONE', #47841, #27088, #32651, .T. ) ;
#40492=ORIENTED_EDGE ( 'NONE', *, *, #30542, .T. ) ;
#40495=EDGE_LOOP ( 'NONE', ( #42885, #35044, #28053, #22051 ) ) ;
#40502=B_SPLINE_CURVE_WITH_KNOTS ( 'NONE', 3,
 ( #12478, #31570, #36289, #22175, #45688, #41008, #50662, #3347, #60068, #17174, #55665, #7747, #41302, #60358, #17474, #4267, #9932, #56902, #24328 ),
 .UNSPECIFIED., .F., .F.,
 ( 4, 3, 3, 3, 3, 3, 4 ),
 ( 4.907736672678014827E-18, 0.0002724573126191874107, 0.0004086839781548697818, 0.0005449106435902069650, 0.0006811373090491784545, 0.0008459866663933876974, 0.001010840725717217919 ),
 .UNSPECIFIED. ) ;
#40508=ORIENTED_EDGE ( 'NONE', *, *, #61847, .F. ) ;
#40509=EDGE_CURVE ( 'NONE', #28286, #2384, #25558, .T. ) ;
#40521=ORIENTED_EDGE ( 'NONE', *, *, #7992, .F. ) ;
#40525=CARTESIAN_POINT ( 'NONE',  ( 0.9752570700956809668, -16.63323182627896202, 39.55341424149101925 ) ) ;
#40527=B_SPLINE_CURVE_WITH_KNOTS ( 'NONE', 3,
 ( #17605, #56107, #55799, #26686, #41129, #7245 ),
 .UNSPECIFIED., .F., .F.,
 ( 4, 2, 4 ),
 ( 1.520334456564901176E-16, 0.0002445252820015204908, 0.0004890505640028888681 ),
 .UNSPECIFIED. ) ;
#40528=DIRECTION ( 'NONE',  ( -0.07836865515943411409, -0.3887811538706065217, -0.9179910502197401456 ) ) ;
#40536=CARTESIAN_POINT ( 'NONE',  ( 0.8557997880470697982, 29.88293891557470516, 37.44587306708108088 ) ) ;
#40548=EDGE_CURVE ( 'NONE', #27319, #26757, #12669, .T. ) ;
#40550=VERTEX_POINT ( 'NONE', #40837 ) ;
#40557=ORIENTED_EDGE ( 'NONE', *, *, #17270, .F. ) ;
#40561=B_SPLINE_CURVE_WITH_KNOTS ( 'NONE', 3,
 ( #985, #53593, #57364, #43014, #53294, #15414, #38617, #352, #15109, #34525, #53, #19202, #58289, #43631, #19502, #33915 ),
 .UNSPECIFIED., .F., .F.,
 ( 4, 3, 3, 3, 3, 4 ),
 ( 1.250973872328959318E-17, 0.0002724568934985643833, 0.0004086836638483846464, 0.0005449104342063632598, 0.0008173270854453735038, 0.001089761613562689009 ),
 .UNSPECIFIED. ) ;
#40562=ORIENTED_EDGE ( 'NONE', *, *, #58886, .F. ) ;
#40563=EDGE_LOOP ( 'NONE', ( #29207, #1536, #22736, #49559, #24825, #7791, #13081, #18838, #48081, #22230, #40806, #53570, #2645, #11038, #18107, #18745, #24505, #21233, #16374, #38825, #46876, #52033, #31761, #35729, #52821, #6853, #40776, #22062, #24142, #12472, #9877, #41428, #48046, #23894, #61170, #19923, #39023, #32460, #36716, #48448, #57766, #36419, #54477, #57161, #7221, #52551, #60630, #26430, #6209, #52890, #50620, #20523, #21117, #18920, #48567, #2818, #37268, #53879, #6425, #47757, #41527, #60347, #60093, #10996, #43251, #29651, #57943, #10724, #8418, #5276, #43898, #31699, #7178, #61242, #48346, #28098, #49099, #11666, #12155, #48318, #53459, #53985, #28966, #60334, #26197, #50952, #29000, #40024, #56231, #52009, #617, #9107, #17455, #7547, #5139, #17014, #1707, #49856, #22728, #2141, #40134, #27514, #4821, #3240, #52078, #6695, #31746, #43900, #42177, #57923, #17223, #51562, #18924, #7538, #50909, #32485, #40842, #50129, #24384, #74, #58478, #174, #1979, #20441, #19083, #27842, #35630, #59238, #53273, #57477, #24784, #7157, #23431, #49681, #28617, #34147, #57244, #39668, #29081, #55631, #1612, #57034, #54496, #9678, #47106, #46655, #47903, #54306 ) ) ;
#40566=CARTESIAN_POINT ( 'NONE',  ( 0.5807400328401574052, 44.45848844984443105, 17.82553128098425077 ) ) ;
#40571=B_SPLINE_CURVE_WITH_KNOTS ( 'NONE', 3,
 ( #54577, #49587, #58985, #39297, #6643, #10466 ),
 .UNSPECIFIED., .F., .F.,
 ( 4, 2, 4 ),
 ( 1.084202172485504434E-19, 0.0002445244328975368061, 0.0004890488657950735037 ),
 .UNSPECIFIED. ) ;
#40573=EDGE_LOOP ( 'NONE', ( #19363, #55124, #56460, #37500 ) ) ;
#40589=ADVANCED_FACE ( 'NONE', ( #42367 ), #1168, .F. ) ;
#40590=CARTESIAN_POINT ( 'NONE',  ( 0.9752570700956793015, -21.25416333281073022, -37.27462300504097925 ) ) ;
#40592=CARTESIAN_POINT ( 'NONE',  ( 5.959547316686252039, -19.82530672674365846, 5.315863417545987346 ) ) ;
#40593=CARTESIAN_POINT ( 'NONE',  ( 0.5786265663353196143, -5.535668456753627176, -47.58023467411543095 ) ) ;
#40601=FACE_OUTER_BOUND ( 'NONE', #33314, .T. ) ;
#40604=CARTESIAN_POINT ( 'NONE',  ( 0.5839879882012674051, 46.26394433311401855, -12.39641777360473540 ) ) ;
#40605=CARTESIAN_POINT ( 'NONE',  ( 0.9757402383260934675, -5.516496958496793113, -42.55239275983117864 ) ) ;
#40608=CARTESIAN_POINT ( 'NONE',  ( 0.5839880159502344181, 37.97080096460581444, 29.19321933421507964 ) ) ;
#40609=CARTESIAN_POINT ( 'NONE',  ( 4.967162193818130511, 0.000000000000000000, 0.000000000000000000 ) ) ;
#40610=ORIENTED_EDGE ( 'NONE', *, *, #57972, .F. ) ;
#40611=CARTESIAN_POINT ( 'NONE',  ( -17.97369999999976642, -12.32233744059949210, -2.099999999999997424 ) ) ;
#40613=CARTESIAN_POINT ( 'NONE',  ( 0.5809828226811544205, 5.711058609466008740, -47.55412398569200150 ) ) ;
#40614=DIRECTION ( 'NONE',  ( -1.000000000000000000, -0.000000000000000000, -0.000000000000000000 ) ) ;
#40615=FACE_OUTER_BOUND ( 'NONE', #41289, .T. ) ;
#40616=SHAPE_DEFINITION_REPRESENTATION ( #18325, #16880 ) ;
#40618=EDGE_CURVE ( 'NONE', #21198, #41494, #51109, .T. ) ;
#40623=CARTESIAN_POINT ( 'NONE',  ( 5.860006189529234355, 9.426589201135499252, 47.30296539008827494 ) ) ;
#40624=VERTEX_POINT ( 'NONE', #51731 ) ;
#40626=CARTESIAN_POINT ( 'NONE',  ( 0.9722240750034575330, 42.46141201102052776, -6.177112354444691533 ) ) ;
#40630=CARTESIAN_POINT ( 'NONE',  ( 2.526552050251864134, 41.18423939305565540, 12.29062829843992688 ) ) ;
#40633=CARTESIAN_POINT ( 'NONE',  ( 5.958863334805807099, 5.311251202228577384, 19.82657410201445103 ) ) ;
#40641=CARTESIAN_POINT ( 'NONE',  ( 3.270143674763207553, -13.68510027222513159, -0.2742231296311014588 ) ) ;
#40651=ORIENTED_EDGE ( 'NONE', *, *, #33947, .T. ) ;
#40655=CARTESIAN_POINT ( 'NONE',  ( 0.6067099128993207469, -41.82996792600761893, -23.33192673707576859 ) ) ;
#40659=ORIENTED_EDGE ( 'NONE', *, *, #43745, .T. ) ;
#40662=ORIENTED_EDGE ( 'NONE', *, *, #6547, .F. ) ;
#40664=EDGE_CURVE ( 'NONE', #14433, #4518, #925, .T. ) ;
#40665=B_SPLINE_CURVE_WITH_KNOTS ( 'NONE', 3,
 ( #57485, #48129, #30235, #6399, #58417, #10525 ),
 .UNSPECIFIED., .F., .F.,
 ( 4, 2, 4 ),
 ( 3.476216610979977084E-18, 0.0002291966416970807048, 0.0004583932833941579401 ),
 .UNSPECIFIED. ) ;
#40667=CARTESIAN_POINT ( 'NONE',  ( 0.9722240741986376555, -36.86535088273189587, -21.95618662952224298 ) ) ;
#40675=AXIS2_PLACEMENT_3D ( 'NONE', #29233, #57405, #38060 ) ;
#40681=CARTESIAN_POINT ( 'NONE',  ( 0.5786265663353196143, -46.45062944555901652, 11.69877690266638481 ) ) ;
#40684=CARTESIAN_POINT ( 'NONE',  ( 0.8557997880470599172, -38.55640757422458620, 28.43566216844957140 ) ) ;
#40688=CARTESIAN_POINT ( 'NONE',  ( 5.981074661064941900, -2.670494474391857942, -20.35019299530687320 ) ) ;
#40689=CARTESIAN_POINT ( 'NONE',  ( 1.227938101723756947, 39.32113113558990847, -17.20315230597801914 ) ) ;
#40695=CARTESIAN_POINT ( 'NONE',  ( 0.8551540677456715978, 23.16399837394545713, 41.94570365541211743 ) ) ;
#40696=CARTESIAN_POINT ( 'NONE',  ( 4.956653778116975495, -20.77844580450591394, 43.37017594958047084 ) ) ;
#40701=CARTESIAN_POINT ( 'NONE',  ( 1.227938101723748288, -10.28900963485351205, -41.66816631169202623 ) ) ;
#40705=CARTESIAN_POINT ( 'NONE',  ( 5.965394784446458765, -10.27521535480974180, -17.76824826579351324 ) ) ;
#40722=ORIENTED_EDGE ( 'NONE', *, *, #6901, .F. ) ;
#40735=ORIENTED_EDGE ( 'NONE', *, *, #33837, .T. ) ;
#40742=( BOUNDED_SURFACE ( )  B_SPLINE_SURFACE ( 3, 1, ( 
 ( #36578, #21231 ),
 ( #11529, #12780 ),
 ( #8051, #27165 ),
 ( #41589, #6788 ) ),
 .UNSPECIFIED., .F., .F., .F. ) 
 B_SPLINE_SURFACE_WITH_KNOTS ( ( 4, 4 ),
 ( 2, 2 ),
 ( 0.000000000000000000, 1.000000000000000000 ),
 ( 0.000000000000000000, 1.000000000000000000 ),
 .UNSPECIFIED. ) 
 GEOMETRIC_REPRESENTATION_ITEM ( )  RATIONAL_B_SPLINE_SURFACE ( (
 ( 1.000000000000000000, 1.000000000000000000),
 ( 0.7269869731126821222, 0.9931720237060910339),
 ( 0.7269869731126821222, 0.9931720237060910339),
 ( 1.000000000000000000, 1.000000000000000000) ) ) 
 REPRESENTATION_ITEM ( '' )  SURFACE ( )  );
#40744=CARTESIAN_POINT ( 'NONE',  ( 0.5839254288179552832, -37.94310411505126268, -29.22920395911552305 ) ) ;
#40750=DIRECTION ( 'NONE',  ( -0.000000000000000000, 0.000000000000000000, 1.000000000000000000 ) ) ;
#40753=CARTESIAN_POINT ( 'NONE',  ( 0.9752570700956798566, 10.88256294660712697, 41.50550328400871081 ) ) ;
#40765=CARTESIAN_POINT ( 'NONE',  ( -18.24996621385825790, -12.32468876802673741, 2.086337228483194917 ) ) ;
#40769=ORIENTED_EDGE ( 'NONE', *, *, #28775, .T. ) ;
#40772=CARTESIAN_POINT ( 'NONE',  ( 4.956653778116990594, -20.77844580450529577, -43.37017594958076927 ) ) ;
#40776=ORIENTED_EDGE ( 'NONE', *, *, #54219, .T. ) ;
#40777=CARTESIAN_POINT ( 'NONE',  ( 0.9749527285493307938, 21.70110358462093458, -37.01618455594552159 ) ) ;
#40786=CARTESIAN_POINT ( 'NONE',  ( 0.5827357941260201679, 5.891356987508307164, -47.53228940613938391 ) ) ;
#40787=CARTESIAN_POINT ( 'NONE',  ( 5.860006189529246790, 43.25137511473251095, 21.34829429597482076 ) ) ;
#40793=VERTEX_POINT ( 'NONE', #24782 ) ;
#40795=CARTESIAN_POINT ( 'NONE',  ( 0.5786265663353153954, 43.97352617418643206, -18.99608782657985628 ) ) ;
#40798=EDGE_CURVE ( 'NONE', #23520, #41282, #42013, .T. ) ;
#40799=CARTESIAN_POINT ( 'NONE',  ( 2.526464513654343769, -42.75268905308553258, -4.405490210168832910 ) ) ;
#40802=ORIENTED_EDGE ( 'NONE', *, *, #60921, .T. ) ;
#40803=CARTESIAN_POINT ( 'NONE',  ( 0.5809828226811617480, -33.48000389720591841, -34.25055090842189287 ) ) ;
#40806=ORIENTED_EDGE ( 'NONE', *, *, #12526, .T. ) ;
#40807=CARTESIAN_POINT ( 'NONE',  ( 5.958863334805807099, 20.35021240744034898, -2.677925489610427867 ) ) ;
#40812=CARTESIAN_POINT ( 'NONE',  ( 0.9749527285493301276, -5.883724875809405397, 42.50314808877159578 ) ) ;
#40814=FACE_OUTER_BOUND ( 'NONE', #9336, .T. ) ;
#40820=VERTEX_POINT ( 'NONE', #14167 ) ;
#40822=DIRECTION ( 'NONE',  ( 0.07439287786467665975, 0.7830499462674470612, 0.6174937095821784183 ) ) ;
#40830=EDGE_CURVE ( 'NONE', #49095, #44905, #16678, .T. ) ;
#40834=CARTESIAN_POINT ( 'NONE',  ( 0.5832367798473389042, -46.19266341874887871, -12.65931911325652415 ) ) ;
#40837=CARTESIAN_POINT ( 'NONE',  ( 4.967162193818130511, 40.93989340068628024, -13.42934394584121094 ) ) ;
#40838=CARTESIAN_POINT ( 'NONE',  ( 4.956653778116982600, -45.35992544608539845, 15.97476558431867844 ) ) ;
#40842=ORIENTED_EDGE ( 'NONE', *, *, #39998, .T. ) ;
#40846=CARTESIAN_POINT ( 'NONE',  ( 1.227938101723748288, -11.92353943227977986, 41.23019537246705823 ) ) ;
#40850=VECTOR ( 'NONE', #52267, 1000.000000000000114 ) ;
#40851=CARTESIAN_POINT ( 'NONE',  ( 0.7056555295713289322, 0.8411712675128016903, 47.89404551051138981 ) ) ;
#40862=CARTESIAN_POINT ( 'NONE',  ( 5.965394784446460541, -16.27505370423073217, -12.50653125159001533 ) ) ;
#40868=CARTESIAN_POINT ( 'NONE',  ( 1.088313998177379505, 6.373602917100794407, -42.43756598879020459 ) ) ;
#40870=EDGE_CURVE ( 'NONE', #23080, #58704, #6880, .T. ) ;
#40877=CARTESIAN_POINT ( 'NONE',  ( 0.5839879882012670720, 47.89596766821092189, -3.018602154015963534E-05 ) ) ;
#40890=CARTESIAN_POINT ( 'NONE',  ( 5.965394784446458765, 7.841344330024942799, -18.96850062921626900 ) ) ;
#40907=EDGE_CURVE ( 'NONE', #45266, #61276, #21011, .T. ) ;
#40912=CARTESIAN_POINT ( 'NONE',  ( 5.981074661064941900, 10.25489689131105919, 17.77917279944636064 ) ) ;
#40916=CARTESIAN_POINT ( 'NONE',  ( 5.960721111146673579, -19.82781442290501417, 5.306302591836237426 ) ) ;
#40918=EDGE_CURVE ( 'NONE', #12140, #54683, #11365, .T. ) ;
#40922=EDGE_CURVE ( 'NONE', #31508, #39205, #35753, .T. ) ;
#40929=CARTESIAN_POINT ( 'NONE',  ( 5.959547316686252039, -17.77392908783941294, 10.26589671991332331 ) ) ;
#40939=ORIENTED_EDGE ( 'NONE', *, *, #19968, .T. ) ;
#40941=CARTESIAN_POINT ( 'NONE',  ( 5.981074661064941900, 17.77917279944632512, -10.25489689131111959 ) ) ;
#40952=EDGE_CURVE ( 'NONE', #23031, #21932, #18030, .T. ) ;
#40953=ORIENTED_EDGE ( 'NONE', *, *, #19477, .T. ) ;
#40958=B_SPLINE_CURVE_WITH_KNOTS ( 'NONE', 3,
 ( #44000, #58037, #38978, #24233, #11076, #34267 ),
 .UNSPECIFIED., .F., .F.,
 ( 4, 2, 4 ),
 ( 1.515731698875470022E-16, 0.0002445252820015211956, 0.0004890505640028908196 ),
 .UNSPECIFIED. ) ;
#40964=LINE ( 'NONE', #55008, #2974 ) ;
#40980=EDGE_LOOP ( 'NONE', ( #50915, #24158, #29445, #37256 ) ) ;
#40984=CARTESIAN_POINT ( 'NONE',  ( 5.959828726073459926, -0.004526594003520726349, 20.52560994243598813 ) ) ;
#40989=ORIENTED_EDGE ( 'NONE', *, *, #37744, .T. ) ;
#40992=DIRECTION ( 'NONE',  ( -0.07836865515943411409, 0.9649662368512218480, 0.2503967164834498549 ) ) ;
#41000=ADVANCED_FACE ( 'NONE', ( #25587 ), #5548, .F. ) ;
#41008=CARTESIAN_POINT ( 'NONE',  ( 0.9756008150404608115, -30.24019526051566586, 30.44122083654206179 ) ) ;
#41012=CARTESIAN_POINT ( 'NONE',  ( 0.5807400328401574052, -6.791881299635267766, -47.41494605191449807 ) ) ;
#41025=CARTESIAN_POINT ( 'NONE',  ( 0.6067375320500707492, 37.56348932307263055, 29.71715680108748714 ) ) ;
#41027=EDGE_CURVE ( 'NONE', #41282, #12597, #8705, .T. ) ;
#41043=ORIENTED_EDGE ( 'NONE', *, *, #36554, .T. ) ;
#41044=CARTESIAN_POINT ( 'NONE',  ( 0.8551540677456715978, 28.44084013485173656, -38.56334384152401640 ) ) ;
#41046=FACE_OUTER_BOUND ( 'NONE', #41961, .T. ) ;
#41060=DIRECTION ( 'NONE',  ( -1.000000000000000000, -0.000000000000000000, -0.000000000000000000 ) ) ;
#41066=CARTESIAN_POINT ( 'NONE',  ( 0.9756950546413938330, 11.19893879603448106, 41.42124338356081381 ) ) ;
#41067=EDGE_CURVE ( 'NONE', #6072, #14441, #24789, .T. ) ;
#41071=ORIENTED_EDGE ( 'NONE', *, *, #20767, .T. ) ;
#41076=CARTESIAN_POINT ( 'NONE',  ( 0.8557997880470599172, -44.60232077416698360, 17.48760788519201981 ) ) ;
#41087=AXIS2_PLACEMENT_3D ( 'NONE', #60552, #31137, #3538 ) ;
#41093=CARTESIAN_POINT ( 'NONE',  ( 0.5807400328401574052, 29.58941477093070205, -37.66660715020834971 ) ) ;
#41101=EDGE_LOOP ( 'NONE', ( #14611, #56177, #60490, #52784 ) ) ;
#41102=CARTESIAN_POINT ( 'NONE',  ( 4.956653778116949738, -36.51451553856396970, -31.29546495791881000 ) ) ;
#41104=CARTESIAN_POINT ( 'NONE',  ( 0.7762777257811891429, 44.59086130178278040, -17.50713318242589622 ) ) ;
#41111=CARTESIAN_POINT ( 'NONE',  ( 0.9756354156337461170, -41.41248945940454718, -11.23134828980320066 ) ) ;
#41112=DIRECTION ( 'NONE',  ( 0.07439287786467665975, 0.9868880006907381208, 0.1432402660415323659 ) ) ;
#41114=CARTESIAN_POINT ( 'NONE',  ( 4.967162193818129623, -18.65818244221285127, 38.83676580803761169 ) ) ;
#41116=VERTEX_POINT ( 'NONE', #54072 ) ;
#41119=CARTESIAN_POINT ( 'NONE',  ( 0.5807400328401574052, 0.5448834511089933885, 47.89582301953903709 ) ) ;
#41124=EDGE_CURVE ( 'NONE', #37598, #1001, #51615, .T. ) ;
#41129=CARTESIAN_POINT ( 'NONE',  ( 0.5800708057587377064, 18.90714313908718580, -44.00606528161367237 ) ) ;
#41135=CARTESIAN_POINT ( 'NONE',  ( 0.9749527285493300166, 25.89384247702570008, 34.21468599366719587 ) ) ;
#41139=DIRECTION ( 'NONE',  ( -0.07439287786467652097, -0.5965490341031320920, 0.7991213610169807247 ) ) ;
#41142=CARTESIAN_POINT ( 'NONE',  ( 4.967162193818130511, 23.56777426397228936, -36.06913038482774425 ) ) ;
#41148=DIRECTION ( 'NONE',  ( 0.000000000000000000, 0.000000000000000000, 1.000000000000000000 ) ) ;
#41153=CARTESIAN_POINT ( 'NONE',  ( 0.6846871229502932144, -11.56285438919599606, -46.49193983736603286 ) ) ;
#41158=VECTOR ( 'NONE', #37932, 1000.000000000000114 ) ;
#41163=B_SPLINE_CURVE_WITH_KNOTS ( 'NONE', 3,
 ( #49579, #6634, #28827, #15057, #53241, #9404 ),
 .UNSPECIFIED., .F., .F.,
 ( 4, 2, 4 ),
 ( 1.541099475799976578E-16, 0.0002445252820015208703, 0.0004890505640028875670 ),
 .UNSPECIFIED. ) ;
#41165=ORIENTED_EDGE ( 'NONE', *, *, #22290, .F. ) ;
#41181=ORIENTED_EDGE ( 'NONE', *, *, #6062, .T. ) ;
#41182=CARTESIAN_POINT ( 'NONE',  ( 4.967162193818130511, -40.65506779172153529, -14.26841313271325795 ) ) ;
#41189=ORIENTED_EDGE ( 'NONE', *, *, #42951, .F. ) ;
#41194=CARTESIAN_POINT ( 'NONE',  ( 0.5809828226811617480, 12.92184523170268839, -46.11980934799325382 ) ) ;
#41206=CARTESIAN_POINT ( 'NONE',  ( 0.9747592971366234593, 30.56898208368274084, 30.11108831501845629 ) ) ;
#41208=ORIENTED_EDGE ( 'NONE', *, *, #45036, .F. ) ;
#41211=CARTESIAN_POINT ( 'NONE',  ( 0.5850706913938534814, 24.10530971368288178, 41.38834827854216769 ) ) ;
#41217=CARTESIAN_POINT ( 'NONE',  ( 4.967162193818130511, -36.06913038482816347, 23.56777426397165698 ) ) ;
#41219=FACE_OUTER_BOUND ( 'NONE', #9668, .T. ) ;
#41220=CARTESIAN_POINT ( 'NONE',  ( 5.959828726073459926, -5.316791119500952512, -19.82504517499711127 ) ) ;
#41224=CARTESIAN_POINT ( 'NONE',  ( -16.30394644734282394, -12.43472632814719070, -1.280860982936265380 ) ) ;
#41225=CARTESIAN_POINT ( 'NONE',  ( 4.956653778116959508, -15.97476558431919180, 45.35992544608522792 ) ) ;
#41226=CARTESIAN_POINT ( 'NONE',  ( 0.5809828226811553087, -0.5448590168529036104, -47.89273459658654275 ) ) ;
#41228=CARTESIAN_POINT ( 'NONE',  ( 0.6846871229502899947, -46.49193983736581970, -11.56285438919680963 ) ) ;
#41241=ADVANCED_FACE ( 'NONE', ( #68 ), #29674, .T. ) ;
#41244=CARTESIAN_POINT ( 'NONE',  ( 0.7762783648524410607, -23.17763242108785349, 41.92424098267934340 ) ) ;
#41247=EDGE_CURVE ( 'NONE', #51225, #23152, #2356, .T. ) ;
#41249=ORIENTED_EDGE ( 'NONE', *, *, #59461, .T. ) ;
#41250=CARTESIAN_POINT ( 'NONE',  ( 0.7762783648524383961, -43.90991295203431832, 19.15108798908297416 ) ) ;
#41265=CARTESIAN_POINT ( 'NONE',  ( 4.967162193818130511, -28.07411493385318124, 32.68434214048159703 ) ) ;
#41271=ORIENTED_EDGE ( 'NONE', *, *, #7259, .T. ) ;
#41278=ORIENTED_EDGE ( 'NONE', *, *, #42801, .T. ) ;
#41282=VERTEX_POINT ( 'NONE', #43038 ) ;
#41284=CARTESIAN_POINT ( 'NONE',  ( 0.5809828226811560858, -41.74875432577632495, -23.47450554821754309 ) ) ;
#41289=EDGE_LOOP ( 'NONE', ( #40288, #30286, #44090, #32307 ) ) ;
#41298=ORIENTED_EDGE ( 'NONE', *, *, #56856, .F. ) ;
#41302=CARTESIAN_POINT ( 'NONE',  ( 0.9754642270333686582, -30.46484943293178205, 30.21634823122154145 ) ) ;
#41305=CARTESIAN_POINT ( 'NONE',  ( 5.960721111146673579, -10.25731071096595137, 17.77882586010649391 ) ) ;
#41307=CARTESIAN_POINT ( 'NONE',  ( 0.5786265663353196143, 23.32245830379028106, 41.83999636203328265 ) ) ;
#41310=CARTESIAN_POINT ( 'NONE',  ( 5.960721111146673579, 5.318514366754933498, -19.82454228767740645 ) ) ;
#41312=CARTESIAN_POINT ( 'NONE',  ( 4.967162193818130511, -42.34252806656598977, 7.970725651239652265 ) ) ;
#41318=EDGE_CURVE ( 'NONE', #25300, #29382, #10588, .T. ) ;
#41323=ADVANCED_FACE ( 'NONE', ( #15133 ), #1641, .F. ) ;
#41324=ORIENTED_EDGE ( 'NONE', *, *, #38917, .F. ) ;
#41325=CARTESIAN_POINT ( 'NONE',  ( 1.088908134280554219, 37.54826033999260915, 20.77739698351946984 ) ) ;
#41328=LINE ( 'NONE', #56309, #60923 ) ;
#41342=CARTESIAN_POINT ( 'NONE',  ( 0.5839879882012661838, -3.018602103822392988E-05, -47.89596766821095031 ) ) ;
#41346=ORIENTED_EDGE ( 'NONE', *, *, #19085, .F. ) ;
#41349=CIRCLE ( 'NONE', #47361, 43.08621763946400307 ) ;
#41355=ORIENTED_EDGE ( 'NONE', *, *, #14045, .F. ) ;
#41356=DIRECTION ( 'NONE',  ( 0.000000000000000000, 0.000000000000000000, 1.000000000000000000 ) ) ;
#41357=PLANE ( 'NONE',  #32458 ) ;
#41358=CARTESIAN_POINT ( 'NONE',  ( 4.960156602257181468, -41.85906677498973494, 20.07163247083132873 ) ) ;
#41359=CARTESIAN_POINT ( 'NONE',  ( 1.227938101723756947, -41.66816631169184859, -10.28900963485423858 ) ) ;
#41368=EDGE_CURVE ( 'NONE', #38729, #3122, #30646, .T. ) ;
#41369=CARTESIAN_POINT ( 'NONE',  ( 0.9730545539215883499, 41.31259007387247095, -11.59290486963463351 ) ) ;
#41370=VERTEX_POINT ( 'NONE', #54859 ) ;
#41378=CARTESIAN_POINT ( 'NONE',  ( 0.9736507210033059634, -34.31386771842680616, 25.76216842460683765 ) ) ;
#41383=VERTEX_POINT ( 'NONE', #54230 ) ;
#41385=DIRECTION ( 'NONE',  ( 1.000000000000000000, -0.000000000000000000, -0.000000000000000000 ) ) ;
#41393=CIRCLE ( 'NONE', #14417, 43.08621763946400307 ) ;
#41394=CARTESIAN_POINT ( 'NONE',  ( 5.960721111146673579, 5.318514366754933498, -19.82454228767740645 ) ) ;
#41398=CARTESIAN_POINT ( 'NONE',  ( 0.5827359174754817017, -28.86822142608426134, -38.21848266111700099 ) ) ;
#41403=CARTESIAN_POINT ( 'NONE',  ( 5.959828726073459926, -18.96492317065699851, 7.850628836606516003 ) ) ;
#41406=EDGE_CURVE ( 'NONE', #27511, #58301, #44578, .T. ) ;
#41409=( NAMED_UNIT ( * ) SI_UNIT ( $, .STERADIAN. ) SOLID_ANGLE_UNIT ( ) );
#41411=CARTESIAN_POINT ( 'NONE',  ( 0.8557997880470599172, -23.15977007032294210, -41.93815086860281127 ) ) ;
#41412=CARTESIAN_POINT ( 'NONE',  ( 0.9730545539215883499, -41.57420493492377744, -10.61654491617608009 ) ) ;
#41424=AXIS2_PLACEMENT_3D ( 'NONE', #57513, #9942, #34071 ) ;
#41425=ORIENTED_EDGE ( 'NONE', *, *, #17929, .T. ) ;
#41428=ORIENTED_EDGE ( 'NONE', *, *, #38994, .T. ) ;
#41434=CARTESIAN_POINT ( 'NONE',  ( 0.5839880159502358614, 44.23273844814462308, 18.37091806000251282 ) ) ;
#41437=CARTESIAN_POINT ( 'NONE',  ( 0.9757892942422815574, -42.90845395884348079, 0.05132855327719211547 ) ) ;
#41438=ORIENTED_EDGE ( 'NONE', *, *, #30491, .F. ) ;
#41439=CARTESIAN_POINT ( 'NONE',  ( 0.9752132459055852243, 26.30543738863344672, 33.89922943039187686 ) ) ;
#41441=B_SPLINE_CURVE_WITH_KNOTS ( 'NONE', 3,
 ( #60344, #3641, #56584, #23091 ),
 .UNSPECIFIED., .F., .F.,
 ( 4, 4 ),
 ( 5.057544569639794935E-18, 0.004050076154993004218 ),
 .UNSPECIFIED. ) ;
#41443=VERTEX_POINT ( 'NONE', #1613 ) ;
#41449=EDGE_LOOP ( 'NONE', ( #60774, #37706, #1864, #13455 ) ) ;
#41451=CARTESIAN_POINT ( 'NONE',  ( 5.981074661064941900, 18.96560215432016960, -7.846517100474624584 ) ) ;
#41452=CARTESIAN_POINT ( 'NONE',  ( 0.9756950546413942771, -16.33093981194350164, 39.67916378221933371 ) ) ;
#41454=CARTESIAN_POINT ( 'NONE',  ( 0.5809828226811617480, 6.791453954331010401, -47.41188724015871969 ) ) ;
#41456=CARTESIAN_POINT ( 'NONE',  ( 4.956653778116966613, 0.000000000000000000, 0.000000000000000000 ) ) ;
#41464=DIRECTION ( 'NONE',  ( -1.000000000000000000, -0.000000000000000000, -0.000000000000000000 ) ) ;
#41466=CARTESIAN_POINT ( 'NONE',  ( 0.5786265663353153954, -23.32245830379058660, 41.83999636203313344 ) ) ;
#41475=CARTESIAN_POINT ( 'NONE',  ( 0.9968887458511638267, 6.251925120322047391, -42.45154664631701280 ) ) ;
#41489=EDGE_CURVE ( 'NONE', #41383, #40152, #6300, .T. ) ;
#41494=VERTEX_POINT ( 'NONE', #55172 ) ;
#41496=B_SPLINE_CURVE_WITH_KNOTS ( 'NONE', 3,
 ( #48740, #16165, #58424, #24633, #10227, #15244 ),
 .UNSPECIFIED., .F., .F.,
 ( 4, 2, 4 ),
 ( 1.517598411722886997E-16, 0.0002445252820015207619, 0.0004890505640028898439 ),
 .UNSPECIFIED. ) ;
#41498=CARTESIAN_POINT ( 'NONE',  ( 0.5832366564991509073, 44.14509737861672534, -18.58038995918305503 ) ) ;
#41499=CARTESIAN_POINT ( 'NONE',  ( 1.227938101723756947, 17.20315230597844192, 39.32113113558972373 ) ) ;
#41502=CARTESIAN_POINT ( 'NONE',  ( 0.8557997880470690211, 41.02602466100812961, -24.73961900479208609 ) ) ;
#41503=ORIENTED_EDGE ( 'NONE', *, *, #51062, .F. ) ;
#41509=ORIENTED_EDGE ( 'NONE', *, *, #4494, .T. ) ;
#41511=CARTESIAN_POINT ( 'NONE',  ( 3.270143674763207553, -13.28976595685391082, -3.277085381513258788 ) ) ;
#41514=B_SPLINE_CURVE_WITH_KNOTS ( 'NONE', 3,
 ( #51940, #42886, #18759, #9030 ),
 .UNSPECIFIED., .F., .F.,
 ( 4, 4 ),
 ( 1.734723475976807094E-18, 0.004050076154993002484 ),
 .UNSPECIFIED. ) ;
#41515=CIRCLE ( 'NONE', #38522, 48.09070567114147110 ) ;
#41517=CARTESIAN_POINT ( 'NONE',  ( 2.624215991343620935, -25.21574086439677487, -40.85210347989558244 ) ) ;
#41525=CARTESIAN_POINT ( 'NONE',  ( 0.5832366564991503521, 38.16363840618255665, 28.94058080282794876 ) ) ;
#41527=ORIENTED_EDGE ( 'NONE', *, *, #32461, .F. ) ;
#41528=CARTESIAN_POINT ( 'NONE',  ( -17.04253418815309118, -12.35682012055057299, -1.887283050050494015 ) ) ;
#41529=CARTESIAN_POINT ( 'NONE',  ( 2.281448460670559175, -17.13756432392869300, 44.80776276180765905 ) ) ;
#41542=CARTESIAN_POINT ( 'NONE',  ( 4.303969348037246512, 10.35452842635843673, 46.98258166031693861 ) ) ;
#41545=CARTESIAN_POINT ( 'NONE',  ( 4.967162193818130511, 42.34252806656594004, 7.970725651239941811 ) ) ;
#41546=CARTESIAN_POINT ( 'NONE',  ( 2.624215991343620935, -42.26352390376081303, -22.77108897942180477 ) ) ;
#41555=EDGE_LOOP ( 'NONE', ( #27701, #46758, #59200, #29543 ) ) ;
#41557=CONICAL_SURFACE ( 'NONE', #30512, 42.88844316795388778, 0.04450589592585932341 ) ;
#41561=CARTESIAN_POINT ( 'NONE',  ( 3.407937589446178528, -5.663729899984980776, -12.47329436636634981 ) ) ;
#41567=CARTESIAN_POINT ( 'NONE',  ( 5.960221823109900008, 20.35070456576731246, 2.673723662181406002 ) ) ;
#41575=CARTESIAN_POINT ( 'NONE',  ( 4.963659409799331179, -24.46566636552851293, 37.47512675766687806 ) ) ;
#41589=CARTESIAN_POINT ( 'NONE',  ( 5.981074661064941900, -20.52466374824937034, 0.008585178657547546527 ) ) ;
#41592=ORIENTED_EDGE ( 'NONE', *, *, #58612, .T. ) ;
#41607=CARTESIAN_POINT ( 'NONE',  ( 0.9730545539215883499, 6.101350888305258735, -42.47233286818610054 ) ) ;
#41609=CARTESIAN_POINT ( 'NONE',  ( 0.8557997880470606944, -19.17299735372040459, 43.90420959842174398 ) ) ;
#41615=DIRECTION ( 'NONE',  ( 0.07836865515943411409, 0.3887811538706197889, -0.9179910502197345945 ) ) ;
#41618=CARTESIAN_POINT ( 'NONE',  ( 5.960221823109900008, 18.96108896995703930, 7.859839668735279616 ) ) ;
#41620=CARTESIAN_POINT ( 'NONE',  ( 0.7762777257811898091, 37.45705273431007498, 29.86325207275890747 ) ) ;
#41623=EDGE_CURVE ( 'NONE', #21629, #45591, #14264, .T. ) ;
#41626=B_SPLINE_CURVE_WITH_KNOTS ( 'NONE', 3,
 ( #28624, #33356, #14249, #4799, #46840, #4183, #23939, #47142, #103, #8585, #57116, #56816, #4489, #38069, #52736, #43063, #13316, #41835, #37439 ),
 .UNSPECIFIED., .F., .F.,
 ( 4, 3, 3, 3, 3, 3, 4 ),
 ( 3.469446951953614189E-18, 0.0002724573126191750507, 0.0004086839781548493988, 0.0005449106435901834378, 0.0006811373090491472295, 0.0008459866663933670976, 0.001010840725717212715 ),
 .UNSPECIFIED. ) ;
#41630=VERTEX_POINT ( 'NONE', #57938 ) ;
#41631=CARTESIAN_POINT ( 'NONE',  ( 4.967162193818129623, -43.02067033766018511, 2.375726030842427061 ) ) ;
#41632=B_SPLINE_CURVE_WITH_KNOTS ( 'NONE', 3,
 ( #59077, #54062, #1439, #49380 ),
 .UNSPECIFIED., .F., .F.,
 ( 4, 4 ),
 ( 3.878959614448864246E-18, 0.004050076154992999014 ),
 .UNSPECIFIED. ) ;
#41634=( BOUNDED_SURFACE ( )  B_SPLINE_SURFACE ( 3, 1, ( 
 ( #16916, #45124 ),
 ( #35721, #59484 ),
 ( #46050, #11275 ),
 ( #59174, #54463 ) ),
 .UNSPECIFIED., .F., .F., .F. ) 
 B_SPLINE_SURFACE_WITH_KNOTS ( ( 4, 4 ),
 ( 2, 2 ),
 ( 0.000000000000000000, 1.000000000000000000 ),
 ( 0.000000000000000000, 1.000000000000000000 ),
 .UNSPECIFIED. ) 
 GEOMETRIC_REPRESENTATION_ITEM ( )  RATIONAL_B_SPLINE_SURFACE ( (
 ( 1.000000000000000000, 1.000000000000000000),
 ( 0.7269869731126821222, 0.9931720237060910339),
 ( 0.7269869731126821222, 0.9931720237060910339),
 ( 1.000000000000000000, 1.000000000000000000) ) ) 
 REPRESENTATION_ITEM ( '' )  SURFACE ( )  );
#41635=CARTESIAN_POINT ( 'NONE',  ( 4.967162193818130511, -28.07411493385318124, 32.68434214048159703 ) ) ;
#41648=ORIENTED_EDGE ( 'NONE', *, *, #2163, .F. ) ;
#41650=ORIENTED_EDGE ( 'NONE', *, *, #27341, .F. ) ;
#41664=DIRECTION ( 'NONE',  ( 0.000000000000000000, 0.000000000000000000, 1.000000000000000000 ) ) ;
#41665=CARTESIAN_POINT ( 'NONE',  ( 4.967162193818130511, 3.259922920618364639, -42.96271701169381885 ) ) ;
#41668=ADVANCED_FACE ( 'NONE', ( #4078 ), #14485, .F. ) ;
#41669=ORIENTED_EDGE ( 'NONE', *, *, #52039, .F. ) ;
#41670=CARTESIAN_POINT ( 'NONE',  ( 0.9730545539215883499, 34.34678117142591702, -25.71816799638743944 ) ) ;
#41673=ORIENTED_EDGE ( 'NONE', *, *, #51541, .T. ) ;
#41678=B_SPLINE_CURVE_WITH_KNOTS ( 'NONE', 3,
 ( #28103, #8674, #42534, #47222 ),
 .UNSPECIFIED., .F., .F.,
 ( 4, 4 ),
 ( 2.964296775167216948E-17, 0.005004741218457446628 ),
 .UNSPECIFIED. ) ;
#41680=CARTESIAN_POINT ( 'NONE',  ( 0.5819845079324650339, 47.54334065046006685, 5.801222053075247409 ) ) ;
#41684=CARTESIAN_POINT ( 'NONE',  ( 0.9756950546413952763, -33.98259063592739437, 26.19769393035354810 ) ) ;
#41705=CARTESIAN_POINT ( 'NONE',  ( 0.5838002273316426072, -29.04904228829587254, -38.08117724016836547 ) ) ;
#41709=CARTESIAN_POINT ( 'NONE',  ( 5.958863334805807099, 17.77634700750914476, 10.26176968287951397 ) ) ;
#41714=CARTESIAN_POINT ( 'NONE',  ( 0.8557997880470697982, -19.17299735371977221, -43.90420959842202109 ) ) ;
#41715=EDGE_CURVE ( 'NONE', #2075, #44883, #19466, .T. ) ;
#41720=CARTESIAN_POINT ( 'NONE',  ( 4.967162193818132288, -24.30453456948087521, -35.57684288742000689 ) ) ;
#41729=VERTEX_POINT ( 'NONE', #43274 ) ;
#41731=CARTESIAN_POINT ( 'NONE',  ( 0.9730545539215883499, 16.88610103448558064, 39.44597740938066721 ) ) ;
#41733=( BOUNDED_SURFACE ( )  B_SPLINE_SURFACE ( 3, 1, ( 
 ( #15725, #34831 ),
 ( #35766, #1584 ),
 ( #40468, #53897 ),
 ( #59218, #7520 ) ),
 .UNSPECIFIED., .F., .F., .F. ) 
 B_SPLINE_SURFACE_WITH_KNOTS ( ( 4, 4 ),
 ( 2, 2 ),
 ( 0.000000000000000000, 1.000000000000000000 ),
 ( 0.000000000000000000, 1.000000000000000000 ),
 .UNSPECIFIED. ) 
 GEOMETRIC_REPRESENTATION_ITEM ( )  RATIONAL_B_SPLINE_SURFACE ( (
 ( 1.000000000000000000, 1.000000000000000000),
 ( 0.9953390228620291325, 0.8624445117760984880),
 ( 0.9953390228620291325, 0.8624445117760984880),
 ( 1.000000000000000000, 1.000000000000000000) ) ) 
 REPRESENTATION_ITEM ( '' )  SURFACE ( )  );
#41736=( GEOMETRIC_REPRESENTATION_CONTEXT ( 3 ) GLOBAL_UNCERTAINTY_ASSIGNED_CONTEXT ( ( #8541 ) ) GLOBAL_UNIT_ASSIGNED_CONTEXT ( ( #57006, #13197, #3453 ) ) REPRESENTATION_CONTEXT ( 'NONE', 'WORKASPACE' ) );
#41746=ORIENTED_EDGE ( 'NONE', *, *, #26678, .T. ) ;
#41747=DIRECTION ( 'NONE',  ( -1.000000000000000000, -0.000000000000000000, -0.000000000000000000 ) ) ;
#41755=EDGE_CURVE ( 'NONE', #21932, #51356, #54160, .T. ) ;
#41760=CARTESIAN_POINT ( 'NONE',  ( 5.960721111146673579, -16.28018152803684515, -12.50019045452732591 ) ) ;
#41775=CARTESIAN_POINT ( 'NONE',  ( 0.9758171775293923433, 37.16279804060133074, 21.44911662810663344 ) ) ;
#41783=CARTESIAN_POINT ( 'NONE',  ( 0.9741495583595179975, 39.48917442789120003, 16.78504838919898745 ) ) ;
#41786=CARTESIAN_POINT ( 'NONE',  ( 4.963659409799330291, 20.22157859941785674, -39.92545197189527784 ) ) ;
#41789=ORIENTED_EDGE ( 'NONE', *, *, #48935, .F. ) ;
#41801=ORIENTED_EDGE ( 'NONE', *, *, #38219, .T. ) ;
#41811=ORIENTED_EDGE ( 'NONE', *, *, #52338, .F. ) ;
#41814=CARTESIAN_POINT ( 'NONE',  ( 0.8557997880470697982, 38.55640757422439435, 28.43566216844983074 ) ) ;
#41821=CARTESIAN_POINT ( 'NONE',  ( 0.9745511491811735816, -21.15859207114723972, -37.32887948083622121 ) ) ;
#41823=CARTESIAN_POINT ( 'NONE',  ( 5.960721111146673579, 7.848955554238242982, 18.96557324978290282 ) ) ;
#41824=EDGE_CURVE ( 'NONE', #50613, #52183, #41891, .T. ) ;
#41825=CARTESIAN_POINT ( 'NONE',  ( 0.9730545539215883499, -26.52009130076794108, 33.73144377768549163 ) ) ;
#41829=EDGE_LOOP ( 'NONE', ( #20462, #48492, #33717, #45815 ) ) ;
#41835=CARTESIAN_POINT ( 'NONE',  ( 0.9736507210033070736, -42.59776535855980484, 5.153758453069401391 ) ) ;
#41838=CARTESIAN_POINT ( 'NONE',  ( 5.959547316686252039, -5.315863417546468739, 19.82530672674353056 ) ) ;
#41839=FACE_OUTER_BOUND ( 'NONE', #45631, .T. ) ;
#41842=FACE_OUTER_BOUND ( 'NONE', #14015, .T. ) ;
#41852=CARTESIAN_POINT ( 'NONE',  ( 0.9730545539215883499, -39.44597740938072405, 16.88610103448544209 ) ) ;
#41857=CARTESIAN_POINT ( 'NONE',  ( 0.8557997880470599172, 34.51495345639595058, -33.22501220301865033 ) ) ;
#41859=ORIENTED_EDGE ( 'NONE', *, *, #10253, .T. ) ;
#41860=VERTEX_POINT ( 'NONE', #24758 ) ;
#41879=B_SPLINE_CURVE_WITH_KNOTS ( 'NONE', 3,
 ( #4137, #60233, #13271, #23276 ),
 .UNSPECIFIED., .F., .F.,
 ( 4, 4 ),
 ( 1.179611963664228824E-16, 0.005004741218457495200 ),
 .UNSPECIFIED. ) ;
#41885=ORIENTED_EDGE ( 'NONE', *, *, #34900, .F. ) ;
#41887=CARTESIAN_POINT ( 'NONE',  ( 5.974727161628367256, 20.52494643607030156, -0.01551142186628274786 ) ) ;
#41891=B_SPLINE_CURVE_WITH_KNOTS ( 'NONE', 3,
 ( #49481, #6536, #25994, #34788 ),
 .UNSPECIFIED., .F., .F.,
 ( 4, 4 ),
 ( 0.000000000000000000, 0.005004741218457366830 ),
 .UNSPECIFIED. ) ;
#41905=VECTOR ( 'NONE', #6039, 1000.000000000000114 ) ;
#41908=CARTESIAN_POINT ( 'NONE',  ( 0.9730545539215892381, 25.71816799638828499, -34.34678117142529175 ) ) ;
#41910=CARTESIAN_POINT ( 'NONE',  ( -19.55613784151982060, -12.42316071588242110, 1.387283936007070562 ) ) ;
#41914=CARTESIAN_POINT ( 'NONE',  ( 5.959547316686252039, -19.82715097195166010, 5.308980600728112620 ) ) ;
#41915=EDGE_LOOP ( 'NONE', ( #4354, #36327, #4242, #17611 ) ) ;
#41919=ORIENTED_EDGE ( 'NONE', *, *, #12680, .T. ) ;
#41924=CARTESIAN_POINT ( 'NONE',  ( 1.227938101723748288, 41.66816631169206886, -10.28900963485336995 ) ) ;
#41929=CARTESIAN_POINT ( 'NONE',  ( 5.960721111146673579, -17.77882586010674260, 10.25731071096551794 ) ) ;
#41933=VECTOR ( 'NONE', #38581, 999.9999999999998863 ) ;
#41934=CARTESIAN_POINT ( 'NONE',  ( 1.227938101723756947, 11.92353943227949387, 41.23019537246713639 ) ) ;
#41943=CARTESIAN_POINT ( 'NONE',  ( 0.9730545539215883499, 10.61654491617622398, -41.57420493492374192 ) ) ;
#41947=CARTESIAN_POINT ( 'NONE',  ( -18.24846456548969797, -7.719455939378113030, -2.099999999999997868 ) ) ;
#41951=EDGE_CURVE ( 'NONE', #52969, #23152, #17835, .T. ) ;
#41961=EDGE_LOOP ( 'NONE', ( #38283, #10678, #41298, #48157 ) ) ;
#41965=CARTESIAN_POINT ( 'NONE',  ( 0.9758171775293923433, 21.45936886481795014, 37.15687890897625323 ) ) ;
#41971=ORIENTED_EDGE ( 'NONE', *, *, #34929, .T. ) ;
#41975=CARTESIAN_POINT ( 'NONE',  ( 0.5786265663353196143, 44.52624106864168141, -17.66171603226031550 ) ) ;
#41978=CARTESIAN_POINT ( 'NONE',  ( 4.956653778116982600, -43.37017594958069111, 20.77844580450546985 ) ) ;
#41985=ORIENTED_EDGE ( 'NONE', *, *, #40471, .T. ) ;
#41986=EDGE_CURVE ( 'NONE', #18352, #12599, #26922, .T. ) ;
#41992=B_SPLINE_CURVE_WITH_KNOTS ( 'NONE', 3,
 ( #31321, #7177, #45443, #44527, #26617, #45747, #2798, #15695, #34800, #1558, #50063, #57346, #24791, #34506, #44236, #10391 ),
 .UNSPECIFIED., .F., .F.,
 ( 4, 3, 3, 3, 3, 4 ),
 ( 6.939740885162003740E-18, 0.0002724568934985503971, 0.0004086836638483758643, 0.0005449104342063602240, 0.0008173270854453667817, 0.001089761613562689226 ),
 .UNSPECIFIED. ) ;
#41993=ORIENTED_EDGE ( 'NONE', *, *, #10680, .F. ) ;
#41994=CARTESIAN_POINT ( 'NONE',  ( 0.5832366564991512403, 47.52097076201152248, 5.981458972433913779 ) ) ;
#41995=CARTESIAN_POINT ( 'NONE',  ( 4.956653778116992370, 3.690426056930664611, -47.94889704119048446 ) ) ;
#42006=CARTESIAN_POINT ( 'NONE',  ( 4.967162193818131399, -3.259922920618036901, 42.96271701169384016 ) ) ;
#42009=CARTESIAN_POINT ( 'NONE',  ( 0.5807400328401574052, 17.82553128098469131, -44.45848844984423920 ) ) ;
#42010=CARTESIAN_POINT ( 'NONE',  ( 0.5832367798473389042, 6.521664418777854522, -47.44985149964043103 ) ) ;
#42013=B_SPLINE_CURVE_WITH_KNOTS ( 'NONE', 3,
 ( #962, #5030, #39215, #57336 ),
 .UNSPECIFIED., .F., .F.,
 ( 4, 4 ),
 ( 6.736447455048116623E-17, 0.005004741218457475251 ),
 .UNSPECIFIED. ) ;
#42017=ORIENTED_EDGE ( 'NONE', *, *, #12680, .F. ) ;
#42021=CARTESIAN_POINT ( 'NONE',  ( 0.5827357941260206120, 46.35666768646135694, 12.04516435546818087 ) ) ;
#42026=CARTESIAN_POINT ( 'NONE',  ( 0.8557997880470690211, 46.03118133706043835, -13.27832040216591380 ) ) ;
#42027=FACE_OUTER_BOUND ( 'NONE', #47195, .T. ) ;
#42030=VERTEX_POINT ( 'NONE', #47573 ) ;
#42040=CARTESIAN_POINT ( 'NONE',  ( 0.5834872094924171693, -6.026535573893806230, -47.51530820063773319 ) ) ;
#42046=CARTESIAN_POINT ( 'NONE',  ( 1.227938101723748288, 15.63977281655842511, 39.96870412324341260 ) ) ;
#42057=CARTESIAN_POINT ( 'NONE',  ( 4.963659409799330291, 20.22157859941729896, 39.92545197189556916 ) ) ;
#42058=ORIENTED_EDGE ( 'NONE', *, *, #5312, .F. ) ;
#42059=CARTESIAN_POINT ( 'NONE',  ( 0.9757787079277449038, -42.90844198810271592, -0.03949005143946147239 ) ) ;
#42061=EDGE_LOOP ( 'NONE', ( #28849, #29235, #43570, #51369 ) ) ;
#42072=VERTEX_POINT ( 'NONE', #51633 ) ;
#42074=CARTESIAN_POINT ( 'NONE',  ( 4.303969348037258058, -43.57722561725972099, 20.38638383586104652 ) ) ;
#42076=CARTESIAN_POINT ( 'NONE',  ( 3.270143674763207553, 7.080034332678258657, 11.71453292426881987 ) ) ;
#42079=CARTESIAN_POINT ( 'NONE',  ( 0.5263152470540294336, 0.000000000000000000, 8.000000000000000000 ) ) ;
#42081=CARTESIAN_POINT ( 'NONE',  ( 0.9722240741986377666, 39.86121768686908240, -15.88116971565344393 ) ) ;
#42088=CARTESIAN_POINT ( 'NONE',  ( 0.9756008150404594792, 37.23069985082546651, 21.33101788548744082 ) ) ;
#42108=CARTESIAN_POINT ( 'NONE',  ( 0.9747592971366226822, -11.41797089479104521, -41.36145845824421485 ) ) ;
#42109=EDGE_CURVE ( 'NONE', #9554, #26349, #25328, .T. ) ;
#42110=( BOUNDED_SURFACE ( )  B_SPLINE_SURFACE ( 3, 1, ( 
 ( #24897, #57764 ),
 ( #44038, #1071 ),
 ( #20207, #43409 ),
 ( #52770, #445 ) ),
 .UNSPECIFIED., .F., .F., .F. ) 
 B_SPLINE_SURFACE_WITH_KNOTS ( ( 4, 4 ),
 ( 2, 2 ),
 ( 0.000000000000000000, 1.000000000000000000 ),
 ( 0.000000000000000000, 1.000000000000000000 ),
 .UNSPECIFIED. ) 
 GEOMETRIC_REPRESENTATION_ITEM ( )  RATIONAL_B_SPLINE_SURFACE ( (
 ( 1.000000000000000000, 1.000000000000000000),
 ( 0.7269869731126821222, 0.9931720237060910339),
 ( 0.7269869731126821222, 0.9931720237060910339),
 ( 1.000000000000000000, 1.000000000000000000) ) ) 
 REPRESENTATION_ITEM ( '' )  SURFACE ( )  );
#42118=CARTESIAN_POINT ( 'NONE',  ( 0.5838002273316417190, -12.26477999444036548, -46.29900743592993706 ) ) ;
#42119=VERTEX_POINT ( 'NONE', #53774 ) ;
#42123=ORIENTED_EDGE ( 'NONE', *, *, #42109, .T. ) ;
#42128=CARTESIAN_POINT ( 'NONE',  ( 0.9730545539215883499, -29.98130006528883129, 30.69604515769640329 ) ) ;
#42132=CARTESIAN_POINT ( 'NONE',  ( 3.660087539127315992, 39.22752134874918539, 27.72868323267822532 ) ) ;
#42135=( BOUNDED_SURFACE ( )  B_SPLINE_SURFACE ( 3, 1, ( 
 ( #12306, #37049 ),
 ( #46747, #27005 ),
 ( #22004, #51723 ),
 ( #47057, #22616 ) ),
 .UNSPECIFIED., .F., .F., .F. ) 
 B_SPLINE_SURFACE_WITH_KNOTS ( ( 4, 4 ),
 ( 2, 2 ),
 ( 0.000000000000000000, 1.000000000000000000 ),
 ( 0.000000000000000000, 1.000000000000000000 ),
 .UNSPECIFIED. ) 
 GEOMETRIC_REPRESENTATION_ITEM ( )  RATIONAL_B_SPLINE_SURFACE ( (
 ( 1.000000000000000000, 1.000000000000000000),
 ( 0.7269869731126817891, 0.9931720237060910339),
 ( 0.7269869731126817891, 0.9931720237060910339),
 ( 1.000000000000000000, 1.000000000000000000) ) ) 
 REPRESENTATION_ITEM ( '' )  SURFACE ( )  );
#42138=CARTESIAN_POINT ( 'NONE',  ( 4.967162193818130511, 23.56777426397228936, -36.06913038482774425 ) ) ;
#42139=B_SPLINE_CURVE_WITH_KNOTS ( 'NONE', 3,
 ( #34412, #58795, #39743, #58183 ),
 .UNSPECIFIED., .F., .F.,
 ( 4, 4 ),
 ( 0.000000000000000000, 0.004446090762761313944 ),
 .UNSPECIFIED. ) ;
#42142=ORIENTED_EDGE ( 'NONE', *, *, #41951, .T. ) ;
#42145=CARTESIAN_POINT ( 'NONE',  ( 0.9736507210033066295, 30.02062799605199572, 30.65767007549924372 ) ) ;
#42148=CARTESIAN_POINT ( 'NONE',  ( 4.956653778116970166, 39.67974989265038488, 27.17045123668485829 ) ) ;
#42150=CARTESIAN_POINT ( 'NONE',  ( 3.407937589446174087, 8.699069120706923286, -10.58239600294629668 ) ) ;
#42154=CARTESIAN_POINT ( 'NONE',  ( 0.9756950546413931669, 42.90834738653779823, -0.09673755062811521810 ) ) ;
#42176=CARTESIAN_POINT ( 'NONE',  ( 0.8557997880470599172, 17.48760788519217257, 44.60232077416692675 ) ) ;
#42177=ORIENTED_EDGE ( 'NONE', *, *, #505, .F. ) ;
#42182=EDGE_LOOP ( 'NONE', ( #57376, #11992, #43849, #1384 ) ) ;
#42185=DIRECTION ( 'NONE',  ( 0.07439287786467665975, 0.9161872986448671430, 0.3937848822959463813 ) ) ;
#42192=CIRCLE ( 'NONE', #49180, 48.09070567114147110 ) ;
#42195=ORIENTED_EDGE ( 'NONE', *, *, #15052, .T. ) ;
#42203=B_SPLINE_CURVE_WITH_KNOTS ( 'NONE', 3,
 ( #19748, #15053, #34159, #49165, #44499, #25054 ),
 .UNSPECIFIED., .F., .F.,
 ( 4, 2, 4 ),
 ( 1.738108305489988542E-18, 0.0002291966416970788616, 0.0004583932833941559886 ),
 .UNSPECIFIED. ) ;
#42211=CARTESIAN_POINT ( 'NONE',  ( 2.624215991343608501, 30.33228621715088380, -37.21129343241572229 ) ) ;
#42212=ORIENTED_EDGE ( 'NONE', *, *, #16443, .F. ) ;
#42224=EDGE_CURVE ( 'NONE', #12597, #22992, #51495, .T. ) ;
#42238=CARTESIAN_POINT ( 'NONE',  ( 5.959547316686252039, 18.96456592444100053, -7.851524054666214170 ) ) ;
#42239=CARTESIAN_POINT ( 'NONE',  ( 0.9722240741986377666, -41.59310805473376860, 10.54237114526869412 ) ) ;
#42241=CARTESIAN_POINT ( 'NONE',  ( 4.967162193818130511, 0.000000000000000000, 0.000000000000000000 ) ) ;
#42242=CARTESIAN_POINT ( 'NONE',  ( 3.270143674763207553, -10.69018354892893718, 8.548517033725214986 ) ) ;
#42244=ORIENTED_EDGE ( 'NONE', *, *, #1677, .T. ) ;
#42245=CARTESIAN_POINT ( 'NONE',  ( 0.9730545539215892381, -15.95224156741857691, 39.83279466599033469 ) ) ;
#42255=CARTESIAN_POINT ( 'NONE',  ( 1.088313998177385278, -29.78798111128807236, -30.89087247895961852 ) ) ;
#42258=CARTESIAN_POINT ( 'NONE',  ( -18.52588630790603474, -7.735090112546274099, -2.044527905409440294 ) ) ;
#42259=ORIENTED_EDGE ( 'NONE', *, *, #58693, .F. ) ;
#42261=CARTESIAN_POINT ( 'NONE',  ( 4.967162193818129623, -18.65818244221285127, 38.83676580803761169 ) ) ;
#42262=CARTESIAN_POINT ( 'NONE',  ( 1.227938101723748288, 42.65467462194924764, -4.762198645644009076 ) ) ;
#42267=CARTESIAN_POINT ( 'NONE',  ( 0.5809828226811617480, 6.791453954331010401, -47.41188724015871969 ) ) ;
#42268=ORIENTED_EDGE ( 'NONE', *, *, #1626, .F. ) ;
#42273=EDGE_CURVE ( 'NONE', #37705, #20429, #47748, .T. ) ;
#42280=ORIENTED_EDGE ( 'NONE', *, *, #45139, .T. ) ;
#42282=CARTESIAN_POINT ( 'NONE',  ( 0.5807400328401637335, 47.55718917606851193, -5.711437504335475701 ) ) ;
#42286=CARTESIAN_POINT ( 'NONE',  ( 0.9757898596046642448, 0.02632670903343587582, -42.90845459940354090 ) ) ;
#42290=ORIENTED_EDGE ( 'NONE', *, *, #5069, .F. ) ;
#42293=CARTESIAN_POINT ( 'NONE',  ( 5.965394784446458765, -5.298374383010773236, 19.82972329408676515 ) ) ;
#42296=B_SPLINE_CURVE_WITH_KNOTS ( 'NONE', 3,
 ( #41226, #17398, #2977, #60286, #36521, #55587 ),
 .UNSPECIFIED., .F., .F.,
 ( 4, 2, 4 ),
 ( 6.149443329761889321E-18, 0.0002445244328975372940, 0.0004890488657950685164 ),
 .UNSPECIFIED. ) ;
#42298=B_SPLINE_CURVE_WITH_KNOTS ( 'NONE', 3,
 ( #60324, #12145, #50936, #41265 ),
 .UNSPECIFIED., .F., .F.,
 ( 4, 4 ),
 ( 8.673617379884035472E-19, 0.004048833967417089091 ),
 .UNSPECIFIED. ) ;
#42313=CARTESIAN_POINT ( 'NONE',  ( 0.5850706913938534814, 18.16120156791940943, -44.31965802246087094 ) ) ;
#42317=B_SPLINE_CURVE_WITH_KNOTS ( 'NONE', 3,
 ( #37271, #24616, #800, #43127, #29307, #52800, #5780, #18153, #29005, #38740, #32563, #48119, #8415, #44069, #5172, #51641 ),
 .UNSPECIFIED., .F., .F.,
 ( 4, 3, 3, 3, 3, 4 ),
 ( 1.250973872328959318E-17, 0.0002724568934985619980, 0.0004086836638483865437, 0.0005449104342063674881, 0.0008173270854453680827, 0.001089761613562689659 ),
 .UNSPECIFIED. ) ;
#42328=ADVANCED_FACE ( 'NONE', ( #60638 ), #3182, .F. ) ;
#42340=ORIENTED_EDGE ( 'NONE', *, *, #55612, .F. ) ;
#42342=CARTESIAN_POINT ( 'NONE',  ( 1.227938101723748288, -15.63977281655813023, -39.96870412324352628 ) ) ;
#42344=CARTESIAN_POINT ( 'NONE',  ( 0.5807400328401574052, -0.5448834511093306743, 47.89582301953903709 ) ) ;
#42347=CARTESIAN_POINT ( 'NONE',  ( 5.965394784446458765, 16.27505370423081388, -12.50653125158990697 ) ) ;
#42355=ORIENTED_EDGE ( 'NONE', *, *, #16014, .T. ) ;
#42362=CARTESIAN_POINT ( 'NONE',  ( 0.7057020205115028810, -47.59410670607640270, 5.417413437617410565 ) ) ;
#42365=CARTESIAN_POINT ( 'NONE',  ( 5.960721111146673579, 2.672857320903303968, -20.35079619394243267 ) ) ;
#42367=FACE_OUTER_BOUND ( 'NONE', #25504, .T. ) ;
#42371=CARTESIAN_POINT ( 'NONE',  ( 5.959547316686252039, 17.77749189599217416, -10.25972575517511487 ) ) ;
#42374=CARTESIAN_POINT ( 'NONE',  ( 0.5809828226811617480, -44.03860873105681151, -18.83114015454746237 ) ) ;
#42377=CARTESIAN_POINT ( 'NONE',  ( 0.7762777257811892540, -29.86325207275904248, 37.45705273430995419 ) ) ;
#42378=DIRECTION ( 'NONE',  ( -0.07439287786467650709, -0.4871392060438084481, 0.8701500408883626747 ) ) ;
#42380=ADVANCED_FACE ( 'NONE', ( #9269 ), #16020, .F. ) ;
#42385=CARTESIAN_POINT ( 'NONE',  ( 3.660176727303400934, -1.881607889988088367, 48.00143922595155033 ) ) ;
#42393=CARTESIAN_POINT ( 'NONE',  ( 0.9752570700956808558, 39.55341424149108320, 16.63323182627884478 ) ) ;
#42398=EDGE_CURVE ( 'NONE', #36654, #39909, #54483, .T. ) ;
#42403=AXIS2_PLACEMENT_3D ( 'NONE', #8755, #27871, #47000 ) ;
#42411=CARTESIAN_POINT ( 'NONE',  ( 0.9754642270333684362, -41.49150764699765404, 10.93570046136892948 ) ) ;
#42412=ORIENTED_EDGE ( 'NONE', *, *, #54240, .F. ) ;
#42417=ADVANCED_FACE ( 'NONE', ( #44661 ), #60932, .F. ) ;
#42425=ORIENTED_EDGE ( 'NONE', *, *, #55588, .T. ) ;
#42427=CARTESIAN_POINT ( 'NONE',  ( 0.9757898596046643558, -0.02632670903323431136, 42.90845459940352669 ) ) ;
#42439=VERTEX_POINT ( 'NONE', #10513 ) ;
#42440=VERTEX_POINT ( 'NONE', #30220 ) ;
#42442=CARTESIAN_POINT ( 'NONE',  ( 4.960156602257181468, 43.79161740034472672, 15.40604254112658644 ) ) ;
#42453=EDGE_CURVE ( 'NONE', #18686, #1320, #34753, .T. ) ;
#42466=CARTESIAN_POINT ( 'NONE',  ( -17.97369999999976642, -7.719455939378112141, -2.099999999999997424 ) ) ;
#42467=CARTESIAN_POINT ( 'NONE',  ( 4.956653778116966613, 0.000000000000000000, 0.000000000000000000 ) ) ;
#42471=CARTESIAN_POINT ( 'NONE',  ( 3.660176727303414701, 35.27264088192925584, -32.61164548483928627 ) ) ;
#42473=VERTEX_POINT ( 'NONE', #26766 ) ;
#42475=CARTESIAN_POINT ( 'NONE',  ( 0.9722240750034564227, -42.90442369954360657, 0.5819398758578646635 ) ) ;
#42478=ORIENTED_EDGE ( 'NONE', *, *, #6944, .F. ) ;
#42484=B_SPLINE_CURVE_WITH_KNOTS ( 'NONE', 3,
 ( #41943, #46326, #27818, #37867, #51606, #37239, #9016, #61009, #28423, #23428, #27203, #42554, #18117, #13422, #46950, #56926, #3985, #4592, #13737 ),
 .UNSPECIFIED., .F., .F.,
 ( 4, 3, 3, 3, 3, 3, 4 ),
 ( 3.469446951953614189E-18, 0.0002724573126191766771, 0.0004086839781548514045, 0.0005449106435901833294, 0.0006811373090491508074, 0.0008459866663933649292, 0.001010840725717214233 ),
 .UNSPECIFIED. ) ;
#42487=CARTESIAN_POINT ( 'NONE',  ( 1.154321485836933281, -34.54400167111882780, -25.46626718279344104 ) ) ;
#42489=ADVANCED_FACE ( 'NONE', ( #50874 ), #49761, .T. ) ;
#42501=CARTESIAN_POINT ( 'NONE',  ( 0.5809828226811556418, 44.03860873105722362, -18.83114015454650314 ) ) ;
#42503=B_SPLINE_CURVE_WITH_KNOTS ( 'NONE', 3,
 ( #20317, #10605, #562, #24699, #58489, #35348 ),
 .UNSPECIFIED., .F., .F.,
 ( 4, 2, 4 ),
 ( 1.497599948434059756E-16, 0.0002445252820015213040, 0.0004890505640028927712 ),
 .UNSPECIFIED. ) ;
#42505=ORIENTED_EDGE ( 'NONE', *, *, #18489, .F. ) ;
#42507=CARTESIAN_POINT ( 'NONE',  ( 0.5836750258453371476, 41.38803015412003816, 24.10509086647765287 ) ) ;
#42512=CARTESIAN_POINT ( 'NONE',  ( 0.9722240741986373225, -5.023189681690476860, -42.61332881199392375 ) ) ;
#42514=ORIENTED_EDGE ( 'NONE', *, *, #25117, .T. ) ;
#42515=CARTESIAN_POINT ( 'NONE',  ( 0.5839879882104922482, -0.04539914087004336823, 47.89596766822081264 ) ) ;
#42517=DIRECTION ( 'NONE',  ( 0.000000000000000000, 0.000000000000000000, 1.000000000000000000 ) ) ;
#42519=CARTESIAN_POINT ( 'NONE',  ( 4.967162193818129623, -13.42934394584134949, -40.93989340068622340 ) ) ;
#42521=CARTESIAN_POINT ( 'NONE',  ( 0.5809828226811544205, 17.82437196699742188, -44.45562576850583270 ) ) ;
#42534=CARTESIAN_POINT ( 'NONE',  ( 4.963659409799328515, 19.36487359954699272, 40.34793212403975105 ) ) ;
#42535=CARTESIAN_POINT ( 'NONE',  ( 0.9754642270333672149, 5.774842730422650838, -42.51806607596982701 ) ) ;
#42537=CARTESIAN_POINT ( 'NONE',  ( 0.5839879327111937579, -47.89596760851021173, 0.09083573661695024115 ) ) ;
#42541=CIRCLE ( 'NONE', #28504, 43.08621763946400307 ) ;
#42544=ORIENTED_EDGE ( 'NONE', *, *, #26324, .T. ) ;
#42546=CARTESIAN_POINT ( 'NONE',  ( 5.960721111146673579, -10.26825948882938278, 17.77250458025974567 ) ) ;
#42548=CIRCLE ( 'NONE', #35522, 43.08621763946400307 ) ;
#42550=CARTESIAN_POINT ( 'NONE',  ( 0.5800708119828337228, -47.89175345941821149, 0.6275298934113306970 ) ) ;
#42554=CARTESIAN_POINT ( 'NONE',  ( 0.9756354156337464500, 11.23134828980333211, -41.41248945940449033 ) ) ;
#42558=B_SPLINE_CURVE_WITH_KNOTS ( 'NONE', 3,
 ( #32681, #47698, #61456, #22974, #32999, #14199, #18577, #33304, #61762, #55851, #52373, #9469, #13270, #9164, #18899, #56158 ),
 .UNSPECIFIED., .F., .F.,
 ( 4, 3, 3, 3, 3, 4 ),
 ( 9.813676791237319219E-18, 0.0002724568934985570107, 0.0004086836638483730996, 0.0005449104342063434189, 0.0008173270854453667817, 0.001089761613562694430 ),
 .UNSPECIFIED. ) ;
#42560=( BOUNDED_SURFACE ( )  B_SPLINE_SURFACE ( 3, 1, ( 
 ( #50388, #45719 ),
 ( #6515, #30353 ),
 ( #21899, #2138 ),
 ( #26583, #49465 ) ),
 .UNSPECIFIED., .F., .F., .F. ) 
 B_SPLINE_SURFACE_WITH_KNOTS ( ( 4, 4 ),
 ( 2, 2 ),
 ( 0.000000000000000000, 1.000000000000000000 ),
 ( 0.000000000000000000, 1.000000000000000000 ),
 .UNSPECIFIED. ) 
 GEOMETRIC_REPRESENTATION_ITEM ( )  RATIONAL_B_SPLINE_SURFACE ( (
 ( 1.000000000000000000, 1.000000000000000000),
 ( 0.7269869731126817891, 0.9931720237060910339),
 ( 0.7269869731126817891, 0.9931720237060910339),
 ( 1.000000000000000000, 1.000000000000000000) ) ) 
 REPRESENTATION_ITEM ( '' )  SURFACE ( )  );
#42566=CARTESIAN_POINT ( 'NONE',  ( 5.960721111146673579, 14.51823969584079599, 14.50930005615021656 ) ) ;
#42570=FACE_OUTER_BOUND ( 'NONE', #25449, .T. ) ;
#42571=CARTESIAN_POINT ( 'NONE',  ( 4.967162193818130511, -42.16965968614200477, 8.839793687085075291 ) ) ;
#42572=CARTESIAN_POINT ( 'NONE',  ( 0.5834872094924173913, -38.13619618345230577, 28.97678700412168951 ) ) ;
#42576=CARTESIAN_POINT ( 'NONE',  ( 0.5807400328401574052, 47.55718917606850482, -5.711437504335486359 ) ) ;
#42584=CARTESIAN_POINT ( 'NONE',  ( 0.5807400328401637335, -5.711437504335642679, -47.55718917606849061 ) ) ;
#42600=EDGE_CURVE ( 'NONE', #50265, #36264, #24551, .T. ) ;
#42602=EDGE_CURVE ( 'NONE', #8164, #30005, #21908, .T. ) ;
#42603=CARTESIAN_POINT ( 'NONE',  ( 3.407937589446178528, -12.47329436636632494, 5.663729899985029625 ) ) ;
#42606=CARTESIAN_POINT ( 'NONE',  ( 0.9756354156337437855, -21.56699035436967193, 37.09450626018208652 ) ) ;
#42609=EDGE_LOOP ( 'NONE', ( #33763, #29894, #40562, #51530 ) ) ;
#42610=CARTESIAN_POINT ( 'NONE',  ( 4.303969348037258058, 2.158280495710214630, 48.06163817123226778 ) ) ;
#42611=CARTESIAN_POINT ( 'NONE',  ( 0.5809828226811553087, 12.92184523170202937, 46.11980934799343856 ) ) ;
#42616=EDGE_CURVE ( 'NONE', #59254, #22938, #18931, .T. ) ;
#42619=CARTESIAN_POINT ( 'NONE',  ( 2.526552050251864134, -39.22765360404638102, -17.56110221699869101 ) ) ;
#42621=CARTESIAN_POINT ( 'NONE',  ( 1.154321485836932837, -39.95809831208268292, -15.65787964449906511 ) ) ;
#42622=CONICAL_SURFACE ( 'NONE', #2573, 43.08621763946400307, 1.568696531533066763 ) ;
#42625=CARTESIAN_POINT ( 'NONE',  ( 5.960721111146673579, -17.77250458025999080, 10.26825948882894934 ) ) ;
#42629=SURFACE_SIDE_STYLE ('',( #60777 ) ) ;
#42631=CARTESIAN_POINT ( 'NONE',  ( 4.963659409799330291, -2.450325214228084025, -44.68724496494576925 ) ) ;
#42639=ORIENTED_EDGE ( 'NONE', *, *, #27933, .F. ) ;
#42646=CARTESIAN_POINT ( 'NONE',  ( 0.7762783648524377300, 13.25585403815120245, 46.03397615175189372 ) ) ;
#42653=ORIENTED_EDGE ( 'NONE', *, *, #22567, .F. ) ;
#42657=CARTESIAN_POINT ( 'NONE',  ( 0.7056555295713301534, 47.59410019435330241, 5.417452459789892316 ) ) ;
#42664=FACE_OUTER_BOUND ( 'NONE', #58140, .T. ) ;
#42668=VECTOR ( 'NONE', #49809, 1000.000000000000341 ) ;
#42671=CARTESIAN_POINT ( 'NONE',  ( 3.660176727303400934, 4.399934609596583002, 47.83637937224826686 ) ) ;
#42673=CARTESIAN_POINT ( 'NONE',  ( 0.6846871229502899947, -41.05093867799203622, 24.69859318104474255 ) ) ;
#42676=CARTESIAN_POINT ( 'NONE',  ( 0.5832366564991507962, -44.35361744978924037, -18.07697797533135642 ) ) ;
#42679=DIRECTION ( 'NONE',  ( 1.000000000000000000, 0.000000000000000000, 0.000000000000000000 ) ) ;
#42680=CARTESIAN_POINT ( 'NONE',  ( 0.5809828226811617480, -46.40184912890847357, 11.86925843957150128 ) ) ;
#42681=VECTOR ( 'NONE', #39235, 1000.000000000000114 ) ;
#42685=DIRECTION ( 'NONE',  ( 1.000000000000000000, 0.000000000000000000, 0.000000000000000000 ) ) ;
#42689=CARTESIAN_POINT ( 'NONE',  ( 0.9757787079277449038, 37.14005577278821590, 21.48842038179446590 ) ) ;
#42697=CARTESIAN_POINT ( 'NONE',  ( 0.6067375320500704161, -34.36594163291733395, 33.36326114377807528 ) ) ;
#42709=CARTESIAN_POINT ( 'NONE',  ( 0.9756950546413949432, -41.42124338356082802, 11.19893879603432296 ) ) ;
#42718=EDGE_CURVE ( 'NONE', #12140, #2858, #23609, .T. ) ;
#42725=VERTEX_POINT ( 'NONE', #15763 ) ;
#42734=CARTESIAN_POINT ( 'NONE',  ( 0.9745511491811756910, -30.09905547141332605, -30.58068216140363660 ) ) ;
#42735=CIRCLE ( 'NONE', #50704, 8.000000000000000000 ) ;
#42736=DIRECTION ( 'NONE',  ( -1.000000000000000000, -0.000000000000000000, -0.000000000000000000 ) ) ;
#42745=VERTEX_POINT ( 'NONE', #10751 ) ;
#42751=CARTESIAN_POINT ( 'NONE',  ( 0.8557997880470690211, -44.60232077416674201, -17.48760788519264153 ) ) ;
#42754=CARTESIAN_POINT ( 'NONE',  ( 1.154321485836932837, -22.16897757994451013, -36.74718014677589650 ) ) ;
#42761=CARTESIAN_POINT ( 'NONE',  ( 5.959547316686252039, -5.308980600728319565, -19.82715097195160325 ) ) ;
#42762=ORIENTED_EDGE ( 'NONE', *, *, #15650, .T. ) ;
#42763=AXIS2_PLACEMENT_3D ( 'NONE', #20839, #44363, #1392 ) ;
#42766=CARTESIAN_POINT ( 'NONE',  ( 5.860006189529234355, -15.48781697582079531, 45.67886430272027098 ) ) ;
#42767=CARTESIAN_POINT ( 'NONE',  ( 1.227938101723756947, -36.73927144310528092, 22.18841447410706635 ) ) ;
#42770=CARTESIAN_POINT ( 'NONE',  ( 1.227938101723756947, -39.32113113558978057, 17.20315230597830336 ) ) ;
#42772=DIRECTION ( 'NONE',  ( 0.000000000000000000, 0.000000000000000000, 1.000000000000000000 ) ) ;
#42775=CARTESIAN_POINT ( 'NONE',  ( 0.5832367798473397924, 12.13303976268060858, 46.33367954572886305 ) ) ;
#42786=CARTESIAN_POINT ( 'NONE',  ( 0.5827357941260202789, -41.65958460246757511, -23.63272379758836195 ) ) ;
#42788=B_SPLINE_CURVE_WITH_KNOTS ( 'NONE', 3,
 ( #27186, #3354, #55987, #35686, #13105, #50668 ),
 .UNSPECIFIED., .F., .F.,
 ( 4, 2, 4 ),
 ( 9.745765416140531346E-18, 0.0002291978881530158619, 0.0004583957763060219660 ),
 .UNSPECIFIED. ) ;
#42798=CARTESIAN_POINT ( 'NONE',  ( 4.967162193818130511, 40.65506779172185503, -14.26841313271238221 ) ) ;
#42799=FACE_OUTER_BOUND ( 'NONE', #36460, .T. ) ;
#42800=ORIENTED_EDGE ( 'NONE', *, *, #51261, .F. ) ;
#42801=EDGE_CURVE ( 'NONE', #24263, #24670, #52161, .T. ) ;
#42803=DIRECTION ( 'NONE',  ( 0.000000000000000000, 0.000000000000000000, 1.000000000000000000 ) ) ;
#42810=CARTESIAN_POINT ( 'NONE',  ( 0.5800708057587384836, -47.89175345272234807, -0.6275304576135395385 ) ) ;
#42811=CARTESIAN_POINT ( 'NONE',  ( 4.960156602257179692, -38.88108289790847039, -25.36362146861427647 ) ) ;
#42812=CARTESIAN_POINT ( 'NONE',  ( 2.526552050251863690, -17.56110221699855245, 39.22765360404644497 ) ) ;
#42816=CARTESIAN_POINT ( 'NONE',  ( 0.9757787079277436826, -42.53619983261573623, -5.639827755377083029 ) ) ;
#42824=EDGE_CURVE ( 'NONE', #20977, #60, #44003, .T. ) ;
#42827=CARTESIAN_POINT ( 'NONE',  ( 0.5827359174754830340, -0.3632382226754043431, 47.89462060834303259 ) ) ;
#42832=CARTESIAN_POINT ( 'NONE',  ( 0.5800708119828336118, -18.90714262039440996, -44.00606550371082193 ) ) ;
#42840=CARTESIAN_POINT ( 'NONE',  ( 0.7057020205115064337, -24.67553336431215172, 41.05685587925830760 ) ) ;
#42843=CARTESIAN_POINT ( 'NONE',  ( 0.5836750258453355933, 0.1816059738423085046, -47.89563095930317616 ) ) ;
#42849=CARTESIAN_POINT ( 'NONE',  ( 0.5834872094924159480, -47.89542889285422689, -0.2270145249678201249 ) ) ;
#42856=CARTESIAN_POINT ( 'NONE',  ( 4.967162193818130511, 0.000000000000000000, 0.000000000000000000 ) ) ;
#42864=B_SPLINE_CURVE_WITH_KNOTS ( 'NONE', 3,
 ( #53024, #24215, #708, #385 ),
 .UNSPECIFIED., .F., .F.,
 ( 4, 4 ),
 ( 2.194270917860438266E-17, 0.005004741218457450097 ),
 .UNSPECIFIED. ) ;
#42865=( BOUNDED_SURFACE ( )  B_SPLINE_SURFACE ( 3, 1, ( 
 ( #84, #9498 ),
 ( #27999, #19232 ),
 ( #38651, #5086 ),
 ( #37735, #52406 ) ),
 .UNSPECIFIED., .F., .F., .F. ) 
 B_SPLINE_SURFACE_WITH_KNOTS ( ( 4, 4 ),
 ( 2, 2 ),
 ( 0.000000000000000000, 1.000000000000000000 ),
 ( 0.000000000000000000, 1.000000000000000000 ),
 .UNSPECIFIED. ) 
 GEOMETRIC_REPRESENTATION_ITEM ( )  RATIONAL_B_SPLINE_SURFACE ( (
 ( 1.000000000000000000, 1.000000000000000000),
 ( 0.7269869731126817891, 0.9931720237060910339),
 ( 0.7269869731126817891, 0.9931720237060910339),
 ( 1.000000000000000000, 1.000000000000000000) ) ) 
 REPRESENTATION_ITEM ( '' )  SURFACE ( )  );
#42867=CARTESIAN_POINT ( 'NONE',  ( 5.981074661064941900, 18.95903134304778348, 7.862380442164206507 ) ) ;
#42868=CARTESIAN_POINT ( 'NONE',  ( -19.25580369308461925, -7.824392703123175252, -1.668825094707770740 ) ) ;
#42874=CARTESIAN_POINT ( 'NONE',  ( 5.860006189529246790, 31.78942168514563349, 36.27483683749448318 ) ) ;
#42881=EDGE_CURVE ( 'NONE', #58891, #49888, #36438, .T. ) ;
#42885=ORIENTED_EDGE ( 'NONE', *, *, #40798, .F. ) ;
#42886=CARTESIAN_POINT ( 'NONE',  ( 3.783278058412224976, -22.99727281874601204, -36.37891728069894270 ) ) ;
#42887=EDGE_CURVE ( 'NONE', #33696, #8188, #20780, .T. ) ;
#42891=ORIENTED_EDGE ( 'NONE', *, *, #8967, .T. ) ;
#42897=EDGE_LOOP ( 'NONE', ( #51556, #49105, #7291, #24711 ) ) ;
#42901=AXIS2_PLACEMENT_3D ( 'NONE', #12690, #59647, #16441 ) ;
#42908=ORIENTED_EDGE ( 'NONE', *, *, #1121, .T. ) ;
#42909=B_SPLINE_CURVE_WITH_KNOTS ( 'NONE', 3,
 ( #25313, #35048, #44158, #58196 ),
 .UNSPECIFIED., .F., .F.,
 ( 4, 4 ),
 ( 1.409462824231155572E-18, 0.004444878191957686055 ),
 .UNSPECIFIED. ) ;
#42916=ORIENTED_EDGE ( 'NONE', *, *, #1423, .F. ) ;
#42917=VERTEX_POINT ( 'NONE', #15005 ) ;
#42920=CARTESIAN_POINT ( 'NONE',  ( 0.5807400328401637335, 5.711437504336647208, -47.55718917606836982 ) ) ;
#42921=CARTESIAN_POINT ( 'NONE',  ( 2.281351352603289140, 11.14238889600285454, 46.66131639318005142 ) ) ;
#42928=CARTESIAN_POINT ( 'NONE',  ( 0.7762783648524390623, -46.49451980369968851, -11.53708172997868253 ) ) ;
#42935=B_SPLINE_CURVE_WITH_KNOTS ( 'NONE', 3,
 ( #12637, #1962, #22024, #21089 ),
 .UNSPECIFIED., .F., .F.,
 ( 4, 4 ),
 ( 9.029002393300562720E-17, 0.005004741218457447495 ),
 .UNSPECIFIED. ) ;
#42936=DIRECTION ( 'NONE',  ( -1.000000000000000000, -0.000000000000000000, -0.000000000000000000 ) ) ;
#42943=VERTEX_POINT ( 'NONE', #14696 ) ;
#42944=CARTESIAN_POINT ( 'NONE',  ( 0.9730545539215883499, -36.90443313492345823, 21.89037132892422832 ) ) ;
#42946=EDGE_CURVE ( 'NONE', #15622, #61570, #17020, .T. ) ;
#42947=CARTESIAN_POINT ( 'NONE',  ( 4.967162193818130511, 8.839793687085215623, 42.16965968614196925 ) ) ;
#42951=EDGE_CURVE ( 'NONE', #44755, #21167, #14031, .T. ) ;
#42961=CARTESIAN_POINT ( 'NONE',  ( 0.5839879327111934249, -6.341736898931618072, -47.47435452316581461 ) ) ;
#42962=EDGE_LOOP ( 'NONE', ( #20, #55847, #26691, #61312 ) ) ;
#42973=ORIENTED_EDGE ( 'NONE', *, *, #23615, .F. ) ;
#42974=CARTESIAN_POINT ( 'NONE',  ( 4.967162193818130511, 2.375726030842579828, 43.02067033766019932 ) ) ;
#42992=CARTESIAN_POINT ( 'NONE',  ( 0.9722240750034583101, 41.59310803641459842, 10.54237121715099867 ) ) ;
#42996=CARTESIAN_POINT ( 'NONE',  ( 0.8557997880470599172, 46.50333260518575429, -11.51622788066409697 ) ) ;
#42997=EDGE_CURVE ( 'NONE', #59309, #59890, #23775, .T. ) ;
#43000=AXIS2_PLACEMENT_3D ( 'NONE', #15507, #53680, #34613 ) ;
#43001=B_SPLINE_CURVE_WITH_KNOTS ( 'NONE', 3,
 ( #49483, #58557, #945, #625, #34173, #10048 ),
 .UNSPECIFIED., .F., .F.,
 ( 4, 2, 4 ),
 ( 3.476216610979977084E-18, 0.0002291966416970802711, 0.0004583932833941570728 ),
 .UNSPECIFIED. ) ;
#43003=DIRECTION ( 'NONE',  ( 0.000000000000000000, 0.000000000000000000, -1.000000000000000000 ) ) ;
#43007=CARTESIAN_POINT ( 'NONE',  ( 0.9745511491811755800, 36.98831798234376578, 21.74846188963790183 ) ) ;
#43009=CARTESIAN_POINT ( 'NONE',  ( 5.959547316686252039, -20.52562247508876681, 0.003562808152837176282 ) ) ;
#43014=CARTESIAN_POINT ( 'NONE',  ( 0.5832367798473401255, 29.37285281143894977, -37.83194459509880403 ) ) ;
#43015=CARTESIAN_POINT ( 'NONE',  ( 0.5839879882012694035, 23.94800997596683345, 41.47910964649803844 ) ) ;
#43025=ORIENTED_EDGE ( 'NONE', *, *, #32383, .F. ) ;
#43029=ORIENTED_EDGE ( 'NONE', *, *, #17540, .F. ) ;
#43038=CARTESIAN_POINT ( 'NONE',  ( 4.967162193818130511, -24.30453456948135482, 35.57684288741969425 ) ) ;
#43040=ORIENTED_EDGE ( 'NONE', *, *, #19412, .T. ) ;
#43048=CARTESIAN_POINT ( 'NONE',  ( 2.526464513654344657, -15.32058692775020070, 40.15570173027688128 ) ) ;
#43063=CARTESIAN_POINT ( 'NONE',  ( 0.9745511491811764682, -42.58443036172448615, 5.262846425219458446 ) ) ;
#43078=CARTESIAN_POINT ( 'NONE',  ( 3.660087539127316880, 25.63019641081328004, 40.62968541507452613 ) ) ;
#43079=CARTESIAN_POINT ( 'NONE',  ( 5.959547316686252039, 0.003562808152622177690, 20.52562247508876681 ) ) ;
#43084=CARTESIAN_POINT ( 'NONE',  ( 0.5839254288179557273, 12.30867641975577342, 46.28738487712331562 ) ) ;
#43087=CARTESIAN_POINT ( 'NONE',  ( 4.956653778116975495, 3.690426056929986043, 47.94889704119053420 ) ) ;
#43093=FACE_OUTER_BOUND ( 'NONE', #25191, .T. ) ;
#43094=ORIENTED_EDGE ( 'NONE', *, *, #42997, .F. ) ;
#43110=CARTESIAN_POINT ( 'NONE',  ( 0.5837374860065631665, 37.88763545422917645, -29.30115996485956842 ) ) ;
#43111=ORIENTED_EDGE ( 'NONE', *, *, #13257, .T. ) ;
#43112=CARTESIAN_POINT ( 'NONE',  ( 0.6067099128993235224, -11.71051825714735806, 46.44339333106611178 ) ) ;
#43115=CARTESIAN_POINT ( 'NONE',  ( 0.9722240750034581991, -37.44729079646477032, -20.94823713380376162 ) ) ;
#43123=CARTESIAN_POINT ( 'NONE',  ( 1.088908134280553996, 10.35121946298470696, -41.64642044161479362 ) ) ;
#43125=( BOUNDED_SURFACE ( )  B_SPLINE_SURFACE ( 3, 1, ( 
 ( #4908, #37543 ),
 ( #38165, #46944 ),
 ( #13729, #520 ),
 ( #9948, #56614 ) ),
 .UNSPECIFIED., .F., .F., .F. ) 
 B_SPLINE_SURFACE_WITH_KNOTS ( ( 4, 4 ),
 ( 2, 2 ),
 ( 0.000000000000000000, 1.000000000000000000 ),
 ( 0.000000000000000000, 1.000000000000000000 ),
 .UNSPECIFIED. ) 
 GEOMETRIC_REPRESENTATION_ITEM ( )  RATIONAL_B_SPLINE_SURFACE ( (
 ( 1.000000000000000000, 1.000000000000000000),
 ( 0.9953390228620291325, 0.8624445117760984880),
 ( 0.9953390228620291325, 0.8624445117760984880),
 ( 1.000000000000000000, 1.000000000000000000) ) ) 
 REPRESENTATION_ITEM ( '' )  SURFACE ( )  );
#43127=CARTESIAN_POINT ( 'NONE',  ( 0.5832367798473401255, 28.94059862654991733, 38.16362489683097436 ) ) ;
#43129=CARTESIAN_POINT ( 'NONE',  ( 0.7762783648524391733, 41.92424098267939314, 23.17763242108770072 ) ) ;
#43138=ORIENTED_EDGE ( 'NONE', *, *, #1264, .T. ) ;
#43139=CARTESIAN_POINT ( 'NONE',  ( 0.5839879882012681822, -18.32902119196533874, -44.25009266679224851 ) ) ;
#43141=CARTESIAN_POINT ( 'NONE',  ( 1.154321713695929619, 26.77578845938227659, -33.53917066545392345 ) ) ;
#43151=DIRECTION ( 'NONE',  ( -0.07836865515943411409, 0.8593913859058619487, -0.5052769534812598939 ) ) ;
#43154=CARTESIAN_POINT ( 'NONE',  ( 0.8557997880470606944, -28.43566216844945771, -38.55640757422467857 ) ) ;
#43161=EDGE_CURVE ( 'NONE', #39811, #51992, #20023, .T. ) ;
#43162=CARTESIAN_POINT ( 'NONE',  ( 1.227938101723748288, 37.58536632582807613, -20.72293514920711033 ) ) ;
#43170=CARTESIAN_POINT ( 'NONE',  ( 0.9756354156337456729, 42.55820231551297184, -5.471460801652982653 ) ) ;
#43171=CARTESIAN_POINT ( 'NONE',  ( 1.227938101723747621, 30.94118573761354440, -29.74462687941193551 ) ) ;
#43178=EDGE_CURVE ( 'NONE', #3369, #21629, #46200, .T. ) ;
#43190=CARTESIAN_POINT ( 'NONE',  ( 4.956653778116970166, 43.37017594958054900, 20.77844580450576117 ) ) ;
#43191=DIRECTION ( 'NONE',  ( -0.07439287786467650709, -0.8701500408883610094, -0.4871392060438115013 ) ) ;
#43204=CARTESIAN_POINT ( 'NONE',  ( 5.959828726073459926, -18.96145866559677629, 7.858992891709805306 ) ) ;
#43205=DIRECTION ( 'NONE',  ( 0.000000000000000000, 0.000000000000000000, 1.000000000000000000 ) ) ;
#43209=CARTESIAN_POINT ( 'NONE',  ( 5.960221823109900008, 16.28072933292531133, 12.49951306783095006 ) ) ;
#43210=ORIENTED_EDGE ( 'NONE', *, *, #28989, .T. ) ;
#43215=FILL_AREA_STYLE ('',( #61960 ) ) ;
#43220=ORIENTED_EDGE ( 'NONE', *, *, #19348, .T. ) ;
#43221=ORIENTED_EDGE ( 'NONE', *, *, #58371, .T. ) ;
#43226=CARTESIAN_POINT ( 'NONE',  ( 0.9758171775293935646, -21.44911662810676489, 37.16279804060124548 ) ) ;
#43230=( BOUNDED_SURFACE ( )  B_SPLINE_SURFACE ( 3, 1, ( 
 ( #7854, #46101 ),
 ( #22275, #16652 ),
 ( #41403, #40795 ),
 ( #59543, #60459 ) ),
 .UNSPECIFIED., .F., .F., .F. ) 
 B_SPLINE_SURFACE_WITH_KNOTS ( ( 4, 4 ),
 ( 2, 2 ),
 ( 0.000000000000000000, 1.000000000000000000 ),
 ( 0.000000000000000000, 1.000000000000000000 ),
 .UNSPECIFIED. ) 
 GEOMETRIC_REPRESENTATION_ITEM ( )  RATIONAL_B_SPLINE_SURFACE ( (
 ( 1.000000000000000000, 1.000000000000000000),
 ( 0.9953390228620291325, 0.8624445117760984880),
 ( 0.9953390228620291325, 0.8624445117760984880),
 ( 1.000000000000000000, 1.000000000000000000) ) ) 
 REPRESENTATION_ITEM ( '' )  SURFACE ( )  );
#43231=ORIENTED_EDGE ( 'NONE', *, *, #19156, .T. ) ;
#43232=CARTESIAN_POINT ( 'NONE',  ( 2.281351352603022242, 47.37344280316144562, 7.562287671717293769 ) ) ;
#43237=CARTESIAN_POINT ( 'NONE',  ( 4.967162193818130511, -42.34252806656598977, 7.970725651239652265 ) ) ;
#43239=EDGE_CURVE ( 'NONE', #33938, #3092, #31200, .T. ) ;
#43248=CARTESIAN_POINT ( 'NONE',  ( 0.5827357941260208340, 17.99287562175647892, -44.38787053017132678 ) ) ;
#43251=ORIENTED_EDGE ( 'NONE', *, *, #24352, .T. ) ;
#43252=CARTESIAN_POINT ( 'NONE',  ( 0.9758171775293903449, -37.15687890897636692, 21.45936886481784001 ) ) ;
#43258=ORIENTED_EDGE ( 'NONE', *, *, #13655, .T. ) ;
#43262=ORIENTED_EDGE ( 'NONE', *, *, #48446, .T. ) ;
#43263=B_SPLINE_CURVE_WITH_KNOTS ( 'NONE', 3,
 ( #39302, #58357, #6037, #19884, #1053, #44617, #20189, #58057, #25175, #20795, #39612, #53059, #44317, #33670, #30175, #14877 ),
 .UNSPECIFIED., .F., .F.,
 ( 4, 3, 3, 3, 3, 4 ),
 ( 6.938893903907228378E-18, 0.0002724568934985532160, 0.0004086836638483783580, 0.0005449104342063567545, 0.0008173270854453719859, 0.001089761613562697899 ),
 .UNSPECIFIED. ) ;
#43264=CARTESIAN_POINT ( 'NONE',  ( 0.9730545539215883499, -6.101350888304360787, -42.47233286818623554 ) ) ;
#43267=ORIENTED_EDGE ( 'NONE', *, *, #46899, .F. ) ;
#43268=CARTESIAN_POINT ( 'NONE',  ( 3.407937589446178528, 2.242416846335596237, 13.51415833181188830 ) ) ;
#43271=CARTESIAN_POINT ( 'NONE',  ( 2.526464513654342880, -39.22765990515334522, 17.56107808841295181 ) ) ;
#43272=EDGE_CURVE ( 'NONE', #42943, #5776, #39669, .T. ) ;
#43274=CARTESIAN_POINT ( 'NONE',  ( 1.227938101723748288, 26.79402671879374864, -33.52879263017835143 ) ) ;
#43276=CARTESIAN_POINT ( 'NONE',  ( 2.526464513654344657, 42.96196573359004134, -1.212545078562930589 ) ) ;
#43285=CARTESIAN_POINT ( 'NONE',  ( 5.959547316686252039, 7.851524054666414010, -18.96456592444092593 ) ) ;
#43288=CARTESIAN_POINT ( 'NONE',  ( 0.8551540677456715978, 0.9122407826475813497, 47.90804413217340851 ) ) ;
#43296=CARTESIAN_POINT ( 'NONE',  ( 0.8551540677456739292, 24.74404575822832797, -41.03346287276401938 ) ) ;
#43309=CARTESIAN_POINT ( 'NONE',  ( -17.97369999999976642, -7.719455939378112141, -2.099999999999997424 ) ) ;
#43315=CARTESIAN_POINT ( 'NONE',  ( 0.6846871229502932144, -28.47437962186101856, -38.52803883689329467 ) ) ;
#43319=CARTESIAN_POINT ( 'NONE',  ( 0.9972139404380270244, 34.43899251299770015, 25.59643345733242370 ) ) ;
#43320=ORIENTED_EDGE ( 'NONE', *, *, #36019, .F. ) ;
#43325=ADVANCED_FACE ( 'NONE', ( #7975 ), #58913, .F. ) ;
#43330=ORIENTED_EDGE ( 'NONE', *, *, #12647, .F. ) ;
#43334=CARTESIAN_POINT ( 'NONE',  ( 5.959828726073459926, -12.49879082830556953, -16.28130559351260587 ) ) ;
#43336=ORIENTED_EDGE ( 'NONE', *, *, #57655, .F. ) ;
#43344=CARTESIAN_POINT ( 'NONE',  ( 0.5809828226811553087, -12.92184523170170607, -46.11980934799353093 ) ) ;
#43353=B_SPLINE_CURVE_WITH_KNOTS ( 'NONE', 3,
 ( #55947, #51549, #33405, #13065 ),
 .UNSPECIFIED., .F., .F.,
 ( 4, 4 ),
 ( 0.000000000000000000, 0.005004741218457401525 ),
 .UNSPECIFIED. ) ;
#43357=DIRECTION ( 'NONE',  ( 0.000000000000000000, 0.000000000000000000, 1.000000000000000000 ) ) ;
#43373=CARTESIAN_POINT ( 'NONE',  ( 1.088908134280552886, -22.12904883058530459, -36.76788378223852760 ) ) ;
#43375=CARTESIAN_POINT ( 'NONE',  ( 1.227938101723748288, 37.58536632582807613, -20.72293514920711033 ) ) ;
#43392=CARTESIAN_POINT ( 'NONE',  ( 0.9756008150404611445, -26.00810955565536275, 34.12792951168094646 ) ) ;
#43393=FACE_OUTER_BOUND ( 'NONE', #23150, .T. ) ;
#43394=CARTESIAN_POINT ( 'NONE',  ( 0.9756950546413932779, -11.01205619898749077, 41.47131842451901917 ) ) ;
#43409=CARTESIAN_POINT ( 'NONE',  ( 4.303969348037246512, -16.39840148505059503, -45.22910199346991789 ) ) ;
#43414=DIRECTION ( 'NONE',  ( -1.000000000000000000, -0.000000000000000000, -0.000000000000000000 ) ) ;
#43417=B_SPLINE_CURVE_WITH_KNOTS ( 'NONE', 3,
 ( #13630, #9219, #32735, #31807 ),
 .UNSPECIFIED., .F., .F.,
 ( 4, 4 ),
 ( 7.112366251504909087E-17, 0.005004741218457488261 ),
 .UNSPECIFIED. ) ;
#43420=CARTESIAN_POINT ( 'NONE',  ( 0.5836750258453351492, 38.10871351907229609, -29.01293504009503366 ) ) ;
#43421=ORIENTED_EDGE ( 'NONE', *, *, #57125, .F. ) ;
#43433=EDGE_LOOP ( 'NONE', ( #32856, #33171, #54538, #29817 ) ) ;
#43434=CARTESIAN_POINT ( 'NONE',  ( 2.624215991343608501, -45.98641578154020948, -13.78323291683831364 ) ) ;
#43435=CARTESIAN_POINT ( 'NONE',  ( 0.9736507210033059634, -42.48017254354720507, -6.046964561328380228 ) ) ;
#43440=ORIENTED_EDGE ( 'NONE', *, *, #15650, .F. ) ;
#43444=CARTESIAN_POINT ( 'NONE',  ( 0.5827359174754831450, -47.43746338751527247, -6.611633125157290181 ) ) ;
#43445=DIRECTION ( 'NONE',  ( 0.000000000000000000, 0.000000000000000000, 1.000000000000000000 ) ) ;
#43451=CARTESIAN_POINT ( 'NONE',  ( 1.227938101723756947, 34.55893248994507161, 25.45152231597068848 ) ) ;
#43454=CARTESIAN_POINT ( 'NONE',  ( 0.5832366564991509073, -23.71163571971552386, 41.61464700196766842 ) ) ;
#43455=EDGE_CURVE ( 'NONE', #58751, #59261, #33902, .T. ) ;
#43456=DIRECTION ( 'NONE',  ( 0.07439287786467664587, 0.9665813013808195464, -0.2453289374370102860 ) ) ;
#43460=CARTESIAN_POINT ( 'NONE',  ( 0.5809828226811553087, 38.32755012159145025, 28.72298383114502229 ) ) ;
#43471=CARTESIAN_POINT ( 'NONE',  ( 4.967162193818130511, -28.07411493385273715, -32.68434214048198072 ) ) ;
#43486=CARTESIAN_POINT ( 'NONE',  ( -18.65472868113690907, -7.748419048184884694, 1.991217322887269825 ) ) ;
#43490=DIRECTION ( 'NONE',  ( 0.000000000000000000, 0.000000000000000000, 1.000000000000000000 ) ) ;
#43491=CARTESIAN_POINT ( 'NONE',  ( 4.956653778116966613, 0.000000000000000000, 0.000000000000000000 ) ) ;
#43494=CARTESIAN_POINT ( 'NONE',  ( 0.7762777257811899201, -44.59086130178263119, 17.50713318242622307 ) ) ;
#43496=B_SPLINE_CURVE_WITH_KNOTS ( 'NONE', 3,
 ( #37595, #56662, #9058, #28166 ),
 .UNSPECIFIED., .F., .F.,
 ( 4, 4 ),
 ( 6.397344083151129036E-17, 0.005004741218457495200 ),
 .UNSPECIFIED. ) ;
#43503=CARTESIAN_POINT ( 'NONE',  ( 0.5839879882012672940, -37.99840755997069408, 29.15724166963637032 ) ) ;
#43504=EDGE_CURVE ( 'NONE', #9360, #22050, #38653, .T. ) ;
#43512=ADVANCED_FACE ( 'NONE', ( #47136 ), #922, .F. ) ;
#43527=FACE_OUTER_BOUND ( 'NONE', #10056, .T. ) ;
#43531=EDGE_CURVE ( 'NONE', #46447, #19529, #37891, .T. ) ;
#43532=VERTEX_POINT ( 'NONE', #8906 ) ;
#43534=DIRECTION ( 'NONE',  ( -1.000000000000000000, 0.000000000000000000, 0.000000000000000000 ) ) ;
#43539=CARTESIAN_POINT ( 'NONE',  ( 3.270143674763207553, 6.605065939546814313, 11.98875605389982013 ) ) ;
#43543=FACE_OUTER_BOUND ( 'NONE', #24588, .T. ) ;
#43544=CARTESIAN_POINT ( 'NONE',  ( 4.963659409799333844, -43.98510776953416013, 8.262218268420326694 ) ) ;
#43551=ORIENTED_EDGE ( 'NONE', *, *, #5980, .F. ) ;
#43560=B_SPLINE_CURVE_WITH_KNOTS ( 'NONE', 3,
 ( #9509, #28613, #53034, #4784 ),
 .UNSPECIFIED., .F., .F.,
 ( 4, 4 ),
 ( 0.000000000000000000, 0.005004741218457429280 ),
 .UNSPECIFIED. ) ;
#43563=ORIENTED_EDGE ( 'NONE', *, *, #51546, .F. ) ;
#43565=VECTOR ( 'NONE', #55624, 1000.000000000000114 ) ;
#43566=CARTESIAN_POINT ( 'NONE',  ( 4.956653778116987041, -48.02038484091099235, -2.599733001514835884 ) ) ;
#43570=ORIENTED_EDGE ( 'NONE', *, *, #48446, .F. ) ;
#43576=VERTEX_POINT ( 'NONE', #58335 ) ;
#43579=CONICAL_SURFACE ( 'NONE', #8525, 43.08621763946400307, 1.568696531533066763 ) ;
#43580=ORIENTED_EDGE ( 'NONE', *, *, #47265, .T. ) ;
#43582=LINE ( 'NONE', #43903, #12753 ) ;
#43588=B_SPLINE_CURVE_WITH_KNOTS ( 'NONE', 3,
 ( #41731, #50788, #51393, #17918, #8182, #59879, #8481, #46425, #36722, #46734, #7878, #60484, #45817, #56101, #36110, #13213, #45504, #16993, #55480 ),
 .UNSPECIFIED., .F., .F.,
 ( 4, 3, 3, 3, 3, 3, 4 ),
 ( 6.938893903907228378E-18, 0.0002724573126191798754, 0.0004086839781548472846, 0.0005449106435901838715, 0.0006811373090491498316, 0.0008459866663933777228, 0.001010840725717216835 ),
 .UNSPECIFIED. ) ;
#43589=CARTESIAN_POINT ( 'NONE',  ( 5.965394784446458765, 2.664747781316112896, -20.35165389555755766 ) ) ;
#43593=CARTESIAN_POINT ( 'NONE',  ( 0.5827357941260206120, -34.12346967353437321, -33.60975216782522068 ) ) ;
#43594=CARTESIAN_POINT ( 'NONE',  ( 4.956653778116980824, -40.28700667097698584, 26.26162724282358951 ) ) ;
#43599=ADVANCED_FACE ( 'NONE', ( #14853 ), #54507, .F. ) ;
#43603=CARTESIAN_POINT ( 'NONE',  ( 3.660176727303405819, -45.06760739764698087, 16.63097650367952340 ) ) ;
#43607=EDGE_CURVE ( 'NONE', #6221, #4433, #6416, .T. ) ;
#43611=FACE_OUTER_BOUND ( 'NONE', #3765, .T. ) ;
#43615=DIRECTION ( 'NONE',  ( 0.000000000000000000, 0.000000000000000000, 1.000000000000000000 ) ) ;
#43616=CARTESIAN_POINT ( 'NONE',  ( 2.281351352603290916, -25.11567449372737215, 40.87339198768986392 ) ) ;
#43619=CARTESIAN_POINT ( 'NONE',  ( 0.5809828226811617480, 38.32755012159184815, -28.72298383114449294 ) ) ;
#43620=CARTESIAN_POINT ( 'NONE',  ( 2.281448460670577383, 45.98107640562115250, -13.68109378871662329 ) ) ;
#43621=CARTESIAN_POINT ( 'NONE',  ( 0.9747592971366210168, 30.11108831501880445, -30.56898208368244596 ) ) ;
#43627=CARTESIAN_POINT ( 'NONE',  ( 4.967162193818130511, 0.000000000000000000, 0.000000000000000000 ) ) ;
#43630=ORIENTED_EDGE ( 'NONE', *, *, #8388, .F. ) ;
#43631=CARTESIAN_POINT ( 'NONE',  ( 0.5827357941260228325, 28.86820951701486493, -38.21849163199643584 ) ) ;
#43636=CARTESIAN_POINT ( 'NONE',  ( 5.960221823109900008, -20.35070456576736220, 2.673723662180992555 ) ) ;
#43641=CARTESIAN_POINT ( 'NONE',  ( 0.5786265663353196143, -13.09387673186367707, 46.07681357296480940 ) ) ;
#43643=CARTESIAN_POINT ( 'NONE',  ( 0.8551540677456715978, 28.44084013485117879, 38.56334384152441430 ) ) ;
#43644=ORIENTED_EDGE ( 'NONE', *, *, #42600, .F. ) ;
#43657=ORIENTED_EDGE ( 'NONE', *, *, #33403, .F. ) ;
#43658=VERTEX_POINT ( 'NONE', #48970 ) ;
#43665=CIRCLE ( 'NONE', #53621, 43.08621763946400307 ) ;
#43669=ORIENTED_EDGE ( 'NONE', *, *, #41715, .F. ) ;
#43683=CARTESIAN_POINT ( 'NONE',  ( 5.981074661064941900, 16.27808421740009592, 12.50143471347286805 ) ) ;
#43687=CARTESIAN_POINT ( 'NONE',  ( 3.407937589446174087, -3.987184287467878896, 13.10584870154465520 ) ) ;
#43695=ORIENTED_EDGE ( 'NONE', *, *, #2309, .T. ) ;
#43697=DIRECTION ( 'NONE',  ( -1.000000000000000000, -0.000000000000000000, -0.000000000000000000 ) ) ;
#43706=EDGE_CURVE ( 'NONE', #46608, #48653, #16229, .T. ) ;
#43707=CARTESIAN_POINT ( 'NONE',  ( 0.9740398440564321803, -10.70454588197315715, 41.55177796653844524 ) ) ;
#43718=CARTESIAN_POINT ( 'NONE',  ( 1.227938101723748288, 39.96870412324358313, -15.63977281655798812 ) ) ;
#43721=FACE_OUTER_BOUND ( 'NONE', #18373, .T. ) ;
#43722=CARTESIAN_POINT ( 'NONE',  ( 0.5809828226811617480, -41.20389530892290253, -24.41822904836968178 ) ) ;
#43725=B_SPLINE_CURVE_WITH_KNOTS ( 'NONE', 3,
 ( #31596, #11898, #36014, #11256, #21581, #45406 ),
 .UNSPECIFIED., .F., .F.,
 ( 4, 2, 4 ),
 ( 3.551486221896847302E-18, 0.0002445244328975372940, 0.0004890488657950710100 ),
 .UNSPECIFIED. ) ;
#43728=AXIS2_PLACEMENT_3D ( 'NONE', #46630, #50991, #27198 ) ;
#43731=CARTESIAN_POINT ( 'NONE',  ( 1.227938101723748288, -10.28900963485351205, -41.66816631169202623 ) ) ;
#43733=CARTESIAN_POINT ( 'NONE',  ( 4.960156602257184133, 43.79161740034498251, -15.40604254112596649 ) ) ;
#43737=EDGE_LOOP ( 'NONE', ( #20610, #49472, #39765, #48178 ) ) ;
#43739=B_SPLINE_CURVE_WITH_KNOTS ( 'NONE', 3,
 ( #29989, #34705, #40655, #10900, #53470, #54701 ),
 .UNSPECIFIED., .F., .F.,
 ( 4, 2, 4 ),
 ( 1.084202172485504434E-19, 0.0002445244328975344208, 0.0004890488657950687332 ),
 .UNSPECIFIED. ) ;
#43745=EDGE_CURVE ( 'NONE', #32075, #16670, #8935, .T. ) ;
#43758=CARTESIAN_POINT ( 'NONE',  ( 0.5837374860065628335, 23.79054246378028026, -41.56971235019459954 ) ) ;
#43762=ORIENTED_EDGE ( 'NONE', *, *, #22576, .F. ) ;
#43781=CARTESIAN_POINT ( 'NONE',  ( -16.69292671586258336, -12.38819954910475118, 1.669860868477914151 ) ) ;
#43791=AXIS2_PLACEMENT_3D ( 'NONE', #42467, #18033, #42772 ) ;
#43799=ADVANCED_FACE ( 'NONE', ( #26702 ), #54888, .F. ) ;
#43800=CARTESIAN_POINT ( 'NONE',  ( 0.5850706913938534814, 47.50996714391782660, 6.071602062250778253 ) ) ;
#43811=DIRECTION ( 'NONE',  ( -1.000000000000000000, -0.000000000000000000, -0.000000000000000000 ) ) ;
#43813=EDGE_LOOP ( 'NONE', ( #11052, #12130, #37355, #26345 ) ) ;
#43825=ORIENTED_EDGE ( 'NONE', *, *, #38350, .T. ) ;
#43828=ORIENTED_EDGE ( 'NONE', *, *, #14011, .F. ) ;
#43830=EDGE_LOOP ( 'NONE', ( #45727, #45954, #57226, #27013 ) ) ;
#43835=FACE_OUTER_BOUND ( 'NONE', #48696, .T. ) ;
#43843=ORIENTED_EDGE ( 'NONE', *, *, #7536, .T. ) ;
#43849=ORIENTED_EDGE ( 'NONE', *, *, #16140, .T. ) ;
#43856=CARTESIAN_POINT ( 'NONE',  ( 0.9741495583595186636, -21.79582154536828753, 36.96045061395525266 ) ) ;
#43869=EDGE_CURVE ( 'NONE', #23834, #9388, #8660, .T. ) ;
#43876=DIRECTION ( 'NONE',  ( -1.000000000000000000, -0.000000000000000000, -0.000000000000000000 ) ) ;
#43877=CARTESIAN_POINT ( 'NONE',  ( 4.967162193818130511, 38.83676580803767564, 18.65818244221271627 ) ) ;
#43878=ORIENTED_EDGE ( 'NONE', *, *, #53780, .F. ) ;
#43881=B_SPLINE_CURVE_WITH_KNOTS ( 'NONE', 3,
 ( #32397, #12369, #32088, #2938, #51468, #42128 ),
 .UNSPECIFIED., .F., .F.,
 ( 4, 2, 4 ),
 ( 1.289608238010044742E-17, 0.0002291978881530118233, 0.0004583957763060107445 ),
 .UNSPECIFIED. ) ;
#43886=CARTESIAN_POINT ( 'NONE',  ( 0.5807400328401637335, 6.791881299635582181, 47.41494605191445544 ) ) ;
#43890=CARTESIAN_POINT ( 'NONE',  ( 1.154321485836934169, -6.418927614505812507, -42.43366804742923648 ) ) ;
#43894=EDGE_CURVE ( 'NONE', #35714, #6983, #9136, .T. ) ;
#43898=ORIENTED_EDGE ( 'NONE', *, *, #38983, .T. ) ;
#43899=CARTESIAN_POINT ( 'NONE',  ( 1.227938101723756947, -39.32113113558978057, 17.20315230597830336 ) ) ;
#43900=ORIENTED_EDGE ( 'NONE', *, *, #52275, .T. ) ;
#43903=CARTESIAN_POINT ( 'NONE',  ( 3.407937589446178528, 5.663729899985073146, 12.47329436636630717 ) ) ;
#43905=ORIENTED_EDGE ( 'NONE', *, *, #45334, .T. ) ;
#43914=EDGE_CURVE ( 'NONE', #42725, #33861, #24426, .T. ) ;
#43920=CARTESIAN_POINT ( 'NONE',  ( 0.5809828226811617480, -47.55412398569210808, 5.711058609465143654 ) ) ;
#43929=CARTESIAN_POINT ( 'NONE',  ( 4.956653778116966613, 0.000000000000000000, 0.000000000000000000 ) ) ;
#43931=CARTESIAN_POINT ( 'NONE',  ( 0.6067375320500725255, 46.07640252006478221, 13.08014790719042253 ) ) ;
#43934=CARTESIAN_POINT ( 'NONE',  ( 5.959547316686252039, -17.77392908783941294, 10.26589671991332331 ) ) ;
#43937=CARTESIAN_POINT ( 'NONE',  ( -15.88721936851159811, -7.996419009245403942, 0.2752209306966177937 ) ) ;
#43938=LINE ( 'NONE', #30100, #60374 ) ;
#43946=CARTESIAN_POINT ( 'NONE',  ( 0.5838002273316416080, 33.77111476497777431, 33.96372661229951007 ) ) ;
#43953=LINE ( 'NONE', #14806, #52711 ) ;
#43955=CARTESIAN_POINT ( 'NONE',  ( 0.9740398440564311811, 6.011466167924099935, 42.48528956276139468 ) ) ;
#43959=CARTESIAN_POINT ( 'NONE',  ( 5.959547316686252039, 16.28190225198618535, -12.49803383497733122 ) ) ;
#43970=LINE ( 'NONE', #19837, #16590 ) ;
#43971=ORIENTED_EDGE ( 'NONE', *, *, #45876, .F. ) ;
#43979=B_SPLINE_CURVE_WITH_KNOTS ( 'NONE', 3,
 ( #39905, #31095, #50196, #40838 ),
 .UNSPECIFIED., .F., .F.,
 ( 4, 4 ),
 ( 0.000000000000000000, 0.005004741218457413668 ),
 .UNSPECIFIED. ) ;
#43980=VECTOR ( 'NONE', #8505, 1000.000000000000114 ) ;
#43981=LINE ( 'NONE', #29218, #26508 ) ;
#43982=FACE_OUTER_BOUND ( 'NONE', #9634, .T. ) ;
#43990=DIRECTION ( 'NONE',  ( 0.000000000000000000, 0.000000000000000000, 1.000000000000000000 ) ) ;
#43991=EDGE_LOOP ( 'NONE', ( #23211, #37670, #59690, #28890 ) ) ;
#43997=ORIENTED_EDGE ( 'NONE', *, *, #1458, .F. ) ;
#44000=CARTESIAN_POINT ( 'NONE',  ( 0.8557997880470606944, -13.27832040216671317, 46.03118133706021808 ) ) ;
#44003=B_SPLINE_CURVE_WITH_KNOTS ( 'NONE', 3,
 ( #32256, #8419, #50422, #13456, #22848, #7810, #41066, #32568, #27543, #51645, #26308, #2490, #21614, #40753, #60125, #17231, #36354, #55414, #12540 ),
 .UNSPECIFIED., .F., .F.,
 ( 4, 3, 3, 3, 3, 3, 4 ),
 ( 1.734723475976807094E-18, 0.0002724573126191750507, 0.0004086839781548473388, 0.0005449106435901799684, 0.0006811373090491421338, 0.0008459866663933654713, 0.001010840725717215968 ),
 .UNSPECIFIED. ) ;
#44004=CARTESIAN_POINT ( 'NONE',  ( 0.8557997880470690211, -29.88293891557446003, -37.44587306708127983 ) ) ;
#44005=CARTESIAN_POINT ( 'NONE',  ( 4.967162193818130511, 35.57684288742009215, -24.30453456948074376 ) ) ;
#44008=CARTESIAN_POINT ( 'NONE',  ( 5.959547316686252039, 16.28624005235099403, -12.49238070347959351 ) ) ;
#44012=CARTESIAN_POINT ( 'NONE',  ( 0.5809828226811617480, -28.72298383114462439, -38.32755012159175578 ) ) ;
#44021=CARTESIAN_POINT ( 'NONE',  ( 0.9758171775293917882, -26.11633498242650830, 34.04519363167623425 ) ) ;
#44023=CARTESIAN_POINT ( 'NONE',  ( 5.960721111146673579, -16.28787783074218964, -12.49016043756465422 ) ) ;
#44027=CARTESIAN_POINT ( 'NONE',  ( 0.7056555295713302645, 41.05687446835474930, -24.67549844185496966 ) ) ;
#44034=CARTESIAN_POINT ( 'NONE',  ( 3.783278058412227640, 40.39104487792942422, 14.86148287637747956 ) ) ;
#44038=CARTESIAN_POINT ( 'NONE',  ( 5.965394784446458765, 7.868087674480683802, 18.95742317323948001 ) ) ;
#44044=CARTESIAN_POINT ( 'NONE',  ( 4.967162193818131399, -42.34252806656588319, -7.970725651240238463 ) ) ;
#44046=CARTESIAN_POINT ( 'NONE',  ( 0.5786265663353196143, 29.72999788434346868, -37.55861529268522503 ) ) ;
#44050=B_SPLINE_CURVE_WITH_KNOTS ( 'NONE', 3,
 ( #35979, #2104, #40374, #49426, #39760, #15933 ),
 .UNSPECIFIED., .F., .F.,
 ( 4, 2, 4 ),
 ( 8.949102196395036105E-18, 0.0002291978881530155638, 0.0004583957763060221829 ),
 .UNSPECIFIED. ) ;
#44053=CARTESIAN_POINT ( 'NONE',  ( 0.9740398440564312921, 42.59352035928887403, 5.189371650077005960 ) ) ;
#44055=B_SPLINE_CURVE_WITH_KNOTS ( 'NONE', 3,
 ( #42770, #61826, #27409, #38083, #18963, #41852 ),
 .UNSPECIFIED., .F., .F.,
 ( 4, 2, 4 ),
 ( 9.543442895606953578E-18, 0.0002291978881530146693, 0.0004583957763060197976 ),
 .UNSPECIFIED. ) ;
#44058=CARTESIAN_POINT ( 'NONE',  ( 0.9722240741986376555, -0.5819399500323430008, 42.90442369863401950 ) ) ;
#44064=ORIENTED_EDGE ( 'NONE', *, *, #3382, .F. ) ;
#44065=CARTESIAN_POINT ( 'NONE',  ( 5.965394784446458765, 19.82972329408678291, 5.298374383010704847 ) ) ;
#44066=CARTESIAN_POINT ( 'NONE',  ( 0.9741495583595174423, -42.48790363482600441, -5.992561317325607817 ) ) ;
#44069=CARTESIAN_POINT ( 'NONE',  ( 0.5827357941260208340, 29.44458568814510713, 37.77622264066022950 ) ) ;
#44071=CARTESIAN_POINT ( 'NONE',  ( 0.5807400328401574052, 24.41979442053226634, -41.20655774452943376 ) ) ;
#44074=CARTESIAN_POINT ( 'NONE',  ( 0.5834872094924171693, 24.14431479207748765, -41.36515088387890415 ) ) ;
#44079=CARTESIAN_POINT ( 'NONE',  ( 0.8557997880470697982, -19.17299735371977221, -43.90420959842202109 ) ) ;
#44080=CARTESIAN_POINT ( 'NONE',  ( 0.9730545539215883499, -6.101350888304360787, -42.47233286818623554 ) ) ;
#44081=CARTESIAN_POINT ( 'NONE',  ( 0.7762783648524373969, 5.369627767360514170, -47.60264408896659916 ) ) ;
#44086=CARTESIAN_POINT ( 'NONE',  ( 0.5834872094924177244, -24.14431479207719633, 41.36515088387906758 ) ) ;
#44090=ORIENTED_EDGE ( 'NONE', *, *, #29356, .T. ) ;
#44091=CARTESIAN_POINT ( 'NONE',  ( 5.959828726073459926, 2.683617577144381983, -20.34941966491236442 ) ) ;
#44093=CARTESIAN_POINT ( 'NONE',  ( 4.303969348037246512, -4.133486515472991840, -47.93217632892352498 ) ) ;
#44096=FACE_OUTER_BOUND ( 'NONE', #34278, .T. ) ;
#44104=CARTESIAN_POINT ( 'NONE',  ( 4.956653778116975495, -2.599733001514665798, 48.02038484091099235 ) ) ;
#44105=ORIENTED_EDGE ( 'NONE', *, *, #15287, .T. ) ;
#44107=CARTESIAN_POINT ( 'NONE',  ( 5.960221823109900008, 16.28736530777590730, -12.49086489703211100 ) ) ;
#44110=CARTESIAN_POINT ( 'NONE',  ( 5.958863334805807099, -16.28335246510359369, -12.49619391867176610 ) ) ;
#44112=CARTESIAN_POINT ( 'NONE',  ( 5.959547316686252039, -20.34955788964374790, -2.682663672454841386 ) ) ;
#44117=EDGE_CURVE ( 'NONE', #44894, #19785, #26526, .T. ) ;
#44137=ORIENTED_EDGE ( 'NONE', *, *, #13892, .T. ) ;
#44143=ORIENTED_EDGE ( 'NONE', *, *, #7150, .F. ) ;
#44146=LINE ( 'NONE', #15919, #48636 ) ;
#44150=ORIENTED_EDGE ( 'NONE', *, *, #19491, .F. ) ;
#44151=CARTESIAN_POINT ( 'NONE',  ( 0.5837374860065653870, 6.431731162805769841, 47.46223477511612288 ) ) ;
#44152=LINE ( 'NONE', #1179, #4739 ) ;
#44156=VERTEX_POINT ( 'NONE', #58900 ) ;
#44158=CARTESIAN_POINT ( 'NONE',  ( 3.660087539127326206, -25.63019641081301003, -40.62968541507471087 ) ) ;
#44159=CARTESIAN_POINT ( 'NONE',  ( 4.967162193818130511, 13.42934394584221280, -40.93989340068594629 ) ) ;
#44176=ADVANCED_FACE ( 'NONE', ( #54187 ), #29949, .T. ) ;
#44187=CARTESIAN_POINT ( 'NONE',  ( 0.5836750258453353712, 18.49664649301250563, -44.18029554260614589 ) ) ;
#44189=CARTESIAN_POINT ( 'NONE',  ( 4.960156602257181468, 41.40608197274663382, -20.99019478193005739 ) ) ;
#44190=ORIENTED_EDGE ( 'NONE', *, *, #25759, .T. ) ;
#44192=CARTESIAN_POINT ( 'NONE',  ( 0.9745511491811744698, -37.32887948083614305, 21.15859207114736407 ) ) ;
#44193=CARTESIAN_POINT ( 'NONE',  ( 5.960721111146673579, 10.26825948882901152, 17.77250458025995528 ) ) ;
#44199=LINE ( 'NONE', #15675, #51847 ) ;
#44205=ORIENTED_EDGE ( 'NONE', *, *, #43531, .F. ) ;
#44206=CARTESIAN_POINT ( 'NONE',  ( 4.960156602257182357, -20.99019478193021371, -41.40608197274659119 ) ) ;
#44213=CARTESIAN_POINT ( 'NONE',  ( 4.967162193818129623, -38.44485641567058565, -19.45289607368863116 ) ) ;
#44219=CARTESIAN_POINT ( 'NONE',  ( 0.9972139404380300221, -10.46878911444705018, 41.61281131482459728 ) ) ;
#44224=ORIENTED_EDGE ( 'NONE', *, *, #45416, .T. ) ;
#44226=CARTESIAN_POINT ( 'NONE',  ( 4.956653778116973719, 31.29546495791849736, 36.51451553856430365 ) ) ;
#44236=CARTESIAN_POINT ( 'NONE',  ( 0.5819845079324663661, -44.07435181061349994, 18.74766465427208217 ) ) ;
#44237=CARTESIAN_POINT ( 'NONE',  ( 0.5809828226811617480, 46.11980934799338883, 12.92184523170220345 ) ) ;
#44239=EDGE_CURVE ( 'NONE', #4479, #44253, #57130, .T. ) ;
#44241=CARTESIAN_POINT ( 'NONE',  ( -17.04037160131633399, -7.774647616731808597, 1.886217860945154534 ) ) ;
#44249=EDGE_CURVE ( 'NONE', #1997, #28601, #24312, .T. ) ;
#44253=VERTEX_POINT ( 'NONE', #3422 ) ;
#44256=CARTESIAN_POINT ( 'NONE',  ( 4.967162193818130511, -35.57684288741994294, 24.30453456948097823 ) ) ;
#44258=EDGE_CURVE ( 'NONE', #60259, #7019, #31085, .T. ) ;
#44259=CARTESIAN_POINT ( 'NONE',  ( 0.9747592971366240144, 5.921534893734127003, 42.49794971112893904 ) ) ;
#44300=CARTESIAN_POINT ( 'NONE',  ( 0.9722240741986378776, -20.94823706911174099, -37.44729083276446602 ) ) ;
#44303=B_SPLINE_CURVE_WITH_KNOTS ( 'NONE', 3,
 ( #27273, #3441, #41398, #26344, #45790, #22580, #41705, #36694, #55760, #55453, #17886, #36391, #59852, #12578, #31666, #60768 ),
 .UNSPECIFIED., .F., .F.,
 ( 4, 3, 3, 3, 3, 4 ),
 ( 1.551621725782133898E-17, 0.0002724568934985577696, 0.0004086836638483767317, 0.0005449104342063555619, 0.0008173270854453671070, 0.001089761613562691828 ),
 .UNSPECIFIED. ) ;
#44307=CARTESIAN_POINT ( 'NONE',  ( 5.960721111146673579, 14.50930005614996610, 14.51823969584104645 ) ) ;
#44308=CARTESIAN_POINT ( 'NONE',  ( 1.088313998177383279, 37.54798835078488395, -20.77783415101586328 ) ) ;
#44309=CARTESIAN_POINT ( 'NONE',  ( 2.526552050251861914, -12.29062829844006721, 41.18423939305560566 ) ) ;
#44315=CARTESIAN_POINT ( 'NONE',  ( 1.227938101723748288, -41.66816631169199070, 10.28900963485366127 ) ) ;
#44317=CARTESIAN_POINT ( 'NONE',  ( 0.5832366564991512403, -41.34220239953998544, 24.18352361336810574 ) ) ;
#44320=CARTESIAN_POINT ( 'NONE',  ( 0.9730545539215883499, -26.52009130076794108, 33.73144377768549163 ) ) ;
#44321=EDGE_CURVE ( 'NONE', #24670, #55943, #25090, .T. ) ;
#44324=CARTESIAN_POINT ( 'NONE',  ( 0.5807400328401637335, -24.41979442053141014, -41.20655774452994535 ) ) ;
#44327=VERTEX_POINT ( 'NONE', #26513 ) ;
#44330=CARTESIAN_POINT ( 'NONE',  ( 2.526464513654346433, 40.15570173027691681, 15.32058692775006037 ) ) ;
#44331=VERTEX_POINT ( 'NONE', #46262 ) ;
#44343=CARTESIAN_POINT ( 'NONE',  ( 2.281448460670572054, -47.71650330356583680, -4.956513608981671482 ) ) ;
#44350=CARTESIAN_POINT ( 'NONE',  ( 0.9745511491811735816, 42.49552597049459735, 5.938142320543482455 ) ) ;
#44360=EDGE_CURVE ( 'NONE', #32791, #46412, #13912, .T. ) ;
#44362=CARTESIAN_POINT ( 'NONE',  ( 0.8551540677456739292, -46.03951182599418246, -13.28067116677249615 ) ) ;
#44363=DIRECTION ( 'NONE',  ( -1.000000000000000000, -0.000000000000000000, -0.000000000000000000 ) ) ;
#44366=CARTESIAN_POINT ( 'NONE',  ( 0.9756008150404603674, -21.57722292874432668, -37.08855330282523255 ) ) ;
#44368=CARTESIAN_POINT ( 'NONE',  ( 0.5850706913938533704, 24.10530971368346442, -41.38834827854183374 ) ) ;
#44384=ADVANCED_FACE ( 'NONE', ( #6442 ), #37739, .F. ) ;
#44392=CARTESIAN_POINT ( 'NONE',  ( 2.281448460670565392, 47.95523685111403722, -1.314143534316070339 ) ) ;
#44396=CARTESIAN_POINT ( 'NONE',  ( 3.783198216974389627, -3.901161703631771172, -42.86118135813608632 ) ) ;
#44398=CARTESIAN_POINT ( 'NONE',  ( 4.967162193818130511, 36.06913038482831979, -23.56777426397140118 ) ) ;
#44399=CARTESIAN_POINT ( 'NONE',  ( 0.9972139404380317984, 41.27214627875024888, -11.74016833743876731 ) ) ;
#44400=B_SPLINE_CURVE_WITH_KNOTS ( 'NONE', 3,
 ( #46451, #37059, #17942, #13238 ),
 .UNSPECIFIED., .F., .F.,
 ( 4, 4 ),
 ( 0.000000000000000000, 0.004444878191957685187 ),
 .UNSPECIFIED. ) ;
#44401=CARTESIAN_POINT ( 'NONE',  ( 3.270143674763207553, 2.058141141425795073, -13.53222904135351889 ) ) ;
#44405=CARTESIAN_POINT ( 'NONE',  ( 4.967162193818130511, 0.000000000000000000, 0.000000000000000000 ) ) ;
#44407=VERTEX_POINT ( 'NONE', #40333 ) ;
#44413=CARTESIAN_POINT ( 'NONE',  ( 3.407937589446178528, -13.51415833181189718, 2.242416846335549607 ) ) ;
#44425=CIRCLE ( 'NONE', #41424, 43.08621763946400307 ) ;
#44427=CARTESIAN_POINT ( 'NONE',  ( 2.624215991343620935, 47.98682984381861161, -1.411420423865646034 ) ) ;
#44431=ORIENTED_EDGE ( 'NONE', *, *, #202, .T. ) ;
#44432=CARTESIAN_POINT ( 'NONE',  ( 1.154321713695927398, -33.53917066545405845, -26.77578845938217711 ) ) ;
#44450=EDGE_CURVE ( 'NONE', #47109, #22114, #30294, .T. ) ;
#44453=CARTESIAN_POINT ( 'NONE',  ( 0.5834872094924171693, 6.026535573894117981, 47.51530820063769056 ) ) ;
#44459=ORIENTED_EDGE ( 'NONE', *, *, #28056, .T. ) ;
#44461=CARTESIAN_POINT ( 'NONE',  ( 1.088313998177381281, -42.90642884828984194, -0.7798619649925772057 ) ) ;
#44470=CARTESIAN_POINT ( 'NONE',  ( 4.967162193818130511, 43.02067033766018511, 2.375726030842731706 ) ) ;
#44473=CARTESIAN_POINT ( 'NONE',  ( 2.281351352603294913, -47.71649595778612252, 4.956540261593589847 ) ) ;
#44476=B_SPLINE_CURVE_WITH_KNOTS ( 'NONE', 3,
 ( #16006, #59506, #34189, #48576 ),
 .UNSPECIFIED., .F., .F.,
 ( 4, 4 ),
 ( 8.673617379884035472E-19, 0.004048833967417089959 ),
 .UNSPECIFIED. ) ;
#44482=CARTESIAN_POINT ( 'NONE',  ( 0.5827359174754822568, -23.63273677570887799, -41.65957726278062268 ) ) ;
#44484=CARTESIAN_POINT ( 'NONE',  ( 3.270143674763207553, -3.277085381513020756, -13.28976595685396944 ) ) ;
#44493=CARTESIAN_POINT ( 'NONE',  ( 5.860006189529246790, -36.27483683749458976, 31.78942168514550204 ) ) ;
#44499=CARTESIAN_POINT ( 'NONE',  ( 1.154321713695928731, -41.23280394713385277, -11.90271797554057542 ) ) ;
#44501=CARTESIAN_POINT ( 'NONE',  ( 3.783278058412225864, -40.39104487792931764, -14.86148287637775844 ) ) ;
#44503=ORIENTED_EDGE ( 'NONE', *, *, #5112, .T. ) ;
#44505=ORIENTED_EDGE ( 'NONE', *, *, #59677, .T. ) ;
#44511=CARTESIAN_POINT ( 'NONE',  ( 3.270143674763207553, -6.605065939546904019, 11.98875605389977395 ) ) ;
#44513=DIRECTION ( 'NONE',  ( -0.07439287786467650709, 0.3937848822959368333, 0.9161872986448712508 ) ) ;
#44519=CARTESIAN_POINT ( 'NONE',  ( 1.227938101723757836, 39.96870412324336996, 15.63977281655856366 ) ) ;
#44526=LINE ( 'NONE', #39511, #7761 ) ;
#44527=CARTESIAN_POINT ( 'NONE',  ( 0.5832367798473370168, -44.35360901387662125, 18.07699868820174771 ) ) ;
#44530=CARTESIAN_POINT ( 'NONE',  ( 0.8557997880470697982, 47.37054680076715840, -7.156447707085226817 ) ) ;
#44538=CARTESIAN_POINT ( 'NONE',  ( -18.52118801082394839, -12.33374936220940477, 2.032088317440561731 ) ) ;
#44545=B_SPLINE_CURVE_WITH_KNOTS ( 'NONE', 3,
 ( #44979, #40287, #29925, #59651, #59339, #44366, #54631, #26149, #35573, #49962, #45285, #2326, #21451, #40590, #13611, #41821, #51798, #7642, #13301 ),
 .UNSPECIFIED., .F., .F.,
 ( 4, 3, 3, 3, 3, 3, 4 ),
 ( 3.469446951953614189E-18, 0.0002724573126191772734, 0.0004086839781548497782, 0.0005449106435901813778, 0.0006811373090491465790, 0.0008459866663933634113, 0.001010840725717218353 ),
 .UNSPECIFIED. ) ;
#44548=DIRECTION ( 'NONE',  ( 0.000000000000000000, 0.000000000000000000, 1.000000000000000000 ) ) ;
#44550=CARTESIAN_POINT ( 'NONE',  ( -17.83428622022626087, -7.719455939378113030, 2.099999999999994316 ) ) ;
#44556=CARTESIAN_POINT ( 'NONE',  ( 0.9730545539215883499, 5.099196237954877198, 42.60426903087355299 ) ) ;
#44569=ORIENTED_EDGE ( 'NONE', *, *, #5543, .F. ) ;
#44574=ORIENTED_EDGE ( 'NONE', *, *, #57561, .F. ) ;
#44576=CARTESIAN_POINT ( 'NONE',  ( 3.783278058412224976, -18.05212641201942247, -39.06943705276849954 ) ) ;
#44577=ORIENTED_EDGE ( 'NONE', *, *, #6875, .T. ) ;
#44578=LINE ( 'NONE', #20143, #30711 ) ;
#44579=( BOUNDED_SURFACE ( )  B_SPLINE_SURFACE ( 3, 1, ( 
 ( #52974, #10077 ),
 ( #657, #17786 ),
 ( #51277, #27481 ),
 ( #46302, #50361 ) ),
 .UNSPECIFIED., .F., .F., .F. ) 
 B_SPLINE_SURFACE_WITH_KNOTS ( ( 4, 4 ),
 ( 2, 2 ),
 ( 0.000000000000000000, 1.000000000000000000 ),
 ( 0.000000000000000000, 1.000000000000000000 ),
 .UNSPECIFIED. ) 
 GEOMETRIC_REPRESENTATION_ITEM ( )  RATIONAL_B_SPLINE_SURFACE ( (
 ( 1.000000000000000000, 1.000000000000000000),
 ( 0.9953390228620291325, 0.8624445117760984880),
 ( 0.9953390228620291325, 0.8624445117760984880),
 ( 1.000000000000000000, 1.000000000000000000) ) ) 
 REPRESENTATION_ITEM ( '' )  SURFACE ( )  );
#44586=CARTESIAN_POINT ( 'NONE',  ( 5.959547316686252039, 16.28624005235082350, 12.49238070347981910 ) ) ;
#44589=ORIENTED_EDGE ( 'NONE', *, *, #19455, .F. ) ;
#44590=CARTESIAN_POINT ( 'NONE',  ( 0.7057020205114953315, -37.48480537461314555, -29.82342581815244742 ) ) ;
#44595=VERTEX_POINT ( 'NONE', #38717 ) ;
#44596=CARTESIAN_POINT ( 'NONE',  ( 2.526464513654347321, 42.75268905308553968, 4.405490210168531817 ) ) ;
#44598=CARTESIAN_POINT ( 'NONE',  ( 4.967162193818130511, 2.375726030843182457, -43.02067033766016380 ) ) ;
#44600=EDGE_LOOP ( 'NONE', ( #17147, #51757, #41189, #8738 ) ) ;
#44602=CARTESIAN_POINT ( 'NONE',  ( 0.8551540677456834771, -38.56334384152411587, -28.44084013485158735 ) ) ;
#44605=EDGE_CURVE ( 'NONE', #12545, #3716, #10188, .T. ) ;
#44617=CARTESIAN_POINT ( 'NONE',  ( 0.5836750258453343720, -41.56963612796205609, 23.79054009282533144 ) ) ;
#44621=LINE ( 'NONE', #11400, #53229 ) ;
#44622=DIRECTION ( 'NONE',  ( 0.000000000000000000, 0.000000000000000000, 1.000000000000000000 ) ) ;
#44633=CARTESIAN_POINT ( 'NONE',  ( 4.956653778116992370, 26.26162724282429650, -40.28700667097652399 ) ) ;
#44635=EDGE_CURVE ( 'NONE', #9930, #42917, #36992, .T. ) ;
#44640=CARTESIAN_POINT ( 'NONE',  ( 0.8551540677456715978, 29.88829867897868553, -37.45266983663464089 ) ) ;
#44651=ORIENTED_EDGE ( 'NONE', *, *, #28499, .F. ) ;
#44655=CARTESIAN_POINT ( 'NONE',  ( 0.5832367798473397924, 44.35360901387671362, -18.07699868820141376 ) ) ;
#44658=CARTESIAN_POINT ( 'NONE',  ( 0.5839254288179557273, 12.48406597209104696, -46.24038938821421851 ) ) ;
#44660=VERTEX_POINT ( 'NONE', #1372 ) ;
#44661=FACE_OUTER_BOUND ( 'NONE', #45218, .T. ) ;
#44663=EDGE_CURVE ( 'NONE', #9163, #47555, #15509, .T. ) ;
#44667=CARTESIAN_POINT ( 'NONE',  ( 0.7057020205115001055, -46.47981817772235047, 11.58334423512220823 ) ) ;
#44668=CARTESIAN_POINT ( 'NONE',  ( 0.6846871229502932144, -5.395516691086876371, -47.60345020167356012 ) ) ;
#44671=CARTESIAN_POINT ( 'NONE',  ( 4.303969348037246512, -43.57722561725945098, -20.38638383586165759 ) ) ;
#44684=VECTOR ( 'NONE', #50646, 1000.000000000000114 ) ;
#44689=VECTOR ( 'NONE', #5555, 1000.000000000000114 ) ;
#44694=B_SPLINE_CURVE_WITH_KNOTS ( 'NONE', 3,
 ( #61597, #8996, #27181, #17790, #36917, #41924 ),
 .UNSPECIFIED., .F., .F.,
 ( 4, 2, 4 ),
 ( 0.000000000000000000, 0.0002291966416970798916, 0.0004583932833941597833 ),
 .UNSPECIFIED. ) ;
#44695=CARTESIAN_POINT ( 'NONE',  ( 1.227938101723748288, -42.65467462194921922, 4.762198645644287076 ) ) ;
#44697=CARTESIAN_POINT ( 'NONE',  ( 2.281448460670572942, -7.562315317391437475, -47.37344300043620393 ) ) ;
#44699=B_SPLINE_CURVE_WITH_KNOTS ( 'NONE', 3,
 ( #11572, #7772, #41325, #26896, #60381, #21577 ),
 .UNSPECIFIED., .F., .F.,
 ( 4, 2, 4 ),
 ( 1.138360651264128102E-17, 0.0002291978881530160788, 0.0004583957763060207734 ),
 .UNSPECIFIED. ) ;
#44710=ORIENTED_EDGE ( 'NONE', *, *, #46344, .T. ) ;
#44712=FACE_OUTER_BOUND ( 'NONE', #3466, .T. ) ;
#44713=EDGE_CURVE ( 'NONE', #1001, #58998, #55575, .T. ) ;
#44715=ORIENTED_EDGE ( 'NONE', *, *, #2945, .T. ) ;
#44720=CARTESIAN_POINT ( 'NONE',  ( 4.303969348037258058, -16.39840148505124162, 45.22910199346969762 ) ) ;
#44728=ORIENTED_EDGE ( 'NONE', *, *, #54437, .F. ) ;
#44730=CARTESIAN_POINT ( 'NONE',  ( 5.860006189529246790, 15.48781697582048089, 45.67886430272036336 ) ) ;
#44735=CARTESIAN_POINT ( 'NONE',  ( 0.8557997880470690211, 19.17299735372009550, 43.90420959842187187 ) ) ;
#44736=CARTESIAN_POINT ( 'NONE',  ( 0.5827357941260209451, 41.29633147056645726, -24.26189667804958461 ) ) ;
#44739=VERTEX_POINT ( 'NONE', #28505 ) ;
#44745=CARTESIAN_POINT ( 'NONE',  ( 0.8551540677456715978, 34.52115452272975205, -33.23105123575864184 ) ) ;
#44747=CARTESIAN_POINT ( 'NONE',  ( 1.154321485836934169, 26.77578840293035611, 33.53917069757662972 ) ) ;
#44754=EDGE_CURVE ( 'NONE', #2809, #30005, #59350, .T. ) ;
#44755=VERTEX_POINT ( 'NONE', #4677 ) ;
#44759=CARTESIAN_POINT ( 'NONE',  ( 0.5839254288179546171, 18.24509008251478193, 44.28478521851629068 ) ) ;
#44765=CARTESIAN_POINT ( 'NONE',  ( 0.5809828226811617480, -47.89273459658653564, -0.5448590168537535972 ) ) ;
#44766=ORIENTED_EDGE ( 'NONE', *, *, #14661, .F. ) ;
#44774=DIRECTION ( 'NONE',  ( 1.000000000000000000, -0.000000000000000000, -0.000000000000000000 ) ) ;
#44776=B_SPLINE_CURVE_WITH_KNOTS ( 'NONE', 3,
 ( #45646, #8028, #55940, #17745 ),
 .UNSPECIFIED., .F., .F.,
 ( 4, 4 ),
 ( 0.000000000000000000, 0.004446090762761359047 ),
 .UNSPECIFIED. ) ;
#44777=CARTESIAN_POINT ( 'NONE',  ( 5.960721111146673579, -19.82454228767749527, 5.318514366754590661 ) ) ;
#44778=( BOUNDED_SURFACE ( )  B_SPLINE_SURFACE ( 3, 1, ( 
 ( #42625, #22894 ),
 ( #23196, #19134 ),
 ( #12893, #18819 ),
 ( #17894, #51373 ) ),
 .UNSPECIFIED., .F., .F., .F. ) 
 B_SPLINE_SURFACE_WITH_KNOTS ( ( 4, 4 ),
 ( 2, 2 ),
 ( 0.000000000000000000, 1.000000000000000000 ),
 ( 0.000000000000000000, 1.000000000000000000 ),
 .UNSPECIFIED. ) 
 GEOMETRIC_REPRESENTATION_ITEM ( )  RATIONAL_B_SPLINE_SURFACE ( (
 ( 1.000000000000000000, 1.000000000000000000),
 ( 0.7269869731126821222, 0.9931720237060910339),
 ( 0.7269869731126821222, 0.9931720237060910339),
 ( 1.000000000000000000, 1.000000000000000000) ) ) 
 REPRESENTATION_ITEM ( '' )  SURFACE ( )  );
#44782=CARTESIAN_POINT ( 'NONE',  ( 0.5786265663353196143, 47.89572889566445468, 0.7221568112308146548 ) ) ;
#44785=VECTOR ( 'NONE', #27606, 1000.000000000000000 ) ;
#44790=CARTESIAN_POINT ( 'NONE',  ( 5.958863334805807099, -20.52565293643016275, -0.001220270596097471809 ) ) ;
#44799=CARTESIAN_POINT ( 'NONE',  ( 5.860006189529246790, -47.30964106197865249, 9.393028332204574227 ) ) ;
#44805=LINE ( 'NONE', #15971, #56296 ) ;
#44822=CARTESIAN_POINT ( 'NONE',  ( 0.5850706913938534814, -12.22095376872069394, 46.31100969101484566 ) ) ;
#44837=ORIENTED_EDGE ( 'NONE', *, *, #58896, .T. ) ;
#44841=ORIENTED_EDGE ( 'NONE', *, *, #19420, .T. ) ;
#44848=DIRECTION ( 'NONE',  ( -1.000000000000000000, -0.000000000000000000, -0.000000000000000000 ) ) ;
#44849=ORIENTED_EDGE ( 'NONE', *, *, #19122, .F. ) ;
#44852=AXIS2_PLACEMENT_3D ( 'NONE', #3263, #36830, #36512 ) ;
#44860=CARTESIAN_POINT ( 'NONE',  ( 5.981074661064941900, -17.77058762078870657, -10.26976685693816727 ) ) ;
#44868=EDGE_CURVE ( 'NONE', #61570, #50538, #27972, .T. ) ;
#44882=CARTESIAN_POINT ( 'NONE',  ( 5.960221823109900008, 16.28072933292548186, -12.49951306783072624 ) ) ;
#44883=VERTEX_POINT ( 'NONE', #48252 ) ;
#44885=CARTESIAN_POINT ( 'NONE',  ( 0.5850706913938533704, -47.50996714391786924, 6.071602062250445186 ) ) ;
#44890=ADVANCED_FACE ( 'NONE', ( #20063 ), #5296, .F. ) ;
#44891=ORIENTED_EDGE ( 'NONE', *, *, #33249, .T. ) ;
#44894=VERTEX_POINT ( 'NONE', #38872 ) ;
#44902=CARTESIAN_POINT ( 'NONE',  ( 0.5850706913938533704, 33.99603398296638090, -33.73916126769415769 ) ) ;
#44904=LINE ( 'NONE', #21065, #11632 ) ;
#44905=VERTEX_POINT ( 'NONE', #43566 ) ;
#44909=EDGE_CURVE ( 'NONE', #50007, #21001, #42203, .T. ) ;
#44912=CARTESIAN_POINT ( 'NONE',  ( 3.783198216974394068, -24.80909581868418101, -35.16829104054195909 ) ) ;
#44916=ORIENTED_EDGE ( 'NONE', *, *, #16319, .F. ) ;
#44918=CARTESIAN_POINT ( 'NONE',  ( 5.981074661064941900, -19.82308078259087480, -5.320466518160866798 ) ) ;
#44926=CARTESIAN_POINT ( 'NONE',  ( 3.407937589446178528, 13.51415833181191317, -2.242416846335461234 ) ) ;
#44933=CARTESIAN_POINT ( 'NONE',  ( 1.227938101723756947, 4.762198645645047357, -42.65467462194912684 ) ) ;
#44935=CARTESIAN_POINT ( 'NONE',  ( 5.974727161628369032, -18.95664195401511876, -7.868887636447555067 ) ) ;
#44937=EDGE_CURVE ( 'NONE', #26085, #10602, #1763, .T. ) ;
#44947=ORIENTED_EDGE ( 'NONE', *, *, #54835, .F. ) ;
#44964=ORIENTED_EDGE ( 'NONE', *, *, #12647, .T. ) ;
#44965=ORIENTED_EDGE ( 'NONE', *, *, #1698, .T. ) ;
#44973=CARTESIAN_POINT ( 'NONE',  ( 0.5832367798473380160, 12.65931911325669113, -46.19266341874884318 ) ) ;
#44974=B_SPLINE_CURVE_WITH_KNOTS ( 'NONE', 3,
 ( #5759, #59323, #10189, #29286, #5457, #43731 ),
 .UNSPECIFIED., .F., .F.,
 ( 4, 2, 4 ),
 ( 1.738108305489988542E-18, 0.0002291966416970807861, 0.0004583932833941598375 ),
 .UNSPECIFIED. ) ;
#44979=CARTESIAN_POINT ( 'NONE',  ( 0.9730545539215883499, -21.89037132892409687, -36.90443313492354349 ) ) ;
#44982=CARTESIAN_POINT ( 'NONE',  ( 5.959547316686252039, -10.26589671991375674, 17.77392908783916070 ) ) ;
#44984=ORIENTED_EDGE ( 'NONE', *, *, #6121, .T. ) ;
#44988=VERTEX_POINT ( 'NONE', #54147 ) ;
#44996=CARTESIAN_POINT ( 'NONE',  ( 0.9730545539215883499, 34.34678117142591702, -25.71816799638743944 ) ) ;
#45001=DIRECTION ( 'NONE',  ( 0.000000000000000000, 0.000000000000000000, 1.000000000000000000 ) ) ;
#45004=CARTESIAN_POINT ( 'NONE',  ( 2.526552050251864134, 42.43615142762125458, 6.809858322089185734 ) ) ;
#45019=CARTESIAN_POINT ( 'NONE',  ( 0.8557997880470606944, -11.51622788066425684, -46.50333260518571876 ) ) ;
#45022=FACE_OUTER_BOUND ( 'NONE', #9198, .T. ) ;
#45036=EDGE_CURVE ( 'NONE', #9174, #18062, #11908, .T. ) ;
#45039=DIRECTION ( 'NONE',  ( -1.000000000000000000, -0.000000000000000000, -0.000000000000000000 ) ) ;
#45044=CARTESIAN_POINT ( 'NONE',  ( 5.960721111146673579, -5.306302591836445259, -19.82781442290496443 ) ) ;
#45050=CARTESIAN_POINT ( 'NONE',  ( 0.9730545539215883499, 16.88610103448612065, -39.44597740938043273 ) ) ;
#45052=ORIENTED_EDGE ( 'NONE', *, *, #23406, .F. ) ;
#45053=CARTESIAN_POINT ( 'NONE',  ( 0.8551540677456739292, 19.17641535420911936, -43.91216198251520808 ) ) ;
#45059=CARTESIAN_POINT ( 'NONE',  ( 0.5786265663353196143, 13.09387673186399859, -46.07681357296471703 ) ) ;
#45069=LINE ( 'NONE', #50343, #58625 ) ;
#45073=ORIENTED_EDGE ( 'NONE', *, *, #40870, .F. ) ;
#45087=CARTESIAN_POINT ( 'NONE',  ( 5.974727161628367256, -18.96851388233653068, -7.840226266082476414 ) ) ;
#45091=CARTESIAN_POINT ( 'NONE',  ( 0.9752570700956794125, -39.72995844664867349, 16.20701641182904851 ) ) ;
#45101=AXIS2_PLACEMENT_3D ( 'NONE', #37063, #55510, #26707 ) ;
#45105=B_SPLINE_CURVE_WITH_KNOTS ( 'NONE', 3,
 ( #50626, #7085, #7715, #54389 ),
 .UNSPECIFIED., .F., .F.,
 ( 4, 4 ),
 ( 3.469446951953614189E-18, 0.004050076154993004218 ),
 .UNSPECIFIED. ) ;
#45106=CARTESIAN_POINT ( 'NONE',  ( 0.9757892942422810023, -39.66188497122482204, -16.37293303864347394 ) ) ;
#45111=CARTESIAN_POINT ( 'NONE',  ( 0.9741495583595168872, 16.78504838919937825, -39.48917442789103660 ) ) ;
#45112=EDGE_CURVE ( 'NONE', #39282, #44660, #45160, .T. ) ;
#45124=CARTESIAN_POINT ( 'NONE',  ( 0.8551540677456739292, -34.52115452272951757, 33.23105123575888342 ) ) ;
#45130=( BOUNDED_SURFACE ( )  B_SPLINE_SURFACE ( 3, 1, ( 
 ( #41760, #27632 ),
 ( #3495, #61426 ),
 ( #52044, #32970 ),
 ( #7904, #28242 ) ),
 .UNSPECIFIED., .F., .F., .F. ) 
 B_SPLINE_SURFACE_WITH_KNOTS ( ( 4, 4 ),
 ( 2, 2 ),
 ( 0.000000000000000000, 1.000000000000000000 ),
 ( 0.000000000000000000, 1.000000000000000000 ),
 .UNSPECIFIED. ) 
 GEOMETRIC_REPRESENTATION_ITEM ( )  RATIONAL_B_SPLINE_SURFACE ( (
 ( 1.000000000000000000, 1.000000000000000000),
 ( 0.9953390228620291325, 0.8624445117760984880),
 ( 0.9953390228620291325, 0.8624445117760984880),
 ( 1.000000000000000000, 1.000000000000000000) ) ) 
 REPRESENTATION_ITEM ( '' )  SURFACE ( )  );
#45139=EDGE_CURVE ( 'NONE', #28235, #1532, #3945, .T. ) ;
#45145=ORIENTED_EDGE ( 'NONE', *, *, #6139, .F. ) ;
#45149=CARTESIAN_POINT ( 'NONE',  ( 5.965394784446458765, 17.76824826579354877, -10.27521535480968140 ) ) ;
#45153=DIRECTION ( 'NONE',  ( -0.07836865515943411409, 0.9608836331491580340, -0.2656332009267214356 ) ) ;
#45160=B_SPLINE_CURVE_WITH_KNOTS ( 'NONE', 3,
 ( #11584, #30989, #50096, #16908, #13431, #61621 ),
 .UNSPECIFIED., .F., .F.,
 ( 4, 2, 4 ),
 ( 1.738108305489988542E-18, 0.0002291966416970796477, 0.0004583932833941575607 ),
 .UNSPECIFIED. ) ;
#45163=DIRECTION ( 'NONE',  ( 0.000000000000000000, 0.000000000000000000, 1.000000000000000000 ) ) ;
#45171=CARTESIAN_POINT ( 'NONE',  ( 0.9757892942422824456, 37.13414688883494108, -21.49867881049906870 ) ) ;
#45173=CARTESIAN_POINT ( 'NONE',  ( 0.9730545539215883499, -37.40983423658487794, 21.01499094264535472 ) ) ;
#45180=B_SPLINE_CURVE_WITH_KNOTS ( 'NONE', 3,
 ( #57797, #24304, #18691, #33725 ),
 .UNSPECIFIED., .F., .F.,
 ( 4, 4 ),
 ( 0.000000000000000000, 0.005004741218457404127 ),
 .UNSPECIFIED. ) ;
#45182=CARTESIAN_POINT ( 'NONE',  ( 0.5827359174754830340, 46.16863801597762773, 12.74690115177623717 ) ) ;
#45183=DIRECTION ( 'NONE',  ( -1.000000000000000000, -0.000000000000000000, -0.000000000000000000 ) ) ;
#45192=CARTESIAN_POINT ( 'NONE',  ( 4.967162193818130511, 0.000000000000000000, 0.000000000000000000 ) ) ;
#45196=CARTESIAN_POINT ( 'NONE',  ( 5.958863334805807099, 20.34989385289157582, -2.680345151634403233 ) ) ;
#45199=CARTESIAN_POINT ( 'NONE',  ( 0.9757787079277442377, -5.639827755376935592, 42.53619983261575754 ) ) ;
#45201=CARTESIAN_POINT ( 'NONE',  ( 0.5807400328401637335, 5.711437504335951765, 47.55718917606844798 ) ) ;
#45209=CARTESIAN_POINT ( 'NONE',  ( 0.5850706913938534814, 33.73916126769498192, -33.99603398296554957 ) ) ;
#45214=CARTESIAN_POINT ( 'NONE',  ( 4.956653778116991482, -9.917440902360828758, -47.05699031914960528 ) ) ;
#45218=EDGE_LOOP ( 'NONE', ( #32889, #6508, #29667, #21526 ) ) ;
#45219=CARTESIAN_POINT ( 'NONE',  ( 5.965394784446458765, -17.78272165951794292, -10.25014670152108742 ) ) ;
#45222=CARTESIAN_POINT ( 'NONE',  ( 3.783198216974387851, 1.726720072276576978, -43.00370179234475643 ) ) ;
#45223=CARTESIAN_POINT ( 'NONE',  ( 0.6067375320500753011, 29.71715680108788149, -37.56348932307230370 ) ) ;
#45224=( BOUNDED_SURFACE ( )  B_SPLINE_SURFACE ( 3, 1, ( 
 ( #13056, #32455 ),
 ( #32150, #27134 ),
 ( #13356, #60315 ),
 ( #20974, #8021 ) ),
 .UNSPECIFIED., .F., .F., .F. ) 
 B_SPLINE_SURFACE_WITH_KNOTS ( ( 4, 4 ),
 ( 2, 2 ),
 ( 0.000000000000000000, 1.000000000000000000 ),
 ( 0.000000000000000000, 1.000000000000000000 ),
 .UNSPECIFIED. ) 
 GEOMETRIC_REPRESENTATION_ITEM ( )  RATIONAL_B_SPLINE_SURFACE ( (
 ( 1.000000000000000000, 1.000000000000000000),
 ( 0.9953390228620291325, 0.8624445117760984880),
 ( 0.9953390228620291325, 0.8624445117760984880),
 ( 1.000000000000000000, 1.000000000000000000) ) ) 
 REPRESENTATION_ITEM ( '' )  SURFACE ( )  );
#45228=CARTESIAN_POINT ( 'NONE',  ( 2.624215991343620935, 46.71702075422651745, 11.05657803851061693 ) ) ;
#45229=EDGE_CURVE ( 'NONE', #10490, #61767, #18285, .T. ) ;
#45233=CARTESIAN_POINT ( 'NONE',  ( 0.9730545539215883499, 21.89037132892435622, 36.90443313492338717 ) ) ;
#45245=CARTESIAN_POINT ( 'NONE',  ( 0.5807400328401574052, 6.791881299636263414, -47.41494605191436307 ) ) ;
#45249=CARTESIAN_POINT ( 'NONE',  ( 5.959828726073459926, 10.25888482581834893, 17.77796293532176719 ) ) ;
#45250=DIRECTION ( 'NONE',  ( -0.000000000000000000, 1.000000000000000000, -0.000000000000000000 ) ) ;
#45266=VERTEX_POINT ( 'NONE', #29063 ) ;
#45272=EDGE_LOOP ( 'NONE', ( #13482, #13727, #32704, #41181, #26228, #45889 ) ) ;
#45279=CARTESIAN_POINT ( 'NONE',  ( 0.5819845901640485764, 12.83441129068598308, -46.14435291605016687 ) ) ;
#45281=CARTESIAN_POINT ( 'NONE',  ( 0.9757402383260939116, -30.28078671294506563, -30.40085236181982253 ) ) ;
#45283=EDGE_CURVE ( 'NONE', #18653, #24624, #31702, .T. ) ;
#45285=CARTESIAN_POINT ( 'NONE',  ( 0.9757402383260949108, -21.38067434779554432, -37.20221273948030927 ) ) ;
#45299=CARTESIAN_POINT ( 'NONE',  ( 0.9756008150404595902, 42.90824081423206593, -0.1421465480004359683 ) ) ;
#45300=CARTESIAN_POINT ( 'NONE',  ( 0.8557997880470697982, -47.60865952216995822, -5.347802024197736870 ) ) ;
#45302=LINE ( 'NONE', #56129, #13862 ) ;
#45303=CARTESIAN_POINT ( 'NONE',  ( 0.5834872094924165031, 37.85980081020222343, 29.33699246747713119 ) ) ;
#45307=FACE_OUTER_BOUND ( 'NONE', #49464, .T. ) ;
#45308=CARTESIAN_POINT ( 'NONE',  ( 0.9968887458511649369, -17.02616470386906755, 39.38692798189856603 ) ) ;
#45315=B_SPLINE_CURVE_WITH_KNOTS ( 'NONE', 3,
 ( #7805, #35732, #36350, #31314 ),
 .UNSPECIFIED., .F., .F.,
 ( 4, 4 ),
 ( 0.000000000000000000, 0.004446090762761383333 ),
 .UNSPECIFIED. ) ;
#45319=B_SPLINE_CURVE_WITH_KNOTS ( 'NONE', 3,
 ( #41635, #28130, #31602, #3685 ),
 .UNSPECIFIED., .F., .F.,
 ( 4, 4 ),
 ( 0.000000000000000000, 0.005004741218457404127 ),
 .UNSPECIFIED. ) ;
#45324=ORIENTED_EDGE ( 'NONE', *, *, #31678, .F. ) ;
#45326=DIRECTION ( 'NONE',  ( -1.000000000000000000, -0.000000000000000000, -0.000000000000000000 ) ) ;
#45327=CARTESIAN_POINT ( 'NONE',  ( 3.783198216974389627, -1.726720072276277218, 43.00370179234475643 ) ) ;
#45329=CARTESIAN_POINT ( 'NONE',  ( 0.5850706913938533704, -12.22095376872004202, -46.31100969101499487 ) ) ;
#45334=EDGE_CURVE ( 'NONE', #11680, #48862, #40964, .T. ) ;
#45338=VERTEX_POINT ( 'NONE', #35320 ) ;
#45339=VERTEX_POINT ( 'NONE', #1455 ) ;
#45340=CARTESIAN_POINT ( 'NONE',  ( 0.6846871229502932144, -0.8641397935262891128, 47.90045233486063836 ) ) ;
#45344=CARTESIAN_POINT ( 'NONE',  ( 0.9741495583595175534, 41.54695848110013401, -10.72301204857613222 ) ) ;
#45350=CARTESIAN_POINT ( 'NONE',  ( 5.974727161628369032, 12.50710176110007588, -16.27409205901363265 ) ) ;
#45351=CARTESIAN_POINT ( 'NONE',  ( 0.5832367798473389042, 41.61463593465337851, -23.71165515427673043 ) ) ;
#45360=CARTESIAN_POINT ( 'NONE',  ( 0.8551540677456715978, 13.28067116677266846, -46.03951182599413272 ) ) ;
#45369=LINE ( 'NONE', #21537, #6608 ) ;
#45377=LINE ( 'NONE', #16541, #22953 ) ;
#45381=CARTESIAN_POINT ( 'NONE',  ( 4.303969348037258058, 8.413118729224057901, 47.36875205922775933 ) ) ;
#45383=VERTEX_POINT ( 'NONE', #2696 ) ;
#45388=CARTESIAN_POINT ( 'NONE',  ( 4.963659409799324962, -42.22332985082299928, -14.83726297270324856 ) ) ;
#45394=CARTESIAN_POINT ( 'NONE',  ( 5.958863334805807099, -2.680345151634473400, -20.34989385289156871 ) ) ;
#45396=CARTESIAN_POINT ( 'NONE',  ( 0.8557997880470697982, 47.37054680076715840, -7.156447707085226817 ) ) ;
#45398=CARTESIAN_POINT ( 'NONE',  ( 0.5809828226811553087, -24.41822904836894637, -41.20389530892332886 ) ) ;
#45402=ORIENTED_EDGE ( 'NONE', *, *, #25635, .T. ) ;
#45404=CARTESIAN_POINT ( 'NONE',  ( 0.7762777257811903642, 5.369627942761623807, 47.60264404062380095 ) ) ;
#45405=CARTESIAN_POINT ( 'NONE',  ( 0.9756008150404600343, -26.23365443298895272, -33.95486284030252477 ) ) ;
#45406=CARTESIAN_POINT ( 'NONE',  ( 0.8557997880470697982, 28.43566216845025352, -38.55640757422408882 ) ) ;
#45411=CARTESIAN_POINT ( 'NONE',  ( 4.960156602257182357, -46.35381625054458254, 2.524999074837397828 ) ) ;
#45416=EDGE_CURVE ( 'NONE', #27464, #28142, #50021, .T. ) ;
#45427=ORIENTED_EDGE ( 'NONE', *, *, #44635, .T. ) ;
#45430=ORIENTED_EDGE ( 'NONE', *, *, #34604, .F. ) ;
#45431=CARTESIAN_POINT ( 'NONE',  ( 0.5827359174754834781, -37.77623182210375319, -29.44457394064658828 ) ) ;
#45434=EDGE_LOOP ( 'NONE', ( #4782, #43267, #35580, #19533 ) ) ;
#45436=CARTESIAN_POINT ( 'NONE',  ( 0.7057020205115018818, 43.92641219669830832, 19.10543569325809798 ) ) ;
#45441=CARTESIAN_POINT ( 'NONE',  ( 4.963659409799330291, -36.94443854030240004, 25.25989740981486165 ) ) ;
#45442=CARTESIAN_POINT ( 'NONE',  ( 5.860006189529246790, -3.171667470662847599, 48.12869875779307449 ) ) ;
#45443=CARTESIAN_POINT ( 'NONE',  ( 0.5827359174754803695, -44.38786494726110732, 17.99288944686878722 ) ) ;
#45460=CARTESIAN_POINT ( 'NONE',  ( 0.9757402383260946888, -34.09320464257829286, 26.05362288587352637 ) ) ;
#45461=EDGE_CURVE ( 'NONE', #23080, #12149, #21271, .T. ) ;
#45463=CARTESIAN_POINT ( 'NONE',  ( 5.959828726073459926, 17.77343634131841910, -10.26672511661737452 ) ) ;
#45466=CARTESIAN_POINT ( 'NONE',  ( 0.9747592971366241255, 21.17324310849283719, -37.32069240268748445 ) ) ;
#45472=CARTESIAN_POINT ( 'NONE',  ( 3.660176727303410260, -43.62748706623509065, -20.10773453922334042 ) ) ;
#45473=B_SPLINE_CURVE_WITH_KNOTS ( 'NONE', 3,
 ( #4979, #42619, #33531, #27889 ),
 .UNSPECIFIED., .F., .F.,
 ( 4, 4 ),
 ( 6.505213034913026604E-19, 0.004048833967417085622 ),
 .UNSPECIFIED. ) ;
#45477=DIRECTION ( 'NONE',  ( 0.07439287786467665975, -0.9971416435352943308, -0.01320009283086585709 ) ) ;
#45482=CARTESIAN_POINT ( 'NONE',  ( 0.8551540677456739292, -11.51835730326447838, -46.51172240253133339 ) ) ;
#45485=( BOUNDED_SURFACE ( )  B_SPLINE_SURFACE ( 3, 1, ( 
 ( #48375, #61305 ),
 ( #41618, #22804 ),
 ( #51595, #13114 ),
 ( #18421, #37542 ) ),
 .UNSPECIFIED., .F., .F., .F. ) 
 B_SPLINE_SURFACE_WITH_KNOTS ( ( 4, 4 ),
 ( 2, 2 ),
 ( 0.000000000000000000, 1.000000000000000000 ),
 ( 0.000000000000000000, 1.000000000000000000 ),
 .UNSPECIFIED. ) 
 GEOMETRIC_REPRESENTATION_ITEM ( )  RATIONAL_B_SPLINE_SURFACE ( (
 ( 1.000000000000000000, 1.000000000000000000),
 ( 0.9953390228620291325, 0.8624445117760984880),
 ( 0.9953390228620291325, 0.8624445117760984880),
 ( 1.000000000000000000, 1.000000000000000000) ) ) 
 REPRESENTATION_ITEM ( '' )  SURFACE ( )  );
#45486=VERTEX_POINT ( 'NONE', #60319 ) ;
#45496=CARTESIAN_POINT ( 'NONE',  ( 0.9754642270333695464, -5.774842730422326653, 42.51806607596982701 ) ) ;
#45504=CARTESIAN_POINT ( 'NONE',  ( 0.9741495583595169983, 16.05424148287325892, 39.79188455996722951 ) ) ;
#45508=CARTESIAN_POINT ( 'NONE',  ( 3.407937589446174087, -10.58239600294632865, -8.699069120706878877 ) ) ;
#45511=VERTEX_POINT ( 'NONE', #28064 ) ;
#45514=CARTESIAN_POINT ( 'NONE',  ( 0.9756008150404602564, 26.23365443298915878, 33.95486284030234714 ) ) ;
#45517=VERTEX_POINT ( 'NONE', #8632 ) ;
#45534=CIRCLE ( 'NONE', #21500, 48.09070567114147110 ) ;
#45535=CARTESIAN_POINT ( 'NONE',  ( 1.088313998177381725, 4.827222641555231064, 42.64115081428565190 ) ) ;
#45543=B_SPLINE_CURVE_WITH_KNOTS ( 'NONE', 3,
 ( #8805, #54935, #27921, #35866, #9110, #18845 ),
 .UNSPECIFIED., .F., .F.,
 ( 4, 2, 4 ),
 ( 1.084202172485504314E-19, 0.0002291966416970794037, 0.0004583932833941586991 ),
 .UNSPECIFIED. ) ;
#45544=CARTESIAN_POINT ( 'NONE',  ( 5.981074661064941900, -18.95903134304784032, -7.862380442164075056 ) ) ;
#45545=CARTESIAN_POINT ( 'NONE',  ( 0.7057020205115008826, -43.92641219669816621, -19.10543569325839286 ) ) ;
#45546=CARTESIAN_POINT ( 'NONE',  ( 3.407937589446178528, 12.47329436636636935, -5.663729899984937255 ) ) ;
#45557=EDGE_CURVE ( 'NONE', #55904, #46829, #30913, .T. ) ;
#45560=CARTESIAN_POINT ( 'NONE',  ( 0.5839254288179548391, 47.89590036163257736, 0.09078831291240967161 ) ) ;
#45561=ADVANCED_FACE ( 'NONE', ( #42799 ), #12119, .F. ) ;
#45563=CARTESIAN_POINT ( 'NONE',  ( 4.956653778116975495, -9.917440902361487787, 47.05699031914946318 ) ) ;
#45568=DIRECTION ( 'NONE',  ( -1.000000000000000000, -0.000000000000000000, -0.000000000000000000 ) ) ;
#45573=CARTESIAN_POINT ( 'NONE',  ( 4.967162193818130511, -7.970725651239513709, -42.34252806656601820 ) ) ;
#45576=CARTESIAN_POINT ( 'NONE',  ( 0.5809828226811556418, 44.03860873105722362, -18.83114015454650314 ) ) ;
#45580=CONICAL_SURFACE ( 'NONE', #19556, 43.08621763946400307, 1.568696531533066763 ) ;
#45588=CARTESIAN_POINT ( 'NONE',  ( 5.959828726073459926, 2.683617577144109756, 20.34941966491240350 ) ) ;
#45590=CARTESIAN_POINT ( 'NONE',  ( 0.9968887458511644928, 36.82760690604627030, 22.02152923727763678 ) ) ;
#45591=VERTEX_POINT ( 'NONE', #38408 ) ;
#45600=EDGE_CURVE ( 'NONE', #31908, #9596, #48898, .T. ) ;
#45601=CARTESIAN_POINT ( 'NONE',  ( 0.9752132459055834479, -5.831562321021290352, -42.51031254975327300 ) ) ;
#45603=CARTESIAN_POINT ( 'NONE',  ( 0.5819845901640493535, 37.72030663501157477, 29.51612926147629778 ) ) ;
#45604=CARTESIAN_POINT ( 'NONE',  ( 0.5850706913938533704, -23.79070617305352542, -41.56998471741253098 ) ) ;
#45609=CARTESIAN_POINT ( 'NONE',  ( 2.526464513654346877, -37.81242626108682714, -20.43088802552603056 ) ) ;
#45611=CARTESIAN_POINT ( 'NONE',  ( 0.5807400328401637335, -47.55718917606846929, 5.711437504335787452 ) ) ;
#45613=CARTESIAN_POINT ( 'NONE',  ( 1.227938101723748288, 4.762198645644436290, 42.65467462194920500 ) ) ;
#45625=VERTEX_POINT ( 'NONE', #11745 ) ;
#45631=EDGE_LOOP ( 'NONE', ( #10172, #34386, #27116, #39521 ) ) ;
#45633=CARTESIAN_POINT ( 'NONE',  ( 0.7056555295713249354, -43.92642606846689546, 19.10539864320384495 ) ) ;
#45634=VECTOR ( 'NONE', #56674, 1000.000000000000114 ) ;
#45635=CARTESIAN_POINT ( 'NONE',  ( 0.8557997880470697982, -23.15977007032352475, 41.93815086860250574 ) ) ;
#45639=B_SPLINE_CURVE_WITH_KNOTS ( 'NONE', 3,
 ( #48241, #52924, #10028, #29122 ),
 .UNSPECIFIED., .F., .F.,
 ( 4, 4 ),
 ( 6.254634441385501517E-18, 0.004050076154993004218 ),
 .UNSPECIFIED. ) ;
#45644=CARTESIAN_POINT ( 'NONE',  ( 3.270143674763207553, -2.058141141425694265, 13.53222904135353311 ) ) ;
#45645=ORIENTED_EDGE ( 'NONE', *, *, #22806, .F. ) ;
#45646=CARTESIAN_POINT ( 'NONE',  ( 4.956653778116975495, -35.79382859084138602, 32.11725092155030836 ) ) ;
#45649=ORIENTED_EDGE ( 'NONE', *, *, #51749, .T. ) ;
#45651=CARTESIAN_POINT ( 'NONE',  ( 3.783278058412227640, 24.80906179324491845, -35.16831859152105721 ) ) ;
#45652=CARTESIAN_POINT ( 'NONE',  ( 5.860006189529246790, 43.26650951066899609, -21.31760477694535894 ) ) ;
#45657=B_SPLINE_CURVE_WITH_KNOTS ( 'NONE', 3,
 ( #28824, #47635, #10347, #5602 ),
 .UNSPECIFIED., .F., .F.,
 ( 4, 4 ),
 ( 6.992893892674702526E-18, 0.004050076154993007688 ),
 .UNSPECIFIED. ) ;
#45659=CARTESIAN_POINT ( 'NONE',  ( 0.9972139404380298000, -15.81078898082016337, 39.89035676513732653 ) ) ;
#45663=ORIENTED_EDGE ( 'NONE', *, *, #43504, .F. ) ;
#45667=CARTESIAN_POINT ( 'NONE',  ( 4.960156602257181468, 46.35381625054450438, 2.524999074837726010 ) ) ;
#45668=ORIENTED_EDGE ( 'NONE', *, *, #43239, .F. ) ;
#45674=( BOUNDED_SURFACE ( )  B_SPLINE_SURFACE ( 3, 1, ( 
 ( #51968, #28167 ),
 ( #9676, #47285 ),
 ( #29095, #19708 ),
 ( #23781, #38833 ) ),
 .UNSPECIFIED., .F., .F., .F. ) 
 B_SPLINE_SURFACE_WITH_KNOTS ( ( 4, 4 ),
 ( 2, 2 ),
 ( 0.000000000000000000, 1.000000000000000000 ),
 ( 0.000000000000000000, 1.000000000000000000 ),
 .UNSPECIFIED. ) 
 GEOMETRIC_REPRESENTATION_ITEM ( )  RATIONAL_B_SPLINE_SURFACE ( (
 ( 1.000000000000000000, 1.000000000000000000),
 ( 0.9953390228620291325, 0.8624445117761032620),
 ( 0.9953390228620291325, 0.8624445117761032620),
 ( 1.000000000000000000, 1.000000000000000000) ) ) 
 REPRESENTATION_ITEM ( '' )  SURFACE ( )  );
#45676=CARTESIAN_POINT ( 'NONE',  ( 4.956653778116992370, 14.93973939759951541, -45.71126949320233734 ) ) ;
#45680=CARTESIAN_POINT ( 'NONE',  ( 0.7056555295713263787, -44.57023068418414624, -17.55111680842085775 ) ) ;
#45688=CARTESIAN_POINT ( 'NONE',  ( 0.9754402186311934564, -30.20795797590421117, 30.47320128434250464 ) ) ;
#45690=CARTESIAN_POINT ( 'NONE',  ( 3.660087539127315992, 45.06758728829470328, 16.63102164621050960 ) ) ;
#45691=CARTESIAN_POINT ( 'NONE',  ( 0.6846871229502932144, 24.69859318104546375, -41.05093867799160989 ) ) ;
#45702=FACE_OUTER_BOUND ( 'NONE', #25445, .T. ) ;
#45703=CARTESIAN_POINT ( 'NONE',  ( 0.5827357941260199459, -24.26189667804973027, -41.29633147056638620 ) ) ;
#45713=VECTOR ( 'NONE', #49855, 1000.000000000000114 ) ;
#45714=CARTESIAN_POINT ( 'NONE',  ( 0.9730545539215883499, -26.52009130076748278, -33.73144377768585400 ) ) ;
#45716=AXIS2_PLACEMENT_3D ( 'NONE', #26511, #45039, #55004 ) ;
#45719=CARTESIAN_POINT ( 'NONE',  ( 5.860006189529246790, -48.13093674595587146, 3.137522369585352688 ) ) ;
#45724=ORIENTED_EDGE ( 'NONE', *, *, #10126, .T. ) ;
#45725=CARTESIAN_POINT ( 'NONE',  ( 0.5809828226811617480, 46.40184912890855884, -11.86925843957117799 ) ) ;
#45727=ORIENTED_EDGE ( 'NONE', *, *, #15136, .F. ) ;
#45734=EDGE_LOOP ( 'NONE', ( #38341, #47644, #531, #6919 ) ) ;
#45744=CARTESIAN_POINT ( 'NONE',  ( 4.963659409799330291, 37.47512675766694201, 24.46566636552837792 ) ) ;
#45747=CARTESIAN_POINT ( 'NONE',  ( 0.5836750258453351492, -44.31929073742205105, 18.16108240858330092 ) ) ;
#45762=CIRCLE ( 'NONE', #740, 43.08621763946400307 ) ;
#45768=CARTESIAN_POINT ( 'NONE',  ( 0.8551540677456715978, -41.94570365541218848, 23.16399837394531147 ) ) ;
#45777=CARTESIAN_POINT ( 'NONE',  ( 3.783198216974389183, 36.37893817280285447, 22.99723434398804400 ) ) ;
#45778=( BOUNDED_SURFACE ( )  B_SPLINE_SURFACE ( 3, 1, ( 
 ( #19385, #42282 ),
 ( #48198, #28770 ),
 ( #52256, #32562 ),
 ( #28455, #61042 ) ),
 .UNSPECIFIED., .F., .F., .F. ) 
 B_SPLINE_SURFACE_WITH_KNOTS ( ( 4, 4 ),
 ( 2, 2 ),
 ( 0.000000000000000000, 1.000000000000000000 ),
 ( 0.000000000000000000, 1.000000000000000000 ),
 .UNSPECIFIED. ) 
 GEOMETRIC_REPRESENTATION_ITEM ( )  RATIONAL_B_SPLINE_SURFACE ( (
 ( 1.000000000000000000, 1.000000000000000000),
 ( 0.9953390228620291325, 0.8624445117761032620),
 ( 0.9953390228620291325, 0.8624445117761032620),
 ( 1.000000000000000000, 1.000000000000000000) ) ) 
 REPRESENTATION_ITEM ( '' )  SURFACE ( )  );
#45780=CARTESIAN_POINT ( 'NONE',  ( 0.9757787079277446818, 37.17954582422768084, -21.42002160630781304 ) ) ;
#45785=B_SPLINE_CURVE_WITH_KNOTS ( 'NONE', 3,
 ( #24792, #48903, #25094, #43931, #971, #44237 ),
 .UNSPECIFIED., .F., .F.,
 ( 4, 2, 4 ),
 ( 1.512800854419661994E-16, 0.0002445252820015220629, 0.0004890505640028927712 ),
 .UNSPECIFIED. ) ;
#45789=CARTESIAN_POINT ( 'NONE',  ( 2.624215991343620935, 17.05978231157464364, -44.87417713512071771 ) ) ;
#45790=CARTESIAN_POINT ( 'NONE',  ( 0.5834872094924165031, -28.97678700412158648, -38.13619618345241236 ) ) ;
#45802=CARTESIAN_POINT ( 'NONE',  ( 5.981074661064941900, 12.50143471347259450, 16.27808421740030553 ) ) ;
#45803=CARTESIAN_POINT ( 'NONE',  ( 0.9754642270333693244, -41.40054989430071686, -11.27515941577618364 ) ) ;
#45808=VECTOR ( 'NONE', #55649, 1000.000000000000114 ) ;
#45812=ORIENTED_EDGE ( 'NONE', *, *, #57972, .T. ) ;
#45815=ORIENTED_EDGE ( 'NONE', *, *, #30838, .F. ) ;
#45817=CARTESIAN_POINT ( 'NONE',  ( 0.9754642270333664378, 16.25787253057936255, 39.70914670678642011 ) ) ;
#45825=CARTESIAN_POINT ( 'NONE',  ( 0.5827359174754830340, 44.10985444762183505, 18.66406616557994269 ) ) ;
#45829=CARTESIAN_POINT ( 'NONE',  ( 0.9752570700956798566, 25.93764562640103222, 34.18150842933886224 ) ) ;
#45832=CARTESIAN_POINT ( 'NONE',  ( 0.5836750258453357043, -46.21662382526645274, -12.57171936981210436 ) ) ;
#45834=CARTESIAN_POINT ( 'NONE',  ( 0.8551540677456739292, -33.23105123575875552, -34.52115452272963836 ) ) ;
#45841=CARTESIAN_POINT ( 'NONE',  ( 0.5800708057587375954, 13.00144577271105817, -46.09746469244086597 ) ) ;
#45842=EDGE_CURVE ( 'NONE', #61052, #56419, #9491, .T. ) ;
#45845=EDGE_CURVE ( 'NONE', #42917, #30001, #15173, .T. ) ;
#45852=CARTESIAN_POINT ( 'NONE',  ( 0.7762783648524380631, 0.8897020150998180554, 47.89627393592489568 ) ) ;
#45854=CARTESIAN_POINT ( 'NONE',  ( 5.959828726073459926, 5.316791119500813068, 19.82504517499715035 ) ) ;
#45857=CARTESIAN_POINT ( 'NONE',  ( 5.981074661064941900, 20.34795181394748909, -2.687517936919787687 ) ) ;
#45870=DIRECTION ( 'NONE',  ( 0.000000000000000000, 0.000000000000000000, 1.000000000000000000 ) ) ;
#45876=EDGE_CURVE ( 'NONE', #18653, #33938, #30754, .T. ) ;
#45880=CARTESIAN_POINT ( 'NONE',  ( 3.660087539127330647, -35.27260502801109965, -32.61167949558423373 ) ) ;
#45889=ORIENTED_EDGE ( 'NONE', *, *, #39489, .F. ) ;
#45891=ORIENTED_EDGE ( 'NONE', *, *, #60187, .T. ) ;
#45892=CARTESIAN_POINT ( 'NONE',  ( 1.227938101723748288, 42.43379953535185933, 6.439911493064710335 ) ) ;
#45899=CARTESIAN_POINT ( 'NONE',  ( 4.956653778116970166, 47.94889704119054130, 3.690426056930153464 ) ) ;
#45905=EDGE_LOOP ( 'NONE', ( #41271, #9487, #26509, #31620 ) ) ;
#45908=CARTESIAN_POINT ( 'NONE',  ( 4.967162193818130511, 0.000000000000000000, 0.000000000000000000 ) ) ;
#45911=ORIENTED_EDGE ( 'NONE', *, *, #48642, .F. ) ;
#45915=CARTESIAN_POINT ( 'NONE',  ( 0.6067375320500719704, -0.7090021732337279392, 47.89177856776003495 ) ) ;
#45921=CARTESIAN_POINT ( 'NONE',  ( 0.9754402186311922351, -5.786576363453280081, -42.51649392388765136 ) ) ;
#45923=EDGE_CURVE ( 'NONE', #8537, #29889, #56974, .T. ) ;
#45924=CARTESIAN_POINT ( 'NONE',  ( 4.967162193818130511, 19.45289607368822615, 38.44485641567079881 ) ) ;
#45926=DIRECTION ( 'NONE',  ( -1.000000000000000000, -0.000000000000000000, -0.000000000000000000 ) ) ;
#45935=CARTESIAN_POINT ( 'NONE',  ( 0.9730545539215883499, -21.01499094264522682, -37.40983423658496321 ) ) ;
#45938=EDGE_CURVE ( 'NONE', #58089, #16817, #1010, .T. ) ;
#45954=ORIENTED_EDGE ( 'NONE', *, *, #21775, .T. ) ;
#45973=ORIENTED_EDGE ( 'NONE', *, *, #3588, .T. ) ;
#45975=CARTESIAN_POINT ( 'NONE',  ( 0.6067099128993229673, -33.36330296770416481, 34.36589933408230735 ) ) ;
#45996=EDGE_CURVE ( 'NONE', #884, #30413, #57737, .T. ) ;
#46005=CARTESIAN_POINT ( 'NONE',  ( 0.7057020205115072109, -23.21851350879788356, -41.89806668505404730 ) ) ;
#46015=CARTESIAN_POINT ( 'NONE',  ( 5.958863334805807099, 2.677925489610365251, 20.35021240744035964 ) ) ;
#46017=CARTESIAN_POINT ( 'NONE',  ( 5.960721111146673579, 18.96557324978287085, -7.848955554238317589 ) ) ;
#46035=VERTEX_POINT ( 'NONE', #26679 ) ;
#46036=DIRECTION ( 'NONE',  ( 0.000000000000000000, 0.000000000000000000, -1.000000000000000000 ) ) ;
#46043=ORIENTED_EDGE ( 'NONE', *, *, #57561, .T. ) ;
#46046=CARTESIAN_POINT ( 'NONE',  ( 0.8551540677456715978, -33.23105123575874842, -34.52115452272964546 ) ) ;
#46049=ORIENTED_EDGE ( 'NONE', *, *, #55415, .F. ) ;
#46050=CARTESIAN_POINT ( 'NONE',  ( 5.974727161628367256, 14.50236057684845115, -14.52429704002348920 ) ) ;
#46052=ORIENTED_EDGE ( 'NONE', *, *, #34816, .F. ) ;
#46055=CARTESIAN_POINT ( 'NONE',  ( 0.5834872094924182795, -37.85980081020200316, -29.33699246747737988 ) ) ;
#46058=ORIENTED_EDGE ( 'NONE', *, *, #32038, .F. ) ;
#46067=CARTESIAN_POINT ( 'NONE',  ( 4.960156602257182357, 3.546989772330555457, -46.28683144126591742 ) ) ;
#46070=CARTESIAN_POINT ( 'NONE',  ( 1.227938101723748288, -42.91134962331486946, -0.8460948827229646252 ) ) ;
#46073=ORIENTED_EDGE ( 'NONE', *, *, #44605, .F. ) ;
#46076=EDGE_CURVE ( 'NONE', #46227, #9975, #43588, .T. ) ;
#46079=CARTESIAN_POINT ( 'NONE',  ( 0.5819845901640494645, 47.42480841519689250, 6.701564444317855695 ) ) ;
#46083=CARTESIAN_POINT ( 'NONE',  ( 5.981074661064941900, 14.50705827991425778, 14.51919955600740764 ) ) ;
#46087=CARTESIAN_POINT ( 'NONE',  ( 3.270143674763207553, 11.98875605389979349, 6.605065939546861387 ) ) ;
#46101=CARTESIAN_POINT ( 'NONE',  ( 0.8551540677456715978, 43.91216198251566283, -19.17641535420805710 ) ) ;
#46103=LINE ( 'NONE', #7856, #13709 ) ;
#46110=ADVANCED_FACE ( 'NONE', ( #28218 ), #32971, .F. ) ;
#46111=CARTESIAN_POINT ( 'NONE',  ( 0.7762777257811873666, -41.03453903600416908, -24.71864134625273124 ) ) ;
#46118=ORIENTED_EDGE ( 'NONE', *, *, #19348, .F. ) ;
#46125=ORIENTED_EDGE ( 'NONE', *, *, #50075, .T. ) ;
#46136=CARTESIAN_POINT ( 'NONE',  ( 0.9757402383260938006, 26.05362288587366493, 34.09320464257820049 ) ) ;
#46139=CARTESIAN_POINT ( 'NONE',  ( 0.5838002273316431623, -46.22850660674012602, -12.52789267095232617 ) ) ;
#46149=ADVANCED_FACE ( 'NONE', ( #47044 ), #24914, .F. ) ;
#46151=CARTESIAN_POINT ( 'NONE',  ( 0.9754642270333696574, -16.58255499746102757, 39.57465882553921688 ) ) ;
#46165=CARTESIAN_POINT ( 'NONE',  ( 0.7762777257811894760, -43.90991299786887225, -19.15108781300977725 ) ) ;
#46178=UNCERTAINTY_MEASURE_WITH_UNIT (LENGTH_MEASURE( 1.000000000000000082E-05 ), #18785, 'distance_accuracy_value', 'NONE');
#46190=ORIENTED_EDGE ( 'NONE', *, *, #60317, .F. ) ;
#46194=ORIENTED_EDGE ( 'NONE', *, *, #55821, .T. ) ;
#46200=B_SPLINE_CURVE_WITH_KNOTS ( 'NONE', 3,
 ( #32806, #47826, #42827, #47206, #57180, #4873, #52496, #9280, #42515, #14313 ),
 .UNSPECIFIED., .F., .F.,
 ( 4, 3, 3, 4 ),
 ( 1.095097866269904440E-17, 0.0002724568934985560891, 0.0004086836638483806890, 0.0005448802484326158158 ),
 .UNSPECIFIED. ) ;
#46202=CARTESIAN_POINT ( 'NONE',  ( 0.9740398440564311811, -30.63262235044608062, -30.04629765303421607 ) ) ;
#46222=CARTESIAN_POINT ( 'NONE',  ( 0.9736507210033064075, 42.90603603725247694, 0.4504567742782497608 ) ) ;
#46223=CARTESIAN_POINT ( 'NONE',  ( 0.9745511491811744698, -5.262846425219327884, -42.58443036172452167 ) ) ;
#46225=CARTESIAN_POINT ( 'NONE',  ( 0.5827359174754817017, 37.77623182210397346, 29.44457394064633959 ) ) ;
#46226=CARTESIAN_POINT ( 'NONE',  ( 0.6067375320500717484, -18.98242280073596078, 43.97491060910881799 ) ) ;
#46227=VERTEX_POINT ( 'NONE', #6775 ) ;
#46229=B_SPLINE_CURVE_WITH_KNOTS ( 'NONE', 3,
 ( #41194, #45279, #35257, #44973, #6693, #55557, #21138, #44658, #22072, #12074, #40283, #60257, #59335, #16438, #36491, #50258 ),
 .UNSPECIFIED., .F., .F.,
 ( 4, 3, 3, 3, 3, 4 ),
 ( 1.040890552917501732E-17, 0.0002724568934985551675, 0.0004086836638483766233, 0.0005449104342063557788, 0.0008173270854453663480, 0.001089761613562691828 ),
 .UNSPECIFIED. ) ;
#46239=CARTESIAN_POINT ( 'NONE',  ( 5.960721111146673579, -5.318514366754798495, -19.82454228767744198 ) ) ;
#46241=ORIENTED_EDGE ( 'NONE', *, *, #5166, .F. ) ;
#46253=B_SPLINE_CURVE_WITH_KNOTS ( 'NONE', 3,
 ( #15728, #34834, #11025, #39862, #29494, #14800, #43946, #34522, #10714, #20117, #21032, #40173, #54204, #48303, #15106, #670 ),
 .UNSPECIFIED., .F., .F.,
 ( 4, 3, 3, 3, 3, 4 ),
 ( 9.813676791237319219E-18, 0.0002724568934985470360, 0.0004086836638483682207, 0.0005449104342063432020, 0.0008173270854453615775, 0.001089761613562694213 ),
 .UNSPECIFIED. ) ;
#46257=ORIENTED_EDGE ( 'NONE', *, *, #16572, .F. ) ;
#46262=CARTESIAN_POINT ( 'NONE',  ( 0.5809828226811553087, 38.32755012159145025, 28.72298383114502229 ) ) ;
#46264=EDGE_LOOP ( 'NONE', ( #24611, #4990, #50313, #12254 ) ) ;
#46268=CARTESIAN_POINT ( 'NONE',  ( 5.959828726073459926, 20.35060134307031277, 2.674641840416243532 ) ) ;
#46272=CARTESIAN_POINT ( 'NONE',  ( 5.860006189529234355, -48.13093674595582883, -3.137522369586017934 ) ) ;
#46273=CARTESIAN_POINT ( 'NONE',  ( 0.8557997880470606944, 38.55640757422477805, -28.43566216844931915 ) ) ;
#46277=CARTESIAN_POINT ( 'NONE',  ( 0.5839879327111925367, 41.52454255611505829, 23.86931774877311696 ) ) ;
#46278=ORIENTED_EDGE ( 'NONE', *, *, #20179, .T. ) ;
#46283=ORIENTED_EDGE ( 'NONE', *, *, #14675, .T. ) ;
#46284=CARTESIAN_POINT ( 'NONE',  ( 0.9730545539215883499, 26.52009130076770305, 33.73144377768567637 ) ) ;
#46286=EDGE_CURVE ( 'NONE', #58089, #41630, #21036, .T. ) ;
#46290=CARTESIAN_POINT ( 'NONE',  ( 5.960221823109900008, -14.51763960716788482, 14.50993159119785858 ) ) ;
#46299=CARTESIAN_POINT ( 'NONE',  ( 5.860006189529246790, 9.393028332204737652, 47.30964106197861696 ) ) ;
#46302=CARTESIAN_POINT ( 'NONE',  ( 5.959547316686252039, -7.858107265727872992, 18.96183906913529782 ) ) ;
#46303=CARTESIAN_POINT ( 'NONE',  ( 4.967162193818131399, -35.57684288741960899, -24.30453456948146851 ) ) ;
#46311=CARTESIAN_POINT ( 'NONE',  ( 5.981074661064941900, 5.320466518160936076, -19.82308078259086059 ) ) ;
#46322=DIRECTION ( 'NONE',  ( -0.07836865515943411409, -0.8672783706145124061, -0.4916162952473585590 ) ) ;
#46326=CARTESIAN_POINT ( 'NONE',  ( 0.9740398440564311811, 10.70454588197344670, -41.55177796653836708 ) ) ;
#46330=ORIENTED_EDGE ( 'NONE', *, *, #1458, .T. ) ;
#46332=CARTESIAN_POINT ( 'NONE',  ( 5.959828726073459926, 14.51059719297116679, -14.51699876360184938 ) ) ;
#46336=ORIENTED_EDGE ( 'NONE', *, *, #13106, .T. ) ;
#46341=CARTESIAN_POINT ( 'NONE',  ( 0.5839879327111902052, -0.09083573661678309707, -47.89596760851026858 ) ) ;
#46342=ORIENTED_EDGE ( 'NONE', *, *, #16407, .T. ) ;
#46344=EDGE_CURVE ( 'NONE', #2381, #5855, #13790, .T. ) ;
#46345=CARTESIAN_POINT ( 'NONE',  ( 0.5839879882012665169, -29.15719377327474859, 37.99844431214160778 ) ) ;
#46347=CARTESIAN_POINT ( 'NONE',  ( 0.9749527285493303497, 21.20640438431190233, 37.30179927241184856 ) ) ;
#46350=VERTEX_POINT ( 'NONE', #53699 ) ;
#46359=LINE ( 'NONE', #31010, #47706 ) ;
#46361=CARTESIAN_POINT ( 'NONE',  ( 4.967162193818130511, -35.57684288741994294, 24.30453456948097823 ) ) ;
#46362=CARTESIAN_POINT ( 'NONE',  ( 2.624215991343608501, -46.71702075422659561, 11.05657803851029364 ) ) ;
#46377=CARTESIAN_POINT ( 'NONE',  ( 0.9754402186311929013, -33.92707563620664502, 26.26956909363305215 ) ) ;
#46382=EDGE_CURVE ( 'NONE', #51030, #36286, #15829, .T. ) ;
#46384=CARTESIAN_POINT ( 'NONE',  ( 0.9741495583595167762, 21.79582154536855754, -36.96045061395513187 ) ) ;
#46403=EDGE_CURVE ( 'NONE', #45625, #46967, #32252, .T. ) ;
#46408=VERTEX_POINT ( 'NONE', #49031 ) ;
#46412=VERTEX_POINT ( 'NONE', #34330 ) ;
#46415=EDGE_LOOP ( 'NONE', ( #29908, #50551, #14618, #55802 ) ) ;
#46422=VECTOR ( 'NONE', #10156, 1000.000000000000114 ) ;
#46423=ORIENTED_EDGE ( 'NONE', *, *, #21369, .T. ) ;
#46425=CARTESIAN_POINT ( 'NONE',  ( 0.9757892942422817795, 16.46777583825603486, 39.62259979733185133 ) ) ;
#46426=ORIENTED_EDGE ( 'NONE', *, *, #48210, .T. ) ;
#46429=CARTESIAN_POINT ( 'NONE',  ( 5.960721111146673579, -19.82781442290494311, -5.306302591836510985 ) ) ;
#46436=ORIENTED_EDGE ( 'NONE', *, *, #52932, .T. ) ;
#46437=CARTESIAN_POINT ( 'NONE',  ( 0.9752570700956786354, -42.90785210525872628, -0.2306661201225728430 ) ) ;
#46442=ORIENTED_EDGE ( 'NONE', *, *, #36389, .F. ) ;
#46445=CARTESIAN_POINT ( 'NONE',  ( 0.7056555295713347054, 24.67549844185537467, 41.05687446835445087 ) ) ;
#46447=VERTEX_POINT ( 'NONE', #49639 ) ;
#46450=CARTESIAN_POINT ( 'NONE',  ( 0.5786265663353153954, -41.11783955080255737, 24.57327059187383611 ) ) ;
#46451=CARTESIAN_POINT ( 'NONE',  ( 0.8557997880470697982, -13.27832040216607190, -46.03118133706039572 ) ) ;
#46457=CARTESIAN_POINT ( 'NONE',  ( 0.5839880159502354173, -46.27569712847338224, 12.35255585954166335 ) ) ;
#46458=CARTESIAN_POINT ( 'NONE',  ( 3.407937589446174087, 13.63405474014710350, -1.331713209622366501 ) ) ;
#46463=CIRCLE ( 'NONE', #54426, 43.08621763946400307 ) ;
#46464=DIRECTION ( 'NONE',  ( -1.000000000000000000, -0.000000000000000000, -0.000000000000000000 ) ) ;
#46465=FACE_OUTER_BOUND ( 'NONE', #32572, .T. ) ;
#46467=CARTESIAN_POINT ( 'NONE',  ( 0.9756950546413942771, -37.20808764646322686, -21.37039651692535358 ) ) ;
#46469=CARTESIAN_POINT ( 'NONE',  ( 1.227938101723756947, 11.92353943227949387, 41.23019537246713639 ) ) ;
#46470=CARTESIAN_POINT ( 'NONE',  ( 0.9752132459055872227, 39.73079175141347008, 16.20487516111966997 ) ) ;
#46474=CARTESIAN_POINT ( 'NONE',  ( 3.407937589446178528, -1.331713209622598315, 13.63405474014708041 ) ) ;
#46494=ORIENTED_EDGE ( 'NONE', *, *, #2477, .T. ) ;
#46495=EDGE_LOOP ( 'NONE', ( #27904, #15617, #19007, #35482 ) ) ;
#46496=CARTESIAN_POINT ( 'NONE',  ( 0.5807400328401637335, -41.20655774452951903, -24.41979442053213489 ) ) ;
#46504=ORIENTED_EDGE ( 'NONE', *, *, #52475, .F. ) ;
#46511=CARTESIAN_POINT ( 'NONE',  ( 1.088313998177380615, -26.73848503423878498, 33.56520876252056240 ) ) ;
#46528=ORIENTED_EDGE ( 'NONE', *, *, #52039, .T. ) ;
#46530=CARTESIAN_POINT ( 'NONE',  ( -16.39102408640302500, -12.42318157589703631, -1.387175274418403825 ) ) ;
#46543=EDGE_CURVE ( 'NONE', #23728, #24263, #1710, .T. ) ;
#46548=LINE ( 'NONE', #4823, #15875 ) ;
#46549=DIRECTION ( 'NONE',  ( 0.000000000000000000, 0.000000000000000000, 1.000000000000000000 ) ) ;
#46555=ORIENTED_EDGE ( 'NONE', *, *, #32774, .F. ) ;
#46583=ORIENTED_EDGE ( 'NONE', *, *, #35331, .T. ) ;
#46592=VERTEX_POINT ( 'NONE', #4171 ) ;
#46596=ORIENTED_EDGE ( 'NONE', *, *, #26880, .F. ) ;
#46597=CARTESIAN_POINT ( 'NONE',  ( -19.55451506711360210, -12.42295183846419704, -1.389156475119130318 ) ) ;
#46599=CARTESIAN_POINT ( 'NONE',  ( 0.8557997880470599172, -7.156447707086029730, 47.37054680076704472 ) ) ;
#46602=CARTESIAN_POINT ( 'NONE',  ( 0.7762783648524399505, 23.17763242108814481, -41.92424098267915866 ) ) ;
#46608=VERTEX_POINT ( 'NONE', #42138 ) ;
#46612=CARTESIAN_POINT ( 'NONE',  ( 1.227938101723748288, 42.91134962331487657, 0.8460948827226649760 ) ) ;
#46616=DIRECTION ( 'NONE',  ( 0.07439287786467665975, -0.1170659376278835873, -0.9903339163990677596 ) ) ;
#46629=DIRECTION ( 'NONE',  ( 1.000000000000000000, -0.000000000000000000, -0.000000000000000000 ) ) ;
#46630=CARTESIAN_POINT ( 'NONE',  ( -48.95476116535499500, 0.000000000000000000, 0.000000000000000000 ) ) ;
#46632=ORIENTED_EDGE ( 'NONE', *, *, #40245, .F. ) ;
#46633=CARTESIAN_POINT ( 'NONE',  ( 0.9722240741986379886, -29.92651525529354117, -30.74950262511632104 ) ) ;
#46637=CARTESIAN_POINT ( 'NONE',  ( 0.9730545539215892381, -21.89037132892461912, 36.90443313492323085 ) ) ;
#46649=CARTESIAN_POINT ( 'NONE',  ( 5.960721111146673579, -12.50019045452750355, 16.28018152803671370 ) ) ;
#46650=FACE_OUTER_BOUND ( 'NONE', #61793, .T. ) ;
#46655=ORIENTED_EDGE ( 'NONE', *, *, #38471, .T. ) ;
#46658=CARTESIAN_POINT ( 'NONE',  ( 0.5807400328401574052, 47.41494605191452649, -6.791881299635100788 ) ) ;
#46667=FACE_OUTER_BOUND ( 'NONE', #45434, .T. ) ;
#46675=LINE ( 'NONE', #4026, #40850 ) ;
#46680=CARTESIAN_POINT ( 'NONE',  ( 0.5809828226811617480, 47.41188724015879785, 6.791453954330491705 ) ) ;
#46686=EDGE_CURVE ( 'NONE', #16591, #26419, #45762, .T. ) ;
#46689=EDGE_LOOP ( 'NONE', ( #21485, #53782, #56653, #57553 ) ) ;
#46697=COLOUR_RGB ( '', 0.66274510, 0.83137255, 0.94901961) ;
#46700=CARTESIAN_POINT ( 'NONE',  ( 5.965394784446460541, -7.841344330024812237, -18.96850062921631874 ) ) ;
#46701=CARTESIAN_POINT ( 'NONE',  ( 0.6846871229502932144, -44.58493949244016363, 17.53234844287726091 ) ) ;
#46708=CIRCLE ( 'NONE', #9661, 48.09070567114147110 ) ;
#46710=CARTESIAN_POINT ( 'NONE',  ( 3.660176727303412925, 14.24118031989659094, -45.87883389004754520 ) ) ;
#46727=CARTESIAN_POINT ( 'NONE',  ( 0.5839880159502351953, -6.206687493267375011, -47.49213420504722905 ) ) ;
#46734=CARTESIAN_POINT ( 'NONE',  ( 0.9757787079277444597, 16.38386580718292507, 39.65734351318506867 ) ) ;
#46737=CARTESIAN_POINT ( 'NONE',  ( 3.407937589446178528, -3.099921468255096624, 13.34359005742688531 ) ) ;
#46742=CARTESIAN_POINT ( 'NONE',  ( 0.5809828226811556418, -5.711058609465654357, 47.55412398569204413 ) ) ;
#46747=CARTESIAN_POINT ( 'NONE',  ( 5.974727161628369032, 12.48248968439907003, 16.29297756969652511 ) ) ;
#46749=B_SPLINE_CURVE_WITH_KNOTS ( 'NONE', 3,
 ( #56934, #34090, #19066, #29358, #53160, #10267 ),
 .UNSPECIFIED., .F., .F.,
 ( 4, 2, 4 ),
 ( 1.111611290687706433E-17, 0.0002291978881530163769, 0.0004583957763060216408 ),
 .UNSPECIFIED. ) ;
#46751=CARTESIAN_POINT ( 'NONE',  ( 5.960721111146673579, 10.26825948882901152, 17.77250458025995528 ) ) ;
#46758=ORIENTED_EDGE ( 'NONE', *, *, #28786, .F. ) ;
#46759=CARTESIAN_POINT ( 'NONE',  ( 1.227938101723756947, 41.66816631169191965, 10.28900963485394904 ) ) ;
#46761=CARTESIAN_POINT ( 'NONE',  ( 5.960721111146673579, -12.49016043756459915, -16.28787783074223228 ) ) ;
#46764=ADVANCED_FACE ( 'NONE', ( #48641 ), #16772, .T. ) ;
#46765=( BOUNDED_SURFACE ( )  B_SPLINE_SURFACE ( 3, 1, ( 
 ( #36049, #27241 ),
 ( #50122, #46362 ),
 ( #12236, #36976 ),
 ( #3406, #2173 ) ),
 .UNSPECIFIED., .F., .F., .F. ) 
 B_SPLINE_SURFACE_WITH_KNOTS ( ( 4, 4 ),
 ( 2, 2 ),
 ( 0.000000000000000000, 1.000000000000000000 ),
 ( 0.000000000000000000, 1.000000000000000000 ),
 .UNSPECIFIED. ) 
 GEOMETRIC_REPRESENTATION_ITEM ( )  RATIONAL_B_SPLINE_SURFACE ( (
 ( 1.000000000000000000, 1.000000000000000000),
 ( 0.7269869731126821222, 0.9931720237060910339),
 ( 0.7269869731126821222, 0.9931720237060910339),
 ( 1.000000000000000000, 1.000000000000000000) ) ) 
 REPRESENTATION_ITEM ( '' )  SURFACE ( )  );
#46766=CARTESIAN_POINT ( 'NONE',  ( 4.960156602257181468, 30.22163187094436054, -35.23783291257134920 ) ) ;
#46775=CARTESIAN_POINT ( 'NONE',  ( 5.965394784446458765, -0.01447339372439073943, -20.52536205633085231 ) ) ;
#46780=CARTESIAN_POINT ( 'NONE',  ( 0.9740398440564312921, 37.36539512268019791, 21.09418882170549736 ) ) ;
#46783=FACE_OUTER_BOUND ( 'NONE', #58604, .T. ) ;
#46785=CARTESIAN_POINT ( 'NONE',  ( 0.9722240750034554235, 11.66659272802858105, 41.29187379046130957 ) ) ;
#46787=ORIENTED_EDGE ( 'NONE', *, *, #38219, .F. ) ;
#46788=ORIENTED_EDGE ( 'NONE', *, *, #20227, .F. ) ;
#46789=EDGE_CURVE ( 'NONE', #33551, #32792, #57400, .T. ) ;
#46793=CARTESIAN_POINT ( 'NONE',  ( 4.967162193818131399, -23.56777426397203357, 36.06913038482792189 ) ) ;
#46796=ORIENTED_EDGE ( 'NONE', *, *, #11790, .T. ) ;
#46800=VERTEX_POINT ( 'NONE', #1317 ) ;
#46801=VERTEX_POINT ( 'NONE', #21068 ) ;
#46802=CARTESIAN_POINT ( 'NONE',  ( 0.9754642270333682141, -10.93570046136878737, -41.49150764699770377 ) ) ;
#46807=DIRECTION ( 'NONE',  ( 0.000000000000000000, 0.000000000000000000, 1.000000000000000000 ) ) ;
#46808=ORIENTED_EDGE ( 'NONE', *, *, #39489, .T. ) ;
#46809=CARTESIAN_POINT ( 'NONE',  ( 0.5263152470540294336, 0.000000000000000000, 0.000000000000000000 ) ) ;
#46813=ADVANCED_FACE ( 'NONE', ( #30447 ), #40128, .F. ) ;
#46817=VERTEX_POINT ( 'NONE', #11364 ) ;
#46818=CARTESIAN_POINT ( 'NONE',  ( 0.8551540677456715978, -41.03346287276411175, -24.74404575822818941 ) ) ;
#46825=ORIENTED_EDGE ( 'NONE', *, *, #7259, .F. ) ;
#46829=VERTEX_POINT ( 'NONE', #16071 ) ;
#46832=CARTESIAN_POINT ( 'NONE',  ( 0.9756950546413939440, 30.40918718457341896, 30.27237962848448660 ) ) ;
#46839=CARTESIAN_POINT ( 'NONE',  ( 5.965394784446460541, -14.50338846149123384, -14.52385693118997700 ) ) ;
#46840=CARTESIAN_POINT ( 'NONE',  ( 0.9754402186311950107, -42.51649392388755189, 5.786576363453401761 ) ) ;
#46854=CARTESIAN_POINT ( 'NONE',  ( -4.473699999999997345, 1.530808498934191127E-15, 12.50000000000000000 ) ) ;
#46862=VECTOR ( 'NONE', #59359, 1000.000000000000114 ) ;
#46867=DIRECTION ( 'NONE',  ( 0.07836865515943411409, 0.3742079063794837568, 0.9240274869783826617 ) ) ;
#46876=ORIENTED_EDGE ( 'NONE', *, *, #6547, .T. ) ;
#46879=VECTOR ( 'NONE', #8398, 1000.000000000000114 ) ;
#46880=CIRCLE ( 'NONE', #56852, 47.67072199303260049 ) ;
#46889=CARTESIAN_POINT ( 'NONE',  ( 4.967162193818130511, 36.06913038482831979, -23.56777426397140118 ) ) ;
#46899=EDGE_CURVE ( 'NONE', #995, #20273, #3817, .T. ) ;
#46901=CARTESIAN_POINT ( 'NONE',  ( 0.5834872094924180574, 41.36515088387913153, 24.14431479207704712 ) ) ;
#46904=VERTEX_POINT ( 'NONE', #45214 ) ;
#46905=CARTESIAN_POINT ( 'NONE',  ( 5.974727161628367256, -12.48248968439940931, 16.29297756969626576 ) ) ;
#46906=EDGE_CURVE ( 'NONE', #22913, #35798, #56075, .T. ) ;
#46907=ORIENTED_EDGE ( 'NONE', *, *, #21862, .F. ) ;
#46917=CARTESIAN_POINT ( 'NONE',  ( 4.960156602257181468, -14.43621227656497297, -44.12083041402478756 ) ) ;
#46930=CARTESIAN_POINT ( 'NONE',  ( 4.963659409799328515, -36.94443854030204477, -25.25989740981538390 ) ) ;
#46932=CARTESIAN_POINT ( 'NONE',  ( 0.9749527285493317930, 5.883724875809718036, -42.50314808877153183 ) ) ;
#46941=VECTOR ( 'NONE', #58350, 1000.000000000000000 ) ;
#46944=CARTESIAN_POINT ( 'NONE',  ( 0.6846871229502899947, 47.90045233486064546, -0.8641397935261211360 ) ) ;
#46950=CARTESIAN_POINT ( 'NONE',  ( 0.9749527285493296835, 11.38116287125111903, -41.37154756071283401 ) ) ;
#46957=( BOUNDED_SURFACE ( )  B_SPLINE_SURFACE ( 3, 1, ( 
 ( #4185, #23026 ),
 ( #27397, #12706 ),
 ( #51194, #2967 ),
 ( #41838, #59983 ) ),
 .UNSPECIFIED., .F., .F., .F. ) 
 B_SPLINE_SURFACE_WITH_KNOTS ( ( 4, 4 ),
 ( 2, 2 ),
 ( 0.000000000000000000, 1.000000000000000000 ),
 ( 0.000000000000000000, 1.000000000000000000 ),
 .UNSPECIFIED. ) 
 GEOMETRIC_REPRESENTATION_ITEM ( )  RATIONAL_B_SPLINE_SURFACE ( (
 ( 1.000000000000000000, 1.000000000000000000),
 ( 0.9953390228620291325, 0.8624445117760984880),
 ( 0.9953390228620291325, 0.8624445117760984880),
 ( 1.000000000000000000, 1.000000000000000000) ) ) 
 REPRESENTATION_ITEM ( '' )  SURFACE ( )  );
#46962=LINE ( 'NONE', #13134, #46879 ) ;
#46965=CARTESIAN_POINT ( 'NONE',  ( 5.860006189529234355, -31.78942168514587507, 36.27483683749426291 ) ) ;
#46967=VERTEX_POINT ( 'NONE', #50800 ) ;
#46970=EDGE_CURVE ( 'NONE', #47841, #9802, #47117, .T. ) ;
#46975=CARTESIAN_POINT ( 'NONE',  ( 5.959547316686252039, -20.34955788964378698, 2.682663672454569159 ) ) ;
#46977=ADVANCED_FACE ( 'NONE', ( #56418 ), #42135, .F. ) ;
#46982=CARTESIAN_POINT ( 'NONE',  ( 0.9757892942422814464, 34.07281211842327906, 26.08029006934548377 ) ) ;
#46984=ORIENTED_EDGE ( 'NONE', *, *, #40365, .F. ) ;
#46985=CARTESIAN_POINT ( 'NONE',  ( 0.9757954354143114628, 0.01316335317109677827, -42.90846090505964838 ) ) ;
#46986=CARTESIAN_POINT ( 'NONE',  ( 1.227938101723756947, 0.8460948827225182045, 42.91134962331487657 ) ) ;
#46990=ORIENTED_EDGE ( 'NONE', *, *, #53326, .T. ) ;
#46991=CARTESIAN_POINT ( 'NONE',  ( 0.9730545539215883499, -41.57420493492393376, 10.61654491617549034 ) ) ;
#47000=DIRECTION ( 'NONE',  ( 0.000000000000000000, 0.000000000000000000, 1.000000000000000000 ) ) ;
#47004=ADVANCED_FACE ( 'NONE', ( #27618 ), #15760, .F. ) ;
#47005=CARTESIAN_POINT ( 'NONE',  ( 0.5809828226811544205, -34.25055090842130312, -33.48000389720652947 ) ) ;
#47007=CARTESIAN_POINT ( 'NONE',  ( 2.281351352603294913, -22.83955855331488038, -42.18750813859382731 ) ) ;
#47012=CARTESIAN_POINT ( 'NONE',  ( 0.5850706913938533704, 18.49682194438024752, -44.18063951072202400 ) ) ;
#47013=CARTESIAN_POINT ( 'NONE',  ( 5.959828726073459926, 16.28681682518064378, -12.49160845136018061 ) ) ;
#47014=EDGE_CURVE ( 'NONE', #28601, #14851, #23253, .T. ) ;
#47015=CARTESIAN_POINT ( 'NONE',  ( 4.963659409799328515, -33.33129552235065773, -29.86601237216442684 ) ) ;
#47016=CARTESIAN_POINT ( 'NONE',  ( 5.959547316686252039, 5.315863417546330183, -19.82530672674356964 ) ) ;
#47023=ORIENTED_EDGE ( 'NONE', *, *, #7228, .F. ) ;
#47025=ORIENTED_EDGE ( 'NONE', *, *, #32477, .T. ) ;
#47033=ORIENTED_EDGE ( 'NONE', *, *, #59677, .F. ) ;
#47035=CARTESIAN_POINT ( 'NONE',  ( 3.407937589446178528, -3.987184287467695043, -13.10584870154470671 ) ) ;
#47039=FACE_OUTER_BOUND ( 'NONE', #2244, .T. ) ;
#47040=ORIENTED_EDGE ( 'NONE', *, *, #22285, .F. ) ;
#47043=FACE_OUTER_BOUND ( 'NONE', #26547, .T. ) ;
#47044=FACE_OUTER_BOUND ( 'NONE', #38627, .T. ) ;
#47057=CARTESIAN_POINT ( 'NONE',  ( 5.960721111146673579, 12.49016043756449434, 16.28787783074231399 ) ) ;
#47062=CARTESIAN_POINT ( 'NONE',  ( 5.959828726073459926, 10.26672511661731058, 17.77343634131845462 ) ) ;
#47070=CARTESIAN_POINT ( 'NONE',  ( 0.8557997880470599172, 5.347802024197243043, 47.60865952217000796 ) ) ;
#47074=B_SPLINE_CURVE_WITH_KNOTS ( 'NONE', 3,
 ( #44398, #14645, #25557, #19648 ),
 .UNSPECIFIED., .F., .F.,
 ( 4, 4 ),
 ( 0.000000000000000000, 0.004050076154992998147 ),
 .UNSPECIFIED. ) ;
#47079=CARTESIAN_POINT ( 'NONE',  ( 0.9972139404380323535, 33.63772329383416348, -26.64066783422301654 ) ) ;
#47080=ADVANCED_FACE ( 'NONE', ( #47348 ), #4938, .F. ) ;
#47091=CARTESIAN_POINT ( 'NONE',  ( 0.5809828226811617480, 23.47450554821709900, 41.74875432577658074 ) ) ;
#47105=CARTESIAN_POINT ( 'NONE',  ( 0.5839880159502339740, -12.35255585954151236, -46.27569712847346750 ) ) ;
#47106=ORIENTED_EDGE ( 'NONE', *, *, #35331, .F. ) ;
#47109=VERTEX_POINT ( 'NONE', #25696 ) ;
#47113=ORIENTED_EDGE ( 'NONE', *, *, #49674, .F. ) ;
#47117=B_SPLINE_CURVE_WITH_KNOTS ( 'NONE', 3,
 ( #18233, #61114, #51099, #7888 ),
 .UNSPECIFIED., .F., .F.,
 ( 4, 4 ),
 ( 8.673617379884035472E-19, 0.004050076154992998147 ),
 .UNSPECIFIED. ) ;
#47122=EDGE_CURVE ( 'NONE', #55130, #24670, #26730, .T. ) ;
#47131=CARTESIAN_POINT ( 'NONE',  ( 0.8557997880470690211, -38.55640757422419540, -28.43566216845010075 ) ) ;
#47132=CARTESIAN_POINT ( 'NONE',  ( 0.9740398440564311811, 30.63262235044629378, 30.04629765303400291 ) ) ;
#47136=FACE_OUTER_BOUND ( 'NONE', #36790, .T. ) ;
#47142=CARTESIAN_POINT ( 'NONE',  ( 0.9757892942422807803, -42.53466646637867399, 5.651566539685677348 ) ) ;
#47145=CARTESIAN_POINT ( 'NONE',  ( 0.5807400328401574052, -28.72484455891667920, 38.33001520688939934 ) ) ;
#47150=CARTESIAN_POINT ( 'NONE',  ( 4.967162193818131399, -23.56777426397203357, 36.06913038482792189 ) ) ;
#47151=EDGE_LOOP ( 'NONE', ( #37393, #37811, #22601, #16791 ) ) ;
#47154=FACE_OUTER_BOUND ( 'NONE', #4392, .T. ) ;
#47163=CARTESIAN_POINT ( 'NONE',  ( 0.8557997880470599172, 33.22501220301901270, 34.51495345639560952 ) ) ;
#47168=CARTESIAN_POINT ( 'NONE',  ( 0.5809828226811617480, 17.82437196699680726, 44.45562576850608139 ) ) ;
#47173=ORIENTED_EDGE ( 'NONE', *, *, #56558, .T. ) ;
#47178=DIRECTION ( 'NONE',  ( -0.07439287786467652097, 0.7144194931003017279, 0.6957517427943097355 ) ) ;
#47180=B_SPLINE_CURVE_WITH_KNOTS ( 'NONE', 3,
 ( #39189, #24755, #43271, #43899 ),
 .UNSPECIFIED., .F., .F.,
 ( 4, 4 ),
 ( 6.992893892674702526E-18, 0.004050076154992999881 ),
 .UNSPECIFIED. ) ;
#47187=CARTESIAN_POINT ( 'NONE',  ( 0.9722240750034581991, 15.88116978453036054, -39.86121765932383454 ) ) ;
#47192=EDGE_CURVE ( 'NONE', #54683, #28511, #30670, .T. ) ;
#47195=EDGE_LOOP ( 'NONE', ( #38447, #9022, #7233, #36819 ) ) ;
#47196=ORIENTED_EDGE ( 'NONE', *, *, #1344, .T. ) ;
#47202=CARTESIAN_POINT ( 'NONE',  ( 0.9968887458511638267, -4.948372828380487753, -42.62316256128688963 ) ) ;
#47206=CARTESIAN_POINT ( 'NONE',  ( 0.5832367798473397924, -0.2724222379463806520, 47.89515946578896433 ) ) ;
#47209=CARTESIAN_POINT ( 'NONE',  ( 0.9756008150404607004, 26.00810955565563631, -34.12792951168081146 ) ) ;
#47210=CARTESIAN_POINT ( 'NONE',  ( 4.963659409799326738, -13.93274247731990911, -42.53037318521008814 ) ) ;
#47221=CARTESIAN_POINT ( 'NONE',  ( 4.960156602257180580, -38.31207700265935756, -26.21519897043469172 ) ) ;
#47222=CARTESIAN_POINT ( 'NONE',  ( 4.967162193818131399, 18.65818244221258126, 38.83676580803773248 ) ) ;
#47223=CARTESIAN_POINT ( 'NONE',  ( 0.9745511491811756910, 5.938142320543945196, -42.49552597049449787 ) ) ;
#47225=CARTESIAN_POINT ( 'NONE',  ( 0.9730545539215883499, 37.40983423658472873, 21.01499094264562473 ) ) ;
#47227=CARTESIAN_POINT ( 'NONE',  ( 0.5819845901640485764, -47.89381229371849003, -0.4540519722835836269 ) ) ;
#47237=CARTESIAN_POINT ( 'NONE',  ( 5.965394784446458765, -2.664747781316264330, 20.35165389555753279 ) ) ;
#47239=CARTESIAN_POINT ( 'NONE',  ( 0.5809828226811553087, -47.89273459658654275, 0.5448590168530708100 ) ) ;
#47244=CARTESIAN_POINT ( 'NONE',  ( -20.06020393719607142, -7.996425831208540558, 0.2746589711620047169 ) ) ;
#47245=VERTEX_POINT ( 'NONE', #15278 ) ;
#47265=EDGE_CURVE ( 'NONE', #8115, #35714, #31455, .T. ) ;
#47272=CARTESIAN_POINT ( 'NONE',  ( 5.960221823109900008, -18.96108896995720983, 7.859839668734879048 ) ) ;
#47278=DIRECTION ( 'NONE',  ( 1.000000000000000000, 0.000000000000000000, 0.000000000000000000 ) ) ;
#47282=CARTESIAN_POINT ( 'NONE',  ( 0.8551540677456739292, 46.03951182599426772, 13.28067116677217641 ) ) ;
#47285=CARTESIAN_POINT ( 'NONE',  ( 0.5786265663353196143, -29.72999788434318802, 37.55861529268543109 ) ) ;
#47286=ORIENTED_EDGE ( 'NONE', *, *, #31249, .F. ) ;
#47292=CARTESIAN_POINT ( 'NONE',  ( 5.860006189529234355, -45.66786516969939669, 15.52021937683260511 ) ) ;
#47294=CARTESIAN_POINT ( 'NONE',  ( 5.860006189529246790, 3.137522369585520998, 48.13093674595586435 ) ) ;
#47298=CARTESIAN_POINT ( 'NONE',  ( 5.860006189529246790, 21.31760477694582789, 43.26650951066876161 ) ) ;
#47302=B_SPLINE_CURVE_WITH_KNOTS ( 'NONE', 3,
 ( #2680, #50602, #45327, #2990 ),
 .UNSPECIFIED., .F., .F.,
 ( 4, 4 ),
 ( 0.000000000000000000, 0.004048833967417082152 ),
 .UNSPECIFIED. ) ;
#47307=EDGE_CURVE ( 'NONE', #37486, #49553, #3050, .T. ) ;
#47324=ORIENTED_EDGE ( 'NONE', *, *, #51546, .T. ) ;
#47331=CARTESIAN_POINT ( 'NONE',  ( 0.8551540677456715978, -47.90804413217341562, 0.9122407826474140391 ) ) ;
#47332=VERTEX_POINT ( 'NONE', #9633 ) ;
#47333=CARTESIAN_POINT ( 'NONE',  ( 0.5832366564991502411, 0.2724446024277419331, 47.89515933308369000 ) ) ;
#47338=CARTESIAN_POINT ( 'NONE',  ( 0.9757787079277443487, -16.38386580718262664, -39.65734351318521078 ) ) ;
#47343=CARTESIAN_POINT ( 'NONE',  ( 0.8551540677456715978, 13.28067116677202364, 46.03951182599431746 ) ) ;
#47346=ORIENTED_EDGE ( 'NONE', *, *, #212, .T. ) ;
#47348=FACE_OUTER_BOUND ( 'NONE', #30584, .T. ) ;
#47361=AXIS2_PLACEMENT_3D ( 'NONE', #42856, #33450, #24341 ) ;
#47363=FACE_OUTER_BOUND ( 'NONE', #57694, .T. ) ;
#47371=CARTESIAN_POINT ( 'NONE',  ( 1.088313998177381503, -34.51470853099735336, 25.50107284445300948 ) ) ;
#47378=( BOUNDED_SURFACE ( )  B_SPLINE_SURFACE ( 3, 1, ( 
 ( #7232, #16347 ),
 ( #40807, #59867 ),
 ( #45196, #44885 ),
 ( #31376, #26669 ) ),
 .UNSPECIFIED., .F., .F., .F. ) 
 B_SPLINE_SURFACE_WITH_KNOTS ( ( 4, 4 ),
 ( 2, 2 ),
 ( 0.000000000000000000, 1.000000000000000000 ),
 ( 0.000000000000000000, 1.000000000000000000 ),
 .UNSPECIFIED. ) 
 GEOMETRIC_REPRESENTATION_ITEM ( )  RATIONAL_B_SPLINE_SURFACE ( (
 ( 1.000000000000000000, 1.000000000000000000),
 ( 0.9732289882329797637, 0.9999525324661233672),
 ( 0.9732289882329797637, 0.9999525324661233672),
 ( 1.000000000000000000, 1.000000000000000000) ) ) 
 REPRESENTATION_ITEM ( '' )  SURFACE ( )  );
#47382=EDGE_LOOP ( 'NONE', ( #33109, #32680, #20100, #46788 ) ) ;
#47384=CARTESIAN_POINT ( 'NONE',  ( 0.5832366564991492419, 24.18352361336827983, 41.34220239953996412 ) ) ;
#47389=CARTESIAN_POINT ( 'NONE',  ( 0.8551540677456715978, 37.45266983663536564, -29.88829867897776893 ) ) ;
#47402=CARTESIAN_POINT ( 'NONE',  ( 0.5827359174754830340, -12.04517879102104416, -46.35666395585283794 ) ) ;
#47411=CARTESIAN_POINT ( 'NONE',  ( 0.9741495583595178864, -33.79932324264165544, -26.43366215195294444 ) ) ;
#47423=CARTESIAN_POINT ( 'NONE',  ( 3.407937589446178528, 4.815089211105230582, -12.82481284928199017 ) ) ;
#47425=EDGE_CURVE ( 'NONE', #59171, #6735, #16618, .T. ) ;
#47428=CARTESIAN_POINT ( 'NONE',  ( 0.5809828226811553087, -38.32755012159125840, -28.72298383114528519 ) ) ;
#47434=CARTESIAN_POINT ( 'NONE',  ( 4.967162193818129623, 40.65506779172164897, 14.26841313271295952 ) ) ;
#47442=B_SPLINE_CURVE_WITH_KNOTS ( 'NONE', 3,
 ( #25251, #31489, #55586, #7994 ),
 .UNSPECIFIED., .F., .F.,
 ( 4, 4 ),
 ( 0.000000000000000000, 0.004446090762761370323 ),
 .UNSPECIFIED. ) ;
#47451=CARTESIAN_POINT ( 'NONE',  ( 5.974727161628367256, 5.297264154380937562, -19.82959049719570288 ) ) ;
#47487=ORIENTED_EDGE ( 'NONE', *, *, #55301, .F. ) ;
#47490=VECTOR ( 'NONE', #20266, 1000.000000000000114 ) ;
#47491=EDGE_LOOP ( 'NONE', ( #34478, #32023, #17830, #50563 ) ) ;
#47495=CARTESIAN_POINT ( 'NONE',  ( 0.9722240741986378776, 15.88116971565388802, 39.86121768686890476 ) ) ;
#47508=ORIENTED_EDGE ( 'NONE', *, *, #41489, .T. ) ;
#47509=CARTESIAN_POINT ( 'NONE',  ( 0.5839879327111920926, -47.49806740880204359, -6.161619650335801168 ) ) ;
#47515=CARTESIAN_POINT ( 'NONE',  ( 1.227938101723756947, 41.23019537246726429, -11.92353943227906399 ) ) ;
#47520=VERTEX_POINT ( 'NONE', #8745 ) ;
#47537=CARTESIAN_POINT ( 'NONE',  ( 0.5850706913938533704, -46.31100969101495934, 12.22095376872020367 ) ) ;
#47538=EDGE_CURVE ( 'NONE', #41116, #12007, #46675, .T. ) ;
#47548=CARTESIAN_POINT ( 'NONE',  ( 0.9752132459055858904, 42.51031254975323748, -5.831562321021135809 ) ) ;
#47551=CARTESIAN_POINT ( 'NONE',  ( 0.9968887458511681565, -29.87314546208208199, -30.80284987750041736 ) ) ;
#47554=CARTESIAN_POINT ( 'NONE',  ( 3.660176727303409372, -32.61164548483939285, -35.27264088192915636 ) ) ;
#47555=VERTEX_POINT ( 'NONE', #14090 ) ;
#47557=CARTESIAN_POINT ( 'NONE',  ( 0.9722240741986373225, -25.65687427836881795, -34.39263045016081577 ) ) ;
#47564=ORIENTED_EDGE ( 'NONE', *, *, #212, .F. ) ;
#47571=CARTESIAN_POINT ( 'NONE',  ( 0.5827359174754825899, -38.21848266111689441, 28.86822142608436437 ) ) ;
#47573=CARTESIAN_POINT ( 'NONE',  ( 0.9730545539215883499, -0.5054011016615761465, 42.90536227157002003 ) ) ;
#47575=CARTESIAN_POINT ( 'NONE',  ( 4.956653778116975495, -31.29546495791875316, 36.51451553856407628 ) ) ;
#47576=ADVANCED_FACE ( 'NONE', ( #47905 ), #24160, .F. ) ;
#47582=AXIS2_PLACEMENT_3D ( 'NONE', #12357, #22052, #2299 ) ;
#47601=CARTESIAN_POINT ( 'NONE',  ( 0.9756950546413950542, -21.37039651692523989, 37.20808764646330502 ) ) ;
#47602=DIRECTION ( 'NONE',  ( 0.07836865515943411409, -0.4916162952473493997, -0.8672783706145176241 ) ) ;
#47612=EDGE_CURVE ( 'NONE', #28131, #16591, #19368, .T. ) ;
#47616=CARTESIAN_POINT ( 'NONE',  ( 4.967162193818130511, 0.000000000000000000, 0.000000000000000000 ) ) ;
#47618=CARTESIAN_POINT ( 'NONE',  ( 5.958863334805807099, -12.49425770716475981, -16.28483817244735121 ) ) ;
#47621=CARTESIAN_POINT ( 'NONE',  ( 0.6067099128993239665, 34.36589933408243525, 33.36330296770405113 ) ) ;
#47630=CARTESIAN_POINT ( 'NONE',  ( 5.960721111146673579, -19.82781442290501417, 5.306302591836237426 ) ) ;
#47631=CARTESIAN_POINT ( 'NONE',  ( 4.956653778116970166, -27.17045123668450657, -39.67974989265067620 ) ) ;
#47635=CARTESIAN_POINT ( 'NONE',  ( 3.783278058412227640, -27.54892951149523483, -33.06594414781525160 ) ) ;
#47638=VERTEX_POINT ( 'NONE', #58197 ) ;
#47644=ORIENTED_EDGE ( 'NONE', *, *, #15720, .F. ) ;
#47657=CARTESIAN_POINT ( 'NONE',  ( 0.8557997880470599172, -47.60865952217002928, 5.347802024197076065 ) ) ;
#47658=FACE_OUTER_BOUND ( 'NONE', #4767, .T. ) ;
#47669=CARTESIAN_POINT ( 'NONE',  ( 5.959828726073459926, -12.49160845136023923, -16.28681682518060114 ) ) ;
#47671=CARTESIAN_POINT ( 'NONE',  ( 4.967162193818130511, -40.93989340068619498, 13.42934394584149871 ) ) ;
#47672=CARTESIAN_POINT ( 'NONE',  ( 0.7057020205115048794, 46.47981817772241442, -11.58334423512187605 ) ) ;
#47675=CARTESIAN_POINT ( 'NONE',  ( 4.967162193818130511, 0.000000000000000000, 0.000000000000000000 ) ) ;
#47686=CARTESIAN_POINT ( 'NONE',  ( 0.5807400328401574052, 18.83234461715182562, 44.04145271122570904 ) ) ;
#47689=CARTESIAN_POINT ( 'NONE',  ( 0.5850706913938534814, 47.89601588673689037, -0.1816364388702012000 ) ) ;
#47692=VERTEX_POINT ( 'NONE', #25624 ) ;
#47694=CARTESIAN_POINT ( 'NONE',  ( 0.5836750258453363704, 23.79054009282546644, 41.56963612796194951 ) ) ;
#47698=CARTESIAN_POINT ( 'NONE',  ( 0.5819845901640493535, -34.18710267837677463, 33.54497622115119526 ) ) ;
#47705=CARTESIAN_POINT ( 'NONE',  ( 3.407937589446174087, -4.815089211104962352, -12.82481284928208964 ) ) ;
#47706=VECTOR ( 'NONE', #32254, 1000.000000000000000 ) ;
#47710=ORIENTED_EDGE ( 'NONE', *, *, #47122, .F. ) ;
#47714=CARTESIAN_POINT ( 'NONE',  ( 1.227938101723748288, 41.66816631169206886, -10.28900963485336995 ) ) ;
#47720=CONICAL_SURFACE ( 'NONE', #54716, 43.08621763946400307, 1.568696531533066763 ) ;
#47721=ORIENTED_EDGE ( 'NONE', *, *, #15426, .T. ) ;
#47724=VERTEX_POINT ( 'NONE', #39443 ) ;
#47727=FACE_OUTER_BOUND ( 'NONE', #36426, .T. ) ;
#47728=CARTESIAN_POINT ( 'NONE',  ( 4.967162193818130511, -14.26841313271309808, 40.65506779172159924 ) ) ;
#47734=CARTESIAN_POINT ( 'NONE',  ( 4.967162193818130511, 0.000000000000000000, 0.000000000000000000 ) ) ;
#47742=ORIENTED_EDGE ( 'NONE', *, *, #44258, .F. ) ;
#47748=B_SPLINE_CURVE_WITH_KNOTS ( 'NONE', 3,
 ( #55951, #54705, #45975, #16519, #7087, #40353 ),
 .UNSPECIFIED., .F., .F.,
 ( 4, 2, 4 ),
 ( 9.851335625380350225E-18, 0.0002445244328975374566, 0.0004890488657950650469 ),
 .UNSPECIFIED. ) ;
#47757=ORIENTED_EDGE ( 'NONE', *, *, #21584, .T. ) ;
#47766=CARTESIAN_POINT ( 'NONE',  ( 2.281448460670565836, 25.11570011049370876, 40.87338159040645280 ) ) ;
#47768=DIRECTION ( 'NONE',  ( 0.000000000000000000, 0.000000000000000000, 1.000000000000000000 ) ) ;
#47774=CARTESIAN_POINT ( 'NONE',  ( 0.9730545539215883499, -6.101350888304943432, 42.47233286818615028 ) ) ;
#47779=CARTESIAN_POINT ( 'NONE',  ( 5.960721111146673579, -14.51823969584089902, -14.50930005615011709 ) ) ;
#47781=B_SPLINE_CURVE_WITH_KNOTS ( 'NONE', 3,
 ( #38190, #13763, #47571, #4308, #42572, #61631, #52555, #4612, #53473, #43503, #53175, #57864, #1776, #34102, #14682, #15907 ),
 .UNSPECIFIED., .F., .F.,
 ( 4, 3, 3, 3, 3, 4 ),
 ( 9.813676791237319219E-18, 0.0002724568934985605886, 0.0004086836638483811769, 0.0005449104342063590314, 0.0008173270854453652638, 0.001089761613562689442 ),
 .UNSPECIFIED. ) ;
#47785=CARTESIAN_POINT ( 'NONE',  ( 0.7056555295713342613, 37.48482836297272769, -29.82339362082558765 ) ) ;
#47786=CARTESIAN_POINT ( 'NONE',  ( 4.956653778116992370, 27.17045123668527751, -39.67974989265010777 ) ) ;
#47788=EDGE_CURVE ( 'NONE', #47109, #54823, #2420, .T. ) ;
#47796=CARTESIAN_POINT ( 'NONE',  ( 4.956653778116996811, 45.35992544608552635, -15.97476558431834626 ) ) ;
#47798=CARTESIAN_POINT ( 'NONE',  ( 0.9752132459055847802, 42.57112816680955802, 5.369621847647748858 ) ) ;
#47805=VECTOR ( 'NONE', #17926, 999.9999999999998863 ) ;
#47806=CARTESIAN_POINT ( 'NONE',  ( 1.088908134280556661, -37.54826033999246704, -20.77739698351972564 ) ) ;
#47807=CARTESIAN_POINT ( 'NONE',  ( 0.6067375320500720814, -47.89177856776002074, -0.7090021732338949167 ) ) ;
#47813=CARTESIAN_POINT ( 'NONE',  ( 0.5807400328401637335, -17.82553128098439998, 44.45848844984437420 ) ) ;
#47821=ORIENTED_EDGE ( 'NONE', *, *, #50072, .F. ) ;
#47826=CARTESIAN_POINT ( 'NONE',  ( 0.5819845901640493535, -0.4540519722834164829, 47.89381229371849713 ) ) ;
#47829=CARTESIAN_POINT ( 'NONE',  ( 0.9741495583595169983, 26.43366215195310076, -33.79932324264157018 ) ) ;
#47841=VERTEX_POINT ( 'NONE', #14247 ) ;
#47846=B_SPLINE_CURVE_WITH_KNOTS ( 'NONE', 3,
 ( #58133, #57505, #9937, #15256, #53730, #507 ),
 .UNSPECIFIED., .F., .F.,
 ( 4, 2, 4 ),
 ( 9.898949898072313973E-18, 0.0002445244328975399502, 0.0004890488657950699258 ),
 .UNSPECIFIED. ) ;
#47857=CARTESIAN_POINT ( 'NONE',  ( 2.624215991343620935, 22.77108897942195043, -42.26352390376072776 ) ) ;
#47860=CARTESIAN_POINT ( 'NONE',  ( 1.154321485836934391, 30.92445806269079611, 29.75729673892710636 ) ) ;
#47862=LINE ( 'NONE', #205, #35556 ) ;
#47865=ORIENTED_EDGE ( 'NONE', *, *, #2673, .T. ) ;
#47888=ORIENTED_EDGE ( 'NONE', *, *, #36593, .F. ) ;
#47890=ORIENTED_EDGE ( 'NONE', *, *, #58906, .T. ) ;
#47895=CARTESIAN_POINT ( 'NONE',  ( 0.9757402383260949108, 33.98983788393820760, 26.18833306844161157 ) ) ;
#47903=ORIENTED_EDGE ( 'NONE', *, *, #21230, .T. ) ;
#47905=FACE_OUTER_BOUND ( 'NONE', #11284, .T. ) ;
#47919=CARTESIAN_POINT ( 'NONE',  ( 5.974727161628367256, 18.95664195401516849, -7.868887636447420952 ) ) ;
#47925=CARTESIAN_POINT ( 'NONE',  ( 0.5809828226811548646, -46.40184912890831015, -11.86925843957216742 ) ) ;
#47931=ORIENTED_EDGE ( 'NONE', *, *, #58693, .T. ) ;
#47932=CARTESIAN_POINT ( 'NONE',  ( 0.8557997880470606944, -11.51622788066425684, -46.50333260518571876 ) ) ;
#47935=CARTESIAN_POINT ( 'NONE',  ( 0.5827359174754808135, 18.66406616558040454, -44.10985444762169294 ) ) ;
#47941=ORIENTED_EDGE ( 'NONE', *, *, #43869, .T. ) ;
#47944=CARTESIAN_POINT ( 'NONE',  ( 2.281351352603294913, -4.956540261593444185, -47.71649595778614383 ) ) ;
#47945=ORIENTED_EDGE ( 'NONE', *, *, #32777, .T. ) ;
#47951=DIRECTION ( 'NONE',  ( 0.000000000000000000, 0.000000000000000000, 1.000000000000000000 ) ) ;
#47953=ORIENTED_EDGE ( 'NONE', *, *, #55378, .F. ) ;
#47955=VERTEX_POINT ( 'NONE', #6023 ) ;
#47957=FACE_OUTER_BOUND ( 'NONE', #2496, .T. ) ;
#47960=ORIENTED_EDGE ( 'NONE', *, *, #54194, .F. ) ;
#47964=EDGE_LOOP ( 'NONE', ( #55536, #46342, #46583, #52631 ) ) ;
#47966=CARTESIAN_POINT ( 'NONE',  ( 0.5839879882012688483, -33.86758487442378396, -33.86754218494331781 ) ) ;
#47967=CARTESIAN_POINT ( 'NONE',  ( 3.407937589446178528, -10.00592723328954570, -9.356405769959156515 ) ) ;
#47968=B_SPLINE_CURVE_WITH_KNOTS ( 'NONE', 3,
 ( #42176, #28048, #32760, #51836, #8938, #47168 ),
 .UNSPECIFIED., .F., .F.,
 ( 4, 2, 4 ),
 ( 1.549946925021254854E-16, 0.0002445252820015224966, 0.0004890505640028900607 ),
 .UNSPECIFIED. ) ;
#47975=CARTESIAN_POINT ( 'NONE',  ( 0.5786265663353153954, 0.7221568112306425702, 47.89572889566446179 ) ) ;
#47976=ORIENTED_EDGE ( 'NONE', *, *, #14753, .F. ) ;
#47986=EDGE_CURVE ( 'NONE', #14441, #44739, #57498, .T. ) ;
#47989=B_SPLINE_CURVE_WITH_KNOTS ( 'NONE', 3,
 ( #27363, #36476, #51772, #3843, #27981, #60549, #42709, #23285, #32079, #56774, #3534, #55541, #42411, #18588, #8239, #9172, #32380, #22668, #61770 ),
 .UNSPECIFIED., .F., .F.,
 ( 4, 3, 3, 3, 3, 3, 4 ),
 ( 8.674294979774126656E-18, 0.0002724573126191752134, 0.0004086839781548500493, 0.0005449106435901828957, 0.0006811373090491488558, 0.0008459866663933638450, 0.001010840725717211197 ),
 .UNSPECIFIED. ) ;
#47991=CARTESIAN_POINT ( 'NONE',  ( 0.5850706913938534814, 37.88789093229845406, -29.30134895053016564 ) ) ;
#47995=CARTESIAN_POINT ( 'NONE',  ( 0.7057020205114998834, 38.50899875908095282, -28.48867101281786773 ) ) ;
#48010=CARTESIAN_POINT ( 'NONE',  ( 0.9752570700956793015, 5.371905812152142801, 42.57087745267993029 ) ) ;
#48011=CARTESIAN_POINT ( 'NONE',  ( 5.959547316686252039, -16.28624005235107930, 12.49238070347948870 ) ) ;
#48018=CARTESIAN_POINT ( 'NONE',  ( 0.9972139404380334637, 25.59643345733279318, -34.43899251299745146 ) ) ;
#48021=ORIENTED_EDGE ( 'NONE', *, *, #38359, .F. ) ;
#48028=CARTESIAN_POINT ( 'NONE',  ( 0.9730545539215883499, -34.34678117142538412, -25.71816799638815354 ) ) ;
#48032=CARTESIAN_POINT ( 'NONE',  ( 4.967162193818130511, 0.000000000000000000, 0.000000000000000000 ) ) ;
#48037=CARTESIAN_POINT ( 'NONE',  ( 0.9730545539215883499, -0.5054011016615761465, 42.90536227157002003 ) ) ;
#48042=DIRECTION ( 'NONE',  ( -0.07836865515943410021, 0.6006129930017499730, -0.7956898808744407026 ) ) ;
#48046=ORIENTED_EDGE ( 'NONE', *, *, #5631, .T. ) ;
#48052=CARTESIAN_POINT ( 'NONE',  ( 1.227938101723756947, 39.32113113558990847, -17.20315230597801914 ) ) ;
#48054=CARTESIAN_POINT ( 'NONE',  ( 0.9972139404380309102, -17.02682566833155420, -39.38665787682681696 ) ) ;
#48073=CARTESIAN_POINT ( 'NONE',  ( 4.956653778116991482, 20.77844580450620526, -43.37017594958032873 ) ) ;
#48081=ORIENTED_EDGE ( 'NONE', *, *, #4675, .T. ) ;
#48089=FACE_OUTER_BOUND ( 'NONE', #3429, .T. ) ;
#48090=B_SPLINE_CURVE_WITH_KNOTS ( 'NONE', 3,
 ( #54583, #60526, #36453, #12038 ),
 .UNSPECIFIED., .F., .F.,
 ( 4, 4 ),
 ( 3.127317220692750759E-18, 0.004050076154993002484 ),
 .UNSPECIFIED. ) ;
#48100=B_SPLINE_CURVE_WITH_KNOTS ( 'NONE', 3,
 ( #27471, #176, #52501, #47515 ),
 .UNSPECIFIED., .F., .F.,
 ( 4, 4 ),
 ( 1.734723475976807094E-18, 0.004050076154993000749 ),
 .UNSPECIFIED. ) ;
#48101=CARTESIAN_POINT ( 'NONE',  ( 0.5839880159502333079, 38.02605095487717790, -29.12121614504424372 ) ) ;
#48114=DIRECTION ( 'NONE',  ( 0.000000000000000000, 0.000000000000000000, 1.000000000000000000 ) ) ;
#48115=CARTESIAN_POINT ( 'NONE',  ( 0.9752570700956786354, -42.51066151201240473, -5.829291291129111485 ) ) ;
#48117=CARTESIAN_POINT ( 'NONE',  ( 0.5850706913938534814, -6.071602062250944343, 47.50996714391780529 ) ) ;
#48119=CARTESIAN_POINT ( 'NONE',  ( 0.5837374860065642768, 29.30115996485994501, 37.88763545422886381 ) ) ;
#48128=CARTESIAN_POINT ( 'NONE',  ( 0.5832367798473397924, -47.44985149964044524, -6.521664418777663563 ) ) ;
#48129=CARTESIAN_POINT ( 'NONE',  ( 0.9722240741986378776, -39.86121768686897582, 15.88116971565374236 ) ) ;
#48136=CARTESIAN_POINT ( 'NONE',  ( 4.956653778116480780, -21.75875759808806720, 42.88673967249081898 ) ) ;
#48157=ORIENTED_EDGE ( 'NONE', *, *, #3280, .F. ) ;
#48161=EDGE_CURVE ( 'NONE', #12689, #14433, #32040, .T. ) ;
#48168=VERTEX_POINT ( 'NONE', #4406 ) ;
#48170=ADVANCED_FACE ( 'NONE', ( #33279 ), #58909, .F. ) ;
#48177=CARTESIAN_POINT ( 'NONE',  ( 0.5838002273316440505, 47.50378804015153378, -6.116619957188266454 ) ) ;
#48178=ORIENTED_EDGE ( 'NONE', *, *, #14284, .F. ) ;
#48179=ADVANCED_FACE ( 'NONE', ( #43611 ), #50503, .F. ) ;
#48181=ORIENTED_EDGE ( 'NONE', *, *, #9772, .T. ) ;
#48197=LINE ( 'NONE', #1477, #44689 ) ;
#48198=CARTESIAN_POINT ( 'NONE',  ( 5.959828726073459926, -20.34941966491241061, 2.683617577144038258 ) ) ;
#48210=EDGE_CURVE ( 'NONE', #29821, #8960, #15597, .T. ) ;
#48211=CARTESIAN_POINT ( 'NONE',  ( 4.967162193818130511, 0.000000000000000000, 0.000000000000000000 ) ) ;
#48213=CARTESIAN_POINT ( 'NONE',  ( 0.9972139404380300221, -26.64066783422312668, -33.63772329383408533 ) ) ;
#48214=ORIENTED_EDGE ( 'NONE', *, *, #41247, .F. ) ;
#48218=B_SPLINE_CURVE_WITH_KNOTS ( 'NONE', 3,
 ( #19974, #29964, #39088, #10555 ),
 .UNSPECIFIED., .F., .F.,
 ( 4, 4 ),
 ( 1.517883041479706015E-18, 0.004444878191957669575 ),
 .UNSPECIFIED. ) ;
#48220=CARTESIAN_POINT ( 'NONE',  ( 0.9740398440564320692, -21.09418882170562881, 37.36539512268012686 ) ) ;
#48226=CARTESIAN_POINT ( 'NONE',  ( 3.660176727303412036, -22.37119938028460453, -42.51126973288305066 ) ) ;
#48234=EDGE_CURVE ( 'NONE', #28122, #60037, #58763, .T. ) ;
#48236=CARTESIAN_POINT ( 'NONE',  ( 2.526552050251864578, -6.809858322089334948, 42.43615142762123327 ) ) ;
#48238=CARTESIAN_POINT ( 'NONE',  ( 0.5807400328401574052, 29.58941477093014782, 37.66660715020876893 ) ) ;
#48241=CARTESIAN_POINT ( 'NONE',  ( 4.967162193818130511, -36.06913038482816347, 23.56777426397165698 ) ) ;
#48242=EDGE_CURVE ( 'NONE', #25196, #57230, #18587, .T. ) ;
#48244=CARTESIAN_POINT ( 'NONE',  ( 0.9754402186311937895, -37.06569162601115153, 21.61645729243100433 ) ) ;
#48252=CARTESIAN_POINT ( 'NONE',  ( 1.227938101723756947, -11.92353943227920610, -41.23019537246722876 ) ) ;
#48259=CARTESIAN_POINT ( 'NONE',  ( 0.5850706913938533704, 41.38834827854208243, 24.10530971368303099 ) ) ;
#48266=B_SPLINE_CURVE_WITH_KNOTS ( 'NONE', 3,
 ( #12717, #40005, #7668, #26173, #16794, #59058 ),
 .UNSPECIFIED., .F., .F.,
 ( 4, 2, 4 ),
 ( 5.294859796737922701E-18, 0.0002445244328975365350, 0.0004890488657950677574 ),
 .UNSPECIFIED. ) ;
#48268=CARTESIAN_POINT ( 'NONE',  ( 0.9752570700956794125, -16.20701641182888153, -39.72995844664874454 ) ) ;
#48273=CARTESIAN_POINT ( 'NONE',  ( 2.281448460670569389, -40.87338159040653807, 25.11570011049356665 ) ) ;
#48286=CARTESIAN_POINT ( 'NONE',  ( 3.660176727303398714, -27.72864483302497263, -39.22755245663876877 ) ) ;
#48287=CARTESIAN_POINT ( 'NONE',  ( 5.959828726073459926, -10.25888482581847327, -17.77796293532169258 ) ) ;
#48289=CARTESIAN_POINT ( 'NONE',  ( 4.956653778116989706, -42.88673967249116004, -21.75875759808752008 ) ) ;
#48292=CARTESIAN_POINT ( 'NONE',  ( 3.270143674763207553, 5.490410281242951385, -12.53844339339229030 ) ) ;
#48293=CARTESIAN_POINT ( 'NONE',  ( -17.42809333609977784, -7.737545843317588101, 2.032524859195957490 ) ) ;
#48303=CARTESIAN_POINT ( 'NONE',  ( 0.5827357941260203900, 34.12346967353462190, 33.60975216782498620 ) ) ;
#48304=CARTESIAN_POINT ( 'NONE',  ( 1.154321485836932837, 34.54400167111899123, 25.46626718279321011 ) ) ;
#48308=CARTESIAN_POINT ( 'NONE',  ( 0.9730545539215883499, 21.89037132892435622, 36.90443313492338717 ) ) ;
#48313=ORIENTED_EDGE ( 'NONE', *, *, #49345, .T. ) ;
#48315=ORIENTED_EDGE ( 'NONE', *, *, #29845, .T. ) ;
#48318=ORIENTED_EDGE ( 'NONE', *, *, #55295, .T. ) ;
#48321=EDGE_CURVE ( 'NONE', #10602, #35182, #38031, .T. ) ;
#48328=CARTESIAN_POINT ( 'NONE',  ( 5.860006189529246790, 26.78264244998098675, 40.11385274514691446 ) ) ;
#48346=ORIENTED_EDGE ( 'NONE', *, *, #7618, .T. ) ;
#48348=CARTESIAN_POINT ( 'NONE',  ( 4.960156602257182357, -25.36362146861359435, -38.88108289790888961 ) ) ;
#48352=EDGE_LOOP ( 'NONE', ( #8750, #31918, #10911, #50768 ) ) ;
#48365=CARTESIAN_POINT ( 'NONE',  ( 0.9730545539215883499, -42.47233286818622133, 6.101350888304490461 ) ) ;
#48372=CARTESIAN_POINT ( 'NONE',  ( 0.9756950546413946102, -26.04419981250910610, 34.10037081504545853 ) ) ;
#48373=CARTESIAN_POINT ( 'NONE',  ( 0.9757892942422816684, -11.05594550521674257, 41.45966865212809438 ) ) ;
#48375=CARTESIAN_POINT ( 'NONE',  ( 5.960721111146673579, 18.96073515164537326, 7.860635756377957861 ) ) ;
#48394=CARTESIAN_POINT ( 'NONE',  ( 4.963659409799330291, -42.53037318521005261, 13.93274247732006721 ) ) ;
#48396=CARTESIAN_POINT ( 'NONE',  ( 0.9972139404380291339, -34.43899251299751541, -25.59643345733265463 ) ) ;
#48409=CARTESIAN_POINT ( 'NONE',  ( 4.967162193818130511, -36.06913038482782952, -23.56777426397217567 ) ) ;
#48417=ORIENTED_EDGE ( 'NONE', *, *, #39485, .F. ) ;
#48422=B_SPLINE_CURVE_WITH_KNOTS ( 'NONE', 3,
 ( #40772, #27258, #36991, #7197 ),
 .UNSPECIFIED., .F., .F.,
 ( 4, 4 ),
 ( 9.159602786276758478E-17, 0.005004741218457508210 ),
 .UNSPECIFIED. ) ;
#48426=CARTESIAN_POINT ( 'NONE',  ( 0.9747592971366230152, 25.86343094887233107, -34.23774590565611220 ) ) ;
#48428=EDGE_CURVE ( 'NONE', #20429, #27219, #59615, .T. ) ;
#48435=CARTESIAN_POINT ( 'NONE',  ( 0.9757892942422807803, 39.62259979733206450, -16.46777583825560853 ) ) ;
#48438=ORIENTED_EDGE ( 'NONE', *, *, #3043, .F. ) ;
#48441=CARTESIAN_POINT ( 'NONE',  ( 3.660087539127321321, -10.60624038924625800, 46.85281175970452949 ) ) ;
#48446=EDGE_CURVE ( 'NONE', #29889, #43532, #17249, .T. ) ;
#48448=ORIENTED_EDGE ( 'NONE', *, *, #25040, .T. ) ;
#48450=CARTESIAN_POINT ( 'NONE',  ( 0.5838002273316444946, -12.52789267095215919, 46.22850660674015444 ) ) ;
#48455=CARTESIAN_POINT ( 'NONE',  ( 0.9741495583595157770, 42.59115242362818066, -5.208308905147688961 ) ) ;
#48457=EDGE_CURVE ( 'NONE', #32075, #14690, #48422, .T. ) ;
#48461=CARTESIAN_POINT ( 'NONE',  ( -18.52085513643809378, -7.737644335448998767, 2.032152541669497658 ) ) ;
#48462=CARTESIAN_POINT ( 'NONE',  ( 2.526464513654347321, -6.809833384818750446, -42.43615126908563440 ) ) ;
#48463=ORIENTED_EDGE ( 'NONE', *, *, #5631, .F. ) ;
#48464=EDGE_CURVE ( 'NONE', #44739, #61394, #35020, .T. ) ;
#48471=( BOUNDED_SURFACE ( )  B_SPLINE_SURFACE ( 3, 1, ( 
 ( #28271, #47389 ),
 ( #9786, #5368 ),
 ( #28888, #61763 ),
 ( #48011, #10099 ) ),
 .UNSPECIFIED., .F., .F., .F. ) 
 B_SPLINE_SURFACE_WITH_KNOTS ( ( 4, 4 ),
 ( 2, 2 ),
 ( 0.000000000000000000, 1.000000000000000000 ),
 ( 0.000000000000000000, 1.000000000000000000 ),
 .UNSPECIFIED. ) 
 GEOMETRIC_REPRESENTATION_ITEM ( )  RATIONAL_B_SPLINE_SURFACE ( (
 ( 1.000000000000000000, 1.000000000000000000),
 ( 0.9953390228620291325, 0.8624445117760984880),
 ( 0.9953390228620291325, 0.8624445117760984880),
 ( 1.000000000000000000, 1.000000000000000000) ) ) 
 REPRESENTATION_ITEM ( '' )  SURFACE ( )  );
#48478=LINE ( 'NONE', #19684, #7354 ) ;
#48479=ORIENTED_EDGE ( 'NONE', *, *, #5935, .F. ) ;
#48482=ORIENTED_EDGE ( 'NONE', *, *, #50112, .F. ) ;
#48491=CARTESIAN_POINT ( 'NONE',  ( 0.5809828226811617480, 41.20389530892307306, 24.41822904836939401 ) ) ;
#48492=ORIENTED_EDGE ( 'NONE', *, *, #20519, .F. ) ;
#48493=CARTESIAN_POINT ( 'NONE',  ( 0.8557997880470599172, 23.15977007032323343, 41.93815086860265495 ) ) ;
#48495=CARTESIAN_POINT ( 'NONE',  ( 0.5827359174754822568, -6.611633125157127644, 47.43746338751530800 ) ) ;
#48506=STYLED_ITEM ( 'NONE', ( #19395 ), #9707 ) ;
#48517=CARTESIAN_POINT ( 'NONE',  ( 4.967162193818130511, -38.83676580803754064, -18.65818244221298983 ) ) ;
#48520=CARTESIAN_POINT ( 'NONE',  ( 0.5809828226811548646, 29.58751527316178809, 37.66417181417562432 ) ) ;
#48538=EDGE_CURVE ( 'NONE', #55943, #42440, #23801, .T. ) ;
#48546=CARTESIAN_POINT ( 'NONE',  ( 0.8557997880470697982, 37.44587306708137930, -29.88293891557432858 ) ) ;
#48549=CARTESIAN_POINT ( 'NONE',  ( 3.660087539127326206, -48.00143792263125420, 1.881558488211557911 ) ) ;
#48553=ORIENTED_EDGE ( 'NONE', *, *, #37154, .F. ) ;
#48564=DIRECTION ( 'NONE',  ( -0.07836865515943411409, -0.6131273243286173846, -0.7860872967108246678 ) ) ;
#48565=CARTESIAN_POINT ( 'NONE',  ( 0.5838002273316423851, 33.96372661229982270, -33.77111476497738352 ) ) ;
#48567=ORIENTED_EDGE ( 'NONE', *, *, #55023, .F. ) ;
#48568=EDGE_CURVE ( 'NONE', #448, #28808, #34232, .T. ) ;
#48576=CARTESIAN_POINT ( 'NONE',  ( 4.967162193818130511, -36.06913038482782952, -23.56777426397217567 ) ) ;
#48577=CARTESIAN_POINT ( 'NONE',  ( 4.956653778116996811, 40.28700667097716348, -26.26162724282331951 ) ) ;
#48585=ORIENTED_EDGE ( 'NONE', *, *, #17586, .F. ) ;
#48589=CARTESIAN_POINT ( 'NONE',  ( 5.959828726073459926, -17.77343634131834804, -10.26672511661749709 ) ) ;
#48590=LINE ( 'NONE', #32975, #11851 ) ;
#48596=CARTESIAN_POINT ( 'NONE',  ( 3.270143674763207553, -12.74832469035455951, 4.983712007628184892 ) ) ;
#48599=B_SPLINE_CURVE_WITH_KNOTS ( 'NONE', 3,
 ( #15783, #33825, #19112, #27024, #36753, #41454 ),
 .UNSPECIFIED., .F., .F.,
 ( 4, 2, 4 ),
 ( 1.530125426324321260E-16, 0.0002445252820015212498, 0.0004890505640028894102 ),
 .UNSPECIFIED. ) ;
#48602=CARTESIAN_POINT ( 'NONE',  ( 2.526464513654346433, 29.52129845577976042, -31.23609615087146452 ) ) ;
#48605=ORIENTED_EDGE ( 'NONE', *, *, #18992, .T. ) ;
#48615=ADVANCED_FACE ( 'NONE', ( #12797 ), #24908, .F. ) ;
#48616=CARTESIAN_POINT ( 'NONE',  ( 0.5839879882104919151, -5.421203860810959572E-16, -47.89596766822081975 ) ) ;
#48626=ORIENTED_EDGE ( 'NONE', *, *, #50360, .T. ) ;
#48627=CARTESIAN_POINT ( 'NONE',  ( 5.981074661064941900, -10.25489689131118176, -17.77917279944628959 ) ) ;
#48628=B_SPLINE_CURVE_WITH_KNOTS ( 'NONE', 3,
 ( #11270, #44501, #20978, #26282 ),
 .UNSPECIFIED., .F., .F.,
 ( 4, 4 ),
 ( 4.670885906470169154E-18, 0.004050076154992999881 ),
 .UNSPECIFIED. ) ;
#48629=CARTESIAN_POINT ( 'NONE',  ( 0.9972139404380282457, 39.89035676513734785, 15.81078898082002837 ) ) ;
#48636=VECTOR ( 'NONE', #35036, 1000.000000000000114 ) ;
#48641=FACE_OUTER_BOUND ( 'NONE', #41915, .T. ) ;
#48642=EDGE_CURVE ( 'NONE', #18131, #54002, #31224, .T. ) ;
#48644=ORIENTED_EDGE ( 'NONE', *, *, #51541, .F. ) ;
#48645=CARTESIAN_POINT ( 'NONE',  ( 0.8551540677456715978, 41.03346287276427518, 24.74404575822789809 ) ) ;
#48653=VERTEX_POINT ( 'NONE', #56904 ) ;
#48662=CYLINDRICAL_SURFACE ( 'NONE', #27995, 8.000000000000000000 ) ;
#48663=CARTESIAN_POINT ( 'NONE',  ( 4.967162193818130511, 0.000000000000000000, 0.000000000000000000 ) ) ;
#48666=CARTESIAN_POINT ( 'NONE',  ( 5.965394784446460541, -2.693446924985777535, 20.34787558161481869 ) ) ;
#48676=CARTESIAN_POINT ( 'NONE',  ( 0.5807400328401637335, 47.41494605191442702, 6.791881299635756264 ) ) ;
#48677=CARTESIAN_POINT ( 'NONE',  ( 0.9757787079277443487, -26.15233402543291774, 34.01751575780809844 ) ) ;
#48678=CARTESIAN_POINT ( 'NONE',  ( 0.6846871229502932144, 37.47592888575248082, 29.84551600520645209 ) ) ;
#48681=CARTESIAN_POINT ( 'NONE',  ( 0.8557997880470697982, 28.43566216845025352, -38.55640757422408882 ) ) ;
#48683=CARTESIAN_POINT ( 'NONE',  ( 5.860006189529246790, 40.09484204000600727, 26.81109398084720752 ) ) ;
#48694=CARTESIAN_POINT ( 'NONE',  ( 0.5819845901640493535, -41.25023214430184737, -24.34012668949530322 ) ) ;
#48696=EDGE_LOOP ( 'NONE', ( #17434, #14751, #34585, #6106 ) ) ;
#48698=ADVANCED_FACE ( 'NONE', ( #56597 ), #20509, .F. ) ;
#48700=AXIS2_PLACEMENT_3D ( 'NONE', #31363, #45183, #50763 ) ;
#48702=CARTESIAN_POINT ( 'NONE',  ( 4.967162193818129623, 32.10009971360071290, 28.74031574030022540 ) ) ;
#48703=CARTESIAN_POINT ( 'NONE',  ( 1.227938101723756947, 42.43379953535195170, -6.439911493064139236 ) ) ;
#48705=VECTOR ( 'NONE', #39387, 1000.000000000000114 ) ;
#48707=CARTESIAN_POINT ( 'NONE',  ( 0.9758171775293909000, 42.54217005300511545, 5.594812732687240775 ) ) ;
#48709=EDGE_LOOP ( 'NONE', ( #43262, #32542, #16548, #61156 ) ) ;
#48719=CARTESIAN_POINT ( 'NONE',  ( 1.227938101723756947, -6.439911493064287562, -42.43379953535192328 ) ) ;
#48728=B_SPLINE_CURVE_WITH_KNOTS ( 'NONE', 3,
 ( #36379, #51053, #45777, #7515 ),
 .UNSPECIFIED., .F., .F.,
 ( 4, 4 ),
 ( 2.168404344971008868E-18, 0.004048833967417085622 ),
 .UNSPECIFIED. ) ;
#48732=VECTOR ( 'NONE', #50706, 1000.000000000000114 ) ;
#48733=EDGE_CURVE ( 'NONE', #38797, #60545, #5013, .T. ) ;
#48739=CARTESIAN_POINT ( 'NONE',  ( 4.956653778117001252, 47.94889704119056972, -3.690426056929486887 ) ) ;
#48740=CARTESIAN_POINT ( 'NONE',  ( 0.8557997880470599172, 47.89938907511594124, 0.9121262075947815795 ) ) ;
#48742=CARTESIAN_POINT ( 'NONE',  ( 0.5819845079324663661, -23.55367910461026071, 41.70428776698889806 ) ) ;
#48745=EDGE_LOOP ( 'NONE', ( #49248, #44916, #15579, #49716 ) ) ;
#48753=CARTESIAN_POINT ( 'NONE',  ( 1.227938101723756947, 41.23019537246726429, -11.92353943227906399 ) ) ;
#48761=CARTESIAN_POINT ( 'NONE',  ( 0.5827357941260213892, -12.04516435546833364, 46.35666768646130009 ) ) ;
#48762=LINE ( 'NONE', #59072, #7484 ) ;
#48764=CARTESIAN_POINT ( 'NONE',  ( 1.088908134280554885, 0.7803765577541792453, 42.90644581410506220 ) ) ;
#48766=CARTESIAN_POINT ( 'NONE',  ( 1.154321713695927842, 30.92445811446689774, -29.75729669971078195 ) ) ;
#48768=ORIENTED_EDGE ( 'NONE', *, *, #22477, .F. ) ;
#48770=EDGE_CURVE ( 'NONE', #2852, #61163, #41678, .T. ) ;
#48786=DIRECTION ( 'NONE',  ( -1.000000000000000000, 0.000000000000000000, 0.000000000000000000 ) ) ;
#48793=VECTOR ( 'NONE', #11085, 1000.000000000000227 ) ;
#48802=ADVANCED_FACE ( 'NONE', ( #61291 ), #39746, .F. ) ;
#48806=CARTESIAN_POINT ( 'NONE',  ( 0.8551540677456739292, -41.03346287276411886, -24.74404575822818231 ) ) ;
#48809=CARTESIAN_POINT ( 'NONE',  ( 0.5838002273316420521, 6.116619957188743406, 47.50378804015148404 ) ) ;
#48811=CARTESIAN_POINT ( 'NONE',  ( 0.5837374860065650539, -6.071555045024926933, 47.50965286059331305 ) ) ;
#48816=CARTESIAN_POINT ( 'NONE',  ( 0.8551540677456715978, -46.51172240253128365, 11.51835730326463292 ) ) ;
#48823=ORIENTED_EDGE ( 'NONE', *, *, #16706, .F. ) ;
#48829=CARTESIAN_POINT ( 'NONE',  ( 0.8551540677456739292, 43.91216198251539993, 19.17641535420868593 ) ) ;
#48847=CARTESIAN_POINT ( 'NONE',  ( 4.956653778117001252, 45.71126949320271393, -14.93973939759840519 ) ) ;
#48851=CARTESIAN_POINT ( 'NONE',  ( 0.9752570700956805227, 16.63323182627922492, -39.55341424149091267 ) ) ;
#48856=EDGE_CURVE ( 'NONE', #23449, #22677, #2022, .T. ) ;
#48860=CARTESIAN_POINT ( 'NONE',  ( 5.974727161628369032, -0.01551142186663802443, 20.52494643607030156 ) ) ;
#48862=VERTEX_POINT ( 'NONE', #19646 ) ;
#48865=CARTESIAN_POINT ( 'NONE',  ( 4.967162193818130511, 2.375726030842579828, 43.02067033766019932 ) ) ;
#48866=DIRECTION ( 'NONE',  ( -0.07836865515943410021, 0.7104869166657039603, 0.6993330359244890326 ) ) ;
#48868=CARTESIAN_POINT ( 'NONE',  ( 4.956653778116966613, 0.000000000000000000, 0.000000000000000000 ) ) ;
#48876=CARTESIAN_POINT ( 'NONE',  ( 4.967162193818129623, -19.45289607368849616, 38.44485641567065670 ) ) ;
#48877=CIRCLE ( 'NONE', #29867, 48.09070567114147110 ) ;
#48882=DIRECTION ( 'NONE',  ( -0.07836865515943411409, 0.4916162952473615566, -0.8672783706145107407 ) ) ;
#48883=CARTESIAN_POINT ( 'NONE',  ( 1.227938101723757836, -10.28900963485409292, 41.66816631169188412 ) ) ;
#48885=CARTESIAN_POINT ( 'NONE',  ( 0.7056555295713310416, 47.37451042924662659, -7.085402321211308418 ) ) ;
#48889=CARTESIAN_POINT ( 'NONE',  ( 0.5800708057587387056, -47.56394202401741467, 5.628966369368871625 ) ) ;
#48891=ORIENTED_EDGE ( 'NONE', *, *, #51261, .T. ) ;
#48898=B_SPLINE_CURVE_WITH_KNOTS ( 'NONE', 3,
 ( #5463, #44053, #14599, #47798, #28987, #39034, #57456, #58087, #48707, #5763, #1082, #20218, #56860, #16130, #20825, #44350, #16746, #7000, #16429 ),
 .UNSPECIFIED., .F., .F.,
 ( 4, 3, 3, 3, 3, 3, 4 ),
 ( 5.204170427930421283E-18, 0.0002724573126191742376, 0.0004086839781548464172, 0.0005449106435901809441, 0.0006811373090491470127, 0.0008459866663933670976, 0.001010840725717214450 ),
 .UNSPECIFIED. ) ;
#48899=VECTOR ( 'NONE', #15259, 1000.000000000000114 ) ;
#48900=CARTESIAN_POINT ( 'NONE',  ( 0.8557997880470599172, -5.347802024196930404, -47.60865952217005059 ) ) ;
#48902=DIRECTION ( 'NONE',  ( -0.07439287786467650709, -0.9597484305373210622, 0.2708295585865034272 ) ) ;
#48903=CARTESIAN_POINT ( 'NONE',  ( 0.7762777257811889209, 46.03397617421228460, 13.25585385760123813 ) ) ;
#48908=CARTESIAN_POINT ( 'NONE',  ( -16.58652169825008116, -7.842521733728388789, -1.582602419930230209 ) ) ;
#48915=CARTESIAN_POINT ( 'NONE',  ( 4.967162193818130511, 28.74031574030056646, -32.10009971360042158 ) ) ;
#48919=CARTESIAN_POINT ( 'NONE',  ( 0.8557997880470697982, 34.51495345639548873, 33.22501220301912639 ) ) ;
#48920=DIRECTION ( 'NONE',  ( 0.000000000000000000, 0.000000000000000000, 1.000000000000000000 ) ) ;
#48921=CARTESIAN_POINT ( 'NONE',  ( 2.526552050251863246, -34.82218744039922598, 25.19159344346109108 ) ) ;
#48922=ORIENTED_EDGE ( 'NONE', *, *, #8967, .F. ) ;
#48928=ORIENTED_EDGE ( 'NONE', *, *, #57655, .T. ) ;
#48930=CARTESIAN_POINT ( 'NONE',  ( 5.959547316686252039, 5.308980600728456345, -19.82715097195157128 ) ) ;
#48934=CARTESIAN_POINT ( 'NONE',  ( 1.088908134280560214, 25.50067491870088787, -34.51503525510825909 ) ) ;
#48935=EDGE_CURVE ( 'NONE', #23152, #30283, #48266, .T. ) ;
#48939=ORIENTED_EDGE ( 'NONE', *, *, #32993, .F. ) ;
#48945=( BOUNDED_SURFACE ( )  B_SPLINE_SURFACE ( 3, 1, ( 
 ( #46083, #2509 ),
 ( #31339, #3127 ),
 ( #26951, #34579 ),
 ( #44307, #25163 ) ),
 .UNSPECIFIED., .F., .F., .F. ) 
 B_SPLINE_SURFACE_WITH_KNOTS ( ( 4, 4 ),
 ( 2, 2 ),
 ( 0.000000000000000000, 1.000000000000000000 ),
 ( 0.000000000000000000, 1.000000000000000000 ),
 .UNSPECIFIED. ) 
 GEOMETRIC_REPRESENTATION_ITEM ( )  RATIONAL_B_SPLINE_SURFACE ( (
 ( 1.000000000000000000, 1.000000000000000000),
 ( 0.7269869731126817891, 0.9931720237060910339),
 ( 0.7269869731126817891, 0.9931720237060910339),
 ( 1.000000000000000000, 1.000000000000000000) ) ) 
 REPRESENTATION_ITEM ( '' )  SURFACE ( )  );
#48947=EDGE_CURVE ( 'NONE', #58301, #25935, #42296, .T. ) ;
#48955=CARTESIAN_POINT ( 'NONE',  ( 0.5809828226811553087, 46.40184912890838831, 11.86925843957183879 ) ) ;
#48968=B_SPLINE_CURVE_WITH_KNOTS ( 'NONE', 3,
 ( #60179, #7235, #31071, #59871, #26989, #50176, #51083, #1926, #21053, #45199, #26360, #2226, #45496, #21668, #40812, #16988, #17288, #36104, #31379 ),
 .UNSPECIFIED., .F., .F.,
 ( 4, 3, 3, 3, 3, 3, 4 ),
 ( 4.336808689942017736E-18, 0.0002724573126191742376, 0.0004086839781548492903, 0.0005449106435901836546, 0.0006811373090491489642, 0.0008459866663933718681, 0.001010840725717213583 ),
 .UNSPECIFIED. ) ;
#48969=ORIENTED_EDGE ( 'NONE', *, *, #57125, .T. ) ;
#48970=CARTESIAN_POINT ( 'NONE',  ( -17.97369999999976642, -7.719455939378113030, 2.099999999999994760 ) ) ;
#48977=CARTESIAN_POINT ( 'NONE',  ( 5.960721111146673579, -20.35079619394247885, 2.672857320902960243 ) ) ;
#48979=DIRECTION ( 'NONE',  ( -1.000000000000000000, -0.000000000000000000, -0.000000000000000000 ) ) ;
#48980=CARTESIAN_POINT ( 'NONE',  ( 5.981074661064941900, 20.35019299530685188, 2.670494474392067996 ) ) ;
#48986=CARTESIAN_POINT ( 'NONE',  ( 0.7056555295713242693, 29.82339362082594647, 37.48482836297240794 ) ) ;
#48990=CARTESIAN_POINT ( 'NONE',  ( 1.227938101723756947, 6.439911493064564674, 42.43379953535188065 ) ) ;
#48991=CARTESIAN_POINT ( 'NONE',  ( 0.9754402186311951217, -10.92425836141448414, 41.49454543482929125 ) ) ;
#48994=CARTESIAN_POINT ( 'NONE',  ( 0.9722240741986382107, 10.54237114526883978, 41.59310805473373307 ) ) ;
#49001=VERTEX_POINT ( 'NONE', #40613 ) ;
#49009=LINE ( 'NONE', #39954, #12581 ) ;
#49013=CARTESIAN_POINT ( 'NONE',  ( 5.960221823109900008, -12.49086489703240055, 16.28736530777569058 ) ) ;
#49015=CARTESIAN_POINT ( 'NONE',  ( 3.407937589446174087, -13.51415833181186699, -2.242416846335737901 ) ) ;
#49020=ORIENTED_EDGE ( 'NONE', *, *, #11547, .F. ) ;
#49029=ORIENTED_EDGE ( 'NONE', *, *, #22916, .T. ) ;
#49031=CARTESIAN_POINT ( 'NONE',  ( 0.8557997880470690211, -29.88293891557446003, -37.44587306708127983 ) ) ;
#49032=CARTESIAN_POINT ( 'NONE',  ( 5.958863334805807099, 2.680345151634613288, -20.34989385289154740 ) ) ;
#49033=CARTESIAN_POINT ( 'NONE',  ( 4.967162193818130511, 13.42934394584164082, 40.93989340068615945 ) ) ;
#49036=CARTESIAN_POINT ( 'NONE',  ( 0.5850706913938534814, -47.89601588673689037, 0.1816364388698667454 ) ) ;
#49040=ORIENTED_EDGE ( 'NONE', *, *, #29902, .F. ) ;
#49049=CARTESIAN_POINT ( 'NONE',  ( 0.5839254288179549501, 46.28738487712343641, -12.30867641975529025 ) ) ;
#49070=CARTESIAN_POINT ( 'NONE',  ( 4.967162193818130511, 18.65818244221310351, -38.83676580803746958 ) ) ;
#49074=CARTESIAN_POINT ( 'NONE',  ( 0.5837374860065648319, -12.22086613152793610, 46.31070423340725029 ) ) ;
#49075=CARTESIAN_POINT ( 'NONE',  ( 0.8551540677456834771, -47.61725548905986471, -5.348818140991398629 ) ) ;
#49078=CARTESIAN_POINT ( 'NONE',  ( 4.956653778116975495, -8.845409907521238679, 47.27023054223749909 ) ) ;
#49087=CARTESIAN_POINT ( 'NONE',  ( 0.8551540677456834771, -17.49081417858818810, 44.61036085020945308 ) ) ;
#49089=ADVANCED_FACE ( 'NONE', ( #47154 ), #54135, .F. ) ;
#49094=DIRECTION ( 'NONE',  ( 0.07836865515943412797, 0.1379401902675633507, -0.9873352307081167956 ) ) ;
#49095=VERTEX_POINT ( 'NONE', #22401 ) ;
#49099=ORIENTED_EDGE ( 'NONE', *, *, #32748, .T. ) ;
#49105=ORIENTED_EDGE ( 'NONE', *, *, #28002, .F. ) ;
#49110=ORIENTED_EDGE ( 'NONE', *, *, #3597, .F. ) ;
#49114=CARTESIAN_POINT ( 'NONE',  ( 5.960721111146673579, 17.77882586010652943, 10.25731071096588920 ) ) ;
#49115=CARTESIAN_POINT ( 'NONE',  ( 0.5800708057587354860, 41.16170989303203953, 24.48933404430274763 ) ) ;
#49121=( BOUNDED_SURFACE ( )  B_SPLINE_SURFACE ( 3, 1, ( 
 ( #11102, #10792 ),
 ( #6046, #54907 ),
 ( #45249, #11401 ),
 ( #25800, #44324 ) ),
 .UNSPECIFIED., .F., .F., .F. ) 
 B_SPLINE_SURFACE_WITH_KNOTS ( ( 4, 4 ),
 ( 2, 2 ),
 ( 0.000000000000000000, 1.000000000000000000 ),
 ( 0.000000000000000000, 1.000000000000000000 ),
 .UNSPECIFIED. ) 
 GEOMETRIC_REPRESENTATION_ITEM ( )  RATIONAL_B_SPLINE_SURFACE ( (
 ( 1.000000000000000000, 1.000000000000000000),
 ( 0.9953390228620291325, 0.8624445117760984880),
 ( 0.9953390228620291325, 0.8624445117760984880),
 ( 1.000000000000000000, 1.000000000000000000) ) ) 
 REPRESENTATION_ITEM ( '' )  SURFACE ( )  );
#49122=VERTEX_POINT ( 'NONE', #59529 ) ;
#49136=CARTESIAN_POINT ( 'NONE',  ( 0.5807400328401574052, 44.45848844984468684, -17.82553128098360418 ) ) ;
#49144=DIRECTION ( 'NONE',  ( 0.000000000000000000, 0.000000000000000000, 1.000000000000000000 ) ) ;
#49145=CARTESIAN_POINT ( 'NONE',  ( 0.5809828226811617480, -23.47450554821680413, -41.74875432577673706 ) ) ;
#49148=CARTESIAN_POINT ( 'NONE',  ( 0.6846871229502932144, -47.90045233486063125, -0.8641397935264564234 ) ) ;
#49154=CARTESIAN_POINT ( 'NONE',  ( 4.956653778116991482, 9.917440902361805755, -47.05699031914939212 ) ) ;
#49165=CARTESIAN_POINT ( 'NONE',  ( 1.088313998177380171, -41.24258460930631998, -11.85828975620052184 ) ) ;
#49171=DIRECTION ( 'NONE',  ( -0.07439287786467652097, -0.01320009283085550773, -0.9971416435352944418 ) ) ;
#49180=AXIS2_PLACEMENT_3D ( 'NONE', #12737, #12420, #27124 ) ;
#49190=B_SPLINE_CURVE_WITH_KNOTS ( 'NONE', 3,
 ( #15445, #30443, #54544, #34866, #53936, #11062 ),
 .UNSPECIFIED., .F., .F.,
 ( 4, 2, 4 ),
 ( 1.449324869460184762E-16, 0.0002445252820015209245, 0.0004890505640028968912 ),
 .UNSPECIFIED. ) ;
#49200=CARTESIAN_POINT ( 'NONE',  ( -18.52475027399287200, -12.33207363406532941, -2.044797646294537419 ) ) ;
#49203=ADVANCED_FACE ( 'NONE', ( #745 ), #22520, .F. ) ;
#49205=CARTESIAN_POINT ( 'NONE',  ( 5.959547316686252039, 14.51128755440541340, -14.51632612601513728 ) ) ;
#49208=CARTESIAN_POINT ( 'NONE',  ( 0.8557997880470599172, 28.43566216844970640, 38.55640757422448672 ) ) ;
#49212=CARTESIAN_POINT ( 'NONE',  ( 0.8557997880470606944, 38.55640757422477805, -28.43566216844931915 ) ) ;
#49213=CARTESIAN_POINT ( 'NONE',  ( 4.967162193818130511, 0.000000000000000000, 0.000000000000000000 ) ) ;
#49218=AXIS2_PLACEMENT_3D ( 'NONE', #55825, #3201, #3813 ) ;
#49223=ORIENTED_EDGE ( 'NONE', *, *, #47192, .T. ) ;
#49228=CARTESIAN_POINT ( 'NONE',  ( 0.9752132459055864455, 5.831562321021558581, 42.51031254975315221 ) ) ;
#49237=VERTEX_POINT ( 'NONE', #7839 ) ;
#49248=ORIENTED_EDGE ( 'NONE', *, *, #4711, .F. ) ;
#49250=CARTESIAN_POINT ( 'NONE',  ( 0.5807400328401574052, 33.48217046439159361, -34.25275203086199838 ) ) ;
#49251=DIRECTION ( 'NONE',  ( 0.000000000000000000, 0.000000000000000000, 1.000000000000000000 ) ) ;
#49254=CARTESIAN_POINT ( 'NONE',  ( 0.8557997880470599172, -37.44587306708076824, -29.88293891557508530 ) ) ;
#49259=FACE_OUTER_BOUND ( 'NONE', #2715, .T. ) ;
#49275=CARTESIAN_POINT ( 'NONE',  ( 4.956653778116995035, 36.51451553856460919, -31.29546495791814209 ) ) ;
#49280=CARTESIAN_POINT ( 'NONE',  ( 1.154321485836933725, -42.43366804742922938, 6.418927614505942181 ) ) ;
#49286=CARTESIAN_POINT ( 'NONE',  ( 1.088908134280554663, 6.374115321933079059, 42.43751564162685241 ) ) ;
#49289=CARTESIAN_POINT ( 'NONE',  ( 0.9756354156337454508, -11.23134828980305855, 41.41248945940461113 ) ) ;
#49295=ORIENTED_EDGE ( 'NONE', *, *, #26670, .T. ) ;
#49301=CARTESIAN_POINT ( 'NONE',  ( 0.5809828226811617480, 44.03860873105695362, 18.83114015454715684 ) ) ;
#49304=B_SPLINE_CURVE_WITH_KNOTS ( 'NONE', 3,
 ( #24349, #47860, #38466, #9950, #61610, #13417 ),
 .UNSPECIFIED., .F., .F.,
 ( 4, 2, 4 ),
 ( 9.590134410337311873E-18, 0.0002291978881530175153, 0.0004583957763060254355 ),
 .UNSPECIFIED. ) ;
#49306=( BOUNDED_SURFACE ( )  B_SPLINE_SURFACE ( 3, 1, ( 
 ( #28025, #47145 ),
 ( #18018, #23327 ),
 ( #51499, #7654 ),
 ( #26785, #34273 ) ),
 .UNSPECIFIED., .F., .F., .F. ) 
 B_SPLINE_SURFACE_WITH_KNOTS ( ( 4, 4 ),
 ( 2, 2 ),
 ( 0.000000000000000000, 1.000000000000000000 ),
 ( 0.000000000000000000, 1.000000000000000000 ),
 .UNSPECIFIED. ) 
 GEOMETRIC_REPRESENTATION_ITEM ( )  RATIONAL_B_SPLINE_SURFACE ( (
 ( 1.000000000000000000, 1.000000000000000000),
 ( 0.9732289882329797637, 0.9999525324661233672),
 ( 0.9732289882329797637, 0.9999525324661233672),
 ( 1.000000000000000000, 1.000000000000000000) ) ) 
 REPRESENTATION_ITEM ( '' )  SURFACE ( )  );
#49314=CARTESIAN_POINT ( 'NONE',  ( 3.660087539127321321, 14.24113226412049293, 45.87884541725750154 ) ) ;
#49315=ADVANCED_FACE ( 'NONE', ( #9379 ), #7301, .F. ) ;
#49319=ORIENTED_EDGE ( 'NONE', *, *, #48210, .F. ) ;
#49327=CARTESIAN_POINT ( 'NONE',  ( 0.5809828226811565299, -17.82437196699712700, 44.45562576850595349 ) ) ;
#49328=B_SPLINE_CURVE_WITH_KNOTS ( 'NONE', 3,
 ( #6555, #7818, #1879, #25699 ),
 .UNSPECIFIED., .F., .F.,
 ( 4, 4 ),
 ( 1.301042606982605321E-18, 0.004048833967417083887 ),
 .UNSPECIFIED. ) ;
#49336=CARTESIAN_POINT ( 'NONE',  ( 0.6067375320500709712, -46.44340905096873939, 11.71046088714736122 ) ) ;
#49341=B_SPLINE_CURVE_WITH_KNOTS ( 'NONE', 3,
 ( #57202, #47227, #33753, #4896, #42849, #32511, #28409, #19043, #4273, #3971, #42537, #23722, #56909, #18101, #28727, #61295 ),
 .UNSPECIFIED., .F., .F.,
 ( 4, 3, 3, 3, 3, 4 ),
 ( 1.095097866269904594E-17, 0.0002724568934985562517, 0.0004086836638483807432, 0.0005449104342063607661, 0.0008173270854453682996, 0.001089761613562689659 ),
 .UNSPECIFIED. ) ;
#49345=EDGE_CURVE ( 'NONE', #14400, #13993, #15424, .T. ) ;
#49358=CARTESIAN_POINT ( 'NONE',  ( 4.967162193818130511, 0.000000000000000000, 0.000000000000000000 ) ) ;
#49361=CARTESIAN_POINT ( 'NONE',  ( -16.92102945109384393, -12.36669815058221289, 1.822278859258224193 ) ) ;
#49371=CARTESIAN_POINT ( 'NONE',  ( 4.967162193818130511, 0.000000000000000000, 0.000000000000000000 ) ) ;
#49379=CARTESIAN_POINT ( 'NONE',  ( 1.227938101723756947, 17.20315230597844192, 39.32113113558972373 ) ) ;
#49380=CARTESIAN_POINT ( 'NONE',  ( 1.227938101723756947, -42.43379953535190197, 6.439911493064418124 ) ) ;
#49382=VERTEX_POINT ( 'NONE', #49448 ) ;
#49389=B_SPLINE_CURVE_WITH_KNOTS ( 'NONE', 3,
 ( #29810, #48921, #34841, #44256 ),
 .UNSPECIFIED., .F., .F.,
 ( 4, 4 ),
 ( 1.084202172485504434E-18, 0.004048833967417086489 ),
 .UNSPECIFIED. ) ;
#49392=CARTESIAN_POINT ( 'NONE',  ( 4.963659409799326738, 43.98510776953422408, -8.262218268420037148 ) ) ;
#49395=CARTESIAN_POINT ( 'NONE',  ( 0.9754402186311955658, 41.39745964575708825, -11.28658745892475324 ) ) ;
#49397=CARTESIAN_POINT ( 'NONE',  ( 5.981074661064941900, -5.303881226583540887, -19.82752479807525958 ) ) ;
#49401=CARTESIAN_POINT ( 'NONE',  ( 5.960721111146673579, 12.50019045452738276, -16.28018152803680252 ) ) ;
#49402=CARTESIAN_POINT ( 'NONE',  ( 0.5839879327111927587, 41.43370681949809864, -24.02664985973661871 ) ) ;
#49409=ORIENTED_EDGE ( 'NONE', *, *, #44360, .T. ) ;
#49412=CARTESIAN_POINT ( 'NONE',  ( 0.6846871229502932144, 34.48177377577881941, -33.25969555998707250 ) ) ;
#49426=CARTESIAN_POINT ( 'NONE',  ( 0.9972139404380304661, -0.6581143129157298599, -42.90441115546389739 ) ) ;
#49431=CARTESIAN_POINT ( 'NONE',  ( 4.956653778116970166, 39.67974989265038488, 27.17045123668485829 ) ) ;
#49439=VECTOR ( 'NONE', #2599, 1000.000000000000000 ) ;
#49448=CARTESIAN_POINT ( 'NONE',  ( 0.5809828226811617480, 12.92184523170268839, -46.11980934799325382 ) ) ;
#49452=EDGE_CURVE ( 'NONE', #30700, #36409, #46880, .T. ) ;
#49454=CIRCLE ( 'NONE', #22449, 48.09070567114147110 ) ;
#49461=CARTESIAN_POINT ( 'NONE',  ( 0.9758171775293913441, -26.12572690811892784, -34.03798695362338123 ) ) ;
#49464=EDGE_LOOP ( 'NONE', ( #60241, #43878, #22314, #21607 ) ) ;
#49465=CARTESIAN_POINT ( 'NONE',  ( 0.8551540677456834771, -47.90804413217341562, 0.9122407826474088210 ) ) ;
#49466=CARTESIAN_POINT ( 'NONE',  ( 0.9752132459055856684, 16.20487516112007498, -39.73079175141334218 ) ) ;
#49468=ORIENTED_EDGE ( 'NONE', *, *, #19382, .F. ) ;
#49472=ORIENTED_EDGE ( 'NONE', *, *, #47014, .F. ) ;
#49473=FACE_OUTER_BOUND ( 'NONE', #14217, .T. ) ;
#49474=ORIENTED_EDGE ( 'NONE', *, *, #46403, .F. ) ;
#49477=CARTESIAN_POINT ( 'NONE',  ( 0.9747592971366232373, 21.73404615330619905, 36.99691261380215934 ) ) ;
#49478=CARTESIAN_POINT ( 'NONE',  ( 3.270143674763207553, 9.870732238228521638, 9.482922169188000794 ) ) ;
#49480=ORIENTED_EDGE ( 'NONE', *, *, #58497, .T. ) ;
#49481=CARTESIAN_POINT ( 'NONE',  ( 4.967162193818131399, -14.26841313271251543, -40.65506779172179108 ) ) ;
#49483=CARTESIAN_POINT ( 'NONE',  ( 0.9730545539215883499, 21.89037132892487847, -36.90443313492307453 ) ) ;
#49488=CARTESIAN_POINT ( 'NONE',  ( 0.5836750258453349272, 33.99574025613956252, -33.73891062492366899 ) ) ;
#49489=CIRCLE ( 'NONE', #22494, 48.09070567114147110 ) ;
#49491=CARTESIAN_POINT ( 'NONE',  ( 0.5807400328401637335, 17.82553128098407669, 44.45848844984449499 ) ) ;
#49497=CARTESIAN_POINT ( 'NONE',  ( 0.5809828226811553087, 47.41188724015889022, -6.791453954329836229 ) ) ;
#49500=( BOUNDED_SURFACE ( )  B_SPLINE_SURFACE ( 3, 1, ( 
 ( #33381, #37788 ),
 ( #56843, #13343 ),
 ( #32444, #52452 ),
 ( #14581, #28658 ) ),
 .UNSPECIFIED., .F., .F., .F. ) 
 B_SPLINE_SURFACE_WITH_KNOTS ( ( 4, 4 ),
 ( 2, 2 ),
 ( 0.000000000000000000, 1.000000000000000000 ),
 ( 0.000000000000000000, 1.000000000000000000 ),
 .UNSPECIFIED. ) 
 GEOMETRIC_REPRESENTATION_ITEM ( )  RATIONAL_B_SPLINE_SURFACE ( (
 ( 1.000000000000000000, 1.000000000000000000),
 ( 0.7269869731126817891, 0.9931720237060910339),
 ( 0.7269869731126817891, 0.9931720237060910339),
 ( 1.000000000000000000, 1.000000000000000000) ) ) 
 REPRESENTATION_ITEM ( '' )  SURFACE ( )  );
#49503=ORIENTED_EDGE ( 'NONE', *, *, #13901, .T. ) ;
#49507=CARTESIAN_POINT ( 'NONE',  ( -19.64448124547968888, -12.43486301536525751, 1.279587518867056239 ) ) ;
#49513=FACE_OUTER_BOUND ( 'NONE', #40029, .T. ) ;
#49515=FACE_OUTER_BOUND ( 'NONE', #20300, .T. ) ;
#49519=CARTESIAN_POINT ( 'NONE',  ( 0.9756354156337452288, 37.22481466014927776, -21.34128958497340989 ) ) ;
#49522=ADVANCED_FACE ( 'NONE', ( #12807 ), #11355, .F. ) ;
#49535=ORIENTED_EDGE ( 'NONE', *, *, #50574, .T. ) ;
#49537=CARTESIAN_POINT ( 'NONE',  ( 0.6846871229502932144, -38.52803883689320941, 28.47437962186113225 ) ) ;
#49553=VERTEX_POINT ( 'NONE', #55369 ) ;
#49557=CARTESIAN_POINT ( 'NONE',  ( 5.959547316686252039, -14.51632612601538952, 14.51128755440516116 ) ) ;
#49559=ORIENTED_EDGE ( 'NONE', *, *, #42887, .T. ) ;
#49560=ORIENTED_EDGE ( 'NONE', *, *, #1121, .F. ) ;
#49562=CARTESIAN_POINT ( 'NONE',  ( 4.956653778116966613, 0.000000000000000000, 0.000000000000000000 ) ) ;
#49564=EDGE_LOOP ( 'NONE', ( #34675, #18582, #33432, #35167 ) ) ;
#49565=CARTESIAN_POINT ( 'NONE',  ( 5.959547316686252039, -17.77749189599210311, -10.25972575517523744 ) ) ;
#49577=AXIS2_PLACEMENT_3D ( 'NONE', #20029, #39141, #34428 ) ;
#49579=CARTESIAN_POINT ( 'NONE',  ( 0.8557997880470606944, -17.48760788519184217, -44.60232077416704755 ) ) ;
#49586=CARTESIAN_POINT ( 'NONE',  ( 0.8557997880470606944, -28.43566216844945771, -38.55640757422467857 ) ) ;
#49587=CARTESIAN_POINT ( 'NONE',  ( 0.5800708119828337228, -41.16171018093176315, 24.48933355903750453 ) ) ;
#49590=CARTESIAN_POINT ( 'NONE',  ( 0.5807400328401637335, -47.55718917606839824, -5.711437504336458915 ) ) ;
#49592=CARTESIAN_POINT ( 'NONE',  ( 3.783278058412224087, 3.901118461247438773, -42.86118820526426276 ) ) ;
#49596=CARTESIAN_POINT ( 'NONE',  ( 4.956653778116827169, 32.11725092155053574, 35.79382859084104496 ) ) ;
#49598=CARTESIAN_POINT ( 'NONE',  ( 1.227938101723747621, 20.72293514920750468, 37.58536632582787007 ) ) ;
#49604=ORIENTED_EDGE ( 'NONE', *, *, #40952, .F. ) ;
#49605=B_SPLINE_CURVE_WITH_KNOTS ( 'NONE', 3,
 ( #16461, #7656, #26163, #2652, #59984, #45300 ),
 .UNSPECIFIED., .F., .F.,
 ( 4, 2, 4 ),
 ( 6.149443329761889321E-18, 0.0002445244328975378903, 0.0004890488657950697090 ),
 .UNSPECIFIED. ) ;
#49610=ORIENTED_EDGE ( 'NONE', *, *, #2961, .T. ) ;
#49611=ORIENTED_EDGE ( 'NONE', *, *, #3995, .F. ) ;
#49612=B_SPLINE_CURVE_WITH_KNOTS ( 'NONE', 3,
 ( #41908, #29316, #48426, #5488, #28391, #47209, #28703, #38750, #33423, #38136, #809, #14626, #4255, #52498, #171, #23700, #47829, #33116, #61580 ),
 .UNSPECIFIED., .F., .F.,
 ( 4, 3, 3, 3, 3, 3, 4 ),
 ( 9.813676791237319219E-18, 0.0002724573126191793876, 0.0004086839781548473388, 0.0005449106435901772579, 0.0006811373090491502653, 0.0008459866663933714344, 0.001010840725717214016 ),
 .UNSPECIFIED. ) ;
#49636=CARTESIAN_POINT ( 'NONE',  ( 0.7762783648524369529, -17.50713302551360684, 44.59086139387537884 ) ) ;
#49638=CARTESIAN_POINT ( 'NONE',  ( 0.9758171775293911221, -30.34506652060224141, -30.33669560438100987 ) ) ;
#49639=CARTESIAN_POINT ( 'NONE',  ( 4.967162193818130511, 42.96271701169388990, -3.259922920617310371 ) ) ;
#49640=B_SPLINE_CURVE_WITH_KNOTS ( 'NONE', 3,
 ( #53726, #2351, #45308, #20557, #35284, #59364 ),
 .UNSPECIFIED., .F., .F.,
 ( 4, 2, 4 ),
 ( 3.476216610979977084E-18, 0.0002291966416970829816, 0.0004583932833941624938 ),
 .UNSPECIFIED. ) ;
#49647=ORIENTED_EDGE ( 'NONE', *, *, #5994, .T. ) ;
#49660=CARTESIAN_POINT ( 'NONE',  ( 0.5839254288179569485, 37.94310411505145453, 29.22920395911524949 ) ) ;
#49665=CARTESIAN_POINT ( 'NONE',  ( -16.29513786217388116, -12.43465849276918078, 1.291204549316803174 ) ) ;
#49674=EDGE_CURVE ( 'NONE', #53979, #14851, #38460, .T. ) ;
#49681=ORIENTED_EDGE ( 'NONE', *, *, #57315, .T. ) ;
#49690=ORIENTED_EDGE ( 'NONE', *, *, #58965, .T. ) ;
#49692=B_SPLINE_CURVE_WITH_KNOTS ( 'NONE', 3,
 ( #28681, #57464, #47806, #23985, #43115, #19298 ),
 .UNSPECIFIED., .F., .F.,
 ( 4, 2, 4 ),
 ( 1.015220885719448790E-17, 0.0002291978881530158890, 0.0004583957763060215866 ),
 .UNSPECIFIED. ) ;
#49704=CONICAL_SURFACE ( 'NONE', #32736, 43.08621763946400307, 1.568696531533066763 ) ;
#49708=CARTESIAN_POINT ( 'NONE',  ( 0.8551540677456834771, 13.28067116677201831, 46.03951182599431746 ) ) ;
#49712=EDGE_CURVE ( 'NONE', #14392, #46447, #41349, .T. ) ;
#49716=ORIENTED_EDGE ( 'NONE', *, *, #8546, .F. ) ;
#49724=CARTESIAN_POINT ( 'NONE',  ( 1.154321713695925622, -36.74718012229642738, -22.16897764010645133 ) ) ;
#49727=CARTESIAN_POINT ( 'NONE',  ( 1.227938101723756947, 29.74462687941269223, -30.94118573761281965 ) ) ;
#49730=CARTESIAN_POINT ( 'NONE',  ( 0.5839254288179543950, 6.161657890844935537, 47.49799454719520497 ) ) ;
#49734=ORIENTED_EDGE ( 'NONE', *, *, #4754, .F. ) ;
#49737=CARTESIAN_POINT ( 'NONE',  ( 0.5832366564991493529, 18.58038995918353820, 44.14509737861656191 ) ) ;
#49744=CARTESIAN_POINT ( 'NONE',  ( 0.5800708119828332787, 6.873289505980640257, 47.40012378203034160 ) ) ;
#49747=CARTESIAN_POINT ( 'NONE',  ( 5.960721111146673579, -18.96557324978281756, -7.848955554238449928 ) ) ;
#49748=CARTESIAN_POINT ( 'NONE',  ( 5.960221823109900008, -10.25807604135634143, 17.77840967225703039 ) ) ;
#49755=CARTESIAN_POINT ( 'NONE',  ( 0.7056555295713301534, -5.417452459790056629, 47.59410019435325268 ) ) ;
#49757=( BOUNDED_SURFACE ( )  B_SPLINE_SURFACE ( 3, 1, ( 
 ( #26756, #55871 ),
 ( #40890, #22680 ),
 ( #59957, #56179 ),
 ( #50553, #12994 ) ),
 .UNSPECIFIED., .F., .F., .F. ) 
 B_SPLINE_SURFACE_WITH_KNOTS ( ( 4, 4 ),
 ( 2, 2 ),
 ( 0.000000000000000000, 1.000000000000000000 ),
 ( 0.000000000000000000, 1.000000000000000000 ),
 .UNSPECIFIED. ) 
 GEOMETRIC_REPRESENTATION_ITEM ( )  RATIONAL_B_SPLINE_SURFACE ( (
 ( 1.000000000000000000, 1.000000000000000000),
 ( 0.7269869731126821222, 0.9931720237060910339),
 ( 0.7269869731126821222, 0.9931720237060910339),
 ( 1.000000000000000000, 1.000000000000000000) ) ) 
 REPRESENTATION_ITEM ( '' )  SURFACE ( )  );
#49758=CARTESIAN_POINT ( 'NONE',  ( 3.783278058412224976, -9.462251542474113819, 41.98530666033912695 ) ) ;
#49761=CONICAL_SURFACE ( 'NONE', #42901, 43.08621763946400307, 1.568696531533066763 ) ;
#49763=CARTESIAN_POINT ( 'NONE',  ( 3.407937589446174087, 13.51415833181188120, 2.242416846335643754 ) ) ;
#49766=CARTESIAN_POINT ( 'NONE',  ( 5.959828726073459926, 10.25888482581859407, -17.77796293532162863 ) ) ;
#49772=CARTESIAN_POINT ( 'NONE',  ( 0.9754402186311939005, -39.71365199966005122, -16.24692483025461343 ) ) ;
#49776=CARTESIAN_POINT ( 'NONE',  ( 5.974727161628369032, 16.29297756969648603, -12.48248968439911799 ) ) ;
#49777=CARTESIAN_POINT ( 'NONE',  ( 0.9757892942422827787, 16.37293303864358762, -39.66188497122476520 ) ) ;
#49789=ORIENTED_EDGE ( 'NONE', *, *, #19491, .T. ) ;
#49790=CARTESIAN_POINT ( 'NONE',  ( 4.303969348037246512, 27.54579249306209832, 39.44373910178619980 ) ) ;
#49800=EDGE_LOOP ( 'NONE', ( #3754, #53678, #5627, #33084 ) ) ;
#49805=VECTOR ( 'NONE', #12167, 1000.000000000000114 ) ;
#49809=DIRECTION ( 'NONE',  ( 0.07439287786467663199, 0.5965490341031214339, 0.7991213610169884962 ) ) ;
#49814=CARTESIAN_POINT ( 'NONE',  ( 4.960156602257181468, -41.40608197274652014, 20.99019478193036292 ) ) ;
#49815=CARTESIAN_POINT ( 'NONE',  ( 4.956653778116975495, -26.26162724282400518, 40.28700667097671584 ) ) ;
#49820=CARTESIAN_POINT ( 'NONE',  ( -19.64312921891423969, -12.43468193047187853, -1.281307455091694303 ) ) ;
#49825=CARTESIAN_POINT ( 'NONE',  ( 5.958863334805807099, 14.51469124124479926, -14.51296551801787871 ) ) ;
#49830=CARTESIAN_POINT ( 'NONE',  ( 5.960721111146673579, -7.860635756377761574, -18.96073515164545498 ) ) ;
#49837=CARTESIAN_POINT ( 'NONE',  ( 5.958863334805807099, -5.313608583996656698, 19.82594244347343704 ) ) ;
#49840=CARTESIAN_POINT ( 'NONE',  ( 0.9730545539215883499, 42.60426903087360984, -5.099196237954451760 ) ) ;
#49841=DIRECTION ( 'NONE',  ( -1.000000000000000000, -0.000000000000000000, -0.000000000000000000 ) ) ;
#49843=CARTESIAN_POINT ( 'NONE',  ( 5.960721111146673579, -7.860635756378015593, 18.96073515164535195 ) ) ;
#49851=CARTESIAN_POINT ( 'NONE',  ( 4.967162193818130511, -42.96271701169384016, -3.259922920618186115 ) ) ;
#49852=CARTESIAN_POINT ( 'NONE',  ( 1.227938101723756947, -4.762198645644731165, 42.65467462194916948 ) ) ;
#49855=DIRECTION ( 'NONE',  ( -0.07836865515943411409, 0.3742079063795031302, -0.9240274869783747791 ) ) ;
#49856=ORIENTED_EDGE ( 'NONE', *, *, #26437, .T. ) ;
#49862=EDGE_LOOP ( 'NONE', ( #33388, #1012, #37424, #59652 ) ) ;
#49863=ADVANCED_FACE ( 'NONE', ( #34674 ), #27327, .T. ) ;
#49867=VERTEX_POINT ( 'NONE', #44104 ) ;
#49870=ORIENTED_EDGE ( 'NONE', *, *, #15470, .T. ) ;
#49875=ORIENTED_EDGE ( 'NONE', *, *, #50830, .F. ) ;
#49884=VERTEX_POINT ( 'NONE', #36224 ) ;
#49888=VERTEX_POINT ( 'NONE', #36532 ) ;
#49892=CARTESIAN_POINT ( 'NONE',  ( 4.956653778116971054, 42.88673967249130925, 21.75875759808722876 ) ) ;
#49893=AXIS2_PLACEMENT_3D ( 'NONE', #3877, #56811, #57410 ) ;
#49903=CARTESIAN_POINT ( 'NONE',  ( 5.958863334805807099, 16.28483817244739384, -12.49425770716470474 ) ) ;
#49904=DIRECTION ( 'NONE',  ( -1.000000000000000000, -0.000000000000000000, -0.000000000000000000 ) ) ;
#49908=CARTESIAN_POINT ( 'NONE',  ( 3.407937589446178528, -10.58239600294644944, 8.699069120706731439 ) ) ;
#49911=B_SPLINE_CURVE_WITH_KNOTS ( 'NONE', 3,
 ( #54643, #20851, #35270, #16777 ),
 .UNSPECIFIED., .F., .F.,
 ( 4, 4 ),
 ( 0.000000000000000000, 0.005004741218457416270 ),
 .UNSPECIFIED. ) ;
#49918=CARTESIAN_POINT ( 'NONE',  ( 0.6067375320500720814, -43.97491060910871852, -18.98242280073610999 ) ) ;
#49922=ORIENTED_EDGE ( 'NONE', *, *, #48242, .F. ) ;
#49931=AXIS2_PLACEMENT_3D ( 'NONE', #7062, #21492, #31511 ) ;
#49936=B_SPLINE_CURVE_WITH_KNOTS ( 'NONE', 3,
 ( #32482, #38430, #8652, #22767 ),
 .UNSPECIFIED., .F., .F.,
 ( 4, 4 ),
 ( 0.000000000000000000, 0.005004741218457418005 ),
 .UNSPECIFIED. ) ;
#49942=CARTESIAN_POINT ( 'NONE',  ( 0.8551540677456834771, 47.61725548905990735, 5.348818140991066450 ) ) ;
#49945=EDGE_CURVE ( 'NONE', #57761, #44156, #51914, .T. ) ;
#49951=AXIS2_PLACEMENT_3D ( 'NONE', #48211, #5872, #30015 ) ;
#49954=CARTESIAN_POINT ( 'NONE',  ( 2.624215991343620935, -32.93378783738872784, 34.92983774302955169 ) ) ;
#49958=CARTESIAN_POINT ( 'NONE',  ( 0.9757892942422827787, -30.37715353261971529, -30.30456399643821896 ) ) ;
#49962=CARTESIAN_POINT ( 'NONE',  ( 0.9757787079277449038, -21.42002160630794450, -37.17954582422758847 ) ) ;
#49981=VECTOR ( 'NONE', #57091, 1000.000000000000000 ) ;
#49982=ADVANCED_FACE ( 'NONE', ( #2364 ), #31298, .F. ) ;
#49985=B_SPLINE_CURVE_WITH_KNOTS ( 'NONE', 3,
 ( #49327, #50561, #2632, #17372, #49636, #1697 ),
 .UNSPECIFIED., .F., .F.,
 ( 4, 2, 4 ),
 ( 3.529906531158615134E-18, 0.0002445244328975344750, 0.0004890488657950654806 ),
 .UNSPECIFIED. ) ;
#49997=ORIENTED_EDGE ( 'NONE', *, *, #34000, .T. ) ;
#49998=CARTESIAN_POINT ( 'NONE',  ( 5.965394784446460541, 17.78272165951801398, -10.25014670152096485 ) ) ;
#50003=CARTESIAN_POINT ( 'NONE',  ( 5.959547316686252039, 5.315863417546055736, 19.82530672674364070 ) ) ;
#50004=CARTESIAN_POINT ( 'NONE',  ( 0.5786265663353153954, 44.52624106864143982, 17.66171603226096920 ) ) ;
#50006=B_SPLINE_CURVE_WITH_KNOTS ( 'NONE', 3,
 ( #56513, #27714, #7982, #3572 ),
 .UNSPECIFIED., .F., .F.,
 ( 4, 4 ),
 ( 0.000000000000000000, 0.004446090762761341700 ),
 .UNSPECIFIED. ) ;
#50007=VERTEX_POINT ( 'NONE', #7361 ) ;
#50014=ORIENTED_EDGE ( 'NONE', *, *, #8765, .T. ) ;
#50019=ORIENTED_EDGE ( 'NONE', *, *, #36566, .F. ) ;
#50021=LINE ( 'NONE', #45644, #19016 ) ;
#50022=ORIENTED_EDGE ( 'NONE', *, *, #27900, .F. ) ;
#50027=CARTESIAN_POINT ( 'NONE',  ( 5.981074661064941900, 12.50143471347281299, -16.27808421740013856 ) ) ;
#50029=CARTESIAN_POINT ( 'NONE',  ( 5.981074661064941900, -18.96560215432023000, 7.846517100474483364 ) ) ;
#50039=CARTESIAN_POINT ( 'NONE',  ( 0.6846871229502932144, 13.23224427737893549, -46.04462816497473199 ) ) ;
#50041=CARTESIAN_POINT ( 'NONE',  ( 0.9972139404380282457, 26.64066783422334694, 33.63772329383390769 ) ) ;
#50049=EDGE_LOOP ( 'NONE', ( #38976, #4905, #50708, #2180 ) ) ;
#50050=ORIENTED_EDGE ( 'NONE', *, *, #45334, .F. ) ;
#50051=( BOUNDED_SURFACE ( )  B_SPLINE_SURFACE ( 3, 1, ( 
 ( #41929, #22798 ),
 ( #13410, #32515 ),
 ( #51589, #27803 ),
 ( #37535, #18726 ) ),
 .UNSPECIFIED., .F., .F., .F. ) 
 B_SPLINE_SURFACE_WITH_KNOTS ( ( 4, 4 ),
 ( 2, 2 ),
 ( 0.000000000000000000, 1.000000000000000000 ),
 ( 0.000000000000000000, 1.000000000000000000 ),
 .UNSPECIFIED. ) 
 GEOMETRIC_REPRESENTATION_ITEM ( )  RATIONAL_B_SPLINE_SURFACE ( (
 ( 1.000000000000000000, 1.000000000000000000),
 ( 0.9953390228620291325, 0.8624445117760984880),
 ( 0.9953390228620291325, 0.8624445117760984880),
 ( 1.000000000000000000, 1.000000000000000000) ) ) 
 REPRESENTATION_ITEM ( '' )  SURFACE ( )  );
#50053=CARTESIAN_POINT ( 'NONE',  ( 4.956653778116973719, 31.29546495791849736, 36.51451553856430365 ) ) ;
#50056=CARTESIAN_POINT ( 'NONE',  ( 0.6067099128993206358, -44.51753430581926096, -17.67241243535530870 ) ) ;
#50060=CARTESIAN_POINT ( 'NONE',  ( 2.526464513654346433, 39.22765990515345891, -17.56107808841265694 ) ) ;
#50061=ORIENTED_EDGE ( 'NONE', *, *, #41986, .F. ) ;
#50063=CARTESIAN_POINT ( 'NONE',  ( 0.5839879327111907603, -44.21534283185616943, 18.41291455875288108 ) ) ;
#50064=CARTESIAN_POINT ( 'NONE',  ( 0.9722240741986377666, 42.90442369863401950, 0.5819399500321930097 ) ) ;
#50069=CARTESIAN_POINT ( 'NONE',  ( 0.8551540677456834771, -11.51835730326512675, 46.51172240253117707 ) ) ;
#50070=CARTESIAN_POINT ( 'NONE',  ( 0.5807400328401574052, -34.25275203086211917, -33.48217046439147282 ) ) ;
#50071=CARTESIAN_POINT ( 'NONE',  ( 0.5807400328401574052, 6.791881299635576852, 47.41494605191445544 ) ) ;
#50072=EDGE_CURVE ( 'NONE', #24678, #23496, #60116, .T. ) ;
#50073=AXIS2_PLACEMENT_3D ( 'NONE', #23358, #8305, #18662 ) ;
#50074=CARTESIAN_POINT ( 'NONE',  ( 1.227938101723757836, -10.28900963485409292, 41.66816631169188412 ) ) ;
#50075=EDGE_CURVE ( 'NONE', #35725, #4600, #37155, .T. ) ;
#50077=EDGE_CURVE ( 'NONE', #9258, #23834, #6272, .T. ) ;
#50080=CARTESIAN_POINT ( 'NONE',  ( 0.9730545539215883499, 11.59290486963506517, 41.31259007387235727 ) ) ;
#50089=CARTESIAN_POINT ( 'NONE',  ( 0.9756354156337453398, -39.59221474545851294, -16.54067710771401778 ) ) ;
#50096=CARTESIAN_POINT ( 'NONE',  ( 0.9968887458511667132, 41.27232779986120192, 11.73947777183236063 ) ) ;
#50097=ORIENTED_EDGE ( 'NONE', *, *, #13106, .F. ) ;
#50106=B_SPLINE_CURVE_WITH_KNOTS ( 'NONE', 3,
 ( #20197, #48994, #53368, #25485, #5738, #58066 ),
 .UNSPECIFIED., .F., .F.,
 ( 4, 2, 4 ),
 ( 1.738108305489988542E-18, 0.0002291966416970806777, 0.0004583932833941596206 ),
 .UNSPECIFIED. ) ;
#50107=EDGE_CURVE ( 'NONE', #28142, #59626, #9051, .T. ) ;
#50108=ORIENTED_EDGE ( 'NONE', *, *, #18626, .F. ) ;
#50111=CARTESIAN_POINT ( 'NONE',  ( 0.5819845079324652559, -38.27312975753793722, -28.79567599618802021 ) ) ;
#50112=EDGE_CURVE ( 'NONE', #18589, #45486, #36702, .T. ) ;
#50115=CARTESIAN_POINT ( 'NONE',  ( 0.9757954354143122400, -4.033171854401937560E-17, -42.90846090505964128 ) ) ;
#50119=CARTESIAN_POINT ( 'NONE',  ( 5.959547316686252039, -14.51632612601518879, -14.51128755440536366 ) ) ;
#50122=CARTESIAN_POINT ( 'NONE',  ( 5.965394784446458765, 19.82223131420054685, -5.326334832595444269 ) ) ;
#50125=VERTEX_POINT ( 'NONE', #8295 ) ;
#50128=CARTESIAN_POINT ( 'NONE',  ( 5.981074661064941900, 17.77058762078877763, -10.26976685693804647 ) ) ;
#50129=ORIENTED_EDGE ( 'NONE', *, *, #9282, .T. ) ;
#50140=FACE_OUTER_BOUND ( 'NONE', #7065, .T. ) ;
#50141=EDGE_CURVE ( 'NONE', #28691, #20504, #287, .T. ) ;
#50144=CARTESIAN_POINT ( 'NONE',  ( 0.9757787079277456810, 21.48842038179486380, -37.14005577278797432 ) ) ;
#50161=CARTESIAN_POINT ( 'NONE',  ( 3.407937589446174087, 13.69123696618924413, 0.4592810312472457857 ) ) ;
#50162=CARTESIAN_POINT ( 'NONE',  ( 0.5839254288179548391, 46.24038938821434641, 12.48406597209056024 ) ) ;
#50164=ORIENTED_EDGE ( 'NONE', *, *, #32774, .T. ) ;
#50165=CARTESIAN_POINT ( 'NONE',  ( 2.624215991343608501, -11.05657803851013021, -46.71702075422663114 ) ) ;
#50171=CARTESIAN_POINT ( 'NONE',  ( 0.8551540677456739292, -28.44084013485093365, -38.56334384152459904 ) ) ;
#50172=CARTESIAN_POINT ( 'NONE',  ( 0.9757787079277443487, -41.43615150473004860, -11.14366644276454466 ) ) ;
#50176=CARTESIAN_POINT ( 'NONE',  ( 0.9756008150404611445, -5.459718823765815188, 42.55970871350804430 ) ) ;
#50180=CARTESIAN_POINT ( 'NONE',  ( 0.5839879327111912044, 0.09083573661711773217, 47.89596760851024015 ) ) ;
#50190=CARTESIAN_POINT ( 'NONE',  ( 0.9740398440564310700, -42.90647580953695694, 0.4145941695171530550 ) ) ;
#50195=CARTESIAN_POINT ( 'NONE',  ( 1.227938101723748288, -37.58536632582793402, 20.72293514920737323 ) ) ;
#50196=CARTESIAN_POINT ( 'NONE',  ( 4.960156602257182357, -43.79161740034487593, 15.40604254112629157 ) ) ;
#50197=ORIENTED_EDGE ( 'NONE', *, *, #3485, .T. ) ;
#50199=CARTESIAN_POINT ( 'NONE',  ( 4.960156602257181468, 25.36362146861438660, -38.88108289790832117 ) ) ;
#50205=EDGE_CURVE ( 'NONE', #49237, #51439, #35922, .T. ) ;
#50206=CARTESIAN_POINT ( 'NONE',  ( 5.959547316686252039, 18.96183906913532269, 7.858107265727816149 ) ) ;
#50209=CARTESIAN_POINT ( 'NONE',  ( 1.227938101723748288, -42.43379953535180960, -6.439911493065006987 ) ) ;
#50215=CARTESIAN_POINT ( 'NONE',  ( 4.956653778116970166, 47.94889704119054130, 3.690426056930153464 ) ) ;
#50223=CARTESIAN_POINT ( 'NONE',  ( 4.967162193818130511, 0.000000000000000000, 0.000000000000000000 ) ) ;
#50228=EDGE_CURVE ( 'NONE', #60, #44595, #50106, .T. ) ;
#50240=CARTESIAN_POINT ( 'NONE',  ( 0.5838002273316426072, 47.89576566046788031, 0.1361971433779728680 ) ) ;
#50255=CARTESIAN_POINT ( 'NONE',  ( 0.5839879882012674051, 44.25009266679231246, -18.32902119196519664 ) ) ;
#50258=CARTESIAN_POINT ( 'NONE',  ( 0.5809828226811553087, 11.86925843957232729, -46.40184912890826752 ) ) ;
#50263=CARTESIAN_POINT ( 'NONE',  ( 0.5807400328401574052, -28.72484455891616406, -38.33001520688979014 ) ) ;
#50265=VERTEX_POINT ( 'NONE', #39011 ) ;
#50277=CARTESIAN_POINT ( 'NONE',  ( 0.9730545539215883499, -6.101350888304360787, -42.47233286818623554 ) ) ;
#50278=CARTESIAN_POINT ( 'NONE',  ( 5.960721111146673579, -5.318514366754798495, -19.82454228767744198 ) ) ;
#50281=CARTESIAN_POINT ( 'NONE',  ( 4.956653778116968390, 48.02038484091101367, -2.599733001514498376 ) ) ;
#50284=CARTESIAN_POINT ( 'NONE',  ( 0.7762783648524382851, 11.53708172997884596, -46.49451980369966009 ) ) ;
#50285=DIRECTION ( 'NONE',  ( -1.000000000000000000, -0.000000000000000000, -0.000000000000000000 ) ) ;
#50299=DIRECTION ( 'NONE',  ( -1.000000000000000000, -0.000000000000000000, -0.000000000000000000 ) ) ;
#50300=CARTESIAN_POINT ( 'NONE',  ( 0.8551540677456834771, -41.94570365541186874, -23.16399837394590477 ) ) ;
#50302=ADVANCED_FACE ( 'NONE', ( #5132 ), #24157, .F. ) ;
#50304=CARTESIAN_POINT ( 'NONE',  ( 5.959547316686252039, 5.308980600728181010, 19.82715097195164233 ) ) ;
#50305=CARTESIAN_POINT ( 'NONE',  ( 0.5839879882012688483, -47.48620708510743782, 6.251708210201897487 ) ) ;
#50313=ORIENTED_EDGE ( 'NONE', *, *, #34394, .T. ) ;
#50314=DIRECTION ( 'NONE',  ( 0.000000000000000000, 0.000000000000000000, 1.000000000000000000 ) ) ;
#50315=CARTESIAN_POINT ( 'NONE',  ( 3.783278058412226308, -33.06594414781516633, 27.54892951149532365 ) ) ;
#50316=ORIENTED_EDGE ( 'NONE', *, *, #48161, .T. ) ;
#50317=CARTESIAN_POINT ( 'NONE',  ( 0.6067375320500736358, 34.36594163291755422, -33.36326114377782659 ) ) ;
#50321=CARTESIAN_POINT ( 'NONE',  ( 5.974727161628369032, 19.82959049719575262, -5.297264154380731505 ) ) ;
#50325=CARTESIAN_POINT ( 'NONE',  ( 1.227938101723748288, 42.65467462194924764, -4.762198645644009076 ) ) ;
#50327=VERTEX_POINT ( 'NONE', #36458 ) ;
#50331=ORIENTED_EDGE ( 'NONE', *, *, #44249, .F. ) ;
#50332=CARTESIAN_POINT ( 'NONE',  ( 1.227938101723757836, -15.63977281655870222, 39.96870412324331312 ) ) ;
#50335=CARTESIAN_POINT ( 'NONE',  ( 0.5827357941260234986, -17.99287562175617694, 44.38787053017142625 ) ) ;
#50343=CARTESIAN_POINT ( 'NONE',  ( 3.270143674763207553, 13.28976595685393391, 3.277085381513166418 ) ) ;
#50345=ORIENTED_EDGE ( 'NONE', *, *, #44321, .F. ) ;
#50349=CARTESIAN_POINT ( 'NONE',  ( 1.227938101723756947, -34.55893248994489397, -25.45152231597092651 ) ) ;
#50355=ORIENTED_EDGE ( 'NONE', *, *, #31343, .T. ) ;
#50359=ORIENTED_EDGE ( 'NONE', *, *, #37459, .T. ) ;
#50360=EDGE_CURVE ( 'NONE', #6072, #33892, #26340, .T. ) ;
#50361=CARTESIAN_POINT ( 'NONE',  ( 0.5807400328401637335, 17.82553128098468420, -44.45848844984423920 ) ) ;
#50365=CARTESIAN_POINT ( 'NONE',  ( 0.5850706913938534814, -6.431767090162503031, -47.46255051844960349 ) ) ;
#50372=CARTESIAN_POINT ( 'NONE',  ( 0.5850706913938534814, -18.16120156791912521, 44.31965802246099884 ) ) ;
#50374=CARTESIAN_POINT ( 'NONE',  ( 4.956653778116975495, -36.51451553856441024, 31.29546495791839078 ) ) ;
#50388=CARTESIAN_POINT ( 'NONE',  ( 5.981074661064941900, 20.52466374824937034, 0.008585178657687824941 ) ) ;
#50389=CARTESIAN_POINT ( 'NONE',  ( 5.860006189529234355, -21.34829429597437311, -43.25137511473273122 ) ) ;
#50394=VERTEX_POINT ( 'NONE', #49598 ) ;
#50395=CARTESIAN_POINT ( 'NONE',  ( 3.407937589446174087, 7.243367523631186522, -11.62731850632876629 ) ) ;
#50402=ORIENTED_EDGE ( 'NONE', *, *, #36566, .T. ) ;
#50407=EDGE_CURVE ( 'NONE', #52413, #43658, #21412, .T. ) ;
#50411=( BOUNDED_SURFACE ( )  B_SPLINE_SURFACE ( 3, 1, ( 
 ( #32056, #23564 ),
 ( #60527, #17640 ),
 ( #55837, #41466 ),
 ( #51136, #37691 ) ),
 .UNSPECIFIED., .F., .F., .F. ) 
 B_SPLINE_SURFACE_WITH_KNOTS ( ( 4, 4 ),
 ( 2, 2 ),
 ( 0.000000000000000000, 1.000000000000000000 ),
 ( 0.000000000000000000, 1.000000000000000000 ),
 .UNSPECIFIED. ) 
 GEOMETRIC_REPRESENTATION_ITEM ( )  RATIONAL_B_SPLINE_SURFACE ( (
 ( 1.000000000000000000, 1.000000000000000000),
 ( 0.9953390228620291325, 0.8624445117760984880),
 ( 0.9953390228620291325, 0.8624445117760984880),
 ( 1.000000000000000000, 1.000000000000000000) ) ) 
 REPRESENTATION_ITEM ( '' )  SURFACE ( )  );
#50412=ORIENTED_EDGE ( 'NONE', *, *, #36442, .F. ) ;
#50417=EDGE_CURVE ( 'NONE', #29889, #437, #51647, .T. ) ;
#50420=FACE_OUTER_BOUND ( 'NONE', #47382, .T. ) ;
#50422=CARTESIAN_POINT ( 'NONE',  ( 0.9747592971366229042, 11.41797089479133476, 41.36145845824412959 ) ) ;
#50423=CARTESIAN_POINT ( 'NONE',  ( 5.974727161628369032, 2.694421823322918463, -20.34732802718244571 ) ) ;
#50440=CARTESIAN_POINT ( 'NONE',  ( 4.963659409799328515, 9.199077662859513893, -43.79875484948436082 ) ) ;
#50446=ORIENTED_EDGE ( 'NONE', *, *, #4768, .F. ) ;
#50450=CARTESIAN_POINT ( 'NONE',  ( 0.9745511491811756910, 37.32887948083628515, -21.15859207114708340 ) ) ;
#50451=CARTESIAN_POINT ( 'NONE',  ( 4.967162193818130511, 14.26841313271282097, 40.65506779172170582 ) ) ;
#50452=CARTESIAN_POINT ( 'NONE',  ( 0.5832366564991500191, 5.981458972434432475, -47.52097076201149406 ) ) ;
#50457=CARTESIAN_POINT ( 'NONE',  ( 0.8551540677456834771, 17.49081417858847942, -44.61036085020932518 ) ) ;
#50459=ORIENTED_EDGE ( 'NONE', *, *, #38247, .F. ) ;
#50465=CARTESIAN_POINT ( 'NONE',  ( 5.960721111146673579, 10.25731071096582880, -17.77882586010657207 ) ) ;
#50469=CARTESIAN_POINT ( 'NONE',  ( 0.9745511491811728044, -41.35688774886282459, -11.43411988112647037 ) ) ;
#50478=CARTESIAN_POINT ( 'NONE',  ( 5.960721111146673579, -2.685391721745896909, -20.34914600876574298 ) ) ;
#50485=ADVANCED_FACE ( 'NONE', ( #34784 ), #914, .F. ) ;
#50493=ORIENTED_EDGE ( 'NONE', *, *, #8600, .T. ) ;
#50495=CARTESIAN_POINT ( 'NONE',  ( 0.9756354156337454508, 26.01752520779911748, 34.12075394380514837 ) ) ;
#50496=AXIS2_PLACEMENT_3D ( 'NONE', #49371, #24338, #9941 ) ;
#50500=CARTESIAN_POINT ( 'NONE',  ( 4.967162193818130511, 0.000000000000000000, 0.000000000000000000 ) ) ;
#50502=CARTESIAN_POINT ( 'NONE',  ( 4.303969348037246512, -32.45857549159277511, -35.51084504003230080 ) ) ;
#50503=( BOUNDED_SURFACE ( )  B_SPLINE_SURFACE ( 3, 1, ( 
 ( #19179, #9441 ),
 ( #35, #9755 ),
 ( #48287, #38294 ),
 ( #27950, #28244 ) ),
 .UNSPECIFIED., .F., .F., .F. ) 
 B_SPLINE_SURFACE_WITH_KNOTS ( ( 4, 4 ),
 ( 2, 2 ),
 ( 0.000000000000000000, 1.000000000000000000 ),
 ( 0.000000000000000000, 1.000000000000000000 ),
 .UNSPECIFIED. ) 
 GEOMETRIC_REPRESENTATION_ITEM ( )  RATIONAL_B_SPLINE_SURFACE ( (
 ( 1.000000000000000000, 1.000000000000000000),
 ( 0.9953390228620291325, 0.8624445117760984880),
 ( 0.9953390228620291325, 0.8624445117760984880),
 ( 1.000000000000000000, 1.000000000000000000) ) ) 
 REPRESENTATION_ITEM ( '' )  SURFACE ( )  );
#50520=CARTESIAN_POINT ( 'NONE',  ( 0.9730545539215883499, 29.98130006528905156, -30.69604515769618658 ) ) ;
#50523=CARTESIAN_POINT ( 'NONE',  ( 0.5850706913938534814, 6.071602062251297838, -47.50996714391775555 ) ) ;
#50526=CARTESIAN_POINT ( 'NONE',  ( 0.5809828226811617480, -44.03860873105681151, -18.83114015454746237 ) ) ;
#50528=CARTESIAN_POINT ( 'NONE',  ( 2.624215991343620935, 38.92973006074512909, 28.09277600149231802 ) ) ;
#50530=ORIENTED_EDGE ( 'NONE', *, *, #31885, .F. ) ;
#50538=VERTEX_POINT ( 'NONE', #24753 ) ;
#50551=ORIENTED_EDGE ( 'NONE', *, *, #44868, .F. ) ;
#50553=CARTESIAN_POINT ( 'NONE',  ( 5.981074661064941900, 7.846517100474821760, -18.96560215432008789 ) ) ;
#50556=CARTESIAN_POINT ( 'NONE',  ( 5.960221823109900008, 14.51763960716778357, -14.50993159119795628 ) ) ;
#50561=CARTESIAN_POINT ( 'NONE',  ( 0.5800708119828343889, -17.74761857127099063, 44.48635609075551400 ) ) ;
#50562=VECTOR ( 'NONE', #1256, 1000.000000000000114 ) ;
#50563=ORIENTED_EDGE ( 'NONE', *, *, #4012, .F. ) ;
#50574=EDGE_CURVE ( 'NONE', #25700, #44327, #1541, .T. ) ;
#50576=( BOUNDED_SURFACE ( )  B_SPLINE_SURFACE ( 3, 1, ( 
 ( #8150, #2195 ),
 ( #27265, #26640 ),
 ( #16961, #12258 ),
 ( #21333, #3432 ) ),
 .UNSPECIFIED., .F., .F., .F. ) 
 B_SPLINE_SURFACE_WITH_KNOTS ( ( 4, 4 ),
 ( 2, 2 ),
 ( 0.000000000000000000, 1.000000000000000000 ),
 ( 0.000000000000000000, 1.000000000000000000 ),
 .UNSPECIFIED. ) 
 GEOMETRIC_REPRESENTATION_ITEM ( )  RATIONAL_B_SPLINE_SURFACE ( (
 ( 1.000000000000000000, 1.000000000000000000),
 ( 0.7269869731126817891, 0.9931720237060910339),
 ( 0.7269869731126817891, 0.9931720237060910339),
 ( 1.000000000000000000, 1.000000000000000000) ) ) 
 REPRESENTATION_ITEM ( '' )  SURFACE ( )  );
#50587=FACE_OUTER_BOUND ( 'NONE', #46264, .T. ) ;
#50596=CARTESIAN_POINT ( 'NONE',  ( 0.8557997880470690211, -38.55640757422419540, -28.43566216845010075 ) ) ;
#50602=CARTESIAN_POINT ( 'NONE',  ( 2.526552050251863246, -1.212569781798230162, 42.96196914573631886 ) ) ;
#50604=CARTESIAN_POINT ( 'NONE',  ( 4.956653778116966613, 0.000000000000000000, 0.000000000000000000 ) ) ;
#50610=CIRCLE ( 'NONE', #613, 43.08621763946400307 ) ;
#50613=VERTEX_POINT ( 'NONE', #22528 ) ;
#50617=CARTESIAN_POINT ( 'NONE',  ( 2.281351352603289140, -38.84542754822344079, 28.15073776031352537 ) ) ;
#50620=ORIENTED_EDGE ( 'NONE', *, *, #17148, .T. ) ;
#50626=CARTESIAN_POINT ( 'NONE',  ( 4.967162193818129623, 32.10009971360071290, 28.74031574030022540 ) ) ;
#50627=CARTESIAN_POINT ( 'NONE',  ( 4.303969348037258058, 43.57722561725987021, -20.38638383586072678 ) ) ;
#50630=CARTESIAN_POINT ( 'NONE',  ( 5.860006189529234355, 21.31760477694640343, -43.26650951066848449 ) ) ;
#50646=DIRECTION ( 'NONE',  ( -0.07836865515943411409, 0.6131273243286226027, 0.7860872967108205600 ) ) ;
#50649=EDGE_LOOP ( 'NONE', ( #40059, #306, #1754, #18190 ) ) ;
#50655=B_SPLINE_CURVE_WITH_KNOTS ( 'NONE', 3,
 ( #13122, #36938, #37551, #32529 ),
 .UNSPECIFIED., .F., .F.,
 ( 4, 4 ),
 ( 4.336808689942017736E-19, 0.004444878191957702535 ),
 .UNSPECIFIED. ) ;
#50662=CARTESIAN_POINT ( 'NONE',  ( 0.9756950546413942771, -30.27237962848458963, 30.40918718457328040 ) ) ;
#50667=CARTESIAN_POINT ( 'NONE',  ( 5.960221823109900008, 18.96526051813980374, -7.849768660536363463 ) ) ;
#50668=CARTESIAN_POINT ( 'NONE',  ( 0.9730545539215883499, -42.60426903087349615, -5.099196237955331057 ) ) ;
#50669=EDGE_CURVE ( 'NONE', #33332, #6666, #26919, .T. ) ;
#50670=LINE ( 'NONE', #42242, #31625 ) ;
#50673=CARTESIAN_POINT ( 'NONE',  ( 3.783278058412225420, 12.79810311738853201, 41.09146792477071131 ) ) ;
#50677=CARTESIAN_POINT ( 'NONE',  ( 0.7762783648524366198, -47.89627393592494542, 0.8897020150996511889 ) ) ;
#50689=LINE ( 'NONE', #27209, #54517 ) ;
#50690=VERTEX_POINT ( 'NONE', #17519 ) ;
#50694=ORIENTED_EDGE ( 'NONE', *, *, #25283, .F. ) ;
#50696=CARTESIAN_POINT ( 'NONE',  ( 3.660176727303394717, 48.00143922595156454, 1.881607889987920501 ) ) ;
#50704=AXIS2_PLACEMENT_3D ( 'NONE', #21253, #44774, #26248 ) ;
#50706=DIRECTION ( 'NONE',  ( -0.07439287786467650709, 0.7830499462674596067, -0.6174937095821624311 ) ) ;
#50708=ORIENTED_EDGE ( 'NONE', *, *, #9257, .T. ) ;
#50709=CARTESIAN_POINT ( 'NONE',  ( 0.5832367798473401255, -37.83194459509889640, -29.37285281143879700 ) ) ;
#50713=FACE_OUTER_BOUND ( 'NONE', #1433, .T. ) ;
#50722=ORIENTED_EDGE ( 'NONE', *, *, #48457, .T. ) ;
#50725=CARTESIAN_POINT ( 'NONE',  ( 0.9754642270333674370, 34.14824330022369026, -25.98138239028824259 ) ) ;
#50741=B_SPLINE_CURVE_WITH_KNOTS ( 'NONE', 3,
 ( #57367, #43955, #44259, #49228, #52686, #5058, #14502, #356, #989, #34843, #5667, #28887, #9785, #48010, #53910, #24187, #33609, #19507, #38622 ),
 .UNSPECIFIED., .F., .F.,
 ( 4, 3, 3, 3, 3, 3, 4 ),
 ( 3.469446951953614189E-18, 0.0002724573126191767855, 0.0004086839781548511335, 0.0005449106435901861483, 0.0006811373090491516747, 0.0008459866663933716512, 0.001010840725717212932 ),
 .UNSPECIFIED. ) ;
#50745=CARTESIAN_POINT ( 'NONE',  ( 1.227938101723756947, -41.23019537246717903, 11.92353943227934998 ) ) ;
#50746=CARTESIAN_POINT ( 'NONE',  ( 5.959828726073459926, -16.28130559351273376, 12.49879082830540789 ) ) ;
#50751=CARTESIAN_POINT ( 'NONE',  ( 0.5819845079324650339, 5.801222053075765217, -47.54334065046000291 ) ) ;
#50753=CARTESIAN_POINT ( 'NONE',  ( 3.783198216974394512, 27.54889409286126778, -33.06596988314768026 ) ) ;
#50761=CARTESIAN_POINT ( 'NONE',  ( 0.8557997880470599172, 13.27832040216703469, -46.03118133706011861 ) ) ;
#50763=DIRECTION ( 'NONE',  ( 0.000000000000000000, 0.000000000000000000, 1.000000000000000000 ) ) ;
#50766=CARTESIAN_POINT ( 'NONE',  ( 5.965394784446458765, 10.25014670152115137, -17.78272165951790740 ) ) ;
#50768=ORIENTED_EDGE ( 'NONE', *, *, #17839, .F. ) ;
#50769=DIRECTION ( 'NONE',  ( 0.000000000000000000, 0.000000000000000000, 1.000000000000000000 ) ) ;
#50771=CARTESIAN_POINT ( 'NONE',  ( 4.960156602257182357, 45.42786611289328391, -9.558288641081281511 ) ) ;
#50773=EDGE_CURVE ( 'NONE', #36851, #1494, #1483, .T. ) ;
#50779=ORIENTED_EDGE ( 'NONE', *, *, #9635, .F. ) ;
#50782=CARTESIAN_POINT ( 'NONE',  ( 5.960221823109900008, -2.684531185214278803, -20.34928172836729843 ) ) ;
#50784=ORIENTED_EDGE ( 'NONE', *, *, #42946, .T. ) ;
#50788=CARTESIAN_POINT ( 'NONE',  ( 0.9740398440564311811, 16.80263250099888239, 39.48175649279239252 ) ) ;
#50791=CIRCLE ( 'NONE', #17813, 48.09070567114147110 ) ;
#50792=CARTESIAN_POINT ( 'NONE',  ( 4.956653778117001252, 45.71126949320271393, -14.93973939759840519 ) ) ;
#50798=VERTEX_POINT ( 'NONE', #61331 ) ;
#50800=CARTESIAN_POINT ( 'NONE',  ( 0.9730545539215883499, -42.47233286818612896, -6.101350888305089093 ) ) ;
#50805=CARTESIAN_POINT ( 'NONE',  ( 0.5786265663353196143, -6.967625775956046041, 47.39171391660389077 ) ) ;
#50814=CARTESIAN_POINT ( 'NONE',  ( 0.9749527285493315709, -16.68386601451066653, 39.53206838353040808 ) ) ;
#50822=CARTESIAN_POINT ( 'NONE',  ( 0.9968887458511649369, 4.948372828380764865, 42.62316256128683989 ) ) ;
#50828=CARTESIAN_POINT ( 'NONE',  ( 5.860006189529234355, -48.12869875779311002, 3.171667470662350663 ) ) ;
#50830=EDGE_CURVE ( 'NONE', #42440, #50327, #47781, .T. ) ;
#50841=EDGE_CURVE ( 'NONE', #23496, #56700, #48478, .T. ) ;
#50842=CARTESIAN_POINT ( 'NONE',  ( 1.227938101723747621, 6.439911493065174852, -42.43379953535178828 ) ) ;
#50851=CARTESIAN_POINT ( 'NONE',  ( 0.5809828226811553087, 47.89273459658653564, -0.5448590168534052092 ) ) ;
#50866=CARTESIAN_POINT ( 'NONE',  ( 0.5786265663353153954, -33.35675271369563433, 34.37803667029800181 ) ) ;
#50872=EDGE_CURVE ( 'NONE', #25685, #18352, #9708, .T. ) ;
#50874=FACE_OUTER_BOUND ( 'NONE', #50049, .T. ) ;
#50892=CARTESIAN_POINT ( 'NONE',  ( 0.5800708119828335008, -6.873289505980332059, -47.40012378203037002 ) ) ;
#50898=DIRECTION ( 'NONE',  ( -1.000000000000000000, -0.000000000000000000, -0.000000000000000000 ) ) ;
#50907=EDGE_CURVE ( 'NONE', #6995, #14400, #5903, .T. ) ;
#50909=ORIENTED_EDGE ( 'NONE', *, *, #13351, .F. ) ;
#50910=ORIENTED_EDGE ( 'NONE', *, *, #2605, .T. ) ;
#50915=ORIENTED_EDGE ( 'NONE', *, *, #20179, .F. ) ;
#50936=CARTESIAN_POINT ( 'NONE',  ( 3.783198216974387851, -27.54889409286103330, 33.06596988314791474 ) ) ;
#50940=ORIENTED_EDGE ( 'NONE', *, *, #1727, .F. ) ;
#50942=CARTESIAN_POINT ( 'NONE',  ( 4.960156602257181468, -25.36362146861414146, 38.88108289790854855 ) ) ;
#50945=CARTESIAN_POINT ( 'NONE',  ( 1.088908134280554219, -15.69861202536780276, 39.93902428011485739 ) ) ;
#50952=ORIENTED_EDGE ( 'NONE', *, *, #23429, .T. ) ;
#50961=B_SPLINE_CURVE_WITH_KNOTS ( 'NONE', 3,
 ( #5376, #10731, #48934, #48018, #39251, #688 ),
 .UNSPECIFIED., .F., .F.,
 ( 4, 2, 4 ),
 ( 8.148123767742043513E-18, 0.0002291978881530126635, 0.0004583957763060171413 ),
 .UNSPECIFIED. ) ;
#50962=EDGE_LOOP ( 'NONE', ( #4243, #61183 ) ) ;
#50967=ORIENTED_EDGE ( 'NONE', *, *, #31885, .T. ) ;
#50973=CARTESIAN_POINT ( 'NONE',  ( 0.5807400328401637335, 44.04145271122565219, 18.83234461715199970 ) ) ;
#50974=CARTESIAN_POINT ( 'NONE',  ( 0.9756354156337442296, 5.729847988735970787, -42.52418499698892873 ) ) ;
#50975=CARTESIAN_POINT ( 'NONE',  ( 0.8551540677456834771, 28.44084013485174012, -38.56334384152401640 ) ) ;
#50978=CARTESIAN_POINT ( 'NONE',  ( 5.965394784446460541, 5.326334832595648550, -19.82223131420049000 ) ) ;
#50980=CARTESIAN_POINT ( 'NONE',  ( 0.9754402186311939005, -39.57010335554342362, 16.59348191374125392 ) ) ;
#50982=ADVANCED_FACE ( 'NONE', ( #21521 ), #54504, .F. ) ;
#50989=CARTESIAN_POINT ( 'NONE',  ( 0.5832366564991497970, -24.18352361336798140, -41.34220239954010623 ) ) ;
#50990=CARTESIAN_POINT ( 'NONE',  ( 3.783198216974388739, 29.18723368117363393, 31.62918462580848455 ) ) ;
#50991=DIRECTION ( 'NONE',  ( 1.000000000000000000, -0.000000000000000000, -0.000000000000000000 ) ) ;
#50994=CARTESIAN_POINT ( 'NONE',  ( 5.960721111146673579, 18.96073515164537326, 7.860635756377957861 ) ) ;
#51001=ORIENTED_EDGE ( 'NONE', *, *, #31047, .F. ) ;
#51014=CARTESIAN_POINT ( 'NONE',  ( 0.5834872094924173913, -29.33699246747726264, 37.85980081020210264 ) ) ;
#51015=ORIENTED_EDGE ( 'NONE', *, *, #40419, .T. ) ;
#51025=CARTESIAN_POINT ( 'NONE',  ( 0.9752132459055860014, -0.2329632697540915398, -42.90780255730425097 ) ) ;
#51030=VERTEX_POINT ( 'NONE', #60634 ) ;
#51035=CARTESIAN_POINT ( 'NONE',  ( 0.9756950546413938330, 33.98259063592758622, -26.19769393035335625 ) ) ;
#51038=ORIENTED_EDGE ( 'NONE', *, *, #12148, .F. ) ;
#51044=CARTESIAN_POINT ( 'NONE',  ( 2.281448460670565392, -32.98023336626259550, 34.83871297539693046 ) ) ;
#51048=CIRCLE ( 'NONE', #27053, 43.08621763946400307 ) ;
#51053=CARTESIAN_POINT ( 'NONE',  ( 2.526552050251864134, 36.59987178591183010, 22.53110080776668767 ) ) ;
#51057=CARTESIAN_POINT ( 'NONE',  ( 4.303969348037258058, 20.38638383586119929, 43.57722561725964994 ) ) ;
#51058=EDGE_CURVE ( 'NONE', #28220, #5855, #4467, .T. ) ;
#51060=CARTESIAN_POINT ( 'NONE',  ( 4.956653778116475451, 47.27023054223744225, 8.845409907520236814 ) ) ;
#51061=CARTESIAN_POINT ( 'NONE',  ( 5.960221823109900008, 5.317678907195437787, -19.82478916873570185 ) ) ;
#51062=EDGE_CURVE ( 'NONE', #9975, #53201, #7472, .T. ) ;
#51066=CARTESIAN_POINT ( 'NONE',  ( 0.8557997880470606944, -24.73961900479280374, 41.02602466100771039 ) ) ;
#51079=VERTEX_POINT ( 'NONE', #42501 ) ;
#51081=ORIENTED_EDGE ( 'NONE', *, *, #41318, .F. ) ;
#51082=ORIENTED_EDGE ( 'NONE', *, *, #29845, .F. ) ;
#51083=CARTESIAN_POINT ( 'NONE',  ( 0.9756950546413946102, -5.504753251348003751, 42.55388731055339235 ) ) ;
#51084=VERTEX_POINT ( 'NONE', #13997 ) ;
#51098=EDGE_LOOP ( 'NONE', ( #32903, #5928, #1030, #56623 ) ) ;
#51099=CARTESIAN_POINT ( 'NONE',  ( 2.526464513654346433, 22.53107770806421684, 36.59988118252409350 ) ) ;
#51100=EDGE_CURVE ( 'NONE', #9101, #22050, #41393, .T. ) ;
#51103=B_SPLINE_CURVE_WITH_KNOTS ( 'NONE', 3,
 ( #45635, #54999, #12128, #25896 ),
 .UNSPECIFIED., .F., .F.,
 ( 4, 4 ),
 ( 4.336808689942017736E-19, 0.004444878191956859459 ),
 .UNSPECIFIED. ) ;
#51105=ORIENTED_EDGE ( 'NONE', *, *, #28188, .F. ) ;
#51106=CARTESIAN_POINT ( 'NONE',  ( 0.5839879882012690704, -46.26395995854825571, -12.39635945869009781 ) ) ;
#51108=ADVANCED_FACE ( 'NONE', ( #56868 ), #61865, .F. ) ;
#51109=LINE ( 'NONE', #26698, #25657 ) ;
#51121=CARTESIAN_POINT ( 'NONE',  ( 0.5838002273316424962, -46.29900743592988022, 12.26477999444052180 ) ) ;
#51122=EDGE_CURVE ( 'NONE', #60647, #35431, #43353, .T. ) ;
#51129=CARTESIAN_POINT ( 'NONE',  ( 0.8557997880470599172, -0.9121262075949487791, 47.89938907511593413 ) ) ;
#51131=CARTESIAN_POINT ( 'NONE',  ( 1.227938101723756947, 4.762198645645047357, -42.65467462194912684 ) ) ;
#51134=( BOUNDED_SURFACE ( )  B_SPLINE_SURFACE ( 3, 1, ( 
 ( #28525, #28223 ),
 ( #37973, #5014 ),
 ( #57946, #631 ),
 ( #14454, #10054 ) ),
 .UNSPECIFIED., .F., .F., .F. ) 
 B_SPLINE_SURFACE_WITH_KNOTS ( ( 4, 4 ),
 ( 2, 2 ),
 ( 0.000000000000000000, 1.000000000000000000 ),
 ( 0.000000000000000000, 1.000000000000000000 ),
 .UNSPECIFIED. ) 
 GEOMETRIC_REPRESENTATION_ITEM ( )  RATIONAL_B_SPLINE_SURFACE ( (
 ( 1.000000000000000000, 1.000000000000000000),
 ( 0.9953390228620291325, 0.8624445117760984880),
 ( 0.9953390228620291325, 0.8624445117760984880),
 ( 1.000000000000000000, 1.000000000000000000) ) ) 
 REPRESENTATION_ITEM ( '' )  SURFACE ( )  );
#51136=CARTESIAN_POINT ( 'NONE',  ( 5.959547316686252039, 10.26589671991363417, -17.77392908783923531 ) ) ;
#51144=FACE_OUTER_BOUND ( 'NONE', #15317, .T. ) ;
#51160=B_SPLINE_CURVE_WITH_KNOTS ( 'NONE', 3,
 ( #52583, #9059, #38518, #48213, #34126, #4960 ),
 .UNSPECIFIED., .F., .F.,
 ( 4, 2, 4 ),
 ( 9.543442895606953578E-18, 0.0002291978881530158890, 0.0004583957763060222371 ),
 .UNSPECIFIED. ) ;
#51169=CARTESIAN_POINT ( 'NONE',  ( 1.088908134280559104, 20.77739698351986064, -37.54826033999239598 ) ) ;
#51170=CARTESIAN_POINT ( 'NONE',  ( 2.281448460670567169, 30.23587867650755001, 37.24544744441590183 ) ) ;
#51174=EDGE_LOOP ( 'NONE', ( #4997, #35536, #215, #50459 ) ) ;
#51179=CONICAL_SURFACE ( 'NONE', #14189, 43.08621763946400307, 1.568696531533066763 ) ;
#51181=ORIENTED_EDGE ( 'NONE', *, *, #41318, .T. ) ;
#51188=EDGE_LOOP ( 'NONE', ( #12218, #8643, #18909, #11852 ) ) ;
#51194=CARTESIAN_POINT ( 'NONE',  ( 5.959828726073459926, -5.316791119501226071, 19.82504517499703667 ) ) ;
#51195=CARTESIAN_POINT ( 'NONE',  ( 0.7056555295713294873, -7.085402321211474508, -47.37451042924661948 ) ) ;
#51199=DIRECTION ( 'NONE',  ( 0.000000000000000000, 0.000000000000000000, 1.000000000000000000 ) ) ;
#51201=CARTESIAN_POINT ( 'NONE',  ( 0.5800708119828338338, 11.78915056783772819, -46.42229822050683907 ) ) ;
#51212=CARTESIAN_POINT ( 'NONE',  ( 1.088313998177380837, -6.373602917100484433, 42.43756598879026143 ) ) ;
#51219=ORIENTED_EDGE ( 'NONE', *, *, #29079, .T. ) ;
#51225=VERTEX_POINT ( 'NONE', #5775 ) ;
#51233=( BOUNDED_SURFACE ( )  B_SPLINE_SURFACE ( 3, 1, ( 
 ( #50119, #55108 ),
 ( #26612, #31628 ),
 ( #31944, #59817 ),
 ( #7808, #12233 ) ),
 .UNSPECIFIED., .F., .F., .F. ) 
 B_SPLINE_SURFACE_WITH_KNOTS ( ( 4, 4 ),
 ( 2, 2 ),
 ( 0.000000000000000000, 1.000000000000000000 ),
 ( 0.000000000000000000, 1.000000000000000000 ),
 .UNSPECIFIED. ) 
 GEOMETRIC_REPRESENTATION_ITEM ( )  RATIONAL_B_SPLINE_SURFACE ( (
 ( 1.000000000000000000, 1.000000000000000000),
 ( 0.9953390228620291325, 0.8624445117761032620),
 ( 0.9953390228620291325, 0.8624445117761032620),
 ( 1.000000000000000000, 1.000000000000000000) ) ) 
 REPRESENTATION_ITEM ( '' )  SURFACE ( )  );
#51239=DIRECTION ( 'NONE',  ( 0.000000000000000000, 0.000000000000000000, 1.000000000000000000 ) ) ;
#51255=CARTESIAN_POINT ( 'NONE',  ( 1.154321713695928064, -4.782433421669802343, -42.64911660416110095 ) ) ;
#51256=CARTESIAN_POINT ( 'NONE',  ( 5.960721111146673579, 18.96557324978276071, 7.848955554238579602 ) ) ;
#51257=EDGE_CURVE ( 'NONE', #14851, #24833, #61172, .T. ) ;
#51259=ORIENTED_EDGE ( 'NONE', *, *, #34000, .F. ) ;
#51261=EDGE_CURVE ( 'NONE', #46800, #355, #7637, .T. ) ;
#51262=CARTESIAN_POINT ( 'NONE',  ( 0.9730545539215883499, 0.5054011016612682816, 42.90536227157002003 ) ) ;
#51266=CARTESIAN_POINT ( 'NONE',  ( -20.06025149405489216, -12.49772002914247437, 0.2740165342859215980 ) ) ;
#51270=EDGE_CURVE ( 'NONE', #37539, #6666, #49985, .T. ) ;
#51271=CARTESIAN_POINT ( 'NONE',  ( 2.526464513654345989, 41.81190200959800052, 9.948146339971373209 ) ) ;
#51272=CARTESIAN_POINT ( 'NONE',  ( 0.6067099128993244106, 23.33192673707591069, -41.82996792600754077 ) ) ;
#51274=CARTESIAN_POINT ( 'NONE',  ( 0.8551540677456834771, 7.157691013574357441, 47.37911285756623414 ) ) ;
#51277=CARTESIAN_POINT ( 'NONE',  ( 5.959828726073459926, -7.858992891710265383, 18.96145866559658799 ) ) ;
#51279=CARTESIAN_POINT ( 'NONE',  ( 5.860006189529234355, 3.171667470662518085, 48.12869875779310291 ) ) ;
#51280=CARTESIAN_POINT ( 'NONE',  ( 0.9756950546413947212, 5.504753251348322607, -42.55388731055334972 ) ) ;
#51286=CARTESIAN_POINT ( 'NONE',  ( 5.959547316686252039, 14.51632612601508754, 14.51128755440546314 ) ) ;
#51290=B_SPLINE_CURVE_WITH_KNOTS ( 'NONE', 3,
 ( #54655, #7986, #2035, #27100 ),
 .UNSPECIFIED., .F., .F.,
 ( 4, 4 ),
 ( 5.421010862427521207E-19, 0.004444878191957673044 ),
 .UNSPECIFIED. ) ;
#51299=LINE ( 'NONE', #23125, #32328 ) ;
#51307=CARTESIAN_POINT ( 'NONE',  ( 0.5809828226811617480, 5.711058609465307967, 47.55412398569209387 ) ) ;
#51308=( BOUNDED_SURFACE ( )  B_SPLINE_SURFACE ( 3, 1, ( 
 ( #35450, #31662 ),
 ( #21645, #12265 ),
 ( #56065, #46701 ),
 ( #51362, #2828 ) ),
 .UNSPECIFIED., .F., .F., .F. ) 
 B_SPLINE_SURFACE_WITH_KNOTS ( ( 4, 4 ),
 ( 2, 2 ),
 ( 0.000000000000000000, 1.000000000000000000 ),
 ( 0.000000000000000000, 1.000000000000000000 ),
 .UNSPECIFIED. ) 
 GEOMETRIC_REPRESENTATION_ITEM ( )  RATIONAL_B_SPLINE_SURFACE ( (
 ( 1.000000000000000000, 1.000000000000000000),
 ( 0.9953390228620291325, 0.8624445117761032620),
 ( 0.9953390228620291325, 0.8624445117761032620),
 ( 1.000000000000000000, 1.000000000000000000) ) ) 
 REPRESENTATION_ITEM ( '' )  SURFACE ( )  );
#51311=EDGE_LOOP ( 'NONE', ( #29988, #39246, #53605, #4498 ) ) ;
#51318=CARTESIAN_POINT ( 'NONE',  ( 0.9752132459055856684, 21.65565338840816167, 37.04276540031517584 ) ) ;
#51320=VECTOR ( 'NONE', #60399, 1000.000000000000114 ) ;
#51325=CARTESIAN_POINT ( 'NONE',  ( 5.960221823109900008, 12.49951306783089322, -16.28072933292535041 ) ) ;
#51328=ORIENTED_EDGE ( 'NONE', *, *, #56900, .T. ) ;
#51334=ORIENTED_EDGE ( 'NONE', *, *, #9824, .T. ) ;
#51336=EDGE_CURVE ( 'NONE', #49382, #31306, #46229, .T. ) ;
#51337=CARTESIAN_POINT ( 'NONE',  ( 4.956653778116966613, 0.000000000000000000, 0.000000000000000000 ) ) ;
#51342=CARTESIAN_POINT ( 'NONE',  ( 0.9756354156337444516, 34.12075394380545390, -26.01752520779878353 ) ) ;
#51348=ORIENTED_EDGE ( 'NONE', *, *, #38917, .T. ) ;
#51352=CARTESIAN_POINT ( 'NONE',  ( 0.9756354156337436745, -34.12075394380529048, 26.01752520779901445 ) ) ;
#51356=VERTEX_POINT ( 'NONE', #36807 ) ;
#51358=FACE_OUTER_BOUND ( 'NONE', #8065, .T. ) ;
#51362=CARTESIAN_POINT ( 'NONE',  ( 5.960721111146673579, 18.96073515164548340, -7.860635756377695849 ) ) ;
#51366=CARTESIAN_POINT ( 'NONE',  ( 0.5807400328401637335, -11.87003418057275539, 46.40483864045141615 ) ) ;
#51369=ORIENTED_EDGE ( 'NONE', *, *, #45923, .F. ) ;
#51370=CARTESIAN_POINT ( 'NONE',  ( 3.660087539127323542, -43.62750476736565730, 20.10768839917389883 ) ) ;
#51373=CARTESIAN_POINT ( 'NONE',  ( 5.860006189529234355, 43.25137511473280938, -21.34829429597422035 ) ) ;
#51375=CARTESIAN_POINT ( 'NONE',  ( 0.7056555295713292653, -46.04438433984162771, 13.20840017675001832 ) ) ;
#51377=ORIENTED_EDGE ( 'NONE', *, *, #16839, .T. ) ;
#51384=ORIENTED_EDGE ( 'NONE', *, *, #23018, .F. ) ;
#51393=CARTESIAN_POINT ( 'NONE',  ( 0.9747592971366236814, 16.71904224817905771, 39.51726118357597528 ) ) ;
#51395=ORIENTED_EDGE ( 'NONE', *, *, #58378, .T. ) ;
#51403=AXIS2_PLACEMENT_3D ( 'NONE', #26302, #41060, #41356 ) ;
#51408=CARTESIAN_POINT ( 'NONE',  ( 0.5807400328401637335, -23.47602859900684535, -41.75144119563910294 ) ) ;
#51416=CARTESIAN_POINT ( 'NONE',  ( 5.965394784446460541, 18.96850062921634361, -7.841344330024745624 ) ) ;
#51417=CARTESIAN_POINT ( 'NONE',  ( 0.9741495583595177754, -16.78504838919912245, 39.48917442789116450 ) ) ;
#51420=B_SPLINE_CURVE_WITH_KNOTS ( 'NONE', 3,
 ( #57198, #14333, #61898, #33439 ),
 .UNSPECIFIED., .F., .F.,
 ( 4, 4 ),
 ( 2.602085213965210642E-18, 0.004050076154993004218 ),
 .UNSPECIFIED. ) ;
#51425=CARTESIAN_POINT ( 'NONE',  ( 0.5839254288179547281, -46.28738487712336536, 12.30867641975561178 ) ) ;
#51427=CARTESIAN_POINT ( 'NONE',  ( 1.227938101723748288, 4.762198645644436290, 42.65467462194920500 ) ) ;
#51432=CARTESIAN_POINT ( 'NONE',  ( 0.9736507210033064075, 36.93248879681210184, 21.84312502845804005 ) ) ;
#51434=CARTESIAN_POINT ( 'NONE',  ( 0.9747592971366237924, -37.32069240268756971, -21.17324310849270930 ) ) ;
#51439=VERTEX_POINT ( 'NONE', #41502 ) ;
#51440=ORIENTED_EDGE ( 'NONE', *, *, #48935, .T. ) ;
#51443=CARTESIAN_POINT ( 'NONE',  ( 0.5809828226811617480, -34.25055090842177208, 33.48000389720603920 ) ) ;
#51446=CARTESIAN_POINT ( 'NONE',  ( 4.956653778116992370, 27.17045123668527751, -39.67974989265010777 ) ) ;
#51453=CARTESIAN_POINT ( 'NONE',  ( 0.9756354156337452288, -10.97961179198170356, -41.47994205070126128 ) ) ;
#51467=ORIENTED_EDGE ( 'NONE', *, *, #12836, .F. ) ;
#51468=CARTESIAN_POINT ( 'NONE',  ( 0.9722240750034587542, -29.92651530838607954, 30.74950257331008885 ) ) ;
#51472=CARTESIAN_POINT ( 'NONE',  ( 4.967162193818130511, 0.000000000000000000, 0.000000000000000000 ) ) ;
#51486=CARTESIAN_POINT ( 'NONE',  ( 0.9754642270333676590, 30.21634823122169777, 30.46484943293168257 ) ) ;
#51487=CARTESIAN_POINT ( 'NONE',  ( 1.227938101723748288, 42.65467462194924764, -4.762198645644009076 ) ) ;
#51488=CIRCLE ( 'NONE', #24492, 43.08621763946400307 ) ;
#51490=CARTESIAN_POINT ( 'NONE',  ( 4.967162193818130511, 18.65818244221310351, -38.83676580803746958 ) ) ;
#51492=CARTESIAN_POINT ( 'NONE',  ( 5.958863334805807099, -10.26388325355075359, -17.77512673691315470 ) ) ;
#51495=B_SPLINE_CURVE_WITH_KNOTS ( 'NONE', 3,
 ( #55632, #41575, #50942, #31230 ),
 .UNSPECIFIED., .F., .F.,
 ( 4, 4 ),
 ( 0.000000000000000000, 0.005004741218457409331 ),
 .UNSPECIFIED. ) ;
#51499=CARTESIAN_POINT ( 'NONE',  ( 5.958863334805807099, 12.49425770716487527, -16.28483817244726950 ) ) ;
#51500=CARTESIAN_POINT ( 'NONE',  ( -48.95476116535499500, 0.000000000000000000, 0.000000000000000000 ) ) ;
#51507=CARTESIAN_POINT ( 'NONE',  ( 2.624215991343608501, -13.78323291683815377, 45.98641578154027343 ) ) ;
#51516=CARTESIAN_POINT ( 'NONE',  ( 1.227938101723756947, -36.73927144310528092, 22.18841447410706635 ) ) ;
#51526=DIRECTION ( 'NONE',  ( 0.000000000000000000, 0.000000000000000000, 1.000000000000000000 ) ) ;
#51527=CARTESIAN_POINT ( 'NONE',  ( 3.407937589446178528, 6.447869442558332942, -12.08659953757602068 ) ) ;
#51529=ORIENTED_EDGE ( 'NONE', *, *, #22135, .F. ) ;
#51530=ORIENTED_EDGE ( 'NONE', *, *, #45996, .F. ) ;
#51531=CARTESIAN_POINT ( 'NONE',  ( 0.9730545539215883499, 41.57420493492384850, 10.61654491617579055 ) ) ;
#51541=EDGE_CURVE ( 'NONE', #10414, #58260, #29016, .T. ) ;
#51546=EDGE_CURVE ( 'NONE', #38319, #5144, #59187, .T. ) ;
#51549=CARTESIAN_POINT ( 'NONE',  ( 4.963659409799330291, -13.93274247732050597, 42.53037318520990340 ) ) ;
#51552=CARTESIAN_POINT ( 'NONE',  ( 0.9757619758474603833, 0.06449181910581339161, 42.90842306541549789 ) ) ;
#51553=CARTESIAN_POINT ( 'NONE',  ( 0.5839879882012685153, 41.47913983251949332, 23.94795769224401027 ) ) ;
#51556=ORIENTED_EDGE ( 'NONE', *, *, #11123, .T. ) ;
#51562=ORIENTED_EDGE ( 'NONE', *, *, #40365, .T. ) ;
#51577=EDGE_LOOP ( 'NONE', ( #32926, #33863, #8495, #35728 ) ) ;
#51583=CARTESIAN_POINT ( 'NONE',  ( 0.9736507210033064075, 6.046964561328548982, -42.48017254354716954 ) ) ;
#51584=CARTESIAN_POINT ( 'NONE',  ( 5.960221823109900008, -10.26751639438355923, -17.77295928189551688 ) ) ;
#51585=CARTESIAN_POINT ( 'NONE',  ( 4.967162193818130511, 14.26841313271282097, 40.65506779172170582 ) ) ;
#51589=CARTESIAN_POINT ( 'NONE',  ( 5.959828726073459926, -17.77796293532179916, 10.25888482581828676 ) ) ;
#51590=CARTESIAN_POINT ( 'NONE',  ( 3.270143674763207553, 1.514386915940589384, 13.60381564321234826 ) ) ;
#51594=CARTESIAN_POINT ( 'NONE',  ( 5.960721111146673579, -10.26825948882913586, -17.77250458025988422 ) ) ;
#51595=CARTESIAN_POINT ( 'NONE',  ( 5.959828726073459926, 18.96145866559661286, 7.858992891710209427 ) ) ;
#51600=DIRECTION ( 'NONE',  ( 0.000000000000000000, 0.000000000000000000, 1.000000000000000000 ) ) ;
#51603=B_SPLINE_CURVE_WITH_KNOTS ( 'NONE', 3,
 ( #18984, #38101, #52457, #47786 ),
 .UNSPECIFIED., .F., .F.,
 ( 4, 4 ),
 ( 0.000000000000000000, 0.004444878191957690391 ),
 .UNSPECIFIED. ) ;
#51606=CARTESIAN_POINT ( 'NONE',  ( 0.9754402186311945666, 10.92425836141477014, -41.49454543482920599 ) ) ;
#51607=ADVANCED_FACE ( 'NONE', ( #20080 ), #52392, .T. ) ;
#51615=B_SPLINE_CURVE_WITH_KNOTS ( 'NONE', 3,
 ( #25281, #16826, #49392, #6446 ),
 .UNSPECIFIED., .F., .F.,
 ( 4, 4 ),
 ( 9.868122050982122734E-17, 0.005004741218457526425 ),
 .UNSPECIFIED. ) ;
#51624=AXIS2_PLACEMENT_3D ( 'NONE', #27070, #17069, #8566 ) ;
#51630=CARTESIAN_POINT ( 'NONE',  ( 0.9745511491811742477, 21.15859207114749196, 37.32887948083607910 ) ) ;
#51633=CARTESIAN_POINT ( 'NONE',  ( 0.8557997880470690211, -34.51495345639526136, -33.22501220301936797 ) ) ;
#51639=CARTESIAN_POINT ( 'NONE',  ( 2.281448460670565836, 46.66132715497963090, 11.14236343022389164 ) ) ;
#51641=CARTESIAN_POINT ( 'NONE',  ( 0.5809828226811548646, 29.58751527316178809, 37.66417181417562432 ) ) ;
#51642=DIRECTION ( 'NONE',  ( -1.000000000000000000, -0.000000000000000000, -0.000000000000000000 ) ) ;
#51643=CARTESIAN_POINT ( 'NONE',  ( 0.8551540677456715978, -37.45266983663474747, -29.88829867897853632 ) ) ;
#51645=CARTESIAN_POINT ( 'NONE',  ( 0.9757787079277443487, 11.06737752163097355, 41.45659305953925866 ) ) ;
#51647=B_SPLINE_CURVE_WITH_KNOTS ( 'NONE', 3,
 ( #60532, #32991, #37379, #46470, #56759, #37081, #3516, #61448, #32674, #13885, #52065, #18570, #23567, #42393, #17643, #22651, #41783, #37695, #8225 ),
 .UNSPECIFIED., .F., .F.,
 ( 4, 3, 3, 3, 3, 3, 4 ),
 ( 3.469446951953614189E-18, 0.0002724573126191831823, 0.0004086839781548642523, 0.0005449106435901963398, 0.0006811373090491628420, 0.0008459866663933848785, 0.001010840725717215751 ),
 .UNSPECIFIED. ) ;
#51651=ORIENTED_EDGE ( 'NONE', *, *, #28444, .F. ) ;
#51654=EDGE_CURVE ( 'NONE', #23158, #21513, #55181, .T. ) ;
#51655=CARTESIAN_POINT ( 'NONE',  ( 5.974727161628367256, -5.297264154381075230, 19.82959049719566380 ) ) ;
#51659=CARTESIAN_POINT ( 'NONE',  ( 0.5809828226811544205, 47.55412398569205834, 5.711058609465488267 ) ) ;
#51674=CARTESIAN_POINT ( 'NONE',  ( 5.959547316686252039, -7.851524054666535690, 18.96456592444086908 ) ) ;
#51675=CARTESIAN_POINT ( 'NONE',  ( 0.5836750258453350382, 6.431686642655440878, -47.46217286060748108 ) ) ;
#51680=EDGE_CURVE ( 'NONE', #13139, #31407, #49454, .T. ) ;
#51685=CARTESIAN_POINT ( 'NONE',  ( 4.956653778116982600, -43.37017594958069111, 20.77844580450546985 ) ) ;
#51688=FACE_OUTER_BOUND ( 'NONE', #20370, .T. ) ;
#51702=ORIENTED_EDGE ( 'NONE', *, *, #15287, .F. ) ;
#51719=VERTEX_POINT ( 'NONE', #36969 ) ;
#51721=DIRECTION ( 'NONE',  ( 0.000000000000000000, 0.000000000000000000, 1.000000000000000000 ) ) ;
#51723=CARTESIAN_POINT ( 'NONE',  ( 2.624215991343620935, -30.33228621715010576, -37.21129343241634047 ) ) ;
#51724=ORIENTED_EDGE ( 'NONE', *, *, #61584, .T. ) ;
#51731=CARTESIAN_POINT ( 'NONE',  ( 0.9730545539215883499, -41.31259007387239279, 11.59290486963492128 ) ) ;
#51735=CARTESIAN_POINT ( 'NONE',  ( 5.959828726073459926, 17.77796293532173166, -10.25888482581841110 ) ) ;
#51737=CARTESIAN_POINT ( 'NONE',  ( 0.5819845079324660331, -44.42187385013350820, -17.90867223323933288 ) ) ;
#51743=CARTESIAN_POINT ( 'NONE',  ( 0.6846871229502899947, -46.04462816497497357, 13.23224427737813258 ) ) ;
#51746=CARTESIAN_POINT ( 'NONE',  ( 4.967162193818130511, 28.07411493385295032, 32.68434214048178177 ) ) ;
#51749=EDGE_CURVE ( 'NONE', #929, #37705, #8118, .T. ) ;
#51750=CARTESIAN_POINT ( 'NONE',  ( 5.959828726073459926, -14.51059719297107087, -14.51699876360195240 ) ) ;
#51757=ORIENTED_EDGE ( 'NONE', *, *, #17684, .F. ) ;
#51764=ORIENTED_EDGE ( 'NONE', *, *, #505, .T. ) ;
#51765=CARTESIAN_POINT ( 'NONE',  ( 4.967162193818130511, 24.30453456948160351, -35.57684288741949530 ) ) ;
#51770=ADVANCED_FACE ( 'NONE', ( #50713 ), #45778, .F. ) ;
#51772=CARTESIAN_POINT ( 'NONE',  ( 0.9747592971366241255, -41.36145845824417933, 11.41797089479118910 ) ) ;
#51776=ADVANCED_FACE ( 'NONE', ( #23155 ), #52142, .F. ) ;
#51789=ORIENTED_EDGE ( 'NONE', *, *, #16715, .T. ) ;
#51792=CARTESIAN_POINT ( 'NONE',  ( 3.407937589446174087, 6.447869442558164188, 12.08659953757610950 ) ) ;
#51795=ORIENTED_EDGE ( 'NONE', *, *, #36514, .F. ) ;
#51796=CARTESIAN_POINT ( 'NONE',  ( 0.9736507210033050752, -30.02062799605179677, -30.65767007549946399 ) ) ;
#51798=CARTESIAN_POINT ( 'NONE',  ( 0.9741495583595158880, -21.11077839432110892, -37.35596046161889205 ) ) ;
#51799=EDGE_CURVE ( 'NONE', #6542, #25300, #58172, .T. ) ;
#51807=CARTESIAN_POINT ( 'NONE',  ( 3.783198216974386963, 18.05208553945200123, -39.06945274417374492 ) ) ;
#51815=CARTESIAN_POINT ( 'NONE',  ( 4.956653778116975495, -36.51451553856441024, 31.29546495791839078 ) ) ;
#51826=CARTESIAN_POINT ( 'NONE',  ( 0.5827357941260222773, 12.74691551863630679, 46.16863402900283120 ) ) ;
#51834=B_SPLINE_CURVE_WITH_KNOTS ( 'NONE', 3,
 ( #2397, #16837, #35954, #59409, #17143, #50325 ),
 .UNSPECIFIED., .F., .F.,
 ( 4, 2, 4 ),
 ( 8.673617379884035472E-19, 0.0002291966416970794309, 0.0004583932833941579943 ),
 .UNSPECIFIED. ) ;
#51836=CARTESIAN_POINT ( 'NONE',  ( 0.6067375320500705271, 17.67235760802263655, 44.51755737952358771 ) ) ;
#51840=DIRECTION ( 'NONE',  ( -1.000000000000000000, -0.000000000000000000, -0.000000000000000000 ) ) ;
#51846=CARTESIAN_POINT ( 'NONE',  ( 0.9747592971366237924, 41.52905920980983012, 10.79247637456133369 ) ) ;
#51847=VECTOR ( 'NONE', #25363, 1000.000000000000114 ) ;
#51856=( BOUNDED_SURFACE ( )  B_SPLINE_SURFACE ( 3, 1, ( 
 ( #57055, #38302 ),
 ( #46775, #14181 ),
 ( #33589, #52667 ),
 ( #5649, #34512 ) ),
 .UNSPECIFIED., .F., .F., .F. ) 
 B_SPLINE_SURFACE_WITH_KNOTS ( ( 4, 4 ),
 ( 2, 2 ),
 ( 0.000000000000000000, 1.000000000000000000 ),
 ( 0.000000000000000000, 1.000000000000000000 ),
 .UNSPECIFIED. ) 
 GEOMETRIC_REPRESENTATION_ITEM ( )  RATIONAL_B_SPLINE_SURFACE ( (
 ( 1.000000000000000000, 1.000000000000000000),
 ( 0.7269869731126821222, 0.9931720237060910339),
 ( 0.7269869731126821222, 0.9931720237060910339),
 ( 1.000000000000000000, 1.000000000000000000) ) ) 
 REPRESENTATION_ITEM ( '' )  SURFACE ( )  );
#51857=B_SPLINE_CURVE_WITH_KNOTS ( 'NONE', 3,
 ( #23405, #52202, #61594, #18714, #19645, #42843, #37847, #9933, #24022, #33130 ),
 .UNSPECIFIED., .F., .F.,
 ( 4, 3, 3, 4 ),
 ( 1.095097866269904594E-17, 0.0002724568934985559807, 0.0004086836638483803638, 0.0005448802484329447627 ),
 .UNSPECIFIED. ) ;
#51871=CARTESIAN_POINT ( 'NONE',  ( 3.407937589446174087, -2.242416846335690828, 13.51415833181187232 ) ) ;
#51875=CARTESIAN_POINT ( 'NONE',  ( 5.965394784446458765, -12.48356622107688985, 16.29267539192321479 ) ) ;
#51880=ORIENTED_EDGE ( 'NONE', *, *, #58418, .F. ) ;
#51884=ADVANCED_FACE ( 'NONE', ( #43835 ), #14120, .F. ) ;
#51895=ORIENTED_EDGE ( 'NONE', *, *, #55301, .T. ) ;
#51898=VECTOR ( 'NONE', #45477, 1000.000000000000000 ) ;
#51903=CARTESIAN_POINT ( 'NONE',  ( 4.960156602257181468, 26.21519897043426894, 38.31207700265959915 ) ) ;
#51904=CARTESIAN_POINT ( 'NONE',  ( 5.981074661064941900, -2.687517936919858297, -20.34795181394747843 ) ) ;
#51914=B_SPLINE_CURVE_WITH_KNOTS ( 'NONE', 3,
 ( #50596, #16804, #25879, #12728 ),
 .UNSPECIFIED., .F., .F.,
 ( 4, 4 ),
 ( 1.084202172485504434E-18, 0.004444878191957692126 ),
 .UNSPECIFIED. ) ;
#51919=VERTEX_POINT ( 'NONE', #49727 ) ;
#51924=CARTESIAN_POINT ( 'NONE',  ( 4.967162193818130511, -24.30453456948135482, 35.57684288741969425 ) ) ;
#51929=CARTESIAN_POINT ( 'NONE',  ( 0.9968887458511677124, -25.59699785741763733, -34.43855515351798147 ) ) ;
#51940=CARTESIAN_POINT ( 'NONE',  ( 4.967162193818130511, -23.56777426397153974, -36.06913038482822742 ) ) ;
#51941=LINE ( 'NONE', #9972, #19597 ) ;
#51944=B_SPLINE_CURVE_WITH_KNOTS ( 'NONE', 3,
 ( #50195, #35499, #31093, #35190 ),
 .UNSPECIFIED., .F., .F.,
 ( 4, 4 ),
 ( 1.517883041479706208E-18, 0.004048833967417075214 ),
 .UNSPECIFIED. ) ;
#51949=ORIENTED_EDGE ( 'NONE', *, *, #1960, .T. ) ;
#51957=CARTESIAN_POINT ( 'NONE',  ( 0.5800708057587364852, -46.09746469244091571, -13.00144577271090185 ) ) ;
#51968=CARTESIAN_POINT ( 'NONE',  ( 5.959547316686252039, 12.49238070347976226, -16.28624005235086614 ) ) ;
#51975=CARTESIAN_POINT ( 'NONE',  ( 4.960156602257182357, 46.35381625054452570, -2.524999074837725566 ) ) ;
#51981=CARTESIAN_POINT ( 'NONE',  ( 5.974727161628369032, 0.01551142186649469810, -20.52494643607030156 ) ) ;
#51984=CARTESIAN_POINT ( 'NONE',  ( 0.8551540677456739292, 47.37911285756620572, 7.157691013574519978 ) ) ;
#51985=CARTESIAN_POINT ( 'NONE',  ( 4.956653778116982600, -47.27023054223759857, 8.845409907520762616 ) ) ;
#51988=CARTESIAN_POINT ( 'NONE',  ( 4.956653778116982600, -45.71126949320260735, 14.93973939759871072 ) ) ;
#51992=VERTEX_POINT ( 'NONE', #16529 ) ;
#51998=VERTEX_POINT ( 'NONE', #54715 ) ;
#52009=ORIENTED_EDGE ( 'NONE', *, *, #12102, .T. ) ;
#52014=DIRECTION ( 'NONE',  ( 1.000000000000000000, 0.000000000000000000, 0.000000000000000000 ) ) ;
#52020=CARTESIAN_POINT ( 'NONE',  ( 2.526552050251864578, -42.75269566045969327, 4.405466163647149713 ) ) ;
#52031=CARTESIAN_POINT ( 'NONE',  ( 0.8557997880470599172, 5.347802024197243043, 47.60865952217000796 ) ) ;
#52033=ORIENTED_EDGE ( 'NONE', *, *, #5166, .T. ) ;
#52039=EDGE_CURVE ( 'NONE', #56918, #20008, #49936, .T. ) ;
#52044=CARTESIAN_POINT ( 'NONE',  ( 5.959828726073459926, -16.28130559351256323, -12.49879082830562460 ) ) ;
#52056=CARTESIAN_POINT ( 'NONE',  ( 0.9741495583595158880, 30.61921547032197566, -30.05988007970366027 ) ) ;
#52057=B_SPLINE_CURVE_WITH_KNOTS ( 'NONE', 3,
 ( #41978, #41358, #61044, #7172 ),
 .UNSPECIFIED., .F., .F.,
 ( 4, 4 ),
 ( 8.384297404680615914E-17, 0.005004741218457495200 ),
 .UNSPECIFIED. ) ;
#52060=CARTESIAN_POINT ( 'NONE',  ( 5.959547316686252039, -7.858107265727618085, -18.96183906913540795 ) ) ;
#52061=CARTESIAN_POINT ( 'NONE',  ( 0.9752570700956822991, -37.04395688491829475, -21.65368877244790724 ) ) ;
#52065=CARTESIAN_POINT ( 'NONE',  ( 0.9757402383260944667, 39.60970160107532934, 16.49876987395742489 ) ) ;
#52067=DIRECTION ( 'NONE',  ( -1.000000000000000000, -0.000000000000000000, -0.000000000000000000 ) ) ;
#52069=CARTESIAN_POINT ( 'NONE',  ( 0.7057020205114975520, -34.46103118762814432, 33.27137945725707624 ) ) ;
#52078=ORIENTED_EDGE ( 'NONE', *, *, #34604, .T. ) ;
#52083=CARTESIAN_POINT ( 'NONE',  ( 0.5839254288179539509, -12.30867641975545546, -46.28738487712342220 ) ) ;
#52085=CARTESIAN_POINT ( 'NONE',  ( 1.154321713695928731, 11.90271797554071398, -41.23280394713380304 ) ) ;
#52101=ORIENTED_EDGE ( 'NONE', *, *, #12883, .T. ) ;
#52106=EDGE_LOOP ( 'NONE', ( #54165, #46190, #43905, #30289 ) ) ;
#52108=ADVANCED_FACE ( 'NONE', ( #24002 ), #3281, .F. ) ;
#52109=CARTESIAN_POINT ( 'NONE',  ( 0.9757402383260944667, 30.28078671294527169, 30.40085236181960937 ) ) ;
#52126=( BOUNDED_SURFACE ( )  B_SPLINE_SURFACE ( 3, 1, ( 
 ( #21468, #26787 ),
 ( #41220, #25857 ),
 ( #16786, #60279 ),
 ( #50278, #54964 ) ),
 .UNSPECIFIED., .F., .F., .F. ) 
 B_SPLINE_SURFACE_WITH_KNOTS ( ( 4, 4 ),
 ( 2, 2 ),
 ( 0.000000000000000000, 1.000000000000000000 ),
 ( 0.000000000000000000, 1.000000000000000000 ),
 .UNSPECIFIED. ) 
 GEOMETRIC_REPRESENTATION_ITEM ( )  RATIONAL_B_SPLINE_SURFACE ( (
 ( 1.000000000000000000, 1.000000000000000000),
 ( 0.9953390228620291325, 0.8624445117761032620),
 ( 0.9953390228620291325, 0.8624445117761032620),
 ( 1.000000000000000000, 1.000000000000000000) ) ) 
 REPRESENTATION_ITEM ( '' )  SURFACE ( )  );
#52140=CARTESIAN_POINT ( 'NONE',  ( 0.5819845901640494645, 11.95725023767357875, 46.37938751183688169 ) ) ;
#52142=( BOUNDED_SURFACE ( )  B_SPLINE_SURFACE ( 3, 1, ( 
 ( #61340, #234 ),
 ( #43204, #41975 ),
 ( #47272, #4947 ),
 ( #18455, #18774 ) ),
 .UNSPECIFIED., .F., .F., .F. ) 
 B_SPLINE_SURFACE_WITH_KNOTS ( ( 4, 4 ),
 ( 2, 2 ),
 ( 0.000000000000000000, 1.000000000000000000 ),
 ( 0.000000000000000000, 1.000000000000000000 ),
 .UNSPECIFIED. ) 
 GEOMETRIC_REPRESENTATION_ITEM ( )  RATIONAL_B_SPLINE_SURFACE ( (
 ( 1.000000000000000000, 1.000000000000000000),
 ( 0.9953390228620291325, 0.8624445117761032620),
 ( 0.9953390228620291325, 0.8624445117761032620),
 ( 1.000000000000000000, 1.000000000000000000) ) ) 
 REPRESENTATION_ITEM ( '' )  SURFACE ( )  );
#52156=EDGE_CURVE ( 'NONE', #15318, #30942, #22254, .T. ) ;
#52159=CARTESIAN_POINT ( 'NONE',  ( 0.9722240750034566448, -34.39263040572770791, -25.65687433776933446 ) ) ;
#52161=B_SPLINE_CURVE_WITH_KNOTS ( 'NONE', 3,
 ( #46361, #45441, #31946, #7488 ),
 .UNSPECIFIED., .F., .F.,
 ( 4, 4 ),
 ( 0.000000000000000000, 0.005004741218457418872 ),
 .UNSPECIFIED. ) ;
#52167=CARTESIAN_POINT ( 'NONE',  ( 4.956653778116966613, 0.000000000000000000, 0.000000000000000000 ) ) ;
#52177=CARTESIAN_POINT ( 'NONE',  ( 5.960221823109900008, 7.859839668735214779, -18.96108896995707482 ) ) ;
#52181=CARTESIAN_POINT ( 'NONE',  ( 0.5800708119828331677, 41.78924007434326882, 23.40241990038051867 ) ) ;
#52183=VERTEX_POINT ( 'NONE', #53708 ) ;
#52187=CARTESIAN_POINT ( 'NONE',  ( 0.5832366564991500191, -47.52097076201151538, -5.981458972434243293 ) ) ;
#52193=CARTESIAN_POINT ( 'NONE',  ( 4.963659409799330291, 44.62477100936214214, 3.403493583737470018 ) ) ;
#52202=CARTESIAN_POINT ( 'NONE',  ( 0.5819845901640494645, 0.4540519722837509375, -47.89381229371849003 ) ) ;
#52203=CARTESIAN_POINT ( 'NONE',  ( 5.974727161628369032, 5.297264154380663115, 19.82959049719577749 ) ) ;
#52208=CARTESIAN_POINT ( 'NONE',  ( 4.967162193818129623, -13.42934394584134949, -40.93989340068622340 ) ) ;
#52213=AXIS2_PLACEMENT_3D ( 'NONE', #33847, #43876, #918 ) ;
#52224=ORIENTED_EDGE ( 'NONE', *, *, #55023, .T. ) ;
#52229=CARTESIAN_POINT ( 'NONE',  ( 0.9722240750034571999, -11.66659272802828085, -41.29187379046135931 ) ) ;
#52233=CARTESIAN_POINT ( 'NONE',  ( 0.5832367798473397924, 47.52096797443093834, -5.981481162905240012 ) ) ;
#52235=EDGE_CURVE ( 'NONE', #16817, #24773, #53607, .T. ) ;
#52242=CARTESIAN_POINT ( 'NONE',  ( 0.5832367798473391263, -29.37285281143867977, 37.83194459509899588 ) ) ;
#52243=CARTESIAN_POINT ( 'NONE',  ( 0.9757892942422824456, 21.49867881049945950, 37.13414688883471371 ) ) ;
#52252=ORIENTED_EDGE ( 'NONE', *, *, #33145, .T. ) ;
#52256=CARTESIAN_POINT ( 'NONE',  ( 5.960221823109900008, -20.34928172836732330, 2.684531185214074966 ) ) ;
#52267=DIRECTION ( 'NONE',  ( 0.07836865515943411409, -0.9968932487286223942, -0.007886984708660975049 ) ) ;
#52275=EDGE_CURVE ( 'NONE', #57230, #39487, #2026, .T. ) ;
#52280=CARTESIAN_POINT ( 'NONE',  ( 0.8557997880470690211, -34.51495345639526136, -33.22501220301936797 ) ) ;
#52282=CARTESIAN_POINT ( 'NONE',  ( 5.981074661064941900, 0.008585178657616161779, -20.52466374824937034 ) ) ;
#52288=CONICAL_SURFACE ( 'NONE', #13331, 43.08621763946400307, 1.568696531533066763 ) ;
#52304=VERTEX_POINT ( 'NONE', #51487 ) ;
#52305=CARTESIAN_POINT ( 'NONE',  ( 5.974727161628369032, -19.82959049719579170, 5.297264154380593837 ) ) ;
#52311=CARTESIAN_POINT ( 'NONE',  ( 1.227938101723756947, -6.439911493064287562, -42.43379953535192328 ) ) ;
#52314=ORIENTED_EDGE ( 'NONE', *, *, #37798, .T. ) ;
#52315=CARTESIAN_POINT ( 'NONE',  ( 0.5839254288179547281, -6.161657890844622010, -47.49799454719524050 ) ) ;
#52316=DIRECTION ( 'NONE',  ( 0.000000000000000000, 0.000000000000000000, 1.000000000000000000 ) ) ;
#52319=ORIENTED_EDGE ( 'NONE', *, *, #16140, .F. ) ;
#52322=CARTESIAN_POINT ( 'NONE',  ( 5.981074661064941900, -18.95903134304795401, 7.862380442163802385 ) ) ;
#52325=ORIENTED_EDGE ( 'NONE', *, *, #31930, .F. ) ;
#52327=CARTESIAN_POINT ( 'NONE',  ( 0.9757402383260943557, -16.34189654378404555, -39.67468066200779475 ) ) ;
#52329=CARTESIAN_POINT ( 'NONE',  ( 0.9722240750034607526, 36.86535092060704244, -21.95618656573963179 ) ) ;
#52337=CARTESIAN_POINT ( 'NONE',  ( 4.303969348037246512, 39.44373910178647691, -27.54579249306170041 ) ) ;
#52338=EDGE_CURVE ( 'NONE', #59093, #29930, #27519, .T. ) ;
#52341=( BOUNDED_SURFACE ( )  B_SPLINE_SURFACE ( 3, 1, ( 
 ( #10574, #42874 ),
 ( #61927, #14979 ),
 ( #19361, #14359 ),
 ( #24668, #853 ) ),
 .UNSPECIFIED., .F., .F., .F. ) 
 B_SPLINE_SURFACE_WITH_KNOTS ( ( 4, 4 ),
 ( 2, 2 ),
 ( 0.000000000000000000, 1.000000000000000000 ),
 ( 0.000000000000000000, 1.000000000000000000 ),
 .UNSPECIFIED. ) 
 GEOMETRIC_REPRESENTATION_ITEM ( )  RATIONAL_B_SPLINE_SURFACE ( (
 ( 1.000000000000000000, 1.000000000000000000),
 ( 0.7269869731126817891, 0.9931720237060910339),
 ( 0.7269869731126817891, 0.9931720237060910339),
 ( 1.000000000000000000, 1.000000000000000000) ) ) 
 REPRESENTATION_ITEM ( '' )  SURFACE ( )  );
#52353=CARTESIAN_POINT ( 'NONE',  ( 0.5809828226811544205, -34.25055090842130312, -33.48000389720652947 ) ) ;
#52355=CARTESIAN_POINT ( 'NONE',  ( 0.5836750258453350382, -46.31062999473594743, 12.22088356912710339 ) ) ;
#52356=CARTESIAN_POINT ( 'NONE',  ( 0.6067099128993201917, 33.36330296770442772, -34.36589933408209419 ) ) ;
#52362=CARTESIAN_POINT ( 'NONE',  ( 0.9972139404380295780, -41.61281131482456175, -10.46878911444719584 ) ) ;
#52373=CARTESIAN_POINT ( 'NONE',  ( 0.5839879327111927587, -33.80333292213281737, 33.93179405280476146 ) ) ;
#52377=UNCERTAINTY_MEASURE_WITH_UNIT (LENGTH_MEASURE( 1.000000000000000082E-05 ), #27903, 'distance_accuracy_value', 'NONE');
#52379=VERTEX_POINT ( 'NONE', #24854 ) ;
#52390=DIRECTION ( 'NONE',  ( 1.000000000000000000, 0.000000000000000000, 0.000000000000000000 ) ) ;
#52392=CONICAL_SURFACE ( 'NONE', #51403, 43.08621763946400307, 1.568696531533066763 ) ;
#52406=CARTESIAN_POINT ( 'NONE',  ( 0.8551540677456834771, -7.157691013574049244, -47.37911285756627677 ) ) ;
#52408=ORIENTED_EDGE ( 'NONE', *, *, #5964, .F. ) ;
#52413=VERTEX_POINT ( 'NONE', #29234 ) ;
#52418=ORIENTED_EDGE ( 'NONE', *, *, #40265, .T. ) ;
#52421=CARTESIAN_POINT ( 'NONE',  ( 3.660087539127338641, 43.62750476736577809, -20.10768839917357553 ) ) ;
#52431=CARTESIAN_POINT ( 'NONE',  ( 0.5807400328401574052, 11.87003418057243387, 46.40483864045149431 ) ) ;
#52433=CARTESIAN_POINT ( 'NONE',  ( 4.967162193818131399, 42.16965968614193372, 8.839793687085363061 ) ) ;
#52440=B_SPLINE_CURVE_WITH_KNOTS ( 'NONE', 3,
 ( #4667, #38245, #10648, #57601 ),
 .UNSPECIFIED., .F., .F.,
 ( 4, 4 ),
 ( 0.000000000000000000, 0.005004741218457414535 ),
 .UNSPECIFIED. ) ;
#52442=CARTESIAN_POINT ( 'NONE',  ( 4.956653778116966613, 0.000000000000000000, 0.000000000000000000 ) ) ;
#52450=CARTESIAN_POINT ( 'NONE',  ( 1.227938101723748288, -30.94118573761333479, 29.74462687941215222 ) ) ;
#52452=CARTESIAN_POINT ( 'NONE',  ( 2.624215991343620935, 11.05657803851110721, -46.71702075422640377 ) ) ;
#52457=CARTESIAN_POINT ( 'NONE',  ( 3.660087539127334200, 27.72868323267864810, -39.22752134874889407 ) ) ;
#52458=EDGE_CURVE ( 'NONE', #32445, #54909, #4391, .T. ) ;
#52461=VERTEX_POINT ( 'NONE', #11689 ) ;
#52462=EDGE_CURVE ( 'NONE', #3092, #8944, #43979, .T. ) ;
#52465=DIRECTION ( 'NONE',  ( 0.000000000000000000, 0.000000000000000000, 1.000000000000000000 ) ) ;
#52467=EDGE_CURVE ( 'NONE', #12616, #36851, #15551, .T. ) ;
#52475=EDGE_CURVE ( 'NONE', #30590, #56316, #59570, .T. ) ;
#52479=CARTESIAN_POINT ( 'NONE',  ( 0.5809828226811617480, -47.89273459658653564, -0.5448590168537535972 ) ) ;
#52487=CARTESIAN_POINT ( 'NONE',  ( 0.9754402186311951217, -42.56545569314704380, -5.414674803234208689 ) ) ;
#52489=ORIENTED_EDGE ( 'NONE', *, *, #30542, .F. ) ;
#52496=CARTESIAN_POINT ( 'NONE',  ( 0.5838002273316426072, -0.1361971433781400675, 47.89576566046788031 ) ) ;
#52498=CARTESIAN_POINT ( 'NONE',  ( 0.9752570700956804117, 26.30364510018356228, -33.90066715551942877 ) ) ;
#52500=CARTESIAN_POINT ( 'NONE',  ( 0.5827357941260211671, -18.66407988912457938, -44.10984861950477409 ) ) ;
#52501=CARTESIAN_POINT ( 'NONE',  ( 2.526464513654346433, 41.18424249084333866, -12.29060355381808201 ) ) ;
#52502=CARTESIAN_POINT ( 'NONE',  ( 4.960156602257181468, -38.88108289790881855, 25.36362146861372935 ) ) ;
#52526=ORIENTED_EDGE ( 'NONE', *, *, #26670, .F. ) ;
#52531=VECTOR ( 'NONE', #40822, 1000.000000000000000 ) ;
#52533=CARTESIAN_POINT ( 'NONE',  ( 5.959547316686252039, -20.35048796920735015, -2.675599016784462769 ) ) ;
#52534=CARTESIAN_POINT ( 'NONE',  ( 0.7762777257811902532, -11.53708189756908098, -46.49451973287614237 ) ) ;
#52535=VERTEX_POINT ( 'NONE', #32965 ) ;
#52545=ORIENTED_EDGE ( 'NONE', *, *, #8672, .T. ) ;
#52550=B_SPLINE_CURVE_WITH_KNOTS ( 'NONE', 3,
 ( #53816, #10946, #6191, #12804, #50980, #12488, #55988, #7756, #26569, #2438, #3059, #54746, #22188, #45091, #31581, #31898, #36925, #40390, #11885 ),
 .UNSPECIFIED., .F., .F.,
 ( 4, 3, 3, 3, 3, 3, 4 ),
 ( 1.250973872328959318E-17, 0.0002724573126191757013, 0.0004086839781548398578, 0.0005449106435901728126, 0.0006811373090491394233, 0.0008459866663933642787, 0.001010840725717206644 ),
 .UNSPECIFIED. ) ;
#52551=ORIENTED_EDGE ( 'NONE', *, *, #9547, .T. ) ;
#52555=CARTESIAN_POINT ( 'NONE',  ( 0.5838002273316440505, -38.08117724016823757, 29.04904228829596491 ) ) ;
#52558=B_SPLINE_CURVE_WITH_KNOTS ( 'NONE', 3,
 ( #4794, #24548, #23935, #48054, #33044, #57412 ),
 .UNSPECIFIED., .F., .F.,
 ( 4, 2, 4 ),
 ( 9.543442895606953578E-18, 0.0002291978881530155367, 0.0004583957763060215324 ),
 .UNSPECIFIED. ) ;
#52569=CARTESIAN_POINT ( 'NONE',  ( 0.9754402186311945666, 34.15542855230937391, 25.97197377940566554 ) ) ;
#52574=CARTESIAN_POINT ( 'NONE',  ( 4.967162193818130511, 3.259922920618364639, -42.96271701169381885 ) ) ;
#52581=ADVANCED_FACE ( 'NONE', ( #28239, #14168 ), #17937, .T. ) ;
#52583=CARTESIAN_POINT ( 'NONE',  ( 1.227938101723756947, -26.79402671879305231, -33.52879263017890565 ) ) ;
#52586=CARTESIAN_POINT ( 'NONE',  ( 100.0000507999999968, 0.000000000000000000, 8.000000000000000000 ) ) ;
#52589=CARTESIAN_POINT ( 'NONE',  ( 4.956653778116988818, -45.35992544608517818, -15.97476558431931082 ) ) ;
#52593=( BOUNDED_SURFACE ( )  B_SPLINE_SURFACE ( 3, 1, ( 
 ( #8592, #23030 ),
 ( #61213, #8919 ),
 ( #18336, #45604 ),
 ( #2656, #33055 ) ),
 .UNSPECIFIED., .F., .F., .F. ) 
 B_SPLINE_SURFACE_WITH_KNOTS ( ( 4, 4 ),
 ( 2, 2 ),
 ( 0.000000000000000000, 1.000000000000000000 ),
 ( 0.000000000000000000, 1.000000000000000000 ),
 .UNSPECIFIED. ) 
 GEOMETRIC_REPRESENTATION_ITEM ( )  RATIONAL_B_SPLINE_SURFACE ( (
 ( 1.000000000000000000, 1.000000000000000000),
 ( 0.9732289882329797637, 0.9999525324661233672),
 ( 0.9732289882329797637, 0.9999525324661233672),
 ( 1.000000000000000000, 1.000000000000000000) ) ) 
 REPRESENTATION_ITEM ( '' )  SURFACE ( )  );
#52594=EDGE_LOOP ( 'NONE', ( #34291, #965, #764, #4150 ) ) ;
#52612=CARTESIAN_POINT ( 'NONE',  ( 0.9756008150404614776, -37.08855330282513307, 21.57722292874444392 ) ) ;
#52626=DIRECTION ( 'NONE',  ( -0.07439287786467650709, -0.2708295585865000410, -0.9597484305373220614 ) ) ;
#52631=ORIENTED_EDGE ( 'NONE', *, *, #50077, .T. ) ;
#52634=CARTESIAN_POINT ( 'NONE',  ( 4.967162193818130511, 43.02067033766019932, -2.375726030842729486 ) ) ;
#52645=ORIENTED_EDGE ( 'NONE', *, *, #47788, .T. ) ;
#52648=VERTEX_POINT ( 'NONE', #34195 ) ;
#52652=AXIS2_PLACEMENT_3D ( 'NONE', #20543, #39056, #43445 ) ;
#52660=B_SPLINE_CURVE_WITH_KNOTS ( 'NONE', 3,
 ( #41825, #13614, #18316, #46511, #2953, #3562 ),
 .UNSPECIFIED., .F., .F.,
 ( 4, 2, 4 ),
 ( 0.000000000000000000, 0.0002291966416970790785, 0.0004583932833941581570 ),
 .UNSPECIFIED. ) ;
#52666=DIRECTION ( 'NONE',  ( 0.07439287786467665975, 0.6174937095821756428, -0.7830499462674492817 ) ) ;
#52667=CARTESIAN_POINT ( 'NONE',  ( 4.303969348037246512, -2.158280495710544589, 48.06163817123225357 ) ) ;
#52671=CARTESIAN_POINT ( 'NONE',  ( 4.956653778116973719, 27.17045123668471973, 39.67974989265048436 ) ) ;
#52680=B_SPLINE_CURVE_WITH_KNOTS ( 'NONE', 3,
 ( #60877, #17997, #51169, #22068, #37113, #60253 ),
 .UNSPECIFIED., .F., .F.,
 ( 4, 2, 4 ),
 ( 1.015220885719448636E-17, 0.0002291978881530140188, 0.0004583957763060178461 ),
 .UNSPECIFIED. ) ;
#52686=CARTESIAN_POINT ( 'NONE',  ( 0.9754402186311951217, 5.786576363453547422, 42.51649392388753057 ) ) ;
#52687=CARTESIAN_POINT ( 'NONE',  ( 3.270143674763207553, -11.71453292426874171, -7.080034332678387443 ) ) ;
#52689=EDGE_LOOP ( 'NONE', ( #57571, #17212, #21509, #298 ) ) ;
#52690=ORIENTED_EDGE ( 'NONE', *, *, #11279, .T. ) ;
#52691=CARTESIAN_POINT ( 'NONE',  ( 0.5809828226811553087, 46.11980934799357357, -12.92184523170154620 ) ) ;
#52694=DIRECTION ( 'NONE',  ( 0.000000000000000000, 0.000000000000000000, 1.000000000000000000 ) ) ;
#52695=VECTOR ( 'NONE', #59203, 1000.000000000000114 ) ;
#52698=CARTESIAN_POINT ( 'NONE',  ( 0.5836750258453341500, -12.22088356912694884, -46.31062999473600428 ) ) ;
#52700=CARTESIAN_POINT ( 'NONE',  ( 1.227938101723747621, 30.94118573761354440, -29.74462687941193551 ) ) ;
#52703=B_SPLINE_CURVE_WITH_KNOTS ( 'NONE', 3,
 ( #630, #30374, #29454, #20687, #54474, #49488, #48565, #1867, #10989, #5620, #20081, #19770, #20993, #59188, #30072, #11603 ),
 .UNSPECIFIED., .F., .F.,
 ( 4, 3, 3, 3, 3, 4 ),
 ( 9.813676791237319219E-18, 0.0002724568934985570649, 0.0004086836638483779785, 0.0005449104342063629345, 0.0008173270854453619028, 0.001089761613562689442 ),
 .UNSPECIFIED. ) ;
#52707=B_SPLINE_CURVE_WITH_KNOTS ( 'NONE', 3,
 ( #36326, #56627, #9021, #60388 ),
 .UNSPECIFIED., .F., .F.,
 ( 4, 4 ),
 ( 0.000000000000000000, 0.004446090762761361649 ),
 .UNSPECIFIED. ) ;
#52708=( BOUNDED_SURFACE ( )  B_SPLINE_SURFACE ( 3, 1, ( 
 ( #23081, #32479 ),
 ( #51875, #42211 ),
 ( #46905, #13075 ),
 ( #22152, #56575 ) ),
 .UNSPECIFIED., .F., .F., .F. ) 
 B_SPLINE_SURFACE_WITH_KNOTS ( ( 4, 4 ),
 ( 2, 2 ),
 ( 0.000000000000000000, 1.000000000000000000 ),
 ( 0.000000000000000000, 1.000000000000000000 ),
 .UNSPECIFIED. ) 
 GEOMETRIC_REPRESENTATION_ITEM ( )  RATIONAL_B_SPLINE_SURFACE ( (
 ( 1.000000000000000000, 1.000000000000000000),
 ( 0.7269869731126821222, 0.9931720237060910339),
 ( 0.7269869731126821222, 0.9931720237060910339),
 ( 1.000000000000000000, 1.000000000000000000) ) ) 
 REPRESENTATION_ITEM ( '' )  SURFACE ( )  );
#52709=CARTESIAN_POINT ( 'NONE',  ( 0.9752132459055858904, -34.18286753639623043, -25.93579301218392530 ) ) ;
#52711=VECTOR ( 'NONE', #19505, 1000.000000000000114 ) ;
#52713=CARTESIAN_POINT ( 'NONE',  ( 5.958863334805807099, 18.96276366205793806, -7.855954700275424862 ) ) ;
#52716=CARTESIAN_POINT ( 'NONE',  ( 0.9972139404380300221, -41.27214627875016362, 11.74016833743905863 ) ) ;
#52736=CARTESIAN_POINT ( 'NONE',  ( 0.9749527285493325701, -42.57770849153627069, 5.317382389863026582 ) ) ;
#52750=CARTESIAN_POINT ( 'NONE',  ( 2.526552050251864134, 25.19159344346121543, 34.82218744039913361 ) ) ;
#52756=EDGE_CURVE ( 'NONE', #33451, #52413, #28181, .T. ) ;
#52760=CARTESIAN_POINT ( 'NONE',  ( 3.407937589446174087, -1.331713209622414240, -13.63405474014709817 ) ) ;
#52767=ORIENTED_EDGE ( 'NONE', *, *, #55742, .F. ) ;
#52770=CARTESIAN_POINT ( 'NONE',  ( 5.981074661064941900, 7.862380442163868111, 18.95903134304792559 ) ) ;
#52776=CARTESIAN_POINT ( 'NONE',  ( 4.963659409799326738, -43.79875484948441766, -9.199077662859362903 ) ) ;
#52784=ORIENTED_EDGE ( 'NONE', *, *, #41067, .F. ) ;
#52796=VERTEX_POINT ( 'NONE', #24010 ) ;
#52800=CARTESIAN_POINT ( 'NONE',  ( 0.5836750258453350382, 29.01293504009540669, 38.10871351907198346 ) ) ;
#52805=CARTESIAN_POINT ( 'NONE',  ( 5.974727161628367256, 18.96851388233647384, 7.840226266082609641 ) ) ;
#52817=DIRECTION ( 'NONE',  ( -1.000000000000000000, -0.000000000000000000, -0.000000000000000000 ) ) ;
#52821=ORIENTED_EDGE ( 'NONE', *, *, #51100, .F. ) ;
#52822=CARTESIAN_POINT ( 'NONE',  ( 0.5827359174754828119, -24.26188383263398407, 41.29633904010504608 ) ) ;
#52828=EDGE_CURVE ( 'NONE', #18299, #57911, #58774, .T. ) ;
#52842=CARTESIAN_POINT ( 'NONE',  ( 3.407937589446178528, 13.63405474014708574, 1.331713209622550576 ) ) ;
#52845=VECTOR ( 'NONE', #4903, 1000.000000000000000 ) ;
#52846=CARTESIAN_POINT ( 'NONE',  ( 2.526552050251865911, -33.34585601411847477, -27.11558601691300652 ) ) ;
#52851=CARTESIAN_POINT ( 'NONE',  ( 1.227938101723756947, -25.45152231597080927, 34.55893248994497924 ) ) ;
#52871=CARTESIAN_POINT ( 'NONE',  ( 4.960156602257179692, 41.85906677498956441, 20.07163247083160584 ) ) ;
#52879=ORIENTED_EDGE ( 'NONE', *, *, #54240, .T. ) ;
#52890=ORIENTED_EDGE ( 'NONE', *, *, #2163, .T. ) ;
#52892=ORIENTED_EDGE ( 'NONE', *, *, #36892, .F. ) ;
#52904=CARTESIAN_POINT ( 'NONE',  ( 0.9730545539215892381, -21.89037132892461912, 36.90443313492323085 ) ) ;
#52911=CARTESIAN_POINT ( 'NONE',  ( 0.6067099128993237445, -46.44339333106605494, -11.71051825714752148 ) ) ;
#52912=CARTESIAN_POINT ( 'NONE',  ( 0.5850706913938533704, -41.56998471741244572, 23.79070617305366753 ) ) ;
#52913=EDGE_CURVE ( 'NONE', #41860, #2075, #25186, .T. ) ;
#52917=FACE_OUTER_BOUND ( 'NONE', #32780, .T. ) ;
#52924=CARTESIAN_POINT ( 'NONE',  ( 3.783278058412224976, -36.37891728069884323, 22.99727281874613638 ) ) ;
#52932=EDGE_CURVE ( 'NONE', #57911, #4945, #5740, .T. ) ;
#52934=ORIENTED_EDGE ( 'NONE', *, *, #22606, .T. ) ;
#52940=DIRECTION ( 'NONE',  ( -1.000000000000000000, -0.000000000000000000, -0.000000000000000000 ) ) ;
#52942=DIRECTION ( 'NONE',  ( 0.000000000000000000, 0.000000000000000000, 1.000000000000000000 ) ) ;
#52948=CARTESIAN_POINT ( 'NONE',  ( 0.9754402186311947887, -16.59348191374109405, -39.57010335554347336 ) ) ;
#52953=CARTESIAN_POINT ( 'NONE',  ( 0.9722240750034574219, -10.54237121715114966, 41.59310803641459131 ) ) ;
#52954=B_SPLINE_CURVE_WITH_KNOTS ( 'NONE', 3,
 ( #36397, #6588, #26660, #31675 ),
 .UNSPECIFIED., .F., .F.,
 ( 4, 4 ),
 ( 1.734723475976807094E-18, 0.004048833967417084755 ),
 .UNSPECIFIED. ) ;
#52956=CARTESIAN_POINT ( 'NONE',  ( 5.959828726073459926, 7.850628836606854399, -18.96492317065686350 ) ) ;
#52969=VERTEX_POINT ( 'NONE', #53117 ) ;
#52974=CARTESIAN_POINT ( 'NONE',  ( 5.960721111146673579, -7.860635756378015593, 18.96073515164535195 ) ) ;
#52979=CARTESIAN_POINT ( 'NONE',  ( 3.783278058412226752, 14.86148287637788279, -40.39104487792928921 ) ) ;
#53018=ORIENTED_EDGE ( 'NONE', *, *, #39772, .T. ) ;
#53023=CARTESIAN_POINT ( 'NONE',  ( 0.9968887458511636046, -30.80284987750029657, 29.87314546208219568 ) ) ;
#53024=CARTESIAN_POINT ( 'NONE',  ( 4.956653778116992370, 15.97476558431944937, -45.35992544608513555 ) ) ;
#53026=ORIENTED_EDGE ( 'NONE', *, *, #19122, .T. ) ;
#53032=CARTESIAN_POINT ( 'NONE',  ( 0.7056555295713275999, -38.50897360867666919, -28.48870155114950364 ) ) ;
#53034=CARTESIAN_POINT ( 'NONE',  ( 4.960156602257185909, -9.558288641081436054, -45.42786611289324128 ) ) ;
#53040=CARTESIAN_POINT ( 'NONE',  ( 0.7057020205115046574, 13.20843872046553180, -46.04437542275030637 ) ) ;
#53044=LINE ( 'NONE', #43687, #15574 ) ;
#53047=CARTESIAN_POINT ( 'NONE',  ( 0.7762777257811904752, 47.60264404062384358, -5.369627942761147743 ) ) ;
#53051=CARTESIAN_POINT ( 'NONE',  ( 1.227938101723748288, -22.18841447410744649, 36.73927144310504644 ) ) ;
#53053=CARTESIAN_POINT ( 'NONE',  ( 1.227938101723756947, -42.43379953535190197, 6.439911493064418124 ) ) ;
#53054=CARTESIAN_POINT ( 'NONE',  ( 3.407937589446178528, -13.69123696618924768, 0.4592810312471504175 ) ) ;
#53059=CARTESIAN_POINT ( 'NONE',  ( 0.5837374860065647209, -41.38807031854326368, 24.10515569139031555 ) ) ;
#53060=CARTESIAN_POINT ( 'NONE',  ( 5.959828726073459926, -20.35060134307033053, -2.674641840416102312 ) ) ;
#53063=CARTESIAN_POINT ( 'NONE',  ( 5.959547316686252039, 12.49238070347954555, 16.28624005235103311 ) ) ;
#53064=CARTESIAN_POINT ( 'NONE',  ( 1.227938101723748288, -4.762198645644156514, -42.65467462194923343 ) ) ;
#53068=ORIENTED_EDGE ( 'NONE', *, *, #30077, .F. ) ;
#53088=CARTESIAN_POINT ( 'NONE',  ( 4.963659409799330291, 42.22332985082334034, -14.83726297270234973 ) ) ;
#53089=CARTESIAN_POINT ( 'NONE',  ( 0.5786265663353153954, -6.967625775955401224, -47.39171391660399735 ) ) ;
#53091=EDGE_CURVE ( 'NONE', #23600, #53354, #21414, .T. ) ;
#53093=CARTESIAN_POINT ( 'NONE',  ( 1.088908134280556883, 15.69861202536805145, -39.93902428011472949 ) ) ;
#53094=CARTESIAN_POINT ( 'NONE',  ( 0.9722240741986376555, 42.46141200043700081, 6.177112427866004118 ) ) ;
#53105=CARTESIAN_POINT ( 'NONE',  ( 5.860006189529246790, 40.11385274514719157, -26.78264244998056398 ) ) ;
#53106=EDGE_LOOP ( 'NONE', ( #8111, #20849, #56940, #15327 ) ) ;
#53110=CARTESIAN_POINT ( 'NONE',  ( 0.5838002273316424962, 24.06583301632262462, -41.41085122398227725 ) ) ;
#53112=ORIENTED_EDGE ( 'NONE', *, *, #13351, .T. ) ;
#53117=CARTESIAN_POINT ( 'NONE',  ( 0.9730545539215883499, -11.59290486963477562, -41.31259007387244253 ) ) ;
#53120=CARTESIAN_POINT ( 'NONE',  ( 3.660176727303420030, 46.85282580473592873, -10.60619300811821475 ) ) ;
#53125=ORIENTED_EDGE ( 'NONE', *, *, #4934, .T. ) ;
#53137=ADVANCED_FACE ( 'NONE', ( #26468 ), #54590, .F. ) ;
#53141=ORIENTED_EDGE ( 'NONE', *, *, #37154, .T. ) ;
#53142=ORIENTED_EDGE ( 'NONE', *, *, #53159, .T. ) ;
#53146=CARTESIAN_POINT ( 'NONE',  ( 1.227938101723756947, 0.8460948827225182045, 42.91134962331487657 ) ) ;
#53147=CARTESIAN_POINT ( 'NONE',  ( 0.9754402186311945666, 42.51649392388761584, -5.786576363453125538 ) ) ;
#53149=( BOUNDED_SURFACE ( )  B_SPLINE_SURFACE ( 3, 1, ( 
 ( #8443, #12565 ),
 ( #50746, #26956 ),
 ( #36679, #13484 ),
 ( #8149, #22566 ) ),
 .UNSPECIFIED., .F., .F., .F. ) 
 B_SPLINE_SURFACE_WITH_KNOTS ( ( 4, 4 ),
 ( 2, 2 ),
 ( 0.000000000000000000, 1.000000000000000000 ),
 ( 0.000000000000000000, 1.000000000000000000 ),
 .UNSPECIFIED. ) 
 GEOMETRIC_REPRESENTATION_ITEM ( )  RATIONAL_B_SPLINE_SURFACE ( (
 ( 1.000000000000000000, 1.000000000000000000),
 ( 0.9953390228620291325, 0.8624445117761032620),
 ( 0.9953390228620291325, 0.8624445117761032620),
 ( 1.000000000000000000, 1.000000000000000000) ) ) 
 REPRESENTATION_ITEM ( '' )  SURFACE ( )  );
#53155=CARTESIAN_POINT ( 'NONE',  ( -19.36298947945248372, -7.842906756447401762, 1.580642502182497466 ) ) ;
#53159=EDGE_CURVE ( 'NONE', #61473, #10306, #41626, .T. ) ;
#53160=CARTESIAN_POINT ( 'NONE',  ( 0.9722240750034539802, -30.74950257331004977, -29.92651530838623586 ) ) ;
#53161=CARTESIAN_POINT ( 'NONE',  ( 0.5839879882012695145, 47.48620708510746624, -6.251708210201584848 ) ) ;
#53166=ORIENTED_EDGE ( 'NONE', *, *, #50669, .F. ) ;
#53170=ORIENTED_EDGE ( 'NONE', *, *, #47612, .T. ) ;
#53171=CARTESIAN_POINT ( 'NONE',  ( 0.5809828226811553087, -24.41822904836894637, -41.20389530892332886 ) ) ;
#53175=CARTESIAN_POINT ( 'NONE',  ( 0.5839879327111913154, -37.94312859586436559, 29.22928252017501549 ) ) ;
#53180=DIRECTION ( 'NONE',  ( -1.000000000000000000, -0.000000000000000000, -0.000000000000000000 ) ) ;
#53182=B_SPLINE_CURVE_WITH_KNOTS ( 'NONE', 3,
 ( #49070, #6423, #39699, #21180 ),
 .UNSPECIFIED., .F., .F.,
 ( 4, 4 ),
 ( 0.000000000000000000, 0.005004741218457413668 ),
 .UNSPECIFIED. ) ;
#53190=DIRECTION ( 'NONE',  ( 0.07836865515943411409, 0.6006129930017333196, 0.7956898808744532481 ) ) ;
#53201=VERTEX_POINT ( 'NONE', #18631 ) ;
#53205=CARTESIAN_POINT ( 'NONE',  ( 0.7057020205115018818, -38.50899875908074677, 28.48867101281811287 ) ) ;
#53222=CARTESIAN_POINT ( 'NONE',  ( 5.959547316686252039, -12.49803383497738807, -16.28190225198614627 ) ) ;
#53224=CARTESIAN_POINT ( 'NONE',  ( 3.660087539127332423, 10.60624038924657953, -46.85281175970442291 ) ) ;
#53227=CARTESIAN_POINT ( 'NONE',  ( 0.9757787079277429054, -37.17954582422755294, 21.42002160630809016 ) ) ;
#53229=VECTOR ( 'NONE', #1659, 1000.000000000000114 ) ;
#53241=CARTESIAN_POINT ( 'NONE',  ( 0.5800708057587378175, -17.74761804745370952, -44.48635630048018186 ) ) ;
#53245=CARTESIAN_POINT ( 'NONE',  ( 0.5807400328401574052, 41.75144119563885425, 23.47602859900729655 ) ) ;
#53256=EDGE_CURVE ( 'NONE', #55855, #56918, #60225, .T. ) ;
#53258=CARTESIAN_POINT ( 'NONE',  ( 0.9730545539215883499, -42.47233286818622133, 6.101350888304490461 ) ) ;
#53261=EDGE_CURVE ( 'NONE', #29768, #60647, #15481, .T. ) ;
#53263=ORIENTED_EDGE ( 'NONE', *, *, #12828, .T. ) ;
#53269=CARTESIAN_POINT ( 'NONE',  ( 3.270143674763207553, -7.080034332678176945, -11.71453292426886783 ) ) ;
#53273=ORIENTED_EDGE ( 'NONE', *, *, #16706, .T. ) ;
#53282=CARTESIAN_POINT ( 'NONE',  ( 0.7762783648524375080, 33.23866576554886620, -34.49689442177313481 ) ) ;
#53283=CARTESIAN_POINT ( 'NONE',  ( 5.959547316686252039, 19.82715097195162457, -5.308980600728250288 ) ) ;
#53284=CARTESIAN_POINT ( 'NONE',  ( 4.956653778116966613, 0.000000000000000000, -48.09070567114147110 ) ) ;
#53294=CARTESIAN_POINT ( 'NONE',  ( 0.5834872094924182795, 29.33699246747753264, -37.85980081020191079 ) ) ;
#53298=CARTESIAN_POINT ( 'NONE',  ( 0.5807400328401637335, 47.41494605191452649, -6.791881299635107005 ) ) ;
#53300=ORIENTED_EDGE ( 'NONE', *, *, #11377, .T. ) ;
#53304=ORIENTED_EDGE ( 'NONE', *, *, #29484, .T. ) ;
#53310=EDGE_LOOP ( 'NONE', ( #5593, #19297, #13953, #47953 ) ) ;
#53312=CARTESIAN_POINT ( 'NONE',  ( 1.154321713695926954, 39.32643513900330134, 17.18284946700643090 ) ) ;
#53313=CARTESIAN_POINT ( 'NONE',  ( 1.227938101723756947, -17.20315230597815059, -39.32113113558984452 ) ) ;
#53320=ORIENTED_EDGE ( 'NONE', *, *, #39485, .T. ) ;
#53324=FACE_OUTER_BOUND ( 'NONE', #5669, .T. ) ;
#53326=EDGE_CURVE ( 'NONE', #41860, #52183, #32471, .T. ) ;
#53335=CARTESIAN_POINT ( 'NONE',  ( 5.860006189529234355, 40.11385274514681498, 26.78264244998112176 ) ) ;
#53348=CARTESIAN_POINT ( 'NONE',  ( 4.956653778116975495, 3.690426056929986043, 47.94889704119053420 ) ) ;
#53351=CARTESIAN_POINT ( 'NONE',  ( 2.624215991343608501, -47.39206852872452913, -7.662883702705155287 ) ) ;
#53354=VERTEX_POINT ( 'NONE', #42342 ) ;
#53363=CARTESIAN_POINT ( 'NONE',  ( 0.8557997880470606944, 19.17299735372068525, -43.90420959842161608 ) ) ;
#53364=CARTESIAN_POINT ( 'NONE',  ( 2.281448460670572942, 32.98023336626282287, -34.83871297539670309 ) ) ;
#53368=CARTESIAN_POINT ( 'NONE',  ( 0.9968887458511656030, 10.46947792236095154, 41.61262323391473927 ) ) ;
#53376=CARTESIAN_POINT ( 'NONE',  ( 2.526552050251864134, 22.53110080776707491, -36.59987178591158852 ) ) ;
#53392=CARTESIAN_POINT ( 'NONE',  ( 0.6846871229502899947, -7.109010606687077072, -47.37786444808401143 ) ) ;
#53396=CARTESIAN_POINT ( 'NONE',  ( 0.9730545539215883499, 42.47233286818616449, 6.101350888304794218 ) ) ;
#53416=CARTESIAN_POINT ( 'NONE',  ( 1.227938101723748288, -39.96870412324346944, 15.63977281655828300 ) ) ;
#53418=CARTESIAN_POINT ( 'NONE',  ( 5.974727161628367256, -20.34732802718249545, 2.694421823322574738 ) ) ;
#53419=AXIS2_PLACEMENT_3D ( 'NONE', #26083, #36430, #16694 ) ;
#53429=ORIENTED_EDGE ( 'NONE', *, *, #10021, .T. ) ;
#53431=CARTESIAN_POINT ( 'NONE',  ( 2.624215991343608501, 34.92983774303012723, -32.93378783738812388 ) ) ;
#53439=B_SPLINE_CURVE_WITH_KNOTS ( 'NONE', 3,
 ( #13049, #2994, #3912, #22116, #41244, #3293 ),
 .UNSPECIFIED., .F., .F.,
 ( 4, 2, 4 ),
 ( 9.885284284422818887E-18, 0.0002445244328975394624, 0.0004890488657950690585 ),
 .UNSPECIFIED. ) ;
#53440=DIRECTION ( 'NONE',  ( 0.07836865515943411409, -0.2656332009267449723, 0.9608836331491514837 ) ) ;
#53446=CARTESIAN_POINT ( 'NONE',  ( 5.960721111146673579, 16.28787783074227136, -12.49016043756454231 ) ) ;
#53449=LINE ( 'NONE', #44413, #6464 ) ;
#53453=ORIENTED_EDGE ( 'NONE', *, *, #27880, .T. ) ;
#53459=ORIENTED_EDGE ( 'NONE', *, *, #14284, .T. ) ;
#53463=CARTESIAN_POINT ( 'NONE',  ( 1.227938101723756947, -20.72293514920776758, 37.58536632582772086 ) ) ;
#53470=CARTESIAN_POINT ( 'NONE',  ( 0.7762783648524397284, -41.92424098267925814, -23.17763242108799915 ) ) ;
#53472=CARTESIAN_POINT ( 'NONE',  ( 0.5809828226811553087, 18.83114015454698631, 44.03860873105701046 ) ) ;
#53473=CARTESIAN_POINT ( 'NONE',  ( 0.5839880159502329748, -38.02605095487699316, 29.12121614504449951 ) ) ;
#53481=CARTESIAN_POINT ( 'NONE',  ( 0.5786265663353196143, 34.37803667029857735, -33.35675271369502326 ) ) ;
#53487=CARTESIAN_POINT ( 'NONE',  ( 4.956653778116973719, 21.75875759808707244, 42.88673967249138741 ) ) ;
#53490=ORIENTED_EDGE ( 'NONE', *, *, #58446, .F. ) ;
#53492=VERTEX_POINT ( 'NONE', #54461 ) ;
#53497=DIRECTION ( 'NONE',  ( 0.07439287786467665975, -0.1432402660415362516, 0.9868880006907374547 ) ) ;
#53502=VECTOR ( 'NONE', #13571, 1000.000000000000114 ) ;
#53509=ADVANCED_FACE ( 'NONE', ( #1537 ), #998, .F. ) ;
#53514=CARTESIAN_POINT ( 'NONE',  ( 0.5800708119828326126, 44.00606550371088588, -18.90714262039425719 ) ) ;
#53518=ADVANCED_FACE ( 'NONE', ( #6527 ), #57088, .F. ) ;
#53520=CARTESIAN_POINT ( 'NONE',  ( 0.8557997880470690211, -43.90420959842193582, 19.17299735371994629 ) ) ;
#53522=CARTESIAN_POINT ( 'NONE',  ( 0.5786265663353196143, -47.89572889566445468, -0.7221568112311492760 ) ) ;
#53530=EDGE_LOOP ( 'NONE', ( #11660, #19514, #9746, #6075 ) ) ;
#53531=CARTESIAN_POINT ( 'NONE',  ( 0.9730545539215883499, -37.40983423658487794, 21.01499094264535472 ) ) ;
#53532=CARTESIAN_POINT ( 'NONE',  ( 0.9756008150404607004, 16.28894658522385086, -39.69644259322190294 ) ) ;
#53534=ORIENTED_EDGE ( 'NONE', *, *, #4134, .T. ) ;
#53536=AXIS2_PLACEMENT_3D ( 'NONE', #32782, #56561, #51239 ) ;
#53537=CARTESIAN_POINT ( 'NONE',  ( 0.8557997880470599172, 23.15977007032323343, 41.93815086860265495 ) ) ;
#53553=ORIENTED_EDGE ( 'NONE', *, *, #50830, .T. ) ;
#53569=CARTESIAN_POINT ( 'NONE',  ( 3.270143674763207553, 13.14781761974174579, -3.806843787665778578 ) ) ;
#53570=ORIENTED_EDGE ( 'NONE', *, *, #33523, .T. ) ;
#53574=CARTESIAN_POINT ( 'NONE',  ( -48.95476116535499500, 0.000000000000000000, 8.000000000000000000 ) ) ;
#53575=CARTESIAN_POINT ( 'NONE',  ( 0.8551540677456739292, 17.49081417858787901, 44.61036085020956676 ) ) ;
#53579=CARTESIAN_POINT ( 'NONE',  ( 5.960221823109900008, -17.77295928189562702, 10.26751639438337271 ) ) ;
#53581=EDGE_CURVE ( 'NONE', #1395, #10414, #29616, .T. ) ;
#53588=FACE_OUTER_BOUND ( 'NONE', #60863, .T. ) ;
#53589=B_SPLINE_CURVE_WITH_KNOTS ( 'NONE', 3,
 ( #47091, #3520, #56763, #4131, #37698, #47694, #4738, #32368, #13890, #43015, #28267, #23270, #47384, #4430, #19203, #22970 ),
 .UNSPECIFIED., .F., .F.,
 ( 4, 3, 3, 3, 3, 4 ),
 ( 6.938893903907228378E-18, 0.0002724568934985554386, 0.0004086836638483802011, 0.0005449104342063607661, 0.0008173270854453615775, 0.001089761613562689876 ),
 .UNSPECIFIED. ) ;
#53593=CARTESIAN_POINT ( 'NONE',  ( 0.5819845901640502417, 29.51612926147670990, -37.72030663501125503 ) ) ;
#53594=CARTESIAN_POINT ( 'NONE',  ( 4.967162193818130511, 0.000000000000000000, 0.000000000000000000 ) ) ;
#53605=ORIENTED_EDGE ( 'NONE', *, *, #58965, .F. ) ;
#53607=B_SPLINE_CURVE_WITH_KNOTS ( 'NONE', 3,
 ( #12086, #17083, #45590, #26460, #31161, #21152 ),
 .UNSPECIFIED., .F., .F.,
 ( 4, 2, 4 ),
 ( 3.471140604459641645E-18, 0.0002291966416970817348, 0.0004583932833941600001 ),
 .UNSPECIFIED. ) ;
#53620=CARTESIAN_POINT ( 'NONE',  ( 5.959547316686252039, -14.51128755440551465, 14.51632612601503602 ) ) ;
#53621=AXIS2_PLACEMENT_3D ( 'NONE', #45908, #39666, #59655 ) ;
#53625=CARTESIAN_POINT ( 'NONE',  ( 5.958863334805807099, 10.26388325355087616, -17.77512673691308720 ) ) ;
#53629=CARTESIAN_POINT ( 'NONE',  ( 0.8551540677456739292, 41.03346287276427518, 24.74404575822789454 ) ) ;
#53641=ADVANCED_FACE ( 'NONE', ( #13137 ), #20242, .F. ) ;
#53647=CARTESIAN_POINT ( 'NONE',  ( 5.960721111146673579, -2.685391721746187343, 20.34914600876570390 ) ) ;
#53658=CARTESIAN_POINT ( 'NONE',  ( 0.9972139404380291339, 6.252633471303369106, 42.45145681504340018 ) ) ;
#53666=EDGE_CURVE ( 'NONE', #13203, #38048, #28067, .T. ) ;
#53668=CARTESIAN_POINT ( 'NONE',  ( 0.8557997880470690211, -44.60232077416674201, -17.48760788519264153 ) ) ;
#53675=CARTESIAN_POINT ( 'NONE',  ( 0.5809828226811553087, 34.25055090842153760, 33.48000389720628789 ) ) ;
#53676=CARTESIAN_POINT ( 'NONE',  ( 0.5832367798473377940, -41.34221369670669333, -24.18350431151206337 ) ) ;
#53678=ORIENTED_EDGE ( 'NONE', *, *, #55163, .F. ) ;
#53680=DIRECTION ( 'NONE',  ( -1.000000000000000000, -0.000000000000000000, -0.000000000000000000 ) ) ;
#53681=CARTESIAN_POINT ( 'NONE',  ( 1.154321485836934169, -11.90271791109283761, -41.23280395520819042 ) ) ;
#53689=ORIENTED_EDGE ( 'NONE', *, *, #34816, .T. ) ;
#53699=CARTESIAN_POINT ( 'NONE',  ( 4.956653778116991482, -8.845409907520609849, -47.27023054223761989 ) ) ;
#53700=CARTESIAN_POINT ( 'NONE',  ( 5.959547316686252039, 2.675599016784533823, -20.35048796920733949 ) ) ;
#53701=DIRECTION ( 'NONE',  ( 0.000000000000000000, 0.000000000000000000, 1.000000000000000000 ) ) ;
#53703=CARTESIAN_POINT ( 'NONE',  ( 5.959547316686252039, 20.52562247508876681, 0.003562808152977453395 ) ) ;
#53708=CARTESIAN_POINT ( 'NONE',  ( 4.956653778116893783, -15.97476558431863758, -45.35992544608534160 ) ) ;
#53718=ORIENTED_EDGE ( 'NONE', *, *, #36389, .T. ) ;
#53722=CARTESIAN_POINT ( 'NONE',  ( 3.660087539127315992, 48.00143792263127551, -1.881558488211890090 ) ) ;
#53723=ORIENTED_EDGE ( 'NONE', *, *, #41824, .T. ) ;
#53726=CARTESIAN_POINT ( 'NONE',  ( 0.9730545539215892381, -16.88610103448586131, 39.44597740938055352 ) ) ;
#53730=CARTESIAN_POINT ( 'NONE',  ( 0.7762783648524391733, -28.45155609988356105, 38.54028518467411857 ) ) ;
#53735=CARTESIAN_POINT ( 'NONE',  ( 0.9722240741986380996, 29.92651525529375434, 30.74950262511610788 ) ) ;
#53744=EDGE_CURVE ( 'NONE', #57079, #24422, #41514, .T. ) ;
#53746=CARTESIAN_POINT ( 'NONE',  ( 5.959547316686252039, -18.96183906913538308, -7.858107265727685586 ) ) ;
#53747=CARTESIAN_POINT ( 'NONE',  ( 0.7057020205115016598, -11.58334423512203948, -46.47981817772236468 ) ) ;
#53751=CARTESIAN_POINT ( 'NONE',  ( 1.227938101723756947, -42.43379953535190197, 6.439911493064418124 ) ) ;
#53752=( BOUNDED_SURFACE ( )  B_SPLINE_SURFACE ( 3, 1, ( 
 ( #44193, #1222 ),
 ( #6516, #1843 ),
 ( #20970, #7455 ),
 ( #22513, #50389 ) ),
 .UNSPECIFIED., .F., .F., .F. ) 
 B_SPLINE_SURFACE_WITH_KNOTS ( ( 4, 4 ),
 ( 2, 2 ),
 ( 0.000000000000000000, 1.000000000000000000 ),
 ( 0.000000000000000000, 1.000000000000000000 ),
 .UNSPECIFIED. ) 
 GEOMETRIC_REPRESENTATION_ITEM ( )  RATIONAL_B_SPLINE_SURFACE ( (
 ( 1.000000000000000000, 1.000000000000000000),
 ( 0.7269869731126821222, 0.9931720237060910339),
 ( 0.7269869731126821222, 0.9931720237060910339),
 ( 1.000000000000000000, 1.000000000000000000) ) ) 
 REPRESENTATION_ITEM ( '' )  SURFACE ( )  );
#53754=CARTESIAN_POINT ( 'NONE',  ( -19.02783903667571508, -7.790278942242345295, 1.821455418571972684 ) ) ;
#53761=CARTESIAN_POINT ( 'NONE',  ( 0.6067375320500714153, 28.59217831627016082, 38.42671567536863364 ) ) ;
#53764=CARTESIAN_POINT ( 'NONE',  ( 5.959547316686252039, 0.003562808152622182027, 20.52562247508876681 ) ) ;
#53765=VERTEX_POINT ( 'NONE', #43190 ) ;
#53766=CARTESIAN_POINT ( 'NONE',  ( 4.956653778116992370, 15.97476558431944937, -45.35992544608513555 ) ) ;
#53774=CARTESIAN_POINT ( 'NONE',  ( 1.227938101723757836, -10.28900963485409292, 41.66816631169188412 ) ) ;
#53780=EDGE_CURVE ( 'NONE', #36466, #1395, #43739, .T. ) ;
#53782=ORIENTED_EDGE ( 'NONE', *, *, #5210, .T. ) ;
#53786=VERTEX_POINT ( 'NONE', #53766 ) ;
#53789=CARTESIAN_POINT ( 'NONE',  ( 4.956653778116990594, -3.690426056929668075, -47.94889704119055551 ) ) ;
#53790=ORIENTED_EDGE ( 'NONE', *, *, #19497, .T. ) ;
#53798=CARTESIAN_POINT ( 'NONE',  ( 3.407937589446174087, 2.242416846335791192, -13.51415833181185633 ) ) ;
#53806=CARTESIAN_POINT ( 'NONE',  ( 4.963659409799330291, -44.62477100936219898, 3.403493583737159600 ) ) ;
#53807=CARTESIAN_POINT ( 'NONE',  ( 3.783198216974388739, 43.00370179234474932, 1.726720072276125340 ) ) ;
#53814=CARTESIAN_POINT ( 'NONE',  ( 5.860006189529234355, 47.30296539008838153, -9.426589201135005425 ) ) ;
#53815=B_SPLINE_CURVE_WITH_KNOTS ( 'NONE', 3,
 ( #17817, #45411, #8096, #41631 ),
 .UNSPECIFIED., .F., .F.,
 ( 4, 4 ),
 ( 7.640664332323339286E-17, 0.005004741218457509078 ),
 .UNSPECIFIED. ) ;
#53816=CARTESIAN_POINT ( 'NONE',  ( 0.9730545539215883499, -39.44597740938072405, 16.88610103448544209 ) ) ;
#53832=CARTESIAN_POINT ( 'NONE',  ( 1.227938101723748288, 39.32113113558966688, 17.20315230597858047 ) ) ;
#53833=VERTEX_POINT ( 'NONE', #5844 ) ;
#53836=LINE ( 'NONE', #2140, #16549 ) ;
#53840=ORIENTED_EDGE ( 'NONE', *, *, #12497, .F. ) ;
#53845=CARTESIAN_POINT ( 'NONE',  ( 5.860006189529234355, 26.81109398084707252, 40.09484204000608543 ) ) ;
#53847=DIRECTION ( 'NONE',  ( -0.07439287786467650709, 0.1432402660415221241, 0.9868880006907395641 ) ) ;
#53868=CARTESIAN_POINT ( 'NONE',  ( 3.407937589446174087, -7.970324840161883806, -11.14158115674381477 ) ) ;
#53872=B_SPLINE_CURVE_WITH_KNOTS ( 'NONE', 3,
 ( #42944, #9710, #33537, #34154, #48244, #52612, #25048, #15353, #43252, #53227, #5297, #39477, #10337, #14735, #24739, #44192, #29429, #1221, #53531 ),
 .UNSPECIFIED., .F., .F.,
 ( 4, 3, 3, 3, 3, 3, 4 ),
 ( 9.813676791237319219E-18, 0.0002724573126191793876, 0.0004086839781548479893, 0.0005449106435901837631, 0.0006811373090491419169, 0.0008459866663933661218, 0.001010840725717210981 ),
 .UNSPECIFIED. ) ;
#53873=ORIENTED_EDGE ( 'NONE', *, *, #48947, .T. ) ;
#53879=ORIENTED_EDGE ( 'NONE', *, *, #13268, .T. ) ;
#53885=ORIENTED_EDGE ( 'NONE', *, *, #4848, .T. ) ;
#53893=CARTESIAN_POINT ( 'NONE',  ( -16.69218136511193151, -7.824295838635327627, 1.669278514306655969 ) ) ;
#53897=CARTESIAN_POINT ( 'NONE',  ( 0.5786265663353153954, 46.45062944555893836, 11.69877690266672055 ) ) ;
#53905=VECTOR ( 'NONE', #12103, 1000.000000000000114 ) ;
#53910=CARTESIAN_POINT ( 'NONE',  ( 0.9749527285493326811, 5.317382389863168690, 42.57770849153624226 ) ) ;
#53923=CARTESIAN_POINT ( 'NONE',  ( 1.088313998177378839, 39.34193117255255601, 17.14007796983248966 ) ) ;
#53929=CARTESIAN_POINT ( 'NONE',  ( 0.9722240750034584211, 39.86121765932399796, 15.88116978452995554 ) ) ;
#53936=CARTESIAN_POINT ( 'NONE',  ( 0.5800708057587393718, 24.48933404430316685, -41.16170989303176952 ) ) ;
#53938=EDGE_CURVE ( 'NONE', #41443, #20504, #42298, .T. ) ;
#53947=CARTESIAN_POINT ( 'NONE',  ( 5.960721111146673579, 14.50930005614996610, 14.51823969584104645 ) ) ;
#53948=CARTESIAN_POINT ( 'NONE',  ( 2.526552050251863690, -25.19159344346098450, -34.82218744039929703 ) ) ;
#53959=CARTESIAN_POINT ( 'NONE',  ( 5.960221823109900008, 17.77295928189555241, -10.26751639438349706 ) ) ;
#53960=LINE ( 'NONE', #29553, #37835 ) ;
#53971=CARTESIAN_POINT ( 'NONE',  ( 0.9730545539215883499, -25.71816799638802920, 34.34678117142546938 ) ) ;
#53973=( BOUNDED_SURFACE ( )  B_SPLINE_SURFACE ( 3, 1, ( 
 ( #6144, #54378 ),
 ( #54071, #2067 ),
 ( #40336, #45340 ),
 ( #58769, #11193 ) ),
 .UNSPECIFIED., .F., .F., .F. ) 
 B_SPLINE_SURFACE_WITH_KNOTS ( ( 4, 4 ),
 ( 2, 2 ),
 ( 0.000000000000000000, 1.000000000000000000 ),
 ( 0.000000000000000000, 1.000000000000000000 ),
 .UNSPECIFIED. ) 
 GEOMETRIC_REPRESENTATION_ITEM ( )  RATIONAL_B_SPLINE_SURFACE ( (
 ( 1.000000000000000000, 1.000000000000000000),
 ( 0.9953390228620291325, 0.8624445117761032620),
 ( 0.9953390228620291325, 0.8624445117761032620),
 ( 1.000000000000000000, 1.000000000000000000) ) ) 
 REPRESENTATION_ITEM ( '' )  SURFACE ( )  );
#53978=CARTESIAN_POINT ( 'NONE',  ( 0.5809828226811553087, 41.20389530892342833, -24.41822904836879715 ) ) ;
#53979=VERTEX_POINT ( 'NONE', #152 ) ;
#53983=CARTESIAN_POINT ( 'NONE',  ( 1.227938101723757836, 39.96870412324336996, 15.63977281655856366 ) ) ;
#53985=ORIENTED_EDGE ( 'NONE', *, *, #45600, .T. ) ;
#53989=B_SPLINE_CURVE_WITH_KNOTS ( 'NONE', 3,
 ( #17097, #36208, #22396, #55903 ),
 .UNSPECIFIED., .F., .F.,
 ( 4, 4 ),
 ( 0.000000000000000000, 0.004446090762761374660 ),
 .UNSPECIFIED. ) ;
#53991=ORIENTED_EDGE ( 'NONE', *, *, #3246, .T. ) ;
#53994=CARTESIAN_POINT ( 'NONE',  ( 5.960721111146673579, -12.49016043756483363, 16.28787783074205819 ) ) ;
#54002=VERTEX_POINT ( 'NONE', #29296 ) ;
#54003=ORIENTED_EDGE ( 'NONE', *, *, #43161, .F. ) ;
#54016=LINE ( 'NONE', #27003, #47805 ) ;
#54018=ORIENTED_EDGE ( 'NONE', *, *, #15018, .T. ) ;
#54028=EDGE_CURVE ( 'NONE', #23595, #36860, #49692, .T. ) ;
#54035=DIRECTION ( 'NONE',  ( 0.000000000000000000, 0.000000000000000000, -1.000000000000000000 ) ) ;
#54038=DIRECTION ( 'NONE',  ( -1.000000000000000000, 0.000000000000000000, 0.000000000000000000 ) ) ;
#54053=CARTESIAN_POINT ( 'NONE',  ( 0.9730545539215892381, 29.98130006528861813, 30.69604515769660935 ) ) ;
#54057=ORIENTED_EDGE ( 'NONE', *, *, #57977, .F. ) ;
#54058=CARTESIAN_POINT ( 'NONE',  ( 0.5786265663353153954, -37.55861529268574373, 29.72999788434278656 ) ) ;
#54059=CARTESIAN_POINT ( 'NONE',  ( 5.981074661064941900, -14.51919955600745737, 14.50705827991420804 ) ) ;
#54062=CARTESIAN_POINT ( 'NONE',  ( 3.783278058412226308, -42.41041238787298795, 7.325100730114140646 ) ) ;
#54070=ORIENTED_EDGE ( 'NONE', *, *, #26446, .F. ) ;
#54071=CARTESIAN_POINT ( 'NONE',  ( 5.959828726073459926, -0.004526594003237118143, -20.52560994243598813 ) ) ;
#54072=CARTESIAN_POINT ( 'NONE',  ( 0.5809828226811617480, 47.89273459658653564, 0.5448590168534191980 ) ) ;
#54076=EDGE_CURVE ( 'NONE', #23849, #47109, #19105, .T. ) ;
#54084=CARTESIAN_POINT ( 'NONE',  ( 0.5838002273316443835, 41.54704836736078732, -23.82993264414519885 ) ) ;
#54087=CARTESIAN_POINT ( 'NONE',  ( 3.783198216974394068, -43.00370179234476353, -1.726720072276429541 ) ) ;
#54092=CARTESIAN_POINT ( 'NONE',  ( 1.227938101723748288, -36.73927144310496828, -22.18841447410757795 ) ) ;
#54096=CARTESIAN_POINT ( 'NONE',  ( 0.9752570700956807448, 33.90066715551972010, 26.30364510018319280 ) ) ;
#54100=EDGE_CURVE ( 'NONE', #46412, #37486, #21304, .T. ) ;
#54116=CARTESIAN_POINT ( 'NONE',  ( 0.5800708119828320575, -47.40012378203037002, 6.873289505980478609 ) ) ;
#54124=CARTESIAN_POINT ( 'NONE',  ( 5.959828726073459926, -20.52560994243598813, 0.004526594003308782171 ) ) ;
#54131=B_SPLINE_CURVE_WITH_KNOTS ( 'NONE', 3,
 ( #61328, #33167, #37565, #52242, #51014, #18761, #32550, #56640, #27218, #46345, #3389, #13761, #17829, #36954, #56020, #8403 ),
 .UNSPECIFIED., .F., .F.,
 ( 4, 3, 3, 3, 3, 4 ),
 ( 3.469446951953614189E-18, 0.0002724568934985433497, 0.0004086836638483668654, 0.0005449104342063524177, 0.0008173270854453568070, 0.001089761613562690093 ),
 .UNSPECIFIED. ) ;
#54132=EDGE_LOOP ( 'NONE', ( #54968, #39891, #17122, #27001 ) ) ;
#54135=( BOUNDED_SURFACE ( )  B_SPLINE_SURFACE ( 3, 1, ( 
 ( #55907, #23335 ),
 ( #13327, #51507 ),
 ( #47451, #4502 ),
 ( #23639, #42766 ) ),
 .UNSPECIFIED., .F., .F., .F. ) 
 B_SPLINE_SURFACE_WITH_KNOTS ( ( 4, 4 ),
 ( 2, 2 ),
 ( 0.000000000000000000, 1.000000000000000000 ),
 ( 0.000000000000000000, 1.000000000000000000 ),
 .UNSPECIFIED. ) 
 GEOMETRIC_REPRESENTATION_ITEM ( )  RATIONAL_B_SPLINE_SURFACE ( (
 ( 1.000000000000000000, 1.000000000000000000),
 ( 0.7269869731126821222, 0.9931720237060910339),
 ( 0.7269869731126821222, 0.9931720237060910339),
 ( 1.000000000000000000, 1.000000000000000000) ) ) 
 REPRESENTATION_ITEM ( '' )  SURFACE ( )  );
#54137=CARTESIAN_POINT ( 'NONE',  ( 0.9754402186311950107, -26.26956909363294201, -33.92707563620669475 ) ) ;
#54142=CARTESIAN_POINT ( 'NONE',  ( 0.7056555295713258236, 17.55111680842097854, -44.57023068418411071 ) ) ;
#54143=CARTESIAN_POINT ( 'NONE',  ( 0.9757402383260936896, 16.49876987395781569, -39.60970160107518012 ) ) ;
#54145=ORIENTED_EDGE ( 'NONE', *, *, #46543, .F. ) ;
#54147=CARTESIAN_POINT ( 'NONE',  ( 4.956653778116992370, 21.75875759808766929, -42.88673967249108188 ) ) ;
#54148=EDGE_CURVE ( 'NONE', #9101, #29673, #13887, .T. ) ;
#54159=ORIENTED_EDGE ( 'NONE', *, *, #36955, .T. ) ;
#54160=LINE ( 'NONE', #44511, #16775 ) ;
#54162=CARTESIAN_POINT ( 'NONE',  ( 5.959547316686252039, 5.308980600728456345, -19.82715097195157128 ) ) ;
#54164=ORIENTED_EDGE ( 'NONE', *, *, #60177, .T. ) ;
#54165=ORIENTED_EDGE ( 'NONE', *, *, #56606, .T. ) ;
#54174=ORIENTED_EDGE ( 'NONE', *, *, #20858, .F. ) ;
#54177=ORIENTED_EDGE ( 'NONE', *, *, #61480, .F. ) ;
#54183=CARTESIAN_POINT ( 'NONE',  ( 0.8557997880470697982, 44.60232077416686991, 17.48760788519232889 ) ) ;
#54187=FACE_OUTER_BOUND ( 'NONE', #16937, .T. ) ;
#54193=CARTESIAN_POINT ( 'NONE',  ( 1.154321713695927842, -42.64911660416107964, 4.782433421669931128 ) ) ;
#54194=EDGE_CURVE ( 'NONE', #42473, #51079, #23506, .T. ) ;
#54195=CARTESIAN_POINT ( 'NONE',  ( -17.83628007174841912, -7.719455939378114806, -2.099999999999997424 ) ) ;
#54202=ADVANCED_FACE ( 'NONE', ( #3548 ), #1473, .F. ) ;
#54204=CARTESIAN_POINT ( 'NONE',  ( 0.5832366564991501301, 34.05963937630803429, 33.67434452455926674 ) ) ;
#54206=ORIENTED_EDGE ( 'NONE', *, *, #387, .T. ) ;
#54209=DIRECTION ( 'NONE',  ( 0.000000000000000000, 0.000000000000000000, 1.000000000000000000 ) ) ;
#54210=ORIENTED_EDGE ( 'NONE', *, *, #37009, .T. ) ;
#54218=CARTESIAN_POINT ( 'NONE',  ( 0.5263152470540364281, 5.252319464604789579E-15, 42.88844316795388778 ) ) ;
#54219=EDGE_CURVE ( 'NONE', #29673, #59493, #52680, .T. ) ;
#54220=ORIENTED_EDGE ( 'NONE', *, *, #54219, .F. ) ;
#54223=VERTEX_POINT ( 'NONE', #17673 ) ;
#54229=ORIENTED_EDGE ( 'NONE', *, *, #14011, .T. ) ;
#54230=CARTESIAN_POINT ( 'NONE',  ( 1.227938101723756947, 42.91134962331487657, -0.8460948827226678626 ) ) ;
#54234=ORIENTED_EDGE ( 'NONE', *, *, #7536, .F. ) ;
#54239=EDGE_LOOP ( 'NONE', ( #14094, #50197, #58804, #31380 ) ) ;
#54240=EDGE_CURVE ( 'NONE', #3716, #51719, #60894, .T. ) ;
#54244=AXIS2_PLACEMENT_3D ( 'NONE', #4622, #51642, #43205 ) ;
#54249=CARTESIAN_POINT ( 'NONE',  ( 0.5807400328401637335, 41.20655774452968245, 24.41979442053184712 ) ) ;
#54272=CARTESIAN_POINT ( 'NONE',  ( 0.9730545539215883499, -36.90443313492315980, -21.89037132892475057 ) ) ;
#54274=CARTESIAN_POINT ( 'NONE',  ( 5.860006189529246790, 45.66786516969929721, 15.52021937683292307 ) ) ;
#54286=ORIENTED_EDGE ( 'NONE', *, *, #8490, .T. ) ;
#54288=CARTESIAN_POINT ( 'NONE',  ( 1.227938101723756947, -39.32113113558978057, 17.20315230597830336 ) ) ;
#54291=B_SPLINE_CURVE_WITH_KNOTS ( 'NONE', 3,
 ( #32666, #37069, #56136, #47079, #4118, #27031 ),
 .UNSPECIFIED., .F., .F.,
 ( 4, 2, 4 ),
 ( 9.745765416140531346E-18, 0.0002291978881530110101, 0.0004583957763060122624 ),
 .UNSPECIFIED. ) ;
#54306=ORIENTED_EDGE ( 'NONE', *, *, #42398, .T. ) ;
#54308=CARTESIAN_POINT ( 'NONE',  ( 3.660087539127321321, 20.10768839917405515, 43.62750476736560046 ) ) ;
#54310=CARTESIAN_POINT ( 'NONE',  ( 0.5839254288179565044, 44.28478521851644700, -18.24509008251428455 ) ) ;
#54312=CARTESIAN_POINT ( 'NONE',  ( 0.9730545539215883499, 29.98130006528905156, -30.69604515769618658 ) ) ;
#54316=CARTESIAN_POINT ( 'NONE',  ( 0.9747592971366227932, -30.56898208368253123, -30.11108831501868011 ) ) ;
#54318=EDGE_CURVE ( 'NONE', #56168, #54683, #43981, .T. ) ;
#54319=CARTESIAN_POINT ( 'NONE',  ( 4.960156602257180580, 14.43621227656528561, 44.12083041402467387 ) ) ;
#54320=EDGE_LOOP ( 'NONE', ( #22503, #60853, #44224, #23447 ) ) ;
#54321=CARTESIAN_POINT ( 'NONE',  ( 0.5786265663353196143, 46.45062944555908757, -11.69877690266605974 ) ) ;
#54332=CARTESIAN_POINT ( 'NONE',  ( 0.6067099128993230783, 5.548253864791079515, -47.57459301987697131 ) ) ;
#54334=CARTESIAN_POINT ( 'NONE',  ( 0.5839879327111915375, 46.24044206955238678, -12.48412918464389065 ) ) ;
#54355=ADVANCED_FACE ( 'NONE', ( #59257 ), #59503, .T. ) ;
#54370=DIRECTION ( 'NONE',  ( 0.07836865515943411409, 0.9649662368512237354, -0.2503967164834429715 ) ) ;
#54371=ADVANCED_FACE ( 'NONE', ( #60188 ), #5375, .F. ) ;
#54378=CARTESIAN_POINT ( 'NONE',  ( 0.5807400328401637335, -0.5448834511093417765, 47.89582301953903709 ) ) ;
#54379=CARTESIAN_POINT ( 'NONE',  ( 5.981074661064941900, -20.52466374824937034, -0.008585178657544500352 ) ) ;
#54382=CARTESIAN_POINT ( 'NONE',  ( 0.9756354156337465611, 41.47994205070128260, -10.97961179198156678 ) ) ;
#54383=ORIENTED_EDGE ( 'NONE', *, *, #31930, .T. ) ;
#54385=FACE_OUTER_BOUND ( 'NONE', #14600, .T. ) ;
#54386=ORIENTED_EDGE ( 'NONE', *, *, #24470, .F. ) ;
#54388=CARTESIAN_POINT ( 'NONE',  ( 2.624215991343620935, -28.09277600149244947, 38.92973006074502962 ) ) ;
#54389=CARTESIAN_POINT ( 'NONE',  ( 1.227938101723756947, 30.94118573761312874, 29.74462687941236538 ) ) ;
#54397=ORIENTED_EDGE ( 'NONE', *, *, #45845, .F. ) ;
#54403=CARTESIAN_POINT ( 'NONE',  ( 5.860006189529234355, -40.11385274514663735, -26.78264244998140597 ) ) ;
#54409=ORIENTED_EDGE ( 'NONE', *, *, #40870, .T. ) ;
#54412=CARTESIAN_POINT ( 'NONE',  ( 0.5837374860065628335, 18.49670552082956121, 44.18034382476631805 ) ) ;
#54419=ORIENTED_EDGE ( 'NONE', *, *, #50907, .T. ) ;
#54421=CARTESIAN_POINT ( 'NONE',  ( 4.956653778116970166, -27.17045123668450657, -39.67974989265067620 ) ) ;
#54426=AXIS2_PLACEMENT_3D ( 'NONE', #50223, #25183, #44622 ) ;
#54427=CARTESIAN_POINT ( 'NONE',  ( 0.5807400328401574052, 44.04145271122592220, -18.83234461715134955 ) ) ;
#54429=CARTESIAN_POINT ( 'NONE',  ( 4.956653778116991482, 9.917440902361805755, -47.05699031914939212 ) ) ;
#54437=EDGE_CURVE ( 'NONE', #995, #15923, #6937, .T. ) ;
#54442=VERTEX_POINT ( 'NONE', #59884 ) ;
#54451=DIRECTION ( 'NONE',  ( 0.07439287786467665975, 0.6957517427943022970, 0.7144194931003088334 ) ) ;
#54455=ORIENTED_EDGE ( 'NONE', *, *, #38177, .F. ) ;
#54458=ORIENTED_EDGE ( 'NONE', *, *, #34382, .F. ) ;
#54461=CARTESIAN_POINT ( 'NONE',  ( 0.9730545539215883499, -39.83279466599027785, -15.95224156741871546 ) ) ;
#54463=CARTESIAN_POINT ( 'NONE',  ( 5.860006189529234355, -36.25227510158484989, 31.81514841426745477 ) ) ;
#54468=EDGE_CURVE ( 'NONE', #13139, #40550, #30154, .T. ) ;
#54474=CARTESIAN_POINT ( 'NONE',  ( 0.5834872094924159480, 34.02770606800808650, -33.70665904794255141 ) ) ;
#54475=AXIS2_PLACEMENT_3D ( 'NONE', #32065, #17341, #21109 ) ;
#54477=ORIENTED_EDGE ( 'NONE', *, *, #28036, .F. ) ;
#54483=B_SPLINE_CURVE_WITH_KNOTS ( 'NONE', 3,
 ( #19304, #4546, #57471, #23076, #14613, #13373, #32474, #51552, #61260, #18380 ),
 .UNSPECIFIED., .F., .F.,
 ( 4, 3, 3, 4 ),
 ( 4.878909776184769953E-18, 0.0002724573126191764060, 0.0004086839781548493446, 0.0005054209210073039738 ),
 .UNSPECIFIED. ) ;
#54489=CARTESIAN_POINT ( 'NONE',  ( 3.270143674763207553, 9.482922169187961714, 9.870732238228558941 ) ) ;
#54492=CARTESIAN_POINT ( 'NONE',  ( -20.05982656558827060, -12.49764874730863085, -0.2771623350404011643 ) ) ;
#54495=CARTESIAN_POINT ( 'NONE',  ( 3.783278058412226752, -41.09146792477075394, 12.79810311738840056 ) ) ;
#54496=ORIENTED_EDGE ( 'NONE', *, *, #29769, .T. ) ;
#54497=CARTESIAN_POINT ( 'NONE',  ( 4.967162193818130511, 8.839793687085803597, -42.16965968614184135 ) ) ;
#54503=CARTESIAN_POINT ( 'NONE',  ( 0.9730545539215883499, -42.60426903087357431, 5.099196237954729760 ) ) ;
#54504=( BOUNDED_SURFACE ( )  B_SPLINE_SURFACE ( 3, 1, ( 
 ( #50029, #45652 ),
 ( #8034, #50627 ),
 ( #36257, #30597 ),
 ( #35644, #2707 ) ),
 .UNSPECIFIED., .F., .F., .F. ) 
 B_SPLINE_SURFACE_WITH_KNOTS ( ( 4, 4 ),
 ( 2, 2 ),
 ( 0.000000000000000000, 1.000000000000000000 ),
 ( 0.000000000000000000, 1.000000000000000000 ),
 .UNSPECIFIED. ) 
 GEOMETRIC_REPRESENTATION_ITEM ( )  RATIONAL_B_SPLINE_SURFACE ( (
 ( 1.000000000000000000, 1.000000000000000000),
 ( 0.7269869731126817891, 0.9931720237060910339),
 ( 0.7269869731126817891, 0.9931720237060910339),
 ( 1.000000000000000000, 1.000000000000000000) ) ) 
 REPRESENTATION_ITEM ( '' )  SURFACE ( )  );
#54505=CARTESIAN_POINT ( 'NONE',  ( 0.5850706913938533704, 12.57184842332082297, -46.21698775168632523 ) ) ;
#54507=( BOUNDED_SURFACE ( )  B_SPLINE_SURFACE ( 3, 1, ( 
 ( #43683, #5412 ),
 ( #35195, #58036 ),
 ( #10452, #20168 ),
 ( #38977, #44602 ) ),
 .UNSPECIFIED., .F., .F., .F. ) 
 B_SPLINE_SURFACE_WITH_KNOTS ( ( 4, 4 ),
 ( 2, 2 ),
 ( 0.000000000000000000, 1.000000000000000000 ),
 ( 0.000000000000000000, 1.000000000000000000 ),
 .UNSPECIFIED. ) 
 GEOMETRIC_REPRESENTATION_ITEM ( )  RATIONAL_B_SPLINE_SURFACE ( (
 ( 1.000000000000000000, 1.000000000000000000),
 ( 0.7269869731126817891, 0.9931720237060910339),
 ( 0.7269869731126817891, 0.9931720237060910339),
 ( 1.000000000000000000, 1.000000000000000000) ) ) 
 REPRESENTATION_ITEM ( '' )  SURFACE ( )  );
#54509=CARTESIAN_POINT ( 'NONE',  ( 5.960721111146673579, -17.77250458025985225, -10.26825948882919626 ) ) ;
#54517=VECTOR ( 'NONE', #17508, 1000.000000000000114 ) ;
#54518=CARTESIAN_POINT ( 'NONE',  ( 4.967162193818129623, -38.44485641567058565, -19.45289607368863116 ) ) ;
#54529=VERTEX_POINT ( 'NONE', #13216 ) ;
#54536=CARTESIAN_POINT ( 'NONE',  ( 5.959828726073459926, -2.683617577144242095, -20.34941966491238219 ) ) ;
#54538=ORIENTED_EDGE ( 'NONE', *, *, #55538, .F. ) ;
#54543=CARTESIAN_POINT ( 'NONE',  ( 0.5807400328401637335, 46.12278621143497048, 12.92266817606032170 ) ) ;
#54544=CARTESIAN_POINT ( 'NONE',  ( 0.7057020205115047684, 24.67553336431243949, -41.05685587925813707 ) ) ;
#54550=CARTESIAN_POINT ( 'NONE',  ( 5.959547316686252039, 10.26589671991363417, -17.77392908783923531 ) ) ;
#54554=AXIS2_PLACEMENT_3D ( 'NONE', #48032, #4460, #56791 ) ;
#54556=CARTESIAN_POINT ( 'NONE',  ( 0.6846871229502899947, -34.48177377577813019, -33.25969555998779015 ) ) ;
#54558=ADVANCED_FACE ( 'NONE', ( #874 ), #55088, .F. ) ;
#54561=CONICAL_SURFACE ( 'NONE', #557, 43.08621763946400307, 1.568696531533066763 ) ;
#54571=CARTESIAN_POINT ( 'NONE',  ( 0.9730545539215883499, 6.101350888304637010, 42.47233286818619291 ) ) ;
#54573=ADVANCED_FACE ( 'NONE', ( #1786 ), #27112, .F. ) ;
#54574=DIRECTION ( 'NONE',  ( -0.07836865515943411409, -0.9240274869783758893, -0.3742079063795003546 ) ) ;
#54575=CARTESIAN_POINT ( 'NONE',  ( 5.959547316686252039, -14.51632612601518879, -14.51128755440536366 ) ) ;
#54577=CARTESIAN_POINT ( 'NONE',  ( 0.5809828226811553087, -41.20389530892325070, 24.41822904836909203 ) ) ;
#54580=CARTESIAN_POINT ( 'NONE',  ( 0.6846871229502899947, -47.60345020167346775, -5.395516691087686389 ) ) ;
#54583=CARTESIAN_POINT ( 'NONE',  ( 4.967162193818130511, 8.839793687085803597, -42.16965968614184135 ) ) ;
#54588=CARTESIAN_POINT ( 'NONE',  ( 4.967162193818130511, 28.74031574030012237, 32.10009971360082659 ) ) ;
#54590=( BOUNDED_SURFACE ( )  B_SPLINE_SURFACE ( 3, 1, ( 
 ( #40916, #17090 ),
 ( #36201, #55268 ),
 ( #12391, #31480 ),
 ( #8912, #23325 ) ),
 .UNSPECIFIED., .F., .F., .F. ) 
 B_SPLINE_SURFACE_WITH_KNOTS ( ( 4, 4 ),
 ( 2, 2 ),
 ( 0.000000000000000000, 1.000000000000000000 ),
 ( 0.000000000000000000, 1.000000000000000000 ),
 .UNSPECIFIED. ) 
 GEOMETRIC_REPRESENTATION_ITEM ( )  RATIONAL_B_SPLINE_SURFACE ( (
 ( 1.000000000000000000, 1.000000000000000000),
 ( 0.9953390228620291325, 0.8624445117760984880),
 ( 0.9953390228620291325, 0.8624445117760984880),
 ( 1.000000000000000000, 1.000000000000000000) ) ) 
 REPRESENTATION_ITEM ( '' )  SURFACE ( )  );
#54592=ORIENTED_EDGE ( 'NONE', *, *, #37744, .F. ) ;
#54593=ORIENTED_EDGE ( 'NONE', *, *, #10195, .T. ) ;
#54598=EDGE_CURVE ( 'NONE', #11517, #4600, #35400, .T. ) ;
#54602=CARTESIAN_POINT ( 'NONE',  ( 1.227938101723748288, -36.73927144310496828, -22.18841447410757795 ) ) ;
#54604=EDGE_LOOP ( 'NONE', ( #14760, #50722, #20210, #57629 ) ) ;
#54608=AXIS2_PLACEMENT_3D ( 'NONE', #40209, #30140, #49251 ) ;
#54621=CARTESIAN_POINT ( 'NONE',  ( 4.956653778116997699, 42.88673967249161478, -21.75875759808661059 ) ) ;
#54622=CARTESIAN_POINT ( 'NONE',  ( 5.860006189529246790, -31.81514841426783136, 36.25227510158452304 ) ) ;
#54625=EDGE_CURVE ( 'NONE', #5464, #37539, #58545, .T. ) ;
#54631=CARTESIAN_POINT ( 'NONE',  ( 0.9756950546413939440, -21.53795086961238425, -37.11135009583549760 ) ) ;
#54633=FACE_OUTER_BOUND ( 'NONE', #60353, .T. ) ;
#54639=ADVANCED_FACE ( 'NONE', ( #18384 ), #52708, .F. ) ;
#54643=CARTESIAN_POINT ( 'NONE',  ( 4.967162193818130511, -38.83676580803754064, -18.65818244221298983 ) ) ;
#54646=CARTESIAN_POINT ( 'NONE',  ( 0.9968887458511638267, -15.81144734640156635, -39.89008038581160775 ) ) ;
#54647=DIRECTION ( 'NONE',  ( 0.000000000000000000, 0.000000000000000000, 1.000000000000000000 ) ) ;
#54653=VECTOR ( 'NONE', #1032, 1000.000000000000114 ) ;
#54655=CARTESIAN_POINT ( 'NONE',  ( 0.8557997880470690211, 7.156447707085701104, 47.37054680076709445 ) ) ;
#54658=MECHANICAL_DESIGN_GEOMETRIC_PRESENTATION_REPRESENTATION('',(#2658),#41736);
#54660=CARTESIAN_POINT ( 'NONE',  ( -15.94111418026541038, -12.48882310846358301, -0.5454162216299145438 ) ) ;
#54674=CARTESIAN_POINT ( 'NONE',  ( 3.660176727303412036, -10.60619300811838706, -46.85282580473590031 ) ) ;
#54683=VERTEX_POINT ( 'NONE', #13689 ) ;
#54684=CARTESIAN_POINT ( 'NONE',  ( 3.270143674763207553, -13.28976595685395878, 3.277085381513066942 ) ) ;
#54686=CARTESIAN_POINT ( 'NONE',  ( 0.7057020205115027700, 41.89806668505412546, -23.21851350879774145 ) ) ;
#54693=CARTESIAN_POINT ( 'NONE',  ( 0.9756008150404594792, 41.40938772927948719, -11.24277293639946151 ) ) ;
#54701=CARTESIAN_POINT ( 'NONE',  ( 0.8557997880470697982, -41.93815086860240626, -23.15977007032367041 ) ) ;
#54705=CARTESIAN_POINT ( 'NONE',  ( 0.5800708119828326126, -33.42085299104044793, 34.30831427709740922 ) ) ;
#54714=CARTESIAN_POINT ( 'NONE',  ( 0.8551540677456715978, -0.9122407826472468395, -47.90804413217341562 ) ) ;
#54715=CARTESIAN_POINT ( 'NONE',  ( 0.8557997880470599172, 37.44587306708097429, 29.88293891557482951 ) ) ;
#54716=AXIS2_PLACEMENT_3D ( 'NONE', #7606, #36465, #45870 ) ;
#54724=ORIENTED_EDGE ( 'NONE', *, *, #41067, .T. ) ;
#54729=CARTESIAN_POINT ( 'NONE',  ( 0.9722240741986378776, -42.90442369863401950, -0.5819399500324929919 ) ) ;
#54740=CARTESIAN_POINT ( 'NONE',  ( 0.6846871229502932144, 43.92355552798038332, 19.12907057981221115 ) ) ;
#54741=CARTESIAN_POINT ( 'NONE',  ( 4.967162193818130511, -35.57684288741994294, 24.30453456948097823 ) ) ;
#54746=CARTESIAN_POINT ( 'NONE',  ( 0.9756354156337448957, -39.69194847698940265, 16.29989858042615225 ) ) ;
#54758=CARTESIAN_POINT ( 'NONE',  ( 0.7762777257811875886, -47.37038525518530463, -7.133808567472758710 ) ) ;
#54763=CARTESIAN_POINT ( 'NONE',  ( 0.9752132459055852243, -39.73079175141339192, -16.20487516111995774 ) ) ;
#54764=B_SPLINE_CURVE_WITH_KNOTS ( 'NONE', 3,
 ( #32589, #48226, #47007, #57581 ),
 .UNSPECIFIED., .F., .F.,
 ( 4, 4 ),
 ( 0.000000000000000000, 0.004446090762761376394 ),
 .UNSPECIFIED. ) ;
#54766=CARTESIAN_POINT ( 'NONE',  ( 0.9730545539215883499, 39.44597740938085195, -16.88610103448514721 ) ) ;
#54768=FACE_OUTER_BOUND ( 'NONE', #41101, .T. ) ;
#54772=FACE_OUTER_BOUND ( 'NONE', #61967, .T. ) ;
#54774=B_SPLINE_CURVE_WITH_KNOTS ( 'NONE', 3,
 ( #26210, #12441, #26837, #45351, #39732, #58781, #54084, #20904, #11205, #30292, #49402, #6455, #25599, #44736, #40050, #59100 ),
 .UNSPECIFIED., .F., .F.,
 ( 4, 3, 3, 3, 3, 4 ),
 ( 9.813676791237319219E-18, 0.0002724568934985644917, 0.0004086836638483901216, 0.0005449104342063723671, 0.0008173270854453691669, 0.001089761613562680986 ),
 .UNSPECIFIED. ) ;
#54781=CARTESIAN_POINT ( 'NONE',  ( 0.8551540677456739292, 28.44084013485118589, 38.56334384152441430 ) ) ;
#54800=EDGE_LOOP ( 'NONE', ( #40047, #29601, #7894, #38943 ) ) ;
#54804=ORIENTED_EDGE ( 'NONE', *, *, #32544, .T. ) ;
#54805=ORIENTED_EDGE ( 'NONE', *, *, #46906, .F. ) ;
#54813=CARTESIAN_POINT ( 'NONE',  ( -19.79535493905475008, -12.45603257510279249, -1.053715328945894036 ) ) ;
#54814=EDGE_CURVE ( 'NONE', #39487, #18847, #45180, .T. ) ;
#54815=CONICAL_SURFACE ( 'NONE', #8809, 43.08621763946400307, 1.568696531533066763 ) ;
#54823=VERTEX_POINT ( 'NONE', #10213 ) ;
#54830=CARTESIAN_POINT ( 'NONE',  ( 5.959547316686252039, 20.35048796920736791, -2.675599016784323769 ) ) ;
#54832=CARTESIAN_POINT ( 'NONE',  ( 1.227938101723748288, -37.58536632582793402, 20.72293514920737323 ) ) ;
#54834=CARTESIAN_POINT ( 'NONE',  ( 3.660176727303412036, 8.130955556895155922, -47.34518114598549943 ) ) ;
#54835=EDGE_CURVE ( 'NONE', #41630, #12616, #3960, .T. ) ;
#54837=ORIENTED_EDGE ( 'NONE', *, *, #58271, .F. ) ;
#54856=ORIENTED_EDGE ( 'NONE', *, *, #387, .F. ) ;
#54859=CARTESIAN_POINT ( 'NONE',  ( 1.227938101723756947, -39.96870412324324917, -15.63977281655884077 ) ) ;
#54867=AXIS2_PLACEMENT_3D ( 'NONE', #59922, #41464, #17033 ) ;
#54872=CARTESIAN_POINT ( 'NONE',  ( 0.5807400328401574052, -24.41979442053198568, 41.20655774452961850 ) ) ;
#54884=B_SPLINE_CURVE_WITH_KNOTS ( 'NONE', 3,
 ( #13949, #3573, #38371, #22704, #13319, #3886 ),
 .UNSPECIFIED., .F., .F.,
 ( 4, 2, 4 ),
 ( 3.471140604459641645E-18, 0.0002291966416970813011, 0.0004583932833941591328 ),
 .UNSPECIFIED. ) ;
#54888=( BOUNDED_SURFACE ( )  B_SPLINE_SURFACE ( 3, 1, ( 
 ( #44918, #31098 ),
 ( #36132, #59274 ),
 ( #35505, #45228 ),
 ( #26393, #55195 ) ),
 .UNSPECIFIED., .F., .F., .F. ) 
 B_SPLINE_SURFACE_WITH_KNOTS ( ( 4, 4 ),
 ( 2, 2 ),
 ( 0.000000000000000000, 1.000000000000000000 ),
 ( 0.000000000000000000, 1.000000000000000000 ),
 .UNSPECIFIED. ) 
 GEOMETRIC_REPRESENTATION_ITEM ( )  RATIONAL_B_SPLINE_SURFACE ( (
 ( 1.000000000000000000, 1.000000000000000000),
 ( 0.7269869731126817891, 0.9931720237060910339),
 ( 0.7269869731126817891, 0.9931720237060910339),
 ( 1.000000000000000000, 1.000000000000000000) ) ) 
 REPRESENTATION_ITEM ( '' )  SURFACE ( )  );
#54889=DIRECTION ( 'NONE',  ( -0.07439287786467650709, 0.1170659376278977565, -0.9903339163990660943 ) ) ;
#54890=ADVANCED_FACE ( 'NONE', ( #56878 ), #61874, .F. ) ;
#54898=CARTESIAN_POINT ( 'NONE',  ( 0.9730545539215883499, 5.099196237954877198, 42.60426903087355299 ) ) ;
#54899=CARTESIAN_POINT ( 'NONE',  ( 0.7762777257811899201, -41.92424087089327855, 23.17763256463755894 ) ) ;
#54903=CARTESIAN_POINT ( 'NONE',  ( 1.088908134280557993, 42.64123480278975364, 4.826714665689003425 ) ) ;
#54907=CARTESIAN_POINT ( 'NONE',  ( 0.6846871229502899947, -24.69859318104460399, -41.05093867799210727 ) ) ;
#54909=VERTEX_POINT ( 'NONE', #38128 ) ;
#54920=ORIENTED_EDGE ( 'NONE', *, *, #4768, .T. ) ;
#54922=CARTESIAN_POINT ( 'NONE',  ( 0.5834872094924179464, 47.89542889285419136, 0.2270145249674854482 ) ) ;
#54924=VECTOR ( 'NONE', #47178, 1000.000000000000000 ) ;
#54933=ADVANCED_FACE ( 'NONE', ( #58715 ), #18707, .F. ) ;
#54935=CARTESIAN_POINT ( 'NONE',  ( 0.9722240741986374335, 0.5819399500326425390, -42.90442369863401950 ) ) ;
#54942=EDGE_CURVE ( 'NONE', #23289, #19565, #22740, .T. ) ;
#54957=CARTESIAN_POINT ( 'NONE',  ( 4.967162193818130511, 38.44485641567072776, 19.45289607368836116 ) ) ;
#54958=ADVANCED_FACE ( 'NONE', ( #54633 ), #25095, .F. ) ;
#54959=B_SPLINE_CURVE_WITH_KNOTS ( 'NONE', 3,
 ( #10250, #32911, #6127, #58443, #24344, #15267, #48450, #20570, #34371, #57836, #5819, #49074, #29652, #48761, #5517, #39703 ),
 .UNSPECIFIED., .F., .F.,
 ( 4, 3, 3, 3, 3, 4 ),
 ( 1.398620802506300720E-17, 0.0002724568934985550049, 0.0004086836638483777075, 0.0005449104342063626092, 0.0008173270854453675406, 0.001089761613562686624 ),
 .UNSPECIFIED. ) ;
#54961=( BOUNDED_SURFACE ( )  B_SPLINE_SURFACE ( 3, 1, ( 
 ( #35888, #13313 ),
 ( #32416, #41211 ),
 ( #51492, #60272 ),
 ( #18324, #28620 ) ),
 .UNSPECIFIED., .F., .F., .F. ) 
 B_SPLINE_SURFACE_WITH_KNOTS ( ( 4, 4 ),
 ( 2, 2 ),
 ( 0.000000000000000000, 1.000000000000000000 ),
 ( 0.000000000000000000, 1.000000000000000000 ),
 .UNSPECIFIED. ) 
 GEOMETRIC_REPRESENTATION_ITEM ( )  RATIONAL_B_SPLINE_SURFACE ( (
 ( 1.000000000000000000, 1.000000000000000000),
 ( 0.9732289882329797637, 0.9999525324661233672),
 ( 0.9732289882329797637, 0.9999525324661233672),
 ( 1.000000000000000000, 1.000000000000000000) ) ) 
 REPRESENTATION_ITEM ( '' )  SURFACE ( )  );
#54963=CARTESIAN_POINT ( 'NONE',  ( 0.9749527285493305717, -5.317382389862895131, -42.57770849153631332 ) ) ;
#54964=CARTESIAN_POINT ( 'NONE',  ( 0.8551540677456715978, 11.51835730326479457, 46.51172240253124812 ) ) ;
#54968=ORIENTED_EDGE ( 'NONE', *, *, #36675, .F. ) ;
#54970=CARTESIAN_POINT ( 'NONE',  ( 5.960721111146673579, 17.77250458025977764, 10.26825948882932060 ) ) ;
#54973=CARTESIAN_POINT ( 'NONE',  ( 3.783278058412227640, -38.10568111914489720, -20.00643011788494263 ) ) ;
#54984=CARTESIAN_POINT ( 'NONE',  ( 2.624215991343620935, -40.85210347989548296, 25.21574086439692053 ) ) ;
#54990=CARTESIAN_POINT ( 'NONE',  ( 0.5850706913938534814, -12.57184842331985131, -46.21698775168658813 ) ) ;
#54994=EDGE_LOOP ( 'NONE', ( #42639, #1792, #37558, #50779 ) ) ;
#54996=CARTESIAN_POINT ( 'NONE',  ( 0.5800708119828336118, -44.00606550371072956, 18.90714262039457694 ) ) ;
#54997=ADVANCED_FACE ( 'NONE', ( #59033 ), #61010, .F. ) ;
#54999=CARTESIAN_POINT ( 'NONE',  ( 2.281448460670306932, -22.83953674062048478, 42.18752512472231331 ) ) ;
#55004=DIRECTION ( 'NONE',  ( 0.000000000000000000, 0.000000000000000000, 1.000000000000000000 ) ) ;
#55007=CARTESIAN_POINT ( 'NONE',  ( 3.783198216974393180, -29.18723368117341366, -31.62918462580868706 ) ) ;
#55008=CARTESIAN_POINT ( 'NONE',  ( 3.270143674763207553, -8.548517033725330450, 10.69018354892884659 ) ) ;
#55009=ORIENTED_EDGE ( 'NONE', *, *, #25209, .T. ) ;
#55012=CARTESIAN_POINT ( 'NONE',  ( 0.8551540677456834771, -46.03951182599436720, 13.28067116677185844 ) ) ;
#55019=EDGE_LOOP ( 'NONE', ( #24810, #22934, #59835, #21321 ) ) ;
#55020=CARTESIAN_POINT ( 'NONE',  ( 5.965394784446458765, -7.841344330025064480, 18.96850062921621571 ) ) ;
#55022=ORIENTED_EDGE ( 'NONE', *, *, #169, .F. ) ;
#55023=EDGE_CURVE ( 'NONE', #38495, #49884, #42548, .T. ) ;
#55026=CARTESIAN_POINT ( 'NONE',  ( 0.5837374860065669413, -18.16107481025629156, 44.31936661703463898 ) ) ;
#55041=CARTESIAN_POINT ( 'NONE',  ( 5.960721111146673579, 19.82454228767745974, -5.318514366754729217 ) ) ;
#55051=CARTESIAN_POINT ( 'NONE',  ( 0.6846871229502932144, 19.12907057981263748, -43.92355552798018437 ) ) ;
#55053=CARTESIAN_POINT ( 'NONE',  ( 0.8557997880470697982, 44.60232077416686991, 17.48760788519232889 ) ) ;
#55060=CARTESIAN_POINT ( 'NONE',  ( 5.959547316686252039, -2.682663672454773440, -20.34955788964375856 ) ) ;
#55062=CARTESIAN_POINT ( 'NONE',  ( 5.958863334805807099, 7.855954700275622038, -18.96276366205785635 ) ) ;
#55065=CARTESIAN_POINT ( 'NONE',  ( 2.526464513654342880, -34.82216969498448833, -25.19161096467265182 ) ) ;
#55070=CARTESIAN_POINT ( 'NONE',  ( 0.8551540677456715978, -24.74404575822804730, 41.03346287276420412 ) ) ;
#55076=ADVANCED_FACE ( 'NONE', ( #26457 ), #31498, .F. ) ;
#55078=CARTESIAN_POINT ( 'NONE',  ( 0.9752570700956811889, -25.93764562640081195, -34.18150842933902567 ) ) ;
#55080=CARTESIAN_POINT ( 'NONE',  ( 0.9754402186311966760, 39.57010335554349467, -16.59348191374094128 ) ) ;
#55088=( BOUNDED_SURFACE ( )  B_SPLINE_SURFACE ( 3, 1, ( 
 ( #39123, #18851 ),
 ( #34410, #53481 ),
 ( #30000, #49412 ),
 ( #7093, #44745 ) ),
 .UNSPECIFIED., .F., .F., .F. ) 
 B_SPLINE_SURFACE_WITH_KNOTS ( ( 4, 4 ),
 ( 2, 2 ),
 ( 0.000000000000000000, 1.000000000000000000 ),
 ( 0.000000000000000000, 1.000000000000000000 ),
 .UNSPECIFIED. ) 
 GEOMETRIC_REPRESENTATION_ITEM ( )  RATIONAL_B_SPLINE_SURFACE ( (
 ( 1.000000000000000000, 1.000000000000000000),
 ( 0.9953390228620291325, 0.8624445117761032620),
 ( 0.9953390228620291325, 0.8624445117761032620),
 ( 1.000000000000000000, 1.000000000000000000) ) ) 
 REPRESENTATION_ITEM ( '' )  SURFACE ( )  );
#55105=DIRECTION ( 'NONE',  ( -1.000000000000000000, -0.000000000000000000, -0.000000000000000000 ) ) ;
#55108=CARTESIAN_POINT ( 'NONE',  ( 0.5807400328401637335, 33.48217046439111755, 34.25275203086248155 ) ) ;
#55120=CARTESIAN_POINT ( 'NONE',  ( 4.967162193818131399, -35.57684288741960899, -24.30453456948146851 ) ) ;
#55124=ORIENTED_EDGE ( 'NONE', *, *, #18905, .F. ) ;
#55126=ORIENTED_EDGE ( 'NONE', *, *, #20670, .T. ) ;
#55128=DIRECTION ( 'NONE',  ( -0.07836865515943410021, 0.9240274869783785539, 0.3742079063794939153 ) ) ;
#55130=VERTEX_POINT ( 'NONE', #33036 ) ;
#55146=ORIENTED_EDGE ( 'NONE', *, *, #23406, .T. ) ;
#55154=CARTESIAN_POINT ( 'NONE',  ( 4.303969348037246512, -25.89994482339398374, 40.54345935592770189 ) ) ;
#55156=B_SPLINE_CURVE_WITH_KNOTS ( 'NONE', 3,
 ( #8103, #36630, #27214, #55701 ),
 .UNSPECIFIED., .F., .F.,
 ( 4, 4 ),
 ( 1.734723475976807094E-17, 0.005004741218457440556 ),
 .UNSPECIFIED. ) ;
#55163=EDGE_CURVE ( 'NONE', #722, #57761, #11419, .T. ) ;
#55164=CARTESIAN_POINT ( 'NONE',  ( 0.5786265663353153954, -29.72999788434269064, -37.55861529268584320 ) ) ;
#55170=CARTESIAN_POINT ( 'NONE',  ( 5.959547316686252039, 0.003562808152905788499, -20.52562247508876681 ) ) ;
#55171=ORIENTED_EDGE ( 'NONE', *, *, #26324, .F. ) ;
#55172=CARTESIAN_POINT ( 'NONE',  ( 0.8557997880470690211, -28.43566216844996930, 38.55640757422429488 ) ) ;
#55181=B_SPLINE_CURVE_WITH_KNOTS ( 'NONE', 3,
 ( #7803, #12535, #45436, #7170, #26930, #2484 ),
 .UNSPECIFIED., .F., .F.,
 ( 4, 2, 4 ),
 ( 1.497895441209388135E-16, 0.0002445252820015227134, 0.0004890505640028956985 ),
 .UNSPECIFIED. ) ;
#55182=CARTESIAN_POINT ( 'NONE',  ( 0.8557997880470599172, -47.89938907511592703, -0.9121262075951160897 ) ) ;
#55184=CARTESIAN_POINT ( 'NONE',  ( 0.9756950546413931669, -42.90834738653779823, 0.09673755062781558278 ) ) ;
#55185=CARTESIAN_POINT ( 'NONE',  ( 0.9757892942422821125, 26.16173342773539900, 34.01031843153901946 ) ) ;
#55188=ORIENTED_EDGE ( 'NONE', *, *, #26800, .T. ) ;
#55189=CARTESIAN_POINT ( 'NONE',  ( 4.956653778116966613, 0.000000000000000000, 0.000000000000000000 ) ) ;
#55195=CARTESIAN_POINT ( 'NONE',  ( 0.8551540677456834771, 46.51172240253119838, 11.51835730326496510 ) ) ;
#55200=CARTESIAN_POINT ( 'NONE',  ( 0.5807400328401574052, -44.04145271122551009, -18.83234461715229102 ) ) ;
#55201=B_SPLINE_CURVE_WITH_KNOTS ( 'NONE', 3,
 ( #26107, #46165, #45545, #49918, #36456, #50526 ),
 .UNSPECIFIED., .F., .F.,
 ( 4, 2, 4 ),
 ( 1.520334456564901176E-16, 0.0002445252820015209787, 0.0004890505640028898439 ),
 .UNSPECIFIED. ) ;
#55207=CARTESIAN_POINT ( 'NONE',  ( 0.8557997880470599172, -47.60865952217002928, 5.347802024197076065 ) ) ;
#55223=ADVANCED_FACE ( 'NONE', ( #40219 ), #18224, .F. ) ;
#55228=ORIENTED_EDGE ( 'NONE', *, *, #40548, .T. ) ;
#55234=ADVANCED_FACE ( 'NONE', ( #20161 ), #16316, .F. ) ;
#55235=CARTESIAN_POINT ( 'NONE',  ( 5.860006189529246790, 48.12869875779309581, 3.171667470662679733 ) ) ;
#55249=EDGE_LOOP ( 'NONE', ( #3322, #43843, #37619, #46528 ) ) ;
#55260=CARTESIAN_POINT ( 'NONE',  ( 4.956653778116992370, 31.29546495791903027, -36.51451553856384180 ) ) ;
#55263=CARTESIAN_POINT ( 'NONE',  ( 4.303969348037258058, -25.89994482339341531, -40.54345935592806427 ) ) ;
#55265=FACE_OUTER_BOUND ( 'NONE', #46689, .T. ) ;
#55268=CARTESIAN_POINT ( 'NONE',  ( 0.6846871229502899947, 46.04462816497506594, -13.23224427737781284 ) ) ;
#55271=CARTESIAN_POINT ( 'NONE',  ( 0.9757787079277434605, -5.561523338226871616, -42.54650880470570939 ) ) ;
#55273=CARTESIAN_POINT ( 'NONE',  ( 0.5832367798473383491, 37.83194459509911667, 29.37285281143854831 ) ) ;
#55275=EDGE_LOOP ( 'NONE', ( #19286, #9235, #57458, #16076 ) ) ;
#55276=CARTESIAN_POINT ( 'NONE',  ( -16.91961043310876889, -12.36682299961459108, -1.821422909846774907 ) ) ;
#55281=CARTESIAN_POINT ( 'NONE',  ( 0.5807400328401637335, -46.40483864045136642, -11.87003418057291704 ) ) ;
#55286=ADVANCED_FACE ( 'NONE', ( #49259 ), #29115, .F. ) ;
#55295=EDGE_CURVE ( 'NONE', #19678, #53979, #9188, .T. ) ;
#55298=DIRECTION ( 'NONE',  ( -1.000000000000000000, -0.000000000000000000, -0.000000000000000000 ) ) ;
#55301=EDGE_CURVE ( 'NONE', #49888, #45339, #27832, .T. ) ;
#55311=DIRECTION ( 'NONE',  ( -1.000000000000000000, -0.000000000000000000, -0.000000000000000000 ) ) ;
#55315=VERTEX_POINT ( 'NONE', #8196 ) ;
#55319=ORIENTED_EDGE ( 'NONE', *, *, #9987, .F. ) ;
#55323=CIRCLE ( 'NONE', #42403, 43.08621763946400307 ) ;
#55329=( BOUNDED_SURFACE ( )  B_SPLINE_SURFACE ( 3, 1, ( 
 ( #55437, #20470 ),
 ( #45463, #55744 ),
 ( #53959, #2814 ),
 ( #26633, #45768 ) ),
 .UNSPECIFIED., .F., .F., .F. ) 
 B_SPLINE_SURFACE_WITH_KNOTS ( ( 4, 4 ),
 ( 2, 2 ),
 ( 0.000000000000000000, 1.000000000000000000 ),
 ( 0.000000000000000000, 1.000000000000000000 ),
 .UNSPECIFIED. ) 
 GEOMETRIC_REPRESENTATION_ITEM ( )  RATIONAL_B_SPLINE_SURFACE ( (
 ( 1.000000000000000000, 1.000000000000000000),
 ( 0.9953390228620291325, 0.8624445117761032620),
 ( 0.9953390228620291325, 0.8624445117761032620),
 ( 1.000000000000000000, 1.000000000000000000) ) ) 
 REPRESENTATION_ITEM ( '' )  SURFACE ( )  );
#55333=CARTESIAN_POINT ( 'NONE',  ( 2.526552050251863246, -41.18423939305557013, -12.29062829844021110 ) ) ;
#55339=CARTESIAN_POINT ( 'NONE',  ( 3.407937589446174087, 13.10584870154466586, 3.987184287467832711 ) ) ;
#55360=CARTESIAN_POINT ( 'NONE',  ( 0.5807400328401574052, -5.711437504335652449, -47.55718917606849061 ) ) ;
#55361=CARTESIAN_POINT ( 'NONE',  ( 4.967162193818131399, -19.45289607368795259, -38.44485641567092671 ) ) ;
#55365=CARTESIAN_POINT ( 'NONE',  ( 5.958863334805807099, 14.51296551801783075, 14.51469124124484900 ) ) ;
#55368=CARTESIAN_POINT ( 'NONE',  ( 3.270143674763207553, -5.490410281242870560, 12.53844339339232938 ) ) ;
#55369=CARTESIAN_POINT ( 'NONE',  ( 0.8557997880470606944, -33.22501220301877112, -34.51495345639583689 ) ) ;
#55371=CARTESIAN_POINT ( 'NONE',  ( 1.227938101723756947, -34.55893248994489397, -25.45152231597092651 ) ) ;
#55375=CIRCLE ( 'NONE', #6296, 43.08621763946400307 ) ;
#55377=CARTESIAN_POINT ( 'NONE',  ( 5.960721111146673579, 10.25731071096582880, -17.77882586010657207 ) ) ;
#55378=EDGE_CURVE ( 'NONE', #28691, #31261, #15861, .T. ) ;
#55379=B_SPLINE_CURVE_WITH_KNOTS ( 'NONE', 3,
 ( #38544, #10331, #38240, #19737 ),
 .UNSPECIFIED., .F., .F.,
 ( 4, 4 ),
 ( 3.469446951953614189E-18, 0.004050076154993001616 ),
 .UNSPECIFIED. ) ;
#55381=CARTESIAN_POINT ( 'NONE',  ( 1.227938101723756947, -29.74462687941247552, 30.94118573761302926 ) ) ;
#55383=CARTESIAN_POINT ( 'NONE',  ( 0.9757787079277439046, -26.08967489699740838, -34.06559579809994176 ) ) ;
#55387=CARTESIAN_POINT ( 'NONE',  ( 5.960221823109900008, 14.50993159119810905, -14.51763960716763258 ) ) ;
#55391=ORIENTED_EDGE ( 'NONE', *, *, #16014, .F. ) ;
#55399=EDGE_LOOP ( 'NONE', ( #39390, #29586, #1599, #6940 ) ) ;
#55404=ORIENTED_EDGE ( 'NONE', *, *, #57022, .F. ) ;
#55413=VERTEX_POINT ( 'NONE', #36126 ) ;
#55414=CARTESIAN_POINT ( 'NONE',  ( 0.9736507210033074067, 10.66979144439368454, 41.56063510425031637 ) ) ;
#55415=EDGE_CURVE ( 'NONE', #9472, #19529, #60567, .T. ) ;
#55420=ADVANCED_FACE ( 'NONE', ( #31714 ), #45580, .T. ) ;
#55422=CARTESIAN_POINT ( 'NONE',  ( 0.9757787079277437936, 34.06559579810004834, -26.08967489699726983 ) ) ;
#55423=CARTESIAN_POINT ( 'NONE',  ( 3.407937589446174087, 3.987184287467969934, -13.10584870154462500 ) ) ;
#55428=ADVANCED_FACE ( 'NONE', ( #26696 ), #35546, .F. ) ;
#55429=EDGE_CURVE ( 'NONE', #36314, #53833, #27, .T. ) ;
#55434=CARTESIAN_POINT ( 'NONE',  ( 0.5807400328401574052, -33.48217046439135913, 34.25275203086223286 ) ) ;
#55435=CARTESIAN_POINT ( 'NONE',  ( 0.9752570700956780803, -34.18150842933900435, 25.93764562640092564 ) ) ;
#55437=CARTESIAN_POINT ( 'NONE',  ( 5.959547316686252039, 17.77392908783934189, -10.26589671991344588 ) ) ;
#55446=CARTESIAN_POINT ( 'NONE',  ( 0.9740398440564310700, 36.95080095316304636, -21.81228698783102971 ) ) ;
#55450=CARTESIAN_POINT ( 'NONE',  ( 2.281351352603294913, -43.80196780981706439, -19.56575819747271083 ) ) ;
#55453=CARTESIAN_POINT ( 'NONE',  ( 0.5839879882012694035, -29.15724166963622821, -37.99840755997075092 ) ) ;
#55459=CARTESIAN_POINT ( 'NONE',  ( 3.660176727303408484, -48.00143922595155743, -1.881607889988255344 ) ) ;
#55469=ORIENTED_EDGE ( 'NONE', *, *, #13784, .T. ) ;
#55473=ORIENTED_EDGE ( 'NONE', *, *, #45938, .T. ) ;
#55480=CARTESIAN_POINT ( 'NONE',  ( 0.9730545539215883499, 15.95224156741828914, 39.83279466599044838 ) ) ;
#55487=CARTESIAN_POINT ( 'NONE',  ( 0.5809828226811617480, 44.03860873105695362, 18.83114015454715684 ) ) ;
#55489=CARTESIAN_POINT ( 'NONE',  ( 0.9741495583595167762, -42.90659993968957053, -0.3955098476636077498 ) ) ;
#55493=CARTESIAN_POINT ( 'NONE',  ( 4.956653778116893783, -15.97476558431863758, -45.35992544608534160 ) ) ;
#55494=EDGE_LOOP ( 'NONE', ( #53718, #7706 ) ) ;
#55495=CARTESIAN_POINT ( 'NONE',  ( 5.959828726073459926, 2.674641840416173810, -20.35060134307031987 ) ) ;
#55510=DIRECTION ( 'NONE',  ( -1.000000000000000000, -0.000000000000000000, -0.000000000000000000 ) ) ;
#55521=CARTESIAN_POINT ( 'NONE',  ( 0.5850706913938533704, 6.431767090163499567, -47.46255051844946848 ) ) ;
#55526=DIRECTION ( 'NONE',  ( 0.000000000000000000, 0.000000000000000000, 1.000000000000000000 ) ) ;
#55530=CARTESIAN_POINT ( 'NONE',  ( 1.154321713695927842, 6.418927679456245095, -42.43366804783609325 ) ) ;
#55536=ORIENTED_EDGE ( 'NONE', *, *, #21279, .F. ) ;
#55538=EDGE_CURVE ( 'NONE', #22241, #13203, #20095, .T. ) ;
#55539=CARTESIAN_POINT ( 'NONE',  ( 0.5827357941260203900, 47.89462047563813485, -0.3632531319016042981 ) ) ;
#55540=FACE_OUTER_BOUND ( 'NONE', #48709, .T. ) ;
#55541=CARTESIAN_POINT ( 'NONE',  ( 0.9756354156337452288, -41.47994205070121154, 10.97961179198184745 ) ) ;
#55542=B_SPLINE_CURVE_WITH_KNOTS ( 'NONE', 3,
 ( #27566, #31036, #45466, #35758, #21636, #3132, #13177, #26955, #7203, #50144, #26331, #8442, #2512, #11960, #40777, #59843, #46384, #16959, #22873 ),
 .UNSPECIFIED., .F., .F.,
 ( 4, 3, 3, 3, 3, 3, 4 ),
 ( 3.469446951953614189E-18, 0.0002724573126191812307, 0.0004086839781548551992, 0.0005449106435902030619, 0.0006811373090491647936, 0.0008459866663933863964, 0.001010840725717218136 ),
 .UNSPECIFIED. ) ;
#55543=ORIENTED_EDGE ( 'NONE', *, *, #5612, .F. ) ;
#55550=CARTESIAN_POINT ( 'NONE',  ( 5.959547316686252039, 17.77749189599203206, 10.25972575517536178 ) ) ;
#55551=AXIS2_PLACEMENT_3D ( 'NONE', #13741, #61315, #9017 ) ;
#55554=CARTESIAN_POINT ( 'NONE',  ( 1.227938101723748288, 39.96870412324358313, -15.63977281655798812 ) ) ;
#55557=CARTESIAN_POINT ( 'NONE',  ( 0.5836750258453360374, 12.57171936981227489, -46.21662382526641721 ) ) ;
#55562=EDGE_CURVE ( 'NONE', #39239, #36997, #6557, .T. ) ;
#55565=DIRECTION ( 'NONE',  ( -1.000000000000000000, -0.000000000000000000, -0.000000000000000000 ) ) ;
#55568=CARTESIAN_POINT ( 'NONE',  ( 0.9730545539215883499, 30.69604515769650632, 29.98130006528872826 ) ) ;
#55573=CARTESIAN_POINT ( 'NONE',  ( 0.5809828226811617480, -33.48000389720591841, -34.25055090842189287 ) ) ;
#55574=CARTESIAN_POINT ( 'NONE',  ( 0.5800708057587397048, -0.6275304576133720058, 47.89175345272233386 ) ) ;
#55575=B_SPLINE_CURVE_WITH_KNOTS ( 'NONE', 3,
 ( #39325, #35239, #58386, #48703 ),
 .UNSPECIFIED., .F., .F.,
 ( 4, 4 ),
 ( 8.673617379884035472E-19, 0.004050076154993000749 ),
 .UNSPECIFIED. ) ;
#55586=CARTESIAN_POINT ( 'NONE',  ( 2.281351352603294469, -40.87339198768977155, -25.11567449372752137 ) ) ;
#55587=CARTESIAN_POINT ( 'NONE',  ( 0.8557997880470690211, -0.9121262075942833114, -47.89938907511595545 ) ) ;
#55588=EDGE_CURVE ( 'NONE', #43576, #31789, #30085, .T. ) ;
#55591=CARTESIAN_POINT ( 'NONE',  ( 0.5786265663353196143, -47.58023467411541674, 5.535668456753771949 ) ) ;
#55612=EDGE_CURVE ( 'NONE', #8944, #18653, #37620, .T. ) ;
#55624=DIRECTION ( 'NONE',  ( 0.07439287786467665975, -0.5965490341031266519, -0.7991213610169847215 ) ) ;
#55628=CARTESIAN_POINT ( 'NONE',  ( 4.956653778116994147, 39.67974989265076857, -27.17045123668430406 ) ) ;
#55631=ORIENTED_EDGE ( 'NONE', *, *, #56123, .T. ) ;
#55632=CARTESIAN_POINT ( 'NONE',  ( 4.967162193818131399, -23.56777426397203357, 36.06913038482792189 ) ) ;
#55640=ORIENTED_EDGE ( 'NONE', *, *, #55378, .T. ) ;
#55641=CARTESIAN_POINT ( 'NONE',  ( 5.960721111146673579, -0.006321279846963646747, 20.52557019979492026 ) ) ;
#55645=ORIENTED_EDGE ( 'NONE', *, *, #16319, .T. ) ;
#55649=DIRECTION ( 'NONE',  ( 0.07439287786467665975, -0.9597484305373191749, -0.2708295585865100885 ) ) ;
#55665=CARTESIAN_POINT ( 'NONE',  ( 0.9757402383260940226, -30.40085236181972306, 30.28078671294513668 ) ) ;
#55666=CARTESIAN_POINT ( 'NONE',  ( 5.959547316686252039, -18.96456592444095435, -7.851524054666348285 ) ) ;
#55679=LINE ( 'NONE', #36933, #28451 ) ;
#55690=CARTESIAN_POINT ( 'NONE',  ( 0.5809828226811553087, -6.791453954330003207, -47.41188724015886180 ) ) ;
#55694=( BOUNDED_SURFACE ( )  B_SPLINE_SURFACE ( 3, 1, ( 
 ( #53446, #34997 ),
 ( #44107, #15570 ),
 ( #47013, #54058 ),
 ( #56680, #15880 ) ),
 .UNSPECIFIED., .F., .F., .F. ) 
 B_SPLINE_SURFACE_WITH_KNOTS ( ( 4, 4 ),
 ( 2, 2 ),
 ( 0.000000000000000000, 1.000000000000000000 ),
 ( 0.000000000000000000, 1.000000000000000000 ),
 .UNSPECIFIED. ) 
 GEOMETRIC_REPRESENTATION_ITEM ( )  RATIONAL_B_SPLINE_SURFACE ( (
 ( 1.000000000000000000, 1.000000000000000000),
 ( 0.9953390228620291325, 0.8624445117760984880),
 ( 0.9953390228620291325, 0.8624445117760984880),
 ( 1.000000000000000000, 1.000000000000000000) ) ) 
 REPRESENTATION_ITEM ( '' )  SURFACE ( )  );
#55699=ORIENTED_EDGE ( 'NONE', *, *, #43894, .T. ) ;
#55700=CARTESIAN_POINT ( 'NONE',  ( 0.5827357941260198348, -0.3632531319011024773, -47.89462047563813485 ) ) ;
#55701=CARTESIAN_POINT ( 'NONE',  ( 4.967162193818130511, 36.06913038482831979, -23.56777426397140118 ) ) ;
#55702=VERTEX_POINT ( 'NONE', #60426 ) ;
#55705=ORIENTED_EDGE ( 'NONE', *, *, #40202, .F. ) ;
#55721=ORIENTED_EDGE ( 'NONE', *, *, #35391, .T. ) ;
#55738=CARTESIAN_POINT ( 'NONE',  ( 0.5832367798473389042, 47.44985149964050208, 6.521664418777336714 ) ) ;
#55741=CARTESIAN_POINT ( 'NONE',  ( 3.270143674763207553, 12.74832469035452576, 4.983712007628279927 ) ) ;
#55742=EDGE_CURVE ( 'NONE', #22861, #56714, #33505, .T. ) ;
#55744=CARTESIAN_POINT ( 'NONE',  ( 0.5786265663353196143, -41.83999636203335371, 23.32245830379013185 ) ) ;
#55746=CARTESIAN_POINT ( 'NONE',  ( 3.270143674763207553, 13.60381564321234293, 1.514386915940642897 ) ) ;
#55753=CARTESIAN_POINT ( 'NONE',  ( 0.9730545539215883499, 36.90443313492362165, -21.89037132892396897 ) ) ;
#55755=CARTESIAN_POINT ( 'NONE',  ( 0.5809828226811617480, 6.791453954331010401, -47.41188724015871969 ) ) ;
#55760=CARTESIAN_POINT ( 'NONE',  ( 0.5839880159502353063, -29.12121614504435740, -38.02605095487705000 ) ) ;
#55772=FILL_AREA_STYLE_COLOUR ( '', #46697 ) ;
#55775=CARTESIAN_POINT ( 'NONE',  ( 0.9741495583595148888, -41.34222751889821978, -11.48707840139629610 ) ) ;
#55791=EDGE_CURVE ( 'NONE', #57258, #6072, #43496, .T. ) ;
#55794=EDGE_LOOP ( 'NONE', ( #58997, #9428, #23469, #40735 ) ) ;
#55799=CARTESIAN_POINT ( 'NONE',  ( 0.7057020205115025480, 19.10543569325853142, -43.92641219669812358 ) ) ;
#55800=ORIENTED_EDGE ( 'NONE', *, *, #45139, .F. ) ;
#55802=ORIENTED_EDGE ( 'NONE', *, *, #19064, .F. ) ;
#55803=VECTOR ( 'NONE', #53497, 1000.000000000000114 ) ;
#55809=ORIENTED_EDGE ( 'NONE', *, *, #8066, .F. ) ;
#55810=CARTESIAN_POINT ( 'NONE',  ( 1.227938101723756947, -29.74462687941247552, 30.94118573761302926 ) ) ;
#55811=CARTESIAN_POINT ( 'NONE',  ( 4.956653778116991482, 8.845409907521601056, -47.27023054223744225 ) ) ;
#55815=ORIENTED_EDGE ( 'NONE', *, *, #24619, .F. ) ;
#55821=EDGE_CURVE ( 'NONE', #18602, #8650, #6533, .T. ) ;
#55822=CARTESIAN_POINT ( 'NONE',  ( 0.8557997880470599172, -29.88293891557496096, 37.44587306708088192 ) ) ;
#55825=CARTESIAN_POINT ( 'NONE',  ( 4.967162193818130511, 0.000000000000000000, 0.000000000000000000 ) ) ;
#55835=CARTESIAN_POINT ( 'NONE',  ( 0.8551540677456739292, -47.61725548905994287, 5.348818140990737824 ) ) ;
#55837=CARTESIAN_POINT ( 'NONE',  ( 5.959828726073459926, 10.26672511661755927, -17.77343634131831607 ) ) ;
#55844=DIRECTION ( 'NONE',  ( 0.000000000000000000, 0.000000000000000000, 1.000000000000000000 ) ) ;
#55845=CARTESIAN_POINT ( 'NONE',  ( 0.8557997880470697982, -19.17299735371977221, -43.90420959842202109 ) ) ;
#55847=ORIENTED_EDGE ( 'NONE', *, *, #27446, .F. ) ;
#55851=CARTESIAN_POINT ( 'NONE',  ( 0.5839879882012687373, -33.86754218494321123, 33.86758487442388343 ) ) ;
#55852=CARTESIAN_POINT ( 'NONE',  ( 0.9722240750034557566, 5.023189755349555696, -42.61332880321398164 ) ) ;
#55855=VERTEX_POINT ( 'NONE', #30320 ) ;
#55859=CARTESIAN_POINT ( 'NONE',  ( 5.958863334805807099, -18.96276366205788122, -7.855954700275556313 ) ) ;
#55869=CIRCLE ( 'NONE', #12887, 48.09070567114147110 ) ;
#55871=CARTESIAN_POINT ( 'NONE',  ( 0.8551540677456739292, -19.17641535420883869, 43.91216198251533598 ) ) ;
#55875=CARTESIAN_POINT ( 'NONE',  ( 1.154321485836933725, 17.18284940416451079, 39.32643515542041257 ) ) ;
#55884=ORIENTED_EDGE ( 'NONE', *, *, #32868, .T. ) ;
#55888=CARTESIAN_POINT ( 'NONE',  ( 4.967162193818129623, 32.68434214048168940, 28.07411493385305334 ) ) ;
#55895=PRODUCT_DEFINITION_FORMATION_WITH_SPECIFIED_SOURCE ( 'ANY', '', #13314, .NOT_KNOWN. ) ;
#55899=ADVANCED_FACE ( 'NONE', ( #43527 ), #27546, .T. ) ;
#55903=CARTESIAN_POINT ( 'NONE',  ( 0.8557997880470599172, -47.37054680076701629, -7.156447707086194043 ) ) ;
#55904=VERTEX_POINT ( 'NONE', #5264 ) ;
#55907=CARTESIAN_POINT ( 'NONE',  ( 5.960721111146673579, 5.306302591836580262, -19.82781442290492890 ) ) ;
#55910=CARTESIAN_POINT ( 'NONE',  ( 0.9730545539215892381, 26.52009130076819687, -33.73144377768529978 ) ) ;
#55931=ADVANCED_FACE ( 'NONE', ( #56200 ), #18347, .F. ) ;
#55932=VECTOR ( 'NONE', #2928, 1000.000000000000114 ) ;
#55940=CARTESIAN_POINT ( 'NONE',  ( 2.281351352603288696, -34.83869092251583766, 32.98025003937404875 ) ) ;
#55941=EDGE_CURVE ( 'NONE', #30590, #41729, #40077, .T. ) ;
#55943=VERTEX_POINT ( 'NONE', #40684 ) ;
#55945=CARTESIAN_POINT ( 'NONE',  ( 0.8551540677456739292, -47.90804413217340141, -0.9122407826480745108 ) ) ;
#55947=CARTESIAN_POINT ( 'NONE',  ( 4.967162193818130511, -13.42934394584192148, 40.93989340068605998 ) ) ;
#55951=CARTESIAN_POINT ( 'NONE',  ( 0.5809828226811553087, -33.48000389720640868, 34.25055090842140970 ) ) ;
#55952=CARTESIAN_POINT ( 'NONE',  ( 0.5832367798473397924, 41.34221369670682122, 24.18350431151176139 ) ) ;
#55956=ORIENTED_EDGE ( 'NONE', *, *, #57332, .T. ) ;
#55982=CARTESIAN_POINT ( 'NONE',  ( 0.9758171775293917882, 5.594812732687712398, -42.54217005300505861 ) ) ;
#55983=B_SPLINE_CURVE_WITH_KNOTS ( 'NONE', 3,
 ( #32497, #22169, #51271, #60980 ),
 .UNSPECIFIED., .F., .F.,
 ( 4, 4 ),
 ( 8.673617379884035472E-19, 0.004050076154993000749 ),
 .UNSPECIFIED. ) ;
#55984=CARTESIAN_POINT ( 'NONE',  ( 4.303969348037258058, 27.54579249306266675, -39.44373910178582321 ) ) ;
#55987=CARTESIAN_POINT ( 'NONE',  ( 1.088908134280555107, -42.64123480278973943, -4.826714665689302741 ) ) ;
#55988=CARTESIAN_POINT ( 'NONE',  ( 0.9756950546413932779, -39.60512406639357863, 16.50968749804426849 ) ) ;
#55990=B_SPLINE_CURVE_WITH_KNOTS ( 'NONE', 3,
 ( #54588, #24884, #1060, #49596 ),
 .UNSPECIFIED., .F., .F.,
 ( 4, 4 ),
 ( 0.000000000000000000, 0.005004741218457314789 ),
 .UNSPECIFIED. ) ;
#55993=CARTESIAN_POINT ( 'NONE',  ( 5.981074661064941900, -10.26976685693810865, -17.77058762078874565 ) ) ;
#56002=DIRECTION ( 'NONE',  ( 0.07836865515943411409, 0.9179910502197331512, 0.3887811538706230086 ) ) ;
#56020=CARTESIAN_POINT ( 'NONE',  ( 0.5819845079324652559, -28.79567599618788520, 38.27312975753802959 ) ) ;
#56021=EDGE_LOOP ( 'NONE', ( #51949, #55391, #7935, #48463 ) ) ;
#56024=EDGE_CURVE ( 'NONE', #8960, #3302, #26268, .T. ) ;
#56027=ORIENTED_EDGE ( 'NONE', *, *, #48464, .T. ) ;
#56028=CARTESIAN_POINT ( 'NONE',  ( 5.959547316686252039, -20.35048796920738923, 2.675599016784190098 ) ) ;
#56044=FACE_OUTER_BOUND ( 'NONE', #37248, .T. ) ;
#56050=CARTESIAN_POINT ( 'NONE',  ( 0.5838002273316443835, 47.46823345111868520, 6.386683873060672312 ) ) ;
#56065=CARTESIAN_POINT ( 'NONE',  ( 5.960221823109900008, 18.96108896995714943, -7.859839668735016716 ) ) ;
#56074=DIRECTION ( 'NONE',  ( 0.07439287786467664587, 0.5100024374914937653, -0.8569499480574966910 ) ) ;
#56075=B_SPLINE_CURVE_WITH_KNOTS ( 'NONE', 3,
 ( #12008, #50190, #36423, #32022, #3791, #22310, #55184, #41437, #23232, #42059, #13224, #31396, #12617, #46437, #22933, #7566, #55489, #26692, #8191 ),
 .UNSPECIFIED., .F., .F.,
 ( 4, 3, 3, 3, 3, 3, 4 ),
 ( 4.878909776184769953E-18, 0.0002724573126191762976, 0.0004086839781548491277, 0.0005449106435901837631, 0.0006811373090491486390, 0.0008459866663933688323, 0.001010840725717212282 ),
 .UNSPECIFIED. ) ;
#56079=EDGE_LOOP ( 'NONE', ( #10501, #4954, #16596, #4883 ) ) ;
#56082=CARTESIAN_POINT ( 'NONE',  ( 0.6067099128993228563, 46.07641759122984126, -13.08009036336154196 ) ) ;
#56083=CARTESIAN_POINT ( 'NONE',  ( 2.281351352603294913, -47.95523304704243372, -1.314116150903955615 ) ) ;
#56086=DIRECTION ( 'NONE',  ( -0.07836865515943411409, 0.3887811538706132941, 0.9179910502197372590 ) ) ;
#56087=CARTESIAN_POINT ( 'NONE',  ( 4.967162193818130511, 2.375726030843182457, -43.02067033766016380 ) ) ;
#56094=ORIENTED_EDGE ( 'NONE', *, *, #22916, .F. ) ;
#56095=CARTESIAN_POINT ( 'NONE',  ( 5.959547316686252039, 20.52562247508876681, 0.003562808152977453395 ) ) ;
#56096=EDGE_CURVE ( 'NONE', #52648, #17303, #53044, .T. ) ;
#56101=CARTESIAN_POINT ( 'NONE',  ( 0.9752570700956777472, 16.20701641182919417, 39.72995844664864507 ) ) ;
#56102=B_SPLINE_CURVE_WITH_KNOTS ( 'NONE', 3,
 ( #25552, #16171, #15865, #29328, #34983, #30246, #49361, #43781, #6412, #49665, #5502, #39076, #25864, #15250, #16468, #54660, #58129, #26791, #18025, #41224, #46530, #2660, #37143, #55276, #41528, #11786, #30867, #36211, #31812, #40611 ),
 .UNSPECIFIED., .F., .F.,
 ( 4, 2, 2, 2, 2, 2, 2, 2, 2, 2, 2, 2, 2, 2, 4 ),
 ( 0.000000000000000000, 0.0004110759757379565276, 0.0008221519514759130553, 0.001233227927213869637, 0.001644303902951826111, 0.002466455854427739708, 0.003288607805903653956, 0.003699683781641610429, 0.004110759757379567336, 0.004521835733117523376, 0.004932911708855479416, 0.005343987684593436323, 0.005755063660331393230, 0.006166139636069349270, 0.006577215611807306177 ),
 .UNSPECIFIED. ) ;
#56107=CARTESIAN_POINT ( 'NONE',  ( 0.7762777257811910303, 19.15108781300990159, -43.90991299786880830 ) ) ;
#56121=CARTESIAN_POINT ( 'NONE',  ( 4.956653778116975495, 3.690426056929986043, 47.94889704119053420 ) ) ;
#56123=EDGE_CURVE ( 'NONE', #47245, #15844, #11303, .T. ) ;
#56129=CARTESIAN_POINT ( 'NONE',  ( 3.270143674763207553, -11.02405647745164430, -8.113405361969626028 ) ) ;
#56131=CARTESIAN_POINT ( 'NONE',  ( 0.5827359174754819238, -46.35666395585283084, 12.04517879102121292 ) ) ;
#56136=CARTESIAN_POINT ( 'NONE',  ( 1.088908134280559770, 33.56490895818201636, -26.73890361625880630 ) ) ;
#56138=CARTESIAN_POINT ( 'NONE',  ( 4.967162193818130511, 0.000000000000000000, 0.000000000000000000 ) ) ;
#56139=CARTESIAN_POINT ( 'NONE',  ( 4.967162193818130511, 0.000000000000000000, 0.000000000000000000 ) ) ;
#56142=AXIS2_PLACEMENT_3D ( 'NONE', #18029, #60915, #56525 ) ;
#56143=CARTESIAN_POINT ( 'NONE',  ( 0.9758171775293911221, -37.16279804060120995, -21.44911662810690345 ) ) ;
#56147=CARTESIAN_POINT ( 'NONE',  ( 0.9972139404380315764, 11.74016833743920252, 41.27214627875013520 ) ) ;
#56158=CARTESIAN_POINT ( 'NONE',  ( 0.5809828226811553087, -33.48000389720640868, 34.25055090842140970 ) ) ;
#56163=ORIENTED_EDGE ( 'NONE', *, *, #23767, .F. ) ;
#56165=CARTESIAN_POINT ( 'NONE',  ( 0.9745511491811748028, -10.77620558745907786, -41.53317535253985682 ) ) ;
#56168=VERTEX_POINT ( 'NONE', #29859 ) ;
#56170=CARTESIAN_POINT ( 'NONE',  ( 0.8557997880470599172, 44.60232077416710439, -17.48760788519168941 ) ) ;
#56177=ORIENTED_EDGE ( 'NONE', *, *, #1408, .F. ) ;
#56179=CARTESIAN_POINT ( 'NONE',  ( 4.303969348037246512, -20.38638383586150127, 43.57722561725952204 ) ) ;
#56191=EDGE_LOOP ( 'NONE', ( #60231, #55705, #50530, #61724 ) ) ;
#56192=CARTESIAN_POINT ( 'NONE',  ( 5.960221823109900008, 7.849768660536287967, 18.96526051813983571 ) ) ;
#56199=EDGE_CURVE ( 'NONE', #46408, #28202, #23945, .T. ) ;
#56200=FACE_OUTER_BOUND ( 'NONE', #1454, .T. ) ;
#56204=CARTESIAN_POINT ( 'NONE',  ( 0.9756354156337461170, 42.90827993934335893, 0.1303083999668459281 ) ) ;
#56206=CARTESIAN_POINT ( 'NONE',  ( 0.9722240741986377666, -21.95618662952211508, 36.86535088273198113 ) ) ;
#56211=VERTEX_POINT ( 'NONE', #58341 ) ;
#56213=CARTESIAN_POINT ( 'NONE',  ( 0.5807400328401637335, 23.47602859900772998, -41.75144119563861267 ) ) ;
#56219=B_SPLINE_CURVE_WITH_KNOTS ( 'NONE', 3,
 ( #7988, #59987, #27101, #46226, #7661, #56518 ),
 .UNSPECIFIED., .F., .F.,
 ( 4, 2, 4 ),
 ( 1.524244818460479926E-16, 0.0002445252820015232013, 0.0004890505640028939638 ),
 .UNSPECIFIED. ) ;
#56221=DIRECTION ( 'NONE',  ( -1.000000000000000000, -0.000000000000000000, -0.000000000000000000 ) ) ;
#56223=CARTESIAN_POINT ( 'NONE',  ( 0.5836750258453360374, 12.22088356912726681, 46.31062999473589059 ) ) ;
#56225=DIRECTION ( 'NONE',  ( 0.07439287786467665975, 0.8569499480574949146, 0.5100024374914968739 ) ) ;
#56226=ORIENTED_EDGE ( 'NONE', *, *, #18681, .F. ) ;
#56230=CARTESIAN_POINT ( 'NONE',  ( 5.974727161628367256, -14.52429704002354072, -14.50236057684839963 ) ) ;
#56231=ORIENTED_EDGE ( 'NONE', *, *, #45112, .T. ) ;
#56232=CARTESIAN_POINT ( 'NONE',  ( 4.956653778116989706, -40.28700667097662347, -26.26162724282415084 ) ) ;
#56235=AXIS2_PLACEMENT_3D ( 'NONE', #26398, #49904, #41148 ) ;
#56238=CARTESIAN_POINT ( 'NONE',  ( 0.9730545539215883499, 41.31259007387230753, 11.59290486963521971 ) ) ;
#56242=EDGE_CURVE ( 'NONE', #2408, #18299, #41163, .T. ) ;
#56244=( BOUNDED_SURFACE ( )  B_SPLINE_SURFACE ( 3, 1, ( 
 ( #19958, #6111 ),
 ( #24954, #59363 ),
 ( #44091, #20261 ),
 ( #24641, #15554 ) ),
 .UNSPECIFIED., .F., .F., .F. ) 
 B_SPLINE_SURFACE_WITH_KNOTS ( ( 4, 4 ),
 ( 2, 2 ),
 ( 0.000000000000000000, 1.000000000000000000 ),
 ( 0.000000000000000000, 1.000000000000000000 ),
 .UNSPECIFIED. ) 
 GEOMETRIC_REPRESENTATION_ITEM ( )  RATIONAL_B_SPLINE_SURFACE ( (
 ( 1.000000000000000000, 1.000000000000000000),
 ( 0.9953390228620291325, 0.8624445117760984880),
 ( 0.9953390228620291325, 0.8624445117760984880),
 ( 1.000000000000000000, 1.000000000000000000) ) ) 
 REPRESENTATION_ITEM ( '' )  SURFACE ( )  );
#56250=VERTEX_POINT ( 'NONE', #24750 ) ;
#56256=ORIENTED_EDGE ( 'NONE', *, *, #5911, .F. ) ;
#56268=CARTESIAN_POINT ( 'NONE',  ( 0.5838002273316429402, -47.46823345111864256, -6.386683873061000938 ) ) ;
#56291=CARTESIAN_POINT ( 'NONE',  ( 3.407937589446174087, 1.331713209622503058, 13.63405474014708929 ) ) ;
#56296=VECTOR ( 'NONE', #54451, 1000.000000000000114 ) ;
#56302=CARTESIAN_POINT ( 'NONE',  ( 4.303969348037246512, 22.16169334783837996, 42.70173985163825137 ) ) ;
#56309=CARTESIAN_POINT ( 'NONE',  ( 3.270143674763207553, 8.113405361969507013, 11.02405647745173134 ) ) ;
#56311=CARTESIAN_POINT ( 'NONE',  ( -19.79470381413520386, -7.930988484581699360, -1.054774614931486720 ) ) ;
#56312=ORIENTED_EDGE ( 'NONE', *, *, #16413, .F. ) ;
#56314=VECTOR ( 'NONE', #54370, 1000.000000000000114 ) ;
#56316=VERTEX_POINT ( 'NONE', #34163 ) ;
#56321=FACE_OUTER_BOUND ( 'NONE', #30263, .T. ) ;
#56322=B_SPLINE_CURVE_WITH_KNOTS ( 'NONE', 3,
 ( #20177, #10461, #58042, #44308, #39602, #43375 ),
 .UNSPECIFIED., .F., .F.,
 ( 4, 2, 4 ),
 ( 6.946513017424995024E-18, 0.0002291966416970823311, 0.0004583932833941577233 ),
 .UNSPECIFIED. ) ;
#56324=CARTESIAN_POINT ( 'NONE',  ( 5.981074661064941900, 12.48781255314288963, -16.28853686865586425 ) ) ;
#56327=CARTESIAN_POINT ( 'NONE',  ( 0.9754642270333676590, 21.30186789325757246, 37.24735125696664539 ) ) ;
#56331=B_SPLINE_CURVE_WITH_KNOTS ( 'NONE', 3,
 ( #54957, #7336, #22086, #27091 ),
 .UNSPECIFIED., .F., .F.,
 ( 4, 4 ),
 ( 0.000000000000000000, 0.004050076154993000749 ),
 .UNSPECIFIED. ) ;
#56334=CARTESIAN_POINT ( 'NONE',  ( 0.6846871229502899947, -28.47437962186153371, 38.52803883689291098 ) ) ;
#56337=EDGE_LOOP ( 'NONE', ( #46825, #38211 ) ) ;
#56338=CARTESIAN_POINT ( 'NONE',  ( 1.227938101723748288, -42.43379953535180960, -6.439911493065006987 ) ) ;
#56353=EDGE_CURVE ( 'NONE', #28471, #34340, #34383, .T. ) ;
#56355=CARTESIAN_POINT ( 'NONE',  ( 0.5836750258453369256, 47.46217286060751661, 6.431686642654920405 ) ) ;
#56365=( BOUNDED_SURFACE ( )  B_SPLINE_SURFACE ( 3, 1, ( 
 ( #43959, #20131 ),
 ( #39556, #15425 ),
 ( #44882, #49537 ),
 ( #58936, #57678 ) ),
 .UNSPECIFIED., .F., .F., .F. ) 
 B_SPLINE_SURFACE_WITH_KNOTS ( ( 4, 4 ),
 ( 2, 2 ),
 ( 0.000000000000000000, 1.000000000000000000 ),
 ( 0.000000000000000000, 1.000000000000000000 ),
 .UNSPECIFIED. ) 
 GEOMETRIC_REPRESENTATION_ITEM ( )  RATIONAL_B_SPLINE_SURFACE ( (
 ( 1.000000000000000000, 1.000000000000000000),
 ( 0.9953390228620291325, 0.8624445117761032620),
 ( 0.9953390228620291325, 0.8624445117761032620),
 ( 1.000000000000000000, 1.000000000000000000) ) ) 
 REPRESENTATION_ITEM ( '' )  SURFACE ( )  );
#56375=B_SPLINE_CURVE_WITH_KNOTS ( 'NONE', 3,
 ( #50277, #26471, #27097, #45601, #45921, #21467, #21784, #40303, #32114, #55271, #40605, #60586, #2344, #17701, #54963, #46223, #22091, #12395, #31482 ),
 .UNSPECIFIED., .F., .F.,
 ( 4, 3, 3, 3, 3, 3, 4 ),
 ( 5.204170427930421283E-18, 0.0002724573126191779239, 0.0004086839781548503745, 0.0005449106435901876662, 0.0006811373090491533010, 0.0008459866663933717596, 0.001010840725717214016 ),
 .UNSPECIFIED. ) ;
#56376=CARTESIAN_POINT ( 'NONE',  ( 4.963659409799330291, 43.98510776953407486, 8.262218268420630451 ) ) ;
#56403=CARTESIAN_POINT ( 'NONE',  ( 0.5839879882074159312, 2.012401425053789955E-05, 47.89596766821753704 ) ) ;
#56406=B_SPLINE_CURVE_WITH_KNOTS ( 'NONE', 3,
 ( #31337, #35440, #50440, #54497 ),
 .UNSPECIFIED., .F., .F.,
 ( 4, 4 ),
 ( 1.430489624538199204E-17, 0.005004741218457437087 ),
 .UNSPECIFIED. ) ;
#56409=CARTESIAN_POINT ( 'NONE',  ( 0.9741495583595165542, -16.05424148287297470, -39.79188455996737872 ) ) ;
#56418=FACE_OUTER_BOUND ( 'NONE', #57677, .T. ) ;
#56419=VERTEX_POINT ( 'NONE', #2434 ) ;
#56425=CARTESIAN_POINT ( 'NONE',  ( 2.624215991343608501, -32.93378783738824467, -34.92983774303001354 ) ) ;
#56428=ORIENTED_EDGE ( 'NONE', *, *, #36892, .T. ) ;
#56446=CARTESIAN_POINT ( 'NONE',  ( 1.227938101723756947, -41.66816631169184859, -10.28900963485423858 ) ) ;
#56448=CARTESIAN_POINT ( 'NONE',  ( 5.960721111146673579, -14.50930005615006912, -14.51823969584094698 ) ) ;
#56451=CARTESIAN_POINT ( 'NONE',  ( 0.9730545539215883499, 11.59290486963506517, 41.31259007387235727 ) ) ;
#56455=ORIENTED_EDGE ( 'NONE', *, *, #26602, .T. ) ;
#56458=CARTESIAN_POINT ( 'NONE',  ( 0.8557997880470606944, -34.51495345639572321, 33.22501220301889191 ) ) ;
#56459=ORIENTED_EDGE ( 'NONE', *, *, #46970, .F. ) ;
#56460=ORIENTED_EDGE ( 'NONE', *, *, #8769, .F. ) ;
#56471=ORIENTED_EDGE ( 'NONE', *, *, #20731, .T. ) ;
#56472=CARTESIAN_POINT ( 'NONE',  ( 0.5832367798473397924, -12.13303976268028350, -46.33367954572893410 ) ) ;
#56496=ORIENTED_EDGE ( 'NONE', *, *, #19120, .F. ) ;
#56501=ADVANCED_FACE ( 'NONE', ( #17793 ), #35174, .F. ) ;
#56504=ORIENTED_EDGE ( 'NONE', *, *, #25437, .F. ) ;
#56512=CARTESIAN_POINT ( 'NONE',  ( 4.956653778116975495, 8.845409907520915382, 47.27023054223757015 ) ) ;
#56513=CARTESIAN_POINT ( 'NONE',  ( 4.956653778116961284, 40.28700667097682953, 26.26162724282386662 ) ) ;
#56517=( BOUNDED_SURFACE ( )  B_SPLINE_SURFACE ( 3, 1, ( 
 ( #1216, #48238 ),
 ( #47618, #4981 ),
 ( #10025, #20351 ),
 ( #53222, #19131 ) ),
 .UNSPECIFIED., .F., .F., .F. ) 
 B_SPLINE_SURFACE_WITH_KNOTS ( ( 4, 4 ),
 ( 2, 2 ),
 ( 0.000000000000000000, 1.000000000000000000 ),
 ( 0.000000000000000000, 1.000000000000000000 ),
 .UNSPECIFIED. ) 
 GEOMETRIC_REPRESENTATION_ITEM ( )  RATIONAL_B_SPLINE_SURFACE ( (
 ( 1.000000000000000000, 1.000000000000000000),
 ( 0.9732289882329797637, 0.9999525324661233672),
 ( 0.9732289882329797637, 0.9999525324661233672),
 ( 1.000000000000000000, 1.000000000000000000) ) ) 
 REPRESENTATION_ITEM ( '' )  SURFACE ( )  );
#56518=CARTESIAN_POINT ( 'NONE',  ( 0.5809828226811626362, -18.83114015454730961, 44.03860873105688967 ) ) ;
#56525=DIRECTION ( 'NONE',  ( 0.000000000000000000, 0.000000000000000000, 1.000000000000000000 ) ) ;
#56527=CARTESIAN_POINT ( 'NONE',  ( 4.956653778116966613, 5.889412876890086925E-15, 48.09070567114147110 ) ) ;
#56528=CARTESIAN_POINT ( 'NONE',  ( 0.5838002273316434954, 12.26477999444068345, 46.29900743592982337 ) ) ;
#56539=ORIENTED_EDGE ( 'NONE', *, *, #46286, .T. ) ;
#56541=CARTESIAN_POINT ( 'NONE',  ( 4.956653778116488773, 2.599733001513538255, 48.02038484091099235 ) ) ;
#56558=EDGE_CURVE ( 'NONE', #18521, #18160, #49341, .T. ) ;
#56561=DIRECTION ( 'NONE',  ( -1.000000000000000000, -0.000000000000000000, -0.000000000000000000 ) ) ;
#56571=CARTESIAN_POINT ( 'NONE',  ( 0.5819845901640493535, 41.25023214430201079, 24.34012668949501901 ) ) ;
#56575=CARTESIAN_POINT ( 'NONE',  ( 5.860006189529234355, 31.78942168514615219, -36.27483683749403554 ) ) ;
#56584=CARTESIAN_POINT ( 'NONE',  ( 2.526464513654345989, -42.96196573359002002, 1.212545078562630607 ) ) ;
#56586=CARTESIAN_POINT ( 'NONE',  ( 0.5839880159502339740, -18.28706857028339527, -44.26747004398436758 ) ) ;
#56593=CARTESIAN_POINT ( 'NONE',  ( 2.281448460670571166, -46.66132715497955274, -11.14236343022421316 ) ) ;
#56597=FACE_OUTER_BOUND ( 'NONE', #40079, .T. ) ;
#56599=CARTESIAN_POINT ( 'NONE',  ( 0.9730545539215883499, 5.099196237955498923, -42.60426903087348194 ) ) ;
#56600=ADVANCED_FACE ( 'NONE', ( #44096 ), #14642, .T. ) ;
#56605=CARTESIAN_POINT ( 'NONE',  ( 0.9730545539215883499, -41.57420493492393376, 10.61654491617549034 ) ) ;
#56606=EDGE_CURVE ( 'NONE', #52461, #40793, #25256, .T. ) ;
#56613=CARTESIAN_POINT ( 'NONE',  ( 4.967162193818130511, 42.16965968614205451, -8.839793687084773310 ) ) ;
#56614=CARTESIAN_POINT ( 'NONE',  ( 0.5807400328401637335, 47.89582301953903709, -0.5448834511091659172 ) ) ;
#56618=( BOUNDED_SURFACE ( )  B_SPLINE_SURFACE ( 3, 1, ( 
 ( #61135, #18257 ),
 ( #32664, #51743 ),
 ( #38002, #57056 ),
 ( #53283, #24797 ) ),
 .UNSPECIFIED., .F., .F., .F. ) 
 B_SPLINE_SURFACE_WITH_KNOTS ( ( 4, 4 ),
 ( 2, 2 ),
 ( 0.000000000000000000, 1.000000000000000000 ),
 ( 0.000000000000000000, 1.000000000000000000 ),
 .UNSPECIFIED. ) 
 GEOMETRIC_REPRESENTATION_ITEM ( )  RATIONAL_B_SPLINE_SURFACE ( (
 ( 1.000000000000000000, 1.000000000000000000),
 ( 0.9953390228620291325, 0.8624445117760984880),
 ( 0.9953390228620291325, 0.8624445117760984880),
 ( 1.000000000000000000, 1.000000000000000000) ) ) 
 REPRESENTATION_ITEM ( '' )  SURFACE ( )  );
#56622=CARTESIAN_POINT ( 'NONE',  ( -19.96581960764538266, -7.972194200162546096, -0.6786982475873951648 ) ) ;
#56623=ORIENTED_EDGE ( 'NONE', *, *, #14244, .F. ) ;
#56624=EDGE_CURVE ( 'NONE', #46800, #23080, #20181, .T. ) ;
#56627=CARTESIAN_POINT ( 'NONE',  ( 3.660176727303406707, -42.51126973288297251, 22.37119938028475374 ) ) ;
#56632=EDGE_CURVE ( 'NONE', #42473, #22519, #508, .T. ) ;
#56635=AXIS2_PLACEMENT_3D ( 'NONE', #51472, #7635, #2630 ) ;
#56640=CARTESIAN_POINT ( 'NONE',  ( 0.5839254288179542840, -29.22920395911540581, 37.94310411505137637 ) ) ;
#56641=CARTESIAN_POINT ( 'NONE',  ( 0.9736507210033072957, 21.06291100879439071, 37.38294557109041705 ) ) ;
#56651=CARTESIAN_POINT ( 'NONE',  ( 3.660087539127316880, 46.85281175970452949, 10.60624038924609991 ) ) ;
#56652=CARTESIAN_POINT ( 'NONE',  ( 0.9754642270333693244, 33.93430397636412721, 26.26019354539047157 ) ) ;
#56653=ORIENTED_EDGE ( 'NONE', *, *, #33958, .T. ) ;
#56659=SURFACE_SIDE_STYLE ('',( #27860 ) ) ;
#56661=CARTESIAN_POINT ( 'NONE',  ( 5.981074661064941900, -5.303881226583815334, 19.82752479807518142 ) ) ;
#56662=CARTESIAN_POINT ( 'NONE',  ( 4.960156602257180580, -35.23783291257192474, 30.22163187094376724 ) ) ;
#56674=DIRECTION ( 'NONE',  ( -0.07836865515943411409, 0.8672783706145159588, 0.4916162952473524528 ) ) ;
#56675=FACE_OUTER_BOUND ( 'NONE', #7884, .T. ) ;
#56680=CARTESIAN_POINT ( 'NONE',  ( 5.959547316686252039, 16.28624005235099403, -12.49238070347959351 ) ) ;
#56685=CARTESIAN_POINT ( 'NONE',  ( 0.6067099128993235224, 47.89177823194874861, -0.7089426894592245620 ) ) ;
#56686=CARTESIAN_POINT ( 'NONE',  ( 0.5850706913938534814, -41.56998471741211176, -23.79070617305425372 ) ) ;
#56689=ORIENTED_EDGE ( 'NONE', *, *, #15235, .F. ) ;
#56698=ORIENTED_EDGE ( 'NONE', *, *, #48733, .F. ) ;
#56700=VERTEX_POINT ( 'NONE', #12721 ) ;
#56712=CARTESIAN_POINT ( 'NONE',  ( 4.303969348037246512, 45.22910199346996762, -16.39840148505043516 ) ) ;
#56714=VERTEX_POINT ( 'NONE', #45935 ) ;
#56722=ORIENTED_EDGE ( 'NONE', *, *, #53938, .F. ) ;
#56723=CARTESIAN_POINT ( 'NONE',  ( 0.5819845079324660331, -34.18710788661927324, -33.54497088780116343 ) ) ;
#56724=ADVANCED_FACE ( 'NONE', ( #26177 ), #17599, .F. ) ;
#56726=VERTEX_POINT ( 'NONE', #55910 ) ;
#56727=CARTESIAN_POINT ( 'NONE',  ( 0.7762783648524403946, 47.60264408896660626, 5.369627767359989257 ) ) ;
#56732=EDGE_LOOP ( 'NONE', ( #13897, #36283, #42800, #55319 ) ) ;
#56739=FACE_OUTER_BOUND ( 'NONE', #29364, .T. ) ;
#56740=CARTESIAN_POINT ( 'NONE',  ( 0.8551540677456715978, 29.88829867897814196, 37.45266983663506721 ) ) ;
#56742=CARTESIAN_POINT ( 'NONE',  ( 5.960721111146673579, -10.25731071096595137, 17.77882586010649391 ) ) ;
#56746=CONICAL_SURFACE ( 'NONE', #8731, 43.08621763946400307, 1.568696531533066763 ) ;
#56750=CARTESIAN_POINT ( 'NONE',  ( 0.9756950546413938330, 30.27237962848480635, -30.40918718457309566 ) ) ;
#56755=CARTESIAN_POINT ( 'NONE',  ( 0.9740398440564319582, -37.36539512268005581, -21.09418882170575671 ) ) ;
#56759=CARTESIAN_POINT ( 'NONE',  ( 0.9754402186311958989, 39.71365199966012938, 16.24692483025432566 ) ) ;
#56760=ORIENTED_EDGE ( 'NONE', *, *, #57794, .F. ) ;
#56761=VECTOR ( 'NONE', #36054, 1000.000000000000114 ) ;
#56763=CARTESIAN_POINT ( 'NONE',  ( 0.5827359174754815907, 23.63273677570916220, 41.65957726278045925 ) ) ;
#56764=FACE_OUTER_BOUND ( 'NONE', #8422, .T. ) ;
#56765=ORIENTED_EDGE ( 'NONE', *, *, #14084, .T. ) ;
#56767=CARTESIAN_POINT ( 'NONE',  ( 1.088908134280555551, 4.826714665689470607, -42.64123480278970391 ) ) ;
#56768=ORIENTED_EDGE ( 'NONE', *, *, #33526, .T. ) ;
#56769=ORIENTED_EDGE ( 'NONE', *, *, #57977, .T. ) ;
#56771=ADVANCED_FACE ( 'NONE', ( #8599 ), #13963, .F. ) ;
#56774=CARTESIAN_POINT ( 'NONE',  ( 0.9757787079277455700, -41.45659305953926577, 11.06737752163081545 ) ) ;
#56777=EDGE_LOOP ( 'NONE', ( #15807, #54837, #56809, #39898 ) ) ;
#56787=CARTESIAN_POINT ( 'NONE',  ( 0.9754642270333683252, -33.93430397636394957, -26.26019354539071671 ) ) ;
#56790=ORIENTED_EDGE ( 'NONE', *, *, #40664, .F. ) ;
#56791=DIRECTION ( 'NONE',  ( 0.000000000000000000, 0.000000000000000000, 1.000000000000000000 ) ) ;
#56795=CARTESIAN_POINT ( 'NONE',  ( 0.9749527285493316819, -0.2856147164661618776, 42.90750796893246388 ) ) ;
#56802=( BOUNDED_SURFACE ( )  B_SPLINE_SURFACE ( 3, 1, ( 
 ( #45544, #54274 ),
 ( #44935, #11715 ),
 ( #59925, #35217 ),
 ( #12337, #21409 ) ),
 .UNSPECIFIED., .F., .F., .F. ) 
 B_SPLINE_SURFACE_WITH_KNOTS ( ( 4, 4 ),
 ( 2, 2 ),
 ( 0.000000000000000000, 1.000000000000000000 ),
 ( 0.000000000000000000, 1.000000000000000000 ),
 .UNSPECIFIED. ) 
 GEOMETRIC_REPRESENTATION_ITEM ( )  RATIONAL_B_SPLINE_SURFACE ( (
 ( 1.000000000000000000, 1.000000000000000000),
 ( 0.7269869731126817891, 0.9931720237060910339),
 ( 0.7269869731126817891, 0.9931720237060910339),
 ( 1.000000000000000000, 1.000000000000000000) ) ) 
 REPRESENTATION_ITEM ( '' )  SURFACE ( )  );
#56809=ORIENTED_EDGE ( 'NONE', *, *, #61480, .T. ) ;
#56811=DIRECTION ( 'NONE',  ( -1.000000000000000000, -0.000000000000000000, -0.000000000000000000 ) ) ;
#56812=CARTESIAN_POINT ( 'NONE',  ( 4.956653778116970166, 45.35992544608529187, 15.97476558431900884 ) ) ;
#56816=CARTESIAN_POINT ( 'NONE',  ( 0.9756354156337457839, -42.55820231551293631, 5.471460801653261541 ) ) ;
#56817=B_SPLINE_CURVE_WITH_KNOTS ( 'NONE', 3,
 ( #34462, #40408, #58225, #49466, #15354, #53532, #30354, #49777, #1523, #58537, #54143, #6838, #10649, #48851, #5905, #25049, #45111, #21276, #20664 ),
 .UNSPECIFIED., .F., .F.,
 ( 4, 3, 3, 3, 3, 3, 4 ),
 ( 6.938893903907228378E-18, 0.0002724573126191734244, 0.0004086839781548483146, 0.0005449106435901873409, 0.0006811373090491491811, 0.0008459866663933664471, 0.001010840725717215534 ),
 .UNSPECIFIED. ) ;
#56820=DIRECTION ( 'NONE',  ( 0.000000000000000000, 0.000000000000000000, -1.000000000000000000 ) ) ;
#56825=AXIS2_PLACEMENT_3D ( 'NONE', #18013, #26466, #22699 ) ;
#56830=DIRECTION ( 'NONE',  ( 0.07836865515943410021, 0.2656332009267382555, -0.9608836331491532601 ) ) ;
#56831=CARTESIAN_POINT ( 'NONE',  ( 4.963659409799330291, -33.33129552235108406, 29.86601237216398275 ) ) ;
#56834=CARTESIAN_POINT ( 'NONE',  ( 0.5819845079324660331, 12.83441846783130558, 46.14435090135479811 ) ) ;
#56837=CARTESIAN_POINT ( 'NONE',  ( 5.965394784446458765, 0.01447339372424741311, 20.52536205633085231 ) ) ;
#56839=VERTEX_POINT ( 'NONE', #42466 ) ;
#56843=CARTESIAN_POINT ( 'NONE',  ( 5.974727161628369032, -5.327229920347563485, 19.82156119440436370 ) ) ;
#56845=CARTESIAN_POINT ( 'NONE',  ( 1.227938101723756947, -42.91134962331487657, 0.8460948827223682134 ) ) ;
#56846=CARTESIAN_POINT ( 'NONE',  ( 4.956653778116973719, 21.75875759808707244, 42.88673967249138741 ) ) ;
#56850=CARTESIAN_POINT ( 'NONE',  ( 0.9756950546413922787, 41.47131842451904760, 11.01205619898733978 ) ) ;
#56852=AXIS2_PLACEMENT_3D ( 'NONE', #35377, #15031, #39780 ) ;
#56853=CARTESIAN_POINT ( 'NONE',  ( 5.960221823109900008, 7.859839668734944773, 18.96108896995718496 ) ) ;
#56856=EDGE_CURVE ( 'NONE', #33892, #33914, #19404, .T. ) ;
#56857=CARTESIAN_POINT ( 'NONE',  ( 4.967162193818130511, 0.000000000000000000, 0.000000000000000000 ) ) ;
#56859=EDGE_CURVE ( 'NONE', #21542, #8227, #44055, .T. ) ;
#56860=CARTESIAN_POINT ( 'NONE',  ( 0.9754642270333694354, 42.51806607596984833, 5.774842730422176551 ) ) ;
#56868=FACE_OUTER_BOUND ( 'NONE', #38993, .T. ) ;
#56871=B_SPLINE_CURVE_WITH_KNOTS ( 'NONE', 3,
 ( #40407, #26274, #6211, #16579 ),
 .UNSPECIFIED., .F., .F.,
 ( 4, 4 ),
 ( 0.000000000000000000, 0.004446090762761362516 ),
 .UNSPECIFIED. ) ;
#56875=DIRECTION ( 'NONE',  ( 0.07439287786467665975, 0.1432402660415289519, -0.9868880006907386759 ) ) ;
#56878=FACE_OUTER_BOUND ( 'NONE', #42182, .T. ) ;
#56888=CARTESIAN_POINT ( 'NONE',  ( 0.5836750258453361484, -18.16108240858311618, -44.31929073742209368 ) ) ;
#56900=EDGE_CURVE ( 'NONE', #3984, #56700, #43263, .T. ) ;
#56902=CARTESIAN_POINT ( 'NONE',  ( 0.9736507210033059634, -30.65767007549935030, 30.02062799605188914 ) ) ;
#56904=CARTESIAN_POINT ( 'NONE',  ( 4.956653778116992370, 26.26162724282429650, -40.28700667097652399 ) ) ;
#56905=CARTESIAN_POINT ( 'NONE',  ( 0.9756008150404611445, 5.459718823766134044, -42.55970871350800167 ) ) ;
#56909=CARTESIAN_POINT ( 'NONE',  ( 0.5832366564991506852, -47.89515933308367579, 0.2724446024275744560 ) ) ;
#56918=VERTEX_POINT ( 'NONE', #1348 ) ;
#56926=CARTESIAN_POINT ( 'NONE',  ( 0.9745511491811735816, 11.43411988112660715, -41.35688774886278196 ) ) ;
#56928=B_SPLINE_CURVE_WITH_KNOTS ( 'NONE', 3,
 ( #37683, #24481, #43616, #37366 ),
 .UNSPECIFIED., .F., .F.,
 ( 4, 4 ),
 ( 0.000000000000000000, 0.004446090762761352976 ),
 .UNSPECIFIED. ) ;
#56933=CARTESIAN_POINT ( 'NONE',  ( 4.963659409799328515, 24.46566636552824292, 37.47512675766701307 ) ) ;
#56934=CARTESIAN_POINT ( 'NONE',  ( 1.227938101723756947, -30.94118573761292623, -29.74462687941258210 ) ) ;
#56937=ORIENTED_EDGE ( 'NONE', *, *, #26880, .T. ) ;
#56940=ORIENTED_EDGE ( 'NONE', *, *, #56096, .T. ) ;
#56946=DIRECTION ( 'NONE',  ( 0.000000000000000000, 0.000000000000000000, 1.000000000000000000 ) ) ;
#56954=ORIENTED_EDGE ( 'NONE', *, *, #4848, .F. ) ;
#56956=CARTESIAN_POINT ( 'NONE',  ( 0.9968887458511642707, -42.45154664631704833, -6.251925120321881302 ) ) ;
#56966=ORIENTED_EDGE ( 'NONE', *, *, #10526, .F. ) ;
#56974=B_SPLINE_CURVE_WITH_KNOTS ( 'NONE', 3,
 ( #29831, #16672, #11997, #48629, #53929, #25133 ),
 .UNSPECIFIED., .F., .F.,
 ( 4, 2, 4 ),
 ( 1.138360651264128102E-17, 0.0002291978881530170003, 0.0004583957763060226166 ),
 .UNSPECIFIED. ) ;
#56984=CARTESIAN_POINT ( 'NONE',  ( 0.8551540677456834771, 0.9122407826475761317, 47.90804413217340851 ) ) ;
#56994=CARTESIAN_POINT ( 'NONE',  ( 3.660087539127330647, -1.881558488211391378, -48.00143792263126841 ) ) ;
#56999=CARTESIAN_POINT ( 'NONE',  ( 0.9730545539215883499, -39.83279466599027785, -15.95224156741871546 ) ) ;
#57006=( LENGTH_UNIT ( ) NAMED_UNIT ( * ) SI_UNIT ( .MILLI., .METRE. ) );
#57016=CARTESIAN_POINT ( 'NONE',  ( 0.5819845079324663661, -6.701571823032408837, -47.42480735454292784 ) ) ;
#57018=EDGE_LOOP ( 'NONE', ( #60425, #26058, #25427, #60494 ) ) ;
#57020=ORIENTED_EDGE ( 'NONE', *, *, #37459, .F. ) ;
#57022=EDGE_CURVE ( 'NONE', #59557, #51084, #5157, .T. ) ;
#57023=DIRECTION ( 'NONE',  ( 0.07439287786467665975, 0.01320009283086933695, -0.9971416435352942198 ) ) ;
#57028=CARTESIAN_POINT ( 'NONE',  ( 2.624215991343608501, -7.662883702704991862, 47.39206852872455045 ) ) ;
#57034=ORIENTED_EDGE ( 'NONE', *, *, #21862, .T. ) ;
#57047=EDGE_CURVE ( 'NONE', #6564, #2091, #19599, .T. ) ;
#57055=CARTESIAN_POINT ( 'NONE',  ( 5.960721111146673579, -0.006321279846680040275, -20.52557019979492026 ) ) ;
#57056=CARTESIAN_POINT ( 'NONE',  ( 0.5786265663353153954, -46.07681357296495150, 13.09387673186319212 ) ) ;
#57058=CARTESIAN_POINT ( 'NONE',  ( 0.9730545539215883499, -34.34678117142574649, 25.71816799638765971 ) ) ;
#57059=CARTESIAN_POINT ( 'NONE',  ( 0.9756950546413930558, 37.20808764646341160, 21.37039651692511555 ) ) ;
#57060=CARTESIAN_POINT ( 'NONE',  ( 0.5809828226811617480, -47.55412398569210808, 5.711058609465143654 ) ) ;
#57061=CARTESIAN_POINT ( 'NONE',  ( 0.9757787079277436826, -37.14005577278808801, -21.48842038179473590 ) ) ;
#57067=CARTESIAN_POINT ( 'NONE',  ( 5.958863334805807099, 19.82657410201435511, 5.311251202228921109 ) ) ;
#57074=CARTESIAN_POINT ( 'NONE',  ( 0.9758171775293916772, -11.11125068417964279, -41.44488232057079102 ) ) ;
#57076=CARTESIAN_POINT ( 'NONE',  ( 5.958863334805807099, 7.855954700275350255, 18.96276366205797004 ) ) ;
#57079=VERTEX_POINT ( 'NONE', #18260 ) ;
#57088=( BOUNDED_SURFACE ( )  B_SPLINE_SURFACE ( 3, 1, ( 
 ( #59172, #16279 ),
 ( #35403, #11590 ),
 ( #25987, #2148 ),
 ( #56324, #46965 ) ),
 .UNSPECIFIED., .F., .F., .F. ) 
 B_SPLINE_SURFACE_WITH_KNOTS ( ( 4, 4 ),
 ( 2, 2 ),
 ( 0.000000000000000000, 1.000000000000000000 ),
 ( 0.000000000000000000, 1.000000000000000000 ),
 .UNSPECIFIED. ) 
 GEOMETRIC_REPRESENTATION_ITEM ( )  RATIONAL_B_SPLINE_SURFACE ( (
 ( 1.000000000000000000, 1.000000000000000000),
 ( 0.7269869731126821222, 0.9931720237060910339),
 ( 0.7269869731126821222, 0.9931720237060910339),
 ( 1.000000000000000000, 1.000000000000000000) ) ) 
 REPRESENTATION_ITEM ( '' )  SURFACE ( )  );
#57091=DIRECTION ( 'NONE',  ( -1.000000000000000000, 0.000000000000000000, 0.000000000000000000 ) ) ;
#57094=CARTESIAN_POINT ( 'NONE',  ( 0.9730545539215883499, 0.5054011016618756846, -42.90536227157002003 ) ) ;
#57095=ORIENTED_EDGE ( 'NONE', *, *, #33173, .F. ) ;
#57096=CARTESIAN_POINT ( 'NONE',  ( 3.660087539127321321, 35.27260502801134834, 32.61167949558399215 ) ) ;
#57098=CARTESIAN_POINT ( 'NONE',  ( 0.9756354156337452288, -0.1303083999669958082, 42.90827993934337314 ) ) ;
#57102=DIRECTION ( 'NONE',  ( -1.000000000000000000, -0.000000000000000000, -0.000000000000000000 ) ) ;
#57111=CARTESIAN_POINT ( 'NONE',  ( 5.959828726073459926, 18.96492317065683153, 7.850628836606922789 ) ) ;
#57113=CARTESIAN_POINT ( 'NONE',  ( 0.8557997880470690211, 43.90420959842208504, -19.17299735371961944 ) ) ;
#57116=CARTESIAN_POINT ( 'NONE',  ( 0.9757402383260945777, -42.55239275983112890, 5.516496958496923675 ) ) ;
#57120=CARTESIAN_POINT ( 'NONE',  ( 5.960721111146673579, 20.35079619394242201, 2.672857320903374578 ) ) ;
#57123=CARTESIAN_POINT ( 'NONE',  ( 3.783278058412225864, -1.726763838445890320, -43.00370293663100085 ) ) ;
#57124=ORIENTED_EDGE ( 'NONE', *, *, #31765, .T. ) ;
#57125=EDGE_CURVE ( 'NONE', #61394, #9477, #1380, .T. ) ;
#57130=B_SPLINE_CURVE_WITH_KNOTS ( 'NONE', 3,
 ( #22252, #12868, #37286, #36668 ),
 .UNSPECIFIED., .F., .F.,
 ( 4, 4 ),
 ( 0.000000000000000000, 0.005004741218457393719 ),
 .UNSPECIFIED. ) ;
#57145=CARTESIAN_POINT ( 'NONE',  ( 0.5800708119828328346, 37.61306658477512599, -29.65250521075907386 ) ) ;
#57148=ORIENTED_EDGE ( 'NONE', *, *, #33173, .T. ) ;
#57150=CARTESIAN_POINT ( 'NONE',  ( 4.956653778116987041, -47.27023054223747067, -8.845409907521421644 ) ) ;
#57151=CARTESIAN_POINT ( 'NONE',  ( 0.8551540677456715978, -17.49081417858753795, -44.61036085020969466 ) ) ;
#57161=ORIENTED_EDGE ( 'NONE', *, *, #50872, .T. ) ;
#57166=B_SPLINE_CURVE_WITH_KNOTS ( 'NONE', 3,
 ( #11482, #54674, #35918, #45019 ),
 .UNSPECIFIED., .F., .F.,
 ( 4, 4 ),
 ( 0.000000000000000000, 0.004446090762761373792 ),
 .UNSPECIFIED. ) ;
#57170=CARTESIAN_POINT ( 'NONE',  ( 0.9730545539215883499, -42.60426903087349615, -5.099196237955331057 ) ) ;
#57180=CARTESIAN_POINT ( 'NONE',  ( 0.5834872094924179464, -0.2270145249676526200, 47.89542889285419136 ) ) ;
#57197=CARTESIAN_POINT ( 'NONE',  ( 0.5800708119828331677, 18.90714262039473681, 44.00606550371067982 ) ) ;
#57198=CARTESIAN_POINT ( 'NONE',  ( 4.967162193818131399, 35.57684288741977241, 24.30453456948122692 ) ) ;
#57202=CARTESIAN_POINT ( 'NONE',  ( 0.5809828226811617480, -47.89273459658653564, -0.5448590168537535972 ) ) ;
#57209=ORIENTED_EDGE ( 'NONE', *, *, #61189, .F. ) ;
#57211=CARTESIAN_POINT ( 'NONE',  ( 0.8551540677456739292, 7.157691013575036010, -47.37911285756612756 ) ) ;
#57214=FACE_OUTER_BOUND ( 'NONE', #23675, .T. ) ;
#57218=CARTESIAN_POINT ( 'NONE',  ( 1.227938101723748288, -29.74462687941204209, -30.94118573761343782 ) ) ;
#57226=ORIENTED_EDGE ( 'NONE', *, *, #26281, .T. ) ;
#57227=( BOUNDED_SURFACE ( )  B_SPLINE_SURFACE ( 3, 1, ( 
 ( #32301, #61389 ),
 ( #52305, #37952 ),
 ( #33235, #9397 ),
 ( #47630, #4674 ) ),
 .UNSPECIFIED., .F., .F., .F. ) 
 B_SPLINE_SURFACE_WITH_KNOTS ( ( 4, 4 ),
 ( 2, 2 ),
 ( 0.000000000000000000, 1.000000000000000000 ),
 ( 0.000000000000000000, 1.000000000000000000 ),
 .UNSPECIFIED. ) 
 GEOMETRIC_REPRESENTATION_ITEM ( )  RATIONAL_B_SPLINE_SURFACE ( (
 ( 1.000000000000000000, 1.000000000000000000),
 ( 0.7269869731126817891, 0.9931720237060910339),
 ( 0.7269869731126817891, 0.9931720237060910339),
 ( 1.000000000000000000, 1.000000000000000000) ) ) 
 REPRESENTATION_ITEM ( '' )  SURFACE ( )  );
#57230=VERTEX_POINT ( 'NONE', #38610 ) ;
#57237=VERTEX_POINT ( 'NONE', #52671 ) ;
#57243=B_SPLINE_CURVE_WITH_KNOTS ( 'NONE', 3,
 ( #23895, #63, #42108, #9169, #9791, #61766, #61461, #18904, #57074, #32378, #5064, #51453, #46802, #8545, #19513, #56165, #37394, #27668, #8868 ),
 .UNSPECIFIED., .F., .F.,
 ( 4, 3, 3, 3, 3, 3, 4 ),
 ( 1.734723475976807094E-18, 0.0002724573126191768939, 0.0004086839781548526514, 0.0005449106435901883167, 0.0006811373090491506990, 0.0008459866663933706754, 0.001010840725717216185 ),
 .UNSPECIFIED. ) ;
#57244=ORIENTED_EDGE ( 'NONE', *, *, #50228, .T. ) ;
#57245=ADVANCED_FACE ( 'NONE', ( #45702 ), #37559, .F. ) ;
#57249=CARTESIAN_POINT ( 'NONE',  ( 0.9747592971366234593, 34.23774590565637510, 25.86343094887193317 ) ) ;
#57252=CARTESIAN_POINT ( 'NONE',  ( 0.9757954354143122400, -4.033171854401937560E-17, -42.90846090505964128 ) ) ;
#57256=B_SPLINE_CURVE_WITH_KNOTS ( 'NONE', 3,
 ( #40362, #27161, #12777, #8343 ),
 .UNSPECIFIED., .F., .F.,
 ( 4, 4 ),
 ( 0.000000000000000000, 0.004446090762761355578 ),
 .UNSPECIFIED. ) ;
#57258=VERTEX_POINT ( 'NONE', #50374 ) ;
#57263=EDGE_LOOP ( 'NONE', ( #38418, #53170, #15150, #50967 ) ) ;
#57265=ORIENTED_EDGE ( 'NONE', *, *, #1037, .F. ) ;
#57271=CARTESIAN_POINT ( 'NONE',  ( 0.9757892942422835558, -21.40977514834409945, 37.18547544211205746 ) ) ;
#57272=DIRECTION ( 'NONE',  ( 0.000000000000000000, 0.000000000000000000, 1.000000000000000000 ) ) ;
#57273=EDGE_CURVE ( 'NONE', #57258, #33914, #49489, .T. ) ;
#57276=ORIENTED_EDGE ( 'NONE', *, *, #54625, .T. ) ;
#57290=CARTESIAN_POINT ( 'NONE',  ( 0.5839254288179550612, 18.41284501069738155, -44.21529885210810562 ) ) ;
#57300=ORIENTED_EDGE ( 'NONE', *, *, #19977, .F. ) ;
#57304=ORIENTED_EDGE ( 'NONE', *, *, #37727, .F. ) ;
#57309=CARTESIAN_POINT ( 'NONE',  ( 5.959547316686252039, -0.003562808152765511386, -20.52562247508876681 ) ) ;
#57315=EDGE_CURVE ( 'NONE', #6564, #27525, #38835, .T. ) ;
#57318=DIRECTION ( 'NONE',  ( -1.000000000000000000, -0.000000000000000000, -0.000000000000000000 ) ) ;
#57323=CARTESIAN_POINT ( 'NONE',  ( 0.5827357941260210561, 44.38787053017151152, 17.99287562175603483 ) ) ;
#57327=VECTOR ( 'NONE', #43151, 1000.000000000000227 ) ;
#57328=CARTESIAN_POINT ( 'NONE',  ( 5.965394784446458765, -16.27505370423089559, 12.50653125158980039 ) ) ;
#57329=( BOUNDED_SURFACE ( )  B_SPLINE_SURFACE ( 3, 1, ( 
 ( #2039, #1419 ),
 ( #6721, #53431 ),
 ( #58738, #20864 ),
 ( #11164, #21168 ) ),
 .UNSPECIFIED., .F., .F., .F. ) 
 B_SPLINE_SURFACE_WITH_KNOTS ( ( 4, 4 ),
 ( 2, 2 ),
 ( 0.000000000000000000, 1.000000000000000000 ),
 ( 0.000000000000000000, 1.000000000000000000 ),
 .UNSPECIFIED. ) 
 GEOMETRIC_REPRESENTATION_ITEM ( )  RATIONAL_B_SPLINE_SURFACE ( (
 ( 1.000000000000000000, 1.000000000000000000),
 ( 0.7269869731126821222, 0.9931720237060910339),
 ( 0.7269869731126821222, 0.9931720237060910339),
 ( 1.000000000000000000, 1.000000000000000000) ) ) 
 REPRESENTATION_ITEM ( '' )  SURFACE ( )  );
#57331=CARTESIAN_POINT ( 'NONE',  ( 0.9730545539215883499, 25.71816799638778406, 34.34678117142565412 ) ) ;
#57332=EDGE_CURVE ( 'NONE', #23013, #9930, #30581, .T. ) ;
#57336=CARTESIAN_POINT ( 'NONE',  ( 4.967162193818130511, -24.30453456948135482, 35.57684288741969425 ) ) ;
#57346=CARTESIAN_POINT ( 'NONE',  ( 0.5837374860065643878, -44.18034382476633937, 18.49670552082939068 ) ) ;
#57358=CARTESIAN_POINT ( 'NONE',  ( 0.5834872094924170582, -23.75111410077682095, -41.59216540884688840 ) ) ;
#57364=CARTESIAN_POINT ( 'NONE',  ( 0.5827359174754833671, 29.44457394064674105, -37.77623182210365371 ) ) ;
#57366=ORIENTED_EDGE ( 'NONE', *, *, #12724, .T. ) ;
#57367=CARTESIAN_POINT ( 'NONE',  ( 0.9730545539215883499, 6.101350888304637010, 42.47233286818619291 ) ) ;
#57373=ORIENTED_EDGE ( 'NONE', *, *, #5911, .T. ) ;
#57375=ORIENTED_EDGE ( 'NONE', *, *, #42398, .F. ) ;
#57376=ORIENTED_EDGE ( 'NONE', *, *, #52756, .F. ) ;
#57377=CARTESIAN_POINT ( 'NONE',  ( 0.5819845901640492425, -11.95725023767325190, -46.37938751183695985 ) ) ;
#57384=ADVANCED_FACE ( 'NONE', ( #28736 ), #39570, .F. ) ;
#57393=CARTESIAN_POINT ( 'NONE',  ( 1.088908134280553996, -41.24246781061824407, 11.85879120571491896 ) ) ;
#57394=CARTESIAN_POINT ( 'NONE',  ( 5.959547316686252039, 16.28190225198601127, 12.49803383497755682 ) ) ;
#57400=LINE ( 'NONE', #28923, #37768 ) ;
#57405=DIRECTION ( 'NONE',  ( -1.000000000000000000, -0.000000000000000000, -0.000000000000000000 ) ) ;
#57408=ORIENTED_EDGE ( 'NONE', *, *, #53091, .F. ) ;
#57410=DIRECTION ( 'NONE',  ( 0.000000000000000000, 0.000000000000000000, 1.000000000000000000 ) ) ;
#57412=CARTESIAN_POINT ( 'NONE',  ( 0.9730545539215883499, -16.88610103448528221, -39.44597740938079511 ) ) ;
#57419=DIRECTION ( 'NONE',  ( -0.07836865515943411409, -0.7104869166656990753, -0.6993330359244940286 ) ) ;
#57421=AXIS2_PLACEMENT_3D ( 'NONE', #6698, #7325, #53701 ) ;
#57435=CARTESIAN_POINT ( 'NONE',  ( 0.9752132459055864455, -10.88033124649650141, 41.50604997043410549 ) ) ;
#57438=ORIENTED_EDGE ( 'NONE', *, *, #8066, .T. ) ;
#57439=ORIENTED_EDGE ( 'NONE', *, *, #18681, .T. ) ;
#57444=CARTESIAN_POINT ( 'NONE',  ( 0.8557997880470697982, 37.44587306708137930, -29.88293891557432858 ) ) ;
#57448=ORIENTED_EDGE ( 'NONE', *, *, #27900, .T. ) ;
#57454=EDGE_CURVE ( 'NONE', #15923, #52379, #25333, .T. ) ;
#57455=CONICAL_SURFACE ( 'NONE', #19498, 43.08621763946400307, 1.568696531533066763 ) ;
#57456=CARTESIAN_POINT ( 'NONE',  ( 0.9756950546413926117, 42.55388731055347762, 5.504753251347860754 ) ) ;
#57457=EDGE_CURVE ( 'NONE', #2852, #15622, #45534, .T. ) ;
#57458=ORIENTED_EDGE ( 'NONE', *, *, #32217, .F. ) ;
#57463=ORIENTED_EDGE ( 'NONE', *, *, #15207, .T. ) ;
#57464=CARTESIAN_POINT ( 'NONE',  ( 1.154321485836933947, -37.57248783354756938, -20.73950273457881366 ) ) ;
#57470=ORIENTED_EDGE ( 'NONE', *, *, #3741, .F. ) ;
#57471=CARTESIAN_POINT ( 'NONE',  ( 0.9747592971366217940, 0.3237797888854979655, 42.90728926179870939 ) ) ;
#57477=ORIENTED_EDGE ( 'NONE', *, *, #46076, .T. ) ;
#57481=ORIENTED_EDGE ( 'NONE', *, *, #45938, .F. ) ;
#57485=CARTESIAN_POINT ( 'NONE',  ( 0.9730545539215883499, -39.83279466599050522, 15.95224156741815236 ) ) ;
#57492=CARTESIAN_POINT ( 'NONE',  ( 2.281351352603298022, 47.71649595778620778, -4.956540261593279872 ) ) ;
#57497=VERTEX_POINT ( 'NONE', #34076 ) ;
#57498=B_SPLINE_CURVE_WITH_KNOTS ( 'NONE', 3,
 ( #16086, #30780, #1332, #20467, #39598, #20779 ),
 .UNSPECIFIED., .F., .F.,
 ( 4, 2, 4 ),
 ( 1.015220885719448636E-17, 0.0002291978881530150217, 0.0004583957763060198518 ),
 .UNSPECIFIED. ) ;
#57505=CARTESIAN_POINT ( 'NONE',  ( 0.5800708119828335008, -28.65679933661821721, 38.37709857409259229 ) ) ;
#57511=DIRECTION ( 'NONE',  ( -1.000000000000000000, -0.000000000000000000, -0.000000000000000000 ) ) ;
#57512=AXIS2_PLACEMENT_3D ( 'NONE', #46809, #52390, #9484 ) ;
#57513=CARTESIAN_POINT ( 'NONE',  ( 4.967162193818130511, 0.000000000000000000, 0.000000000000000000 ) ) ;
#57520=AXIS2_PLACEMENT_3D ( 'NONE', #14004, #33108, #19012 ) ;
#57522=CARTESIAN_POINT ( 'NONE',  ( 0.9736507210033065185, 42.59776535855984037, -5.153758453069121614 ) ) ;
#57524=CIRCLE ( 'NONE', #30522, 12.50000000000000000 ) ;
#57526=VERTEX_POINT ( 'NONE', #42245 ) ;
#57529=CARTESIAN_POINT ( 'NONE',  ( -18.11307558806116802, -7.719455939378113030, 2.099999999999994760 ) ) ;
#57546=CARTESIAN_POINT ( 'NONE',  ( 4.956653778116982600, -47.27023054223759857, 8.845409907520762616 ) ) ;
#57553=ORIENTED_EDGE ( 'NONE', *, *, #32659, .T. ) ;
#57559=CARTESIAN_POINT ( 'NONE',  ( 0.9736507210033064075, 0.4504567742786991236, -42.90603603725247694 ) ) ;
#57561=EDGE_CURVE ( 'NONE', #35873, #9554, #48762, .T. ) ;
#57567=( NAMED_UNIT ( * ) PLANE_ANGLE_UNIT ( ) SI_UNIT ( $, .RADIAN. ) );
#57571=ORIENTED_EDGE ( 'NONE', *, *, #1626, .T. ) ;
#57576=B_SPLINE_CURVE_WITH_KNOTS ( 'NONE', 3,
 ( #56458, #60851, #52069, #42697, #17967, #51443 ),
 .UNSPECIFIED., .F., .F.,
 ( 4, 2, 4 ),
 ( 1.550814302699561017E-16, 0.0002445252820015144735, 0.0004890505640028737977 ),
 .UNSPECIFIED. ) ;
#57581=CARTESIAN_POINT ( 'NONE',  ( 0.8557997880470599172, -23.15977007032294210, -41.93815086860281127 ) ) ;
#57588=CARTESIAN_POINT ( 'NONE',  ( 5.959547316686252039, 20.52562247508876681, -0.003562808152693842153 ) ) ;
#57589=ADVANCED_FACE ( 'NONE', ( #58753 ), #30384, .F. ) ;
#57590=B_SPLINE_CURVE_WITH_KNOTS ( 'NONE', 3,
 ( #28428, #47557, #51929, #8708, #37875, #1076 ),
 .UNSPECIFIED., .F., .F.,
 ( 4, 2, 4 ),
 ( 0.000000000000000000, 0.0002291966416970791056, 0.0004583932833941582112 ),
 .UNSPECIFIED. ) ;
#57601=CARTESIAN_POINT ( 'NONE',  ( 4.956653778116975495, -2.599733001514665798, 48.02038484091099235 ) ) ;
#57604=CARTESIAN_POINT ( 'NONE',  ( 4.963659409799330291, 9.199077662858906379, 43.79875484948450293 ) ) ;
#57610=CIRCLE ( 'NONE', #39647, 43.08621763946400307 ) ;
#57615=ADVANCED_FACE ( 'NONE', ( #6428 ), #28382, .F. ) ;
#57627=B_SPLINE_CURVE_WITH_KNOTS ( 'NONE', 3,
 ( #24257, #53364, #19577, #38693 ),
 .UNSPECIFIED., .F., .F.,
 ( 4, 4 ),
 ( 1.192622389734054877E-18, 0.004444878191957691259 ),
 .UNSPECIFIED. ) ;
#57629=ORIENTED_EDGE ( 'NONE', *, *, #1334, .T. ) ;
#57631=EDGE_CURVE ( 'NONE', #33472, #2188, #27419, .T. ) ;
#57632=CARTESIAN_POINT ( 'NONE',  ( 1.088908134280555773, -10.35121946298442097, 41.64642044161487888 ) ) ;
#57634=CARTESIAN_POINT ( 'NONE',  ( 0.8557997880470697982, 47.60865952216998664, 5.347802024197403803 ) ) ;
#57655=EDGE_CURVE ( 'NONE', #58260, #19313, #51488, .T. ) ;
#57656=CARTESIAN_POINT ( 'NONE',  ( 0.7762777257811881437, 38.54028505510758151, -28.45155622761391356 ) ) ;
#57657=CARTESIAN_POINT ( 'NONE',  ( 4.956653778116966613, 0.000000000000000000, 0.000000000000000000 ) ) ;
#57660=CARTESIAN_POINT ( 'NONE',  ( 4.967162193818130511, -40.93989340068600313, -13.42934394584206359 ) ) ;
#57662=CARTESIAN_POINT ( 'NONE',  ( 0.7762783648524379521, 44.59086139387540015, 17.50713302551343986 ) ) ;
#57666=CARTESIAN_POINT ( 'NONE',  ( 1.227938101723756947, -4.762198645644731165, 42.65467462194916948 ) ) ;
#57668=EDGE_CURVE ( 'NONE', #8537, #18131, #3595, .T. ) ;
#57673=VERTEX_POINT ( 'NONE', #27119 ) ;
#57677=EDGE_LOOP ( 'NONE', ( #1252, #28698, #34001, #43551 ) ) ;
#57678=CARTESIAN_POINT ( 'NONE',  ( 0.8551540677456715978, -38.56334384152451378, 28.44084013485104023 ) ) ;
#57684=B_SPLINE_CURVE_WITH_KNOTS ( 'NONE', 3,
 ( #35135, #21025, #30402, #974 ),
 .UNSPECIFIED., .F., .F.,
 ( 4, 4 ),
 ( 0.000000000000000000, 0.005004741218457420607 ),
 .UNSPECIFIED. ) ;
#57685=VECTOR ( 'NONE', #45153, 1000.000000000000114 ) ;
#57692=B_SPLINE_CURVE_WITH_KNOTS ( 'NONE', 3,
 ( #49145, #6198, #44482, #24175, #57358, #14490, #58837, #348, #19495, #38612, #27195, #12496, #50989, #45703, #26890, #45398 ),
 .UNSPECIFIED., .F., .F.,
 ( 4, 3, 3, 3, 3, 4 ),
 ( 1.551621725782133898E-17, 0.0002724568934985618896, 0.0004086836638483852969, 0.0005449104342063618503, 0.0008173270854453600597, 0.001089761613562687491 ),
 .UNSPECIFIED. ) ;
#57694=EDGE_LOOP ( 'NONE', ( #55146, #27047, #30694, #16038 ) ) ;
#57695=CARTESIAN_POINT ( 'NONE',  ( 4.963659409799328515, 43.79875484948446740, 9.199077662859053817 ) ) ;
#57697=( BOUNDED_SURFACE ( )  B_SPLINE_SURFACE ( 3, 1, ( 
 ( #16039, #45482 ),
 ( #2535, #50165 ),
 ( #35150, #30419 ),
 ( #40180, #59547 ) ),
 .UNSPECIFIED., .F., .F., .F. ) 
 B_SPLINE_SURFACE_WITH_KNOTS ( ( 4, 4 ),
 ( 2, 2 ),
 ( 0.000000000000000000, 1.000000000000000000 ),
 ( 0.000000000000000000, 1.000000000000000000 ),
 .UNSPECIFIED. ) 
 GEOMETRIC_REPRESENTATION_ITEM ( )  RATIONAL_B_SPLINE_SURFACE ( (
 ( 1.000000000000000000, 1.000000000000000000),
 ( 0.7269869731126821222, 0.9931720237060910339),
 ( 0.7269869731126821222, 0.9931720237060910339),
 ( 1.000000000000000000, 1.000000000000000000) ) ) 
 REPRESENTATION_ITEM ( '' )  SURFACE ( )  );
#57698=CARTESIAN_POINT ( 'NONE',  ( 100.0000507999999968, 9.797174393178825657E-16, -8.000000000000000000 ) ) ;
#57704=CARTESIAN_POINT ( 'NONE',  ( 0.9730545539215883499, -30.69604515769671949, 29.98130006528850444 ) ) ;
#57705=CARTESIAN_POINT ( 'NONE',  ( 0.9757787079277449038, -0.03949005143931162004, 42.90844198810271592 ) ) ;
#57706=CARTESIAN_POINT ( 'NONE',  ( 0.8557997880470690211, 5.347802024197924275, -47.60865952216993691 ) ) ;
#57708=ORIENTED_EDGE ( 'NONE', *, *, #9476, .T. ) ;
#57711=ADVANCED_FACE ( 'NONE', ( #36228 ), #36829, .F. ) ;
#57720=CIRCLE ( 'NONE', #54867, 48.09070567114147110 ) ;
#57724=CARTESIAN_POINT ( 'NONE',  ( 0.8557997880470599172, 13.27832040216703469, -46.03118133706011861 ) ) ;
#57731=CARTESIAN_POINT ( 'NONE',  ( -48.95476116535499500, 0.000000000000000000, -12.50000000000000000 ) ) ;
#57737=B_SPLINE_CURVE_WITH_KNOTS ( 'NONE', 3,
 ( #30439, #6606, #1935, #21060 ),
 .UNSPECIFIED., .F., .F.,
 ( 4, 4 ),
 ( 4.336808689942017736E-19, 0.004048833967417083887 ),
 .UNSPECIFIED. ) ;
#57739=CARTESIAN_POINT ( 'NONE',  ( 0.9972139404380291339, -42.45145681504344282, 6.252633471303223445 ) ) ;
#57742=CARTESIAN_POINT ( 'NONE',  ( 5.959547316686252039, -12.49803383497762255, 16.28190225198596863 ) ) ;
#57748=CARTESIAN_POINT ( 'NONE',  ( 0.9754402186311947887, -25.97197377940579699, 34.15542855230926733 ) ) ;
#57753=FACE_OUTER_BOUND ( 'NONE', #51311, .T. ) ;
#57761=VERTEX_POINT ( 'NONE', #33687 ) ;
#57764=CARTESIAN_POINT ( 'NONE',  ( 0.8551540677456739292, -17.49081417858754506, -44.61036085020969466 ) ) ;
#57766=ORIENTED_EDGE ( 'NONE', *, *, #7137, .T. ) ;
#57772=CARTESIAN_POINT ( 'NONE',  ( 1.088313998177379283, -39.34193117255244942, -17.14007796983277387 ) ) ;
#57776=CARTESIAN_POINT ( 'NONE',  ( 0.5827359174754813687, 38.21848266111710757, -28.86822142608413344 ) ) ;
#57794=EDGE_CURVE ( 'NONE', #53765, #23158, #36484, .T. ) ;
#57797=CARTESIAN_POINT ( 'NONE',  ( 4.967162193818129623, 32.68434214048168940, 28.07411493385305334 ) ) ;
#57801=CONICAL_SURFACE ( 'NONE', #30801, 43.08621763946400307, 1.568696531533066763 ) ;
#57821=CARTESIAN_POINT ( 'NONE',  ( 0.8551540677456834771, -13.28067116677169679, -46.03951182599441694 ) ) ;
#57824=CARTESIAN_POINT ( 'NONE',  ( 0.9722240750034597534, 41.29187379046135931, -11.66659272802813163 ) ) ;
#57835=ORIENTED_EDGE ( 'NONE', *, *, #17944, .F. ) ;
#57836=CARTESIAN_POINT ( 'NONE',  ( 0.5839879882012697365, -12.39635945868993794, 46.26395995854833387 ) ) ;
#57838=CARTESIAN_POINT ( 'NONE',  ( 5.965394784446460541, -10.27521535480999049, 17.76824826579336758 ) ) ;
#57841=DIRECTION ( 'NONE',  ( -0.07439287786467652097, -0.9868880006907401192, 0.1432402660415187101 ) ) ;
#57843=CARTESIAN_POINT ( 'NONE',  ( 0.5809828226811617480, -11.86925843957133786, -46.40184912890851621 ) ) ;
#57854=CARTESIAN_POINT ( 'NONE',  ( 0.9730545539215883499, -21.01499094264575618, 37.40983423658466478 ) ) ;
#57856=CARTESIAN_POINT ( 'NONE',  ( 0.6067375320500711933, -44.51755737952363745, 17.67235760802248024 ) ) ;
#57860=EDGE_LOOP ( 'NONE', ( #54234, #56094, #55815, #41648 ) ) ;
#57864=CARTESIAN_POINT ( 'NONE',  ( 0.5837374860065640547, -37.88763545422897039, 29.30115996485980645 ) ) ;
#57865=ORIENTED_EDGE ( 'NONE', *, *, #33216, .T. ) ;
#57880=CARTESIAN_POINT ( 'NONE',  ( -48.95476116535499500, 0.000000000000000000, 0.000000000000000000 ) ) ;
#57883=( BOUNDED_SURFACE ( )  B_SPLINE_SURFACE ( 3, 1, ( 
 ( #40688, #46299 ),
 ( #3344, #45381 ),
 ( #13093, #22473 ),
 ( #2425, #51274 ) ),
 .UNSPECIFIED., .F., .F., .F. ) 
 B_SPLINE_SURFACE_WITH_KNOTS ( ( 4, 4 ),
 ( 2, 2 ),
 ( 0.000000000000000000, 1.000000000000000000 ),
 ( 0.000000000000000000, 1.000000000000000000 ),
 .UNSPECIFIED. ) 
 GEOMETRIC_REPRESENTATION_ITEM ( )  RATIONAL_B_SPLINE_SURFACE ( (
 ( 1.000000000000000000, 1.000000000000000000),
 ( 0.7269869731126817891, 0.9931720237060910339),
 ( 0.7269869731126817891, 0.9931720237060910339),
 ( 1.000000000000000000, 1.000000000000000000) ) ) 
 REPRESENTATION_ITEM ( '' )  SURFACE ( )  );
#57884=VERTEX_POINT ( 'NONE', #10483 ) ;
#57887=CARTESIAN_POINT ( 'NONE',  ( 0.8557997880470606944, -46.50333260518566902, 11.51622788066442027 ) ) ;
#57888=DIRECTION ( 'NONE',  ( 0.000000000000000000, 0.000000000000000000, 1.000000000000000000 ) ) ;
#57898=CARTESIAN_POINT ( 'NONE',  ( 5.960721111146673579, 18.96073515164548340, -7.860635756377695849 ) ) ;
#57909=CARTESIAN_POINT ( 'NONE',  ( 5.958863334805807099, 20.35021240744030990, 2.677925489610707643 ) ) ;
#57911=VERTEX_POINT ( 'NONE', #21727 ) ;
#57915=CARTESIAN_POINT ( 'NONE',  ( 0.5809828226811617480, 47.41188724015879785, 6.791453954330491705 ) ) ;
#57920=CARTESIAN_POINT ( 'NONE',  ( 0.5809828226811544205, 17.82437196699742188, -44.45562576850583270 ) ) ;
#57923=ORIENTED_EDGE ( 'NONE', *, *, #39006, .T. ) ;
#57925=CARTESIAN_POINT ( 'NONE',  ( 0.6846871229502899947, 7.109010606687386158, 47.37786444808395458 ) ) ;
#57926=ORIENTED_EDGE ( 'NONE', *, *, #47788, .F. ) ;
#57927=CARTESIAN_POINT ( 'NONE',  ( 3.660087539127338641, 36.93668088065486188, -30.71416465583017441 ) ) ;
#57929=B_SPLINE_CURVE_WITH_KNOTS ( 'NONE', 3,
 ( #48865, #10662, #30062, #9722 ),
 .UNSPECIFIED., .F., .F.,
 ( 4, 4 ),
 ( 0.000000000000000000, 0.004050076154992999881 ),
 .UNSPECIFIED. ) ;
#57930=ORIENTED_EDGE ( 'NONE', *, *, #8388, .T. ) ;
#57931=CARTESIAN_POINT ( 'NONE',  ( 2.281448460670570277, -47.95523685111403722, 1.314143534315736828 ) ) ;
#57936=CARTESIAN_POINT ( 'NONE',  ( 0.8557997880470697982, -41.93815086860240626, -23.15977007032367041 ) ) ;
#57938=CARTESIAN_POINT ( 'NONE',  ( 0.5809828226811553087, 41.74875432577648837, 23.47450554821725532 ) ) ;
#57941=CARTESIAN_POINT ( 'NONE',  ( 0.8557997880470697982, -7.156447707085392018, -47.37054680076713709 ) ) ;
#57943=ORIENTED_EDGE ( 'NONE', *, *, #29550, .F. ) ;
#57946=CARTESIAN_POINT ( 'NONE',  ( 5.959828726073459926, -7.850628836606722949, -18.96492317065690969 ) ) ;
#57948=VERTEX_POINT ( 'NONE', #26114 ) ;
#57951=ORIENTED_EDGE ( 'NONE', *, *, #3382, .T. ) ;
#57953=EDGE_CURVE ( 'NONE', #36851, #53765, #37540, .T. ) ;
#57957=CARTESIAN_POINT ( 'NONE',  ( 5.959828726073459926, 0.004526594003377396556, -20.52560994243598813 ) ) ;
#57964=VECTOR ( 'NONE', #39889, 1000.000000000000000 ) ;
#57968=CARTESIAN_POINT ( 'NONE',  ( 1.088313998177382613, 33.56520876252064767, 26.73848503423867484 ) ) ;
#57969=LINE ( 'NONE', #39223, #5877 ) ;
#57972=EDGE_CURVE ( 'NONE', #4945, #32075, #27478, .T. ) ;
#57977=EDGE_CURVE ( 'NONE', #27219, #35226, #41515, .T. ) ;
#57983=EDGE_CURVE ( 'NONE', #35431, #52648, #25262, .T. ) ;
#57992=CARTESIAN_POINT ( 'NONE',  ( 5.959547316686252039, -20.35048796920738923, 2.675599016784190098 ) ) ;
#57995=ORIENTED_EDGE ( 'NONE', *, *, #47538, .T. ) ;
#58003=EDGE_LOOP ( 'NONE', ( #11446, #17930, #23297, #44505 ) ) ;
#58005=CARTESIAN_POINT ( 'NONE',  ( 0.9968887458511640487, 39.38692798189865130, 17.02616470386893610 ) ) ;
#58010=VECTOR ( 'NONE', #17738, 999.9999999999998863 ) ;
#58011=CARTESIAN_POINT ( 'NONE',  ( 0.9749527285493317930, -33.86694354778337157, -26.34702925571532361 ) ) ;
#58012=VERTEX_POINT ( 'NONE', #18896 ) ;
#58015=CONICAL_SURFACE ( 'NONE', #38093, 43.08621763946400307, 1.568696531533066763 ) ;
#58016=DIRECTION ( 'NONE',  ( -0.07836865515943411409, 0.9873352307081191270, -0.1379401902675465030 ) ) ;
#58025=B_SPLINE_CURVE_WITH_KNOTS ( 'NONE', 3,
 ( #21663, #46111, #3158, #16983, #59236, #21047 ),
 .UNSPECIFIED., .F., .F.,
 ( 4, 2, 4 ),
 ( 1.502890766741732611E-16, 0.0002445252820015207077, 0.0004890505640028911449 ),
 .UNSPECIFIED. ) ;
#58036=CARTESIAN_POINT ( 'NONE',  ( 4.303969348037258058, -39.44373910178591558, -27.54579249306250688 ) ) ;
#58037=CARTESIAN_POINT ( 'NONE',  ( 0.7762777257811899201, -13.25585385760139623, 46.03397617421224197 ) ) ;
#58042=CARTESIAN_POINT ( 'NONE',  ( 0.9968887458511660471, 37.48500720268757647, -20.88287852258405053 ) ) ;
#58044=EDGE_CURVE ( 'NONE', #30729, #59093, #27967, .T. ) ;
#58047=CARTESIAN_POINT ( 'NONE',  ( 2.526464513654345989, -1.212545078562481393, -42.96196573359005555 ) ) ;
#58050=EDGE_CURVE ( 'NONE', #50538, #14433, #53589, .T. ) ;
#58051=CARTESIAN_POINT ( 'NONE',  ( 0.5800708057587414812, -28.65679888493032124, -38.37709891224491798 ) ) ;
#58052=CARTESIAN_POINT ( 'NONE',  ( 2.281448460670572498, 22.83953674062072636, -42.18752512472219252 ) ) ;
#58057=CARTESIAN_POINT ( 'NONE',  ( 0.5839254288179541730, -41.52446060675843853, 23.86932519546715881 ) ) ;
#58066=CARTESIAN_POINT ( 'NONE',  ( 1.227938101723748288, 10.28900963485380693, 41.66816631169195517 ) ) ;
#58074=CARTESIAN_POINT ( 'NONE',  ( 4.956653778116959508, -15.97476558431919180, 45.35992544608522792 ) ) ;
#58076=CARTESIAN_POINT ( 'NONE',  ( 0.5809828226811560858, -41.74875432577632495, -23.47450554821754309 ) ) ;
#58077=( BOUNDED_SURFACE ( )  B_SPLINE_SURFACE ( 3, 1, ( 
 ( #35742, #2804 ),
 ( #45149, #60132 ),
 ( #35430, #30699 ),
 ( #50128, #40151 ) ),
 .UNSPECIFIED., .F., .F., .F. ) 
 B_SPLINE_SURFACE_WITH_KNOTS ( ( 4, 4 ),
 ( 2, 2 ),
 ( 0.000000000000000000, 1.000000000000000000 ),
 ( 0.000000000000000000, 1.000000000000000000 ),
 .UNSPECIFIED. ) 
 GEOMETRIC_REPRESENTATION_ITEM ( )  RATIONAL_B_SPLINE_SURFACE ( (
 ( 1.000000000000000000, 1.000000000000000000),
 ( 0.7269869731126821222, 0.9931720237060910339),
 ( 0.7269869731126821222, 0.9931720237060910339),
 ( 1.000000000000000000, 1.000000000000000000) ) ) 
 REPRESENTATION_ITEM ( '' )  SURFACE ( )  );
#58078=ORIENTED_EDGE ( 'NONE', *, *, #60535, .F. ) ;
#58082=CARTESIAN_POINT ( 'NONE',  ( 1.154321713695929397, -39.32643513900316634, -17.18284946700669380 ) ) ;
#58087=CARTESIAN_POINT ( 'NONE',  ( 0.9757892942422810023, 42.54806590760161100, 5.549787678908529642 ) ) ;
#58088=ORIENTED_EDGE ( 'NONE', *, *, #50107, .T. ) ;
#58089=VERTEX_POINT ( 'NONE', #3832 ) ;
#58095=CARTESIAN_POINT ( 'NONE',  ( 4.956653778116989706, -40.28700667097662347, -26.26162724282415084 ) ) ;
#58097=EDGE_CURVE ( 'NONE', #60198, #49001, #61153, .T. ) ;
#58100=CARTESIAN_POINT ( 'NONE',  ( 0.9756950546413921677, -42.55388731055342788, -5.504753251348157406 ) ) ;
#58105=ORIENTED_EDGE ( 'NONE', *, *, #19085, .T. ) ;
#58107=EDGE_CURVE ( 'NONE', #31261, #20429, #35146, .T. ) ;
#58110=CARTESIAN_POINT ( 'NONE',  ( 0.5827357941260193908, 23.63272379758851471, -41.65958460246748984 ) ) ;
#58112=ORIENTED_EDGE ( 'NONE', *, *, #11583, .F. ) ;
#58120=EDGE_CURVE ( 'NONE', #10038, #50798, #35518, .T. ) ;
#58129=CARTESIAN_POINT ( 'NONE',  ( -15.98086288067142924, -12.48233498196030133, -0.6764478645581437632 ) ) ;
#58133=CARTESIAN_POINT ( 'NONE',  ( 0.5809828226811544205, -28.72298383114515374, 38.32755012159135077 ) ) ;
#58138=CARTESIAN_POINT ( 'NONE',  ( 3.783198216974388739, 38.10565824507926891, -20.00646744835626123 ) ) ;
#58140=EDGE_LOOP ( 'NONE', ( #36422, #40284, #41249, #51348 ) ) ;
#58151=CIRCLE ( 'NONE', #4124, 48.09070567114147110 ) ;
#58155=( BOUNDED_SURFACE ( )  B_SPLINE_SURFACE ( 3, 1, ( 
 ( #55550, #46496 ),
 ( #8561, #31777 ),
 ( #37111, #8251 ),
 ( #27687, #46818 ) ),
 .UNSPECIFIED., .F., .F., .F. ) 
 B_SPLINE_SURFACE_WITH_KNOTS ( ( 4, 4 ),
 ( 2, 2 ),
 ( 0.000000000000000000, 1.000000000000000000 ),
 ( 0.000000000000000000, 1.000000000000000000 ),
 .UNSPECIFIED. ) 
 GEOMETRIC_REPRESENTATION_ITEM ( )  RATIONAL_B_SPLINE_SURFACE ( (
 ( 1.000000000000000000, 1.000000000000000000),
 ( 0.9953390228620291325, 0.8624445117761032620),
 ( 0.9953390228620291325, 0.8624445117761032620),
 ( 1.000000000000000000, 1.000000000000000000) ) ) 
 REPRESENTATION_ITEM ( '' )  SURFACE ( )  );
#58163=ORIENTED_EDGE ( 'NONE', *, *, #1698, .F. ) ;
#58172=B_SPLINE_CURVE_WITH_KNOTS ( 'NONE', 3,
 ( #18152, #51639, #56651, #8734 ),
 .UNSPECIFIED., .F., .F.,
 ( 4, 4 ),
 ( 8.673617379884035472E-19, 0.004444878191957666105 ),
 .UNSPECIFIED. ) ;
#58173=ORIENTED_EDGE ( 'NONE', *, *, #60535, .T. ) ;
#58175=CARTESIAN_POINT ( 'NONE',  ( 5.965394784446458765, 16.29267539192326097, 12.48356622107682590 ) ) ;
#58183=CARTESIAN_POINT ( 'NONE',  ( 0.8557997880470599172, -37.44587306708076824, -29.88293891557508530 ) ) ;
#58193=B_SPLINE_CURVE_WITH_KNOTS ( 'NONE', 3,
 ( #5111, #33358, #5716, #23941, #731, #19253 ),
 .UNSPECIFIED., .F., .F.,
 ( 4, 2, 4 ),
 ( 1.517598411722886997E-16, 0.0002445252820015209787, 0.0004890505640028902775 ),
 .UNSPECIFIED. ) ;
#58196=CARTESIAN_POINT ( 'NONE',  ( 4.956653778116990594, -26.26162724282345096, -40.28700667097706400 ) ) ;
#58197=CARTESIAN_POINT ( 'NONE',  ( 4.967162193818130511, -8.839793687084915419, -42.16965968614202609 ) ) ;
#58201=ORIENTED_EDGE ( 'NONE', *, *, #5612, .T. ) ;
#58215=CARTESIAN_POINT ( 'NONE',  ( 1.227938101723756947, -17.20315230597815059, -39.32113113558984452 ) ) ;
#58217=ADVANCED_FACE ( 'NONE', ( #7219 ), #43230, .F. ) ;
#58218=ORIENTED_EDGE ( 'NONE', *, *, #46899, .T. ) ;
#58225=CARTESIAN_POINT ( 'NONE',  ( 0.9747592971366232373, 16.12077520819504528, -39.76507150545817382 ) ) ;
#58226=AXIS2_PLACEMENT_3D ( 'NONE', #25339, #24106, #49144 ) ;
#58229=ORIENTED_EDGE ( 'NONE', *, *, #28910, .F. ) ;
#58237=FACE_OUTER_BOUND ( 'NONE', #20209, .T. ) ;
#58244=( BOUNDED_SURFACE ( )  B_SPLINE_SURFACE ( 3, 1, ( 
 ( #10395, #29486 ),
 ( #6895, #36077 ),
 ( #40464, #21335 ),
 ( #54830, #36685 ) ),
 .UNSPECIFIED., .F., .F., .F. ) 
 B_SPLINE_SURFACE_WITH_KNOTS ( ( 4, 4 ),
 ( 2, 2 ),
 ( 0.000000000000000000, 1.000000000000000000 ),
 ( 0.000000000000000000, 1.000000000000000000 ),
 .UNSPECIFIED. ) 
 GEOMETRIC_REPRESENTATION_ITEM ( )  RATIONAL_B_SPLINE_SURFACE ( (
 ( 1.000000000000000000, 1.000000000000000000),
 ( 0.9953390228620291325, 0.8624445117760984880),
 ( 0.9953390228620291325, 0.8624445117760984880),
 ( 1.000000000000000000, 1.000000000000000000) ) ) 
 REPRESENTATION_ITEM ( '' )  SURFACE ( )  );
#58249=CARTESIAN_POINT ( 'NONE',  ( 4.956653778116989706, -42.88673967249116004, -21.75875759808752008 ) ) ;
#58260=VERTEX_POINT ( 'NONE', #54518 ) ;
#58268=EDGE_CURVE ( 'NONE', #35182, #38122, #26347, .T. ) ;
#58271=EDGE_CURVE ( 'NONE', #19687, #17001, #14798, .T. ) ;
#58274=CARTESIAN_POINT ( 'NONE',  ( 5.960221823109900008, -17.77295928189549201, -10.26751639438361963 ) ) ;
#58276=CARTESIAN_POINT ( 'NONE',  ( 0.5807400328401637335, 41.75144119563919531, -23.47602859900669969 ) ) ;
#58278=CARTESIAN_POINT ( 'NONE',  ( -17.69733060968885852, -7.723231777284044419, 2.086255951469231373 ) ) ;
#58279=CARTESIAN_POINT ( 'NONE',  ( 0.8557997880470690211, 46.03118133706043835, -13.27832040216591380 ) ) ;
#58281=DIRECTION ( 'NONE',  ( 0.07439287786467665975, -0.7991213610169907167, 0.5965490341031185473 ) ) ;
#58286=CARTESIAN_POINT ( 'NONE',  ( 1.227938101723756947, 29.74462687941269223, -30.94118573761281965 ) ) ;
#58289=CARTESIAN_POINT ( 'NONE',  ( 0.5832366564991526836, 28.94058080282834311, -38.16363840618222980 ) ) ;
#58298=CARTESIAN_POINT ( 'NONE',  ( 5.959828726073459926, 5.308046411395249464, -19.82738831247208111 ) ) ;
#58301=VERTEX_POINT ( 'NONE', #24931 ) ;
#58302=EDGE_LOOP ( 'NONE', ( #9658, #4453, #51105, #12544 ) ) ;
#58304=ORIENTED_EDGE ( 'NONE', *, *, #169, .T. ) ;
#58318=CARTESIAN_POINT ( 'NONE',  ( 2.624215991343608501, 37.21129343241604914, 30.33228621715047169 ) ) ;
#58319=ADVANCED_FACE ( 'NONE', ( #27894 ), #13581, .F. ) ;
#58321=B_SPLINE_CURVE_WITH_KNOTS ( 'NONE', 3,
 ( #14019, #52502, #18705, #24012 ),
 .UNSPECIFIED., .F., .F.,
 ( 4, 4 ),
 ( 9.047210765559599389E-17, 0.005004741218457501271 ),
 .UNSPECIFIED. ) ;
#58329=CARTESIAN_POINT ( 'NONE',  ( 0.5786265663353196143, 41.11783955080237263, 24.57327059187413099 ) ) ;
#58331=CARTESIAN_POINT ( 'NONE',  ( 2.526552050251863246, -20.43086833796931856, -37.81244156771011689 ) ) ;
#58335=CARTESIAN_POINT ( 'NONE',  ( 0.5809828226811617480, 33.48000389720616710, 34.25055090842165839 ) ) ;
#58341=CARTESIAN_POINT ( 'NONE',  ( 0.5809828226811617480, 11.86925843957166471, 46.40184912890843805 ) ) ;
#58348=ORIENTED_EDGE ( 'NONE', *, *, #59314, .F. ) ;
#58349=B_SPLINE_CURVE_WITH_KNOTS ( 'NONE', 3,
 ( #48883, #316, #57632, #44219, #52953, #10059 ),
 .UNSPECIFIED., .F., .F.,
 ( 4, 2, 4 ),
 ( 9.140795285775094282E-18, 0.0002291978881530158348, 0.0004583957763060225623 ),
 .UNSPECIFIED. ) ;
#58350=DIRECTION ( 'NONE',  ( 0.07439287786467665975, 0.4871392060437964022, 0.8701500408883694471 ) ) ;
#58353=CARTESIAN_POINT ( 'NONE',  ( 1.227938101723748288, 25.45152231597057124, 34.55893248994515687 ) ) ;
#58356=VECTOR ( 'NONE', #43534, 1000.000000000000000 ) ;
#58357=CARTESIAN_POINT ( 'NONE',  ( 0.5819845901640492425, -41.70428411658543411, 23.55368560422327562 ) ) ;
#58359=CARTESIAN_POINT ( 'NONE',  ( 0.5807400328401574052, 5.711437504336651649, -47.55718917606836982 ) ) ;
#58362=CARTESIAN_POINT ( 'NONE',  ( 0.8551540677456715978, 37.45266983663495353, 29.88829867897827341 ) ) ;
#58371=EDGE_CURVE ( 'NONE', #9098, #1997, #17022, .T. ) ;
#58377=CARTESIAN_POINT ( 'NONE',  ( 0.8551540677456715978, -13.28067116677170034, -46.03951182599441694 ) ) ;
#58378=EDGE_CURVE ( 'NONE', #4978, #35128, #18566, .T. ) ;
#58380=ORIENTED_EDGE ( 'NONE', *, *, #609, .T. ) ;
#58386=CARTESIAN_POINT ( 'NONE',  ( 2.526464513654346877, 42.43615126908567703, -6.809833384818603008 ) ) ;
#58392=ORIENTED_EDGE ( 'NONE', *, *, #39795, .F. ) ;
#58396=CARTESIAN_POINT ( 'NONE',  ( 2.281351352603298466, 42.18750813859391968, -22.83955855331473117 ) ) ;
#58401=AXIS2_PLACEMENT_3D ( 'NONE', #36838, #50898, #27104 ) ;
#58405=ADVANCED_FACE ( 'NONE', ( #30655 ), #19993, .F. ) ;
#58406=CARTESIAN_POINT ( 'NONE',  ( 5.959547316686252039, 2.682663672454912440, -20.34955788964373724 ) ) ;
#58411=ORIENTED_EDGE ( 'NONE', *, *, #15938, .F. ) ;
#58413=CARTESIAN_POINT ( 'NONE',  ( 0.5809828226811553087, 23.47450554821769231, -41.74875432577623258 ) ) ;
#58417=CARTESIAN_POINT ( 'NONE',  ( 1.154321713695927842, -39.95809834491012680, 15.65787958845404582 ) ) ;
#58418=EDGE_CURVE ( 'NONE', #38319, #42745, #25996, .T. ) ;
#58423=CARTESIAN_POINT ( 'NONE',  ( 1.227938101723756947, -37.58536632582764980, -20.72293514920789903 ) ) ;
#58424=CARTESIAN_POINT ( 'NONE',  ( 0.7057020205115017708, 47.89404687311023423, 0.8412108057954452711 ) ) ;
#58426=CARTESIAN_POINT ( 'NONE',  ( 0.5832367798473394593, -24.18350431151191415, 41.34221369670675017 ) ) ;
#58433=CARTESIAN_POINT ( 'NONE',  ( 3.270143674763207553, -9.482922169187890660, -9.870732238228624666 ) ) ;
#58443=CARTESIAN_POINT ( 'NONE',  ( 0.5832367798473394593, -12.65931911325636072, 46.19266341874892845 ) ) ;
#58444=CARTESIAN_POINT ( 'NONE',  ( 5.860006189529246790, -48.12869875779306739, -3.171667470663014576 ) ) ;
#58446=EDGE_CURVE ( 'NONE', #53492, #35268, #8787, .T. ) ;
#58448=CARTESIAN_POINT ( 'NONE',  ( 0.5832367798473389042, -47.52096797443091702, 5.981481162905551763 ) ) ;
#58449=CARTESIAN_POINT ( 'NONE',  ( 0.9968887458511647148, 30.80284987750050618, -29.87314546208197186 ) ) ;
#58451=EDGE_LOOP ( 'NONE', ( #32693, #36713, #56226, #35030 ) ) ;
#58470=ORIENTED_EDGE ( 'NONE', *, *, #16950, .T. ) ;
#58473=CARTESIAN_POINT ( 'NONE',  ( 2.281448460670571166, -47.37344300043617551, 7.562315317391583136 ) ) ;
#58475=ORIENTED_EDGE ( 'NONE', *, *, #28778, .F. ) ;
#58477=CARTESIAN_POINT ( 'NONE',  ( 5.860006189529234355, 45.66786516969951037, -15.52021937683227115 ) ) ;
#58478=ORIENTED_EDGE ( 'NONE', *, *, #40491, .F. ) ;
#58480=B_SPLINE_CURVE_WITH_KNOTS ( 'NONE', 3,
 ( #59224, #35457, #6277, #21653 ),
 .UNSPECIFIED., .F., .F.,
 ( 4, 4 ),
 ( 8.441528768080324345E-17, 0.005004741218457493465 ),
 .UNSPECIFIED. ) ;
#58482=CARTESIAN_POINT ( 'NONE',  ( 0.5827359174754828119, -18.66406616558009901, 44.10985444762177821 ) ) ;
#58486=CARTESIAN_POINT ( 'NONE',  ( 0.9736507210033056303, 33.76542629919406835, 26.47691119766800938 ) ) ;
#58487=ORIENTED_EDGE ( 'NONE', *, *, #42453, .F. ) ;
#58489=CARTESIAN_POINT ( 'NONE',  ( 0.5800708057587385946, 11.78915002112722554, 46.42229836006539756 ) ) ;
#58497=EDGE_CURVE ( 'NONE', #30064, #24857, #22541, .T. ) ;
#58510=CARTESIAN_POINT ( 'NONE',  ( 4.956653778116982600, -47.94889704119054130, 3.690426056929806631 ) ) ;
#58513=CARTESIAN_POINT ( 'NONE',  ( 4.303969348037246512, 46.98258166031703809, -10.35452842635794468 ) ) ;
#58515=CARTESIAN_POINT ( 'NONE',  ( 4.967162193818130511, -8.839793687084915419, -42.16965968614202609 ) ) ;
#58521=CARTESIAN_POINT ( 'NONE',  ( 4.956653778116988818, -45.71126949320240840, -14.93973939759935021 ) ) ;
#58529=CARTESIAN_POINT ( 'NONE',  ( 0.8557997880470599172, 5.347802024197243043, 47.60865952217000796 ) ) ;
#58537=CARTESIAN_POINT ( 'NONE',  ( 0.9757787079277436826, 16.45683390770838983, -39.62711913632683292 ) ) ;
#58541=EDGE_CURVE ( 'NONE', #31029, #4050, #49009, .T. ) ;
#58545=B_SPLINE_CURVE_WITH_KNOTS ( 'NONE', 3,
 ( #26534, #11214, #58482, #59733, #6780, #30303, #25924, #35963, #2089, #40358, #59419, #55026, #31235, #50335, #1172, #16526 ),
 .UNSPECIFIED., .F., .F.,
 ( 4, 3, 3, 3, 3, 4 ),
 ( 1.250973872328959318E-17, 0.0002724568934985565770, 0.0004086836638483839958, 0.0005449104342063665124, 0.0008173270854453630954, 0.001089761613562689659 ),
 .UNSPECIFIED. ) ;
#58548=EDGE_LOOP ( 'NONE', ( #44651, #30994, #8404, #48939 ) ) ;
#58550=LINE ( 'NONE', #43268, #28742 ) ;
#58552=VERTEX_POINT ( 'NONE', #34930 ) ;
#58557=CARTESIAN_POINT ( 'NONE',  ( 0.9722240741986377666, 21.95618662952236733, -36.86535088273183192 ) ) ;
#58567=DIRECTION ( 'NONE',  ( -1.000000000000000000, -0.000000000000000000, -0.000000000000000000 ) ) ;
#58583=DIRECTION ( 'NONE',  ( -1.000000000000000000, -0.000000000000000000, -0.000000000000000000 ) ) ;
#58585=CARTESIAN_POINT ( 'NONE',  ( -16.14013041205553378, -7.933563399346938994, -1.060327575359547359 ) ) ;
#58587=CARTESIAN_POINT ( 'NONE',  ( 0.8557997880470606944, 38.55640757422477805, -28.43566216844931915 ) ) ;
#58589=CARTESIAN_POINT ( 'NONE',  ( 5.974727161628369032, -17.76736931401853070, -10.27590650342031076 ) ) ;
#58604=EDGE_LOOP ( 'NONE', ( #11909, #34422, #14768, #49604 ) ) ;
#58605=CARTESIAN_POINT ( 'NONE',  ( 4.967162193818130511, 8.839793687085215623, 42.16965968614196925 ) ) ;
#58612=EDGE_CURVE ( 'NONE', #8115, #47638, #2532, .T. ) ;
#58623=DIRECTION ( 'NONE',  ( 0.07836865515943411409, -0.8593913859058549543, -0.5052769534812721064 ) ) ;
#58625=VECTOR ( 'NONE', #40992, 1000.000000000000114 ) ;
#58632=CARTESIAN_POINT ( 'NONE',  ( 5.981074661064941900, -16.28853686865590689, -12.48781255314283278 ) ) ;
#58637=B_SPLINE_CURVE_WITH_KNOTS ( 'NONE', 3,
 ( #44633, #6058, #59006, #35228 ),
 .UNSPECIFIED., .F., .F.,
 ( 4, 4 ),
 ( 0.000000000000000000, 0.004446090762761376394 ),
 .UNSPECIFIED. ) ;
#58641=CARTESIAN_POINT ( 'NONE',  ( 5.959828726073459926, 14.51059719297096606, 14.51699876360205188 ) ) ;
#58642=CARTESIAN_POINT ( 'NONE',  ( 1.227938101723748288, -25.45152231597034387, -34.55893248994532030 ) ) ;
#58654=CARTESIAN_POINT ( 'NONE',  ( 2.526552050251864578, 34.82218744039938940, -25.19159344346087082 ) ) ;
#58660=CARTESIAN_POINT ( 'NONE',  ( 0.8551540677456834771, 5.348818140991586034, -47.61725548905984340 ) ) ;
#58661=CARTESIAN_POINT ( 'NONE',  ( 3.270143674763207553, -4.983712007628325225, 12.74832469035450977 ) ) ;
#58664=CARTESIAN_POINT ( 'NONE',  ( 0.8557997880470697982, 24.73961900479251952, 41.02602466100786671 ) ) ;
#58674=VERTEX_POINT ( 'NONE', #11735 ) ;
#58681=ORIENTED_EDGE ( 'NONE', *, *, #18992, .F. ) ;
#58689=CIRCLE ( 'NONE', #29691, 43.08621763946400307 ) ;
#58693=EDGE_CURVE ( 'NONE', #41116, #13682, #447, .T. ) ;
#58703=B_SPLINE_CURVE_WITH_KNOTS ( 'NONE', 3,
 ( #50209, #2893, #31416, #6961 ),
 .UNSPECIFIED., .F., .F.,
 ( 4, 4 ),
 ( 2.168404344971008868E-19, 0.004048833967417087357 ),
 .UNSPECIFIED. ) ;
#58704=VERTEX_POINT ( 'NONE', #52691 ) ;
#58715=FACE_OUTER_BOUND ( 'NONE', #61709, .T. ) ;
#58734=CARTESIAN_POINT ( 'NONE',  ( 0.5839879882012679602, -23.94795769224416659, 41.47913983251944359 ) ) ;
#58738=CARTESIAN_POINT ( 'NONE',  ( 5.974727161628367256, -14.50236057684855417, 14.52429704002338973 ) ) ;
#58745=CARTESIAN_POINT ( 'NONE',  ( 3.407937589446178528, 9.356405769959192043, -10.00592723328951195 ) ) ;
#58746=CARTESIAN_POINT ( 'NONE',  ( 3.407937589446174087, 10.58239600294638905, 8.699069120706806046 ) ) ;
#58747=EDGE_CURVE ( 'NONE', #52969, #34606, #57243, .T. ) ;
#58751=VERTEX_POINT ( 'NONE', #3841 ) ;
#58752=CARTESIAN_POINT ( 'NONE',  ( 4.956653778116971054, 47.05699031914949160, 9.917440902361329691 ) ) ;
#58753=FACE_OUTER_BOUND ( 'NONE', #41829, .T. ) ;
#58757=CARTESIAN_POINT ( 'NONE',  ( 0.5836750258453360374, -47.50958153310754994, 6.071582023534099370 ) ) ;
#58763=CIRCLE ( 'NONE', #17801, 48.09070567114147110 ) ;
#58765=CIRCLE ( 'NONE', #31797, 48.09070567114147110 ) ;
#58769=CARTESIAN_POINT ( 'NONE',  ( 5.960721111146673579, -0.006321279846680040275, -20.52557019979492026 ) ) ;
#58774=B_SPLINE_CURVE_WITH_KNOTS ( 'NONE', 3,
 ( #14319, #19319, #33737, #4877, #18085, #56888, #28706, #37205, #56586, #43139, #23093, #175, #8983, #52500, #33427, #38439 ),
 .UNSPECIFIED., .F., .F.,
 ( 4, 3, 3, 3, 3, 4 ),
 ( 6.938893903907228378E-18, 0.0002724568934985511560, 0.0004086836638483824780, 0.0005449104342063647776, 0.0008173270854453713354, 0.001089761613562694213 ),
 .UNSPECIFIED. ) ;
#58781=CARTESIAN_POINT ( 'NONE',  ( 0.5836750258453369256, 41.56963612796216978, -23.79054009282503301 ) ) ;
#58783=B_SPLINE_CURVE_WITH_KNOTS ( 'NONE', 3,
 ( #10562, #523, #20279, #58448, #16813, #58757, #16492, #11180, #35925, #50305, #2683, #25888, #59383, #25271, #7061, #40026 ),
 .UNSPECIFIED., .F., .F.,
 ( 4, 3, 3, 3, 3, 4 ),
 ( 1.127622383284612036E-17, 0.0002724568934985564144, 0.0004086836638483807432, 0.0005449104342063628261, 0.0008173270854453688417, 0.001089761613562689226 ),
 .UNSPECIFIED. ) ;
#58794=ORIENTED_EDGE ( 'NONE', *, *, #29923, .T. ) ;
#58795=CARTESIAN_POINT ( 'NONE',  ( 3.660176727303386279, -36.93665184075199193, -30.71420464230603287 ) ) ;
#58800=CARTESIAN_POINT ( 'NONE',  ( 0.5819845901640490204, 5.801229454883947589, 47.54333976522119087 ) ) ;
#58801=ADVANCED_FACE ( 'NONE', ( #34848 ), #56365, .F. ) ;
#58804=ORIENTED_EDGE ( 'NONE', *, *, #51100, .T. ) ;
#58810=CARTESIAN_POINT ( 'NONE',  ( 0.5838002273316422741, 18.20308624554832377, 44.30203797796946930 ) ) ;
#58818=CARTESIAN_POINT ( 'NONE',  ( 4.967162193818130511, 28.74031574030012237, 32.10009971360082659 ) ) ;
#58825=CARTESIAN_POINT ( 'NONE',  ( 3.270143674763207553, -11.02405647745176154, 8.113405361969469709 ) ) ;
#58830=EDGE_CURVE ( 'NONE', #59261, #39909, #5373, .T. ) ;
#58831=CARTESIAN_POINT ( 'NONE',  ( 5.959547316686252039, -20.52562247508876681, 0.003562808152837171945 ) ) ;
#58837=CARTESIAN_POINT ( 'NONE',  ( 0.5838002273316428292, -23.82993264414535872, -41.54704836736074469 ) ) ;
#58841=ADVANCED_FACE ( 'NONE', ( #39249 ), #754, .F. ) ;
#58845=CARTESIAN_POINT ( 'NONE',  ( 0.7057020205115042133, 5.417413437617573990, 47.59410670607640270 ) ) ;
#58846=CARTESIAN_POINT ( 'NONE',  ( 0.9756354156337466721, -26.01752520779890077, -34.12075394380531179 ) ) ;
#58848=CARTESIAN_POINT ( 'NONE',  ( 0.8557997880470697982, 17.48760788519276943, -44.60232077416669227 ) ) ;
#58850=CARTESIAN_POINT ( 'NONE',  ( 0.8551540677456834771, -37.45266983663517379, 29.88829867897800696 ) ) ;
#58854=CARTESIAN_POINT ( 'NONE',  ( 1.227938101723756947, 15.63977281655895979, -39.96870412324319943 ) ) ;
#58856=CARTESIAN_POINT ( 'NONE',  ( 0.8557997880470690211, 46.03118133706043835, -13.27832040216591380 ) ) ;
#58858=B_SPLINE_CURVE_WITH_KNOTS ( 'NONE', 3,
 ( #278, #48236, #10023, #10640 ),
 .UNSPECIFIED., .F., .F.,
 ( 4, 4 ),
 ( 2.168404344971008868E-19, 0.004048833967417089091 ),
 .UNSPECIFIED. ) ;
#58873=CARTESIAN_POINT ( 'NONE',  ( 5.958863334805807099, 5.313608583996519030, -19.82594244347347612 ) ) ;
#58875=VERTEX_POINT ( 'NONE', #48616 ) ;
#58876=CARTESIAN_POINT ( 'NONE',  ( 4.960156602257180580, -41.40608197274622171, -20.99019478193095267 ) ) ;
#58880=DIRECTION ( 'NONE',  ( 0.07836865515943411409, -0.9608836331491542593, -0.2656332009267349248 ) ) ;
#58886=EDGE_CURVE ( 'NONE', #30413, #40820, #60247, .T. ) ;
#58889=CARTESIAN_POINT ( 'NONE',  ( 0.6067375320500723035, -47.57460111700601857, 5.548194933739998724 ) ) ;
#58890=CARTESIAN_POINT ( 'NONE',  ( 1.227938101723756947, -20.72293514920776758, 37.58536632582772086 ) ) ;
#58891=VERTEX_POINT ( 'NONE', #26355 ) ;
#58895=CARTESIAN_POINT ( 'NONE',  ( -19.96645934342861395, -12.48232314026188838, 0.6766079297640726908 ) ) ;
#58896=EDGE_CURVE ( 'NONE', #35725, #7287, #58025, .T. ) ;
#58900=CARTESIAN_POINT ( 'NONE',  ( 4.956653778116990594, -39.67974989265022145, -27.17045123668512474 ) ) ;
#58906=EDGE_CURVE ( 'NONE', #44407, #50007, #37107, .T. ) ;
#58909=( BOUNDED_SURFACE ( )  B_SPLINE_SURFACE ( 3, 1, ( 
 ( #56742, #43296 ),
 ( #4716, #33895 ),
 ( #14475, #23863 ),
 ( #23247, #655 ) ),
 .UNSPECIFIED., .F., .F., .F. ) 
 B_SPLINE_SURFACE_WITH_KNOTS ( ( 4, 4 ),
 ( 2, 2 ),
 ( 0.000000000000000000, 1.000000000000000000 ),
 ( 0.000000000000000000, 1.000000000000000000 ),
 .UNSPECIFIED. ) 
 GEOMETRIC_REPRESENTATION_ITEM ( )  RATIONAL_B_SPLINE_SURFACE ( (
 ( 1.000000000000000000, 1.000000000000000000),
 ( 0.7269869731126821222, 0.9931720237060910339),
 ( 0.7269869731126821222, 0.9931720237060910339),
 ( 1.000000000000000000, 1.000000000000000000) ) ) 
 REPRESENTATION_ITEM ( '' )  SURFACE ( )  );
#58911=CARTESIAN_POINT ( 'NONE',  ( -15.98127814905383026, -7.972271164889759731, -0.6777338475379729443 ) ) ;
#58913=( BOUNDED_SURFACE ( )  B_SPLINE_SURFACE ( 3, 1, ( 
 ( #40912, #30851 ),
 ( #22386, #55263 ),
 ( #26778, #41517 ),
 ( #17086, #59658 ) ),
 .UNSPECIFIED., .F., .F., .F. ) 
 B_SPLINE_SURFACE_WITH_KNOTS ( ( 4, 4 ),
 ( 2, 2 ),
 ( 0.000000000000000000, 1.000000000000000000 ),
 ( 0.000000000000000000, 1.000000000000000000 ),
 .UNSPECIFIED. ) 
 GEOMETRIC_REPRESENTATION_ITEM ( )  RATIONAL_B_SPLINE_SURFACE ( (
 ( 1.000000000000000000, 1.000000000000000000),
 ( 0.7269869731126817891, 0.9931720237060910339),
 ( 0.7269869731126817891, 0.9931720237060910339),
 ( 1.000000000000000000, 1.000000000000000000) ) ) 
 REPRESENTATION_ITEM ( '' )  SURFACE ( )  );
#58919=FACE_OUTER_BOUND ( 'NONE', #24702, .T. ) ;
#58936=CARTESIAN_POINT ( 'NONE',  ( 5.960721111146673579, 16.28018152803692686, -12.50019045452721222 ) ) ;
#58938=CARTESIAN_POINT ( 'NONE',  ( 1.227938101723748288, 29.74462687941226235, 30.94118573761323177 ) ) ;
#58941=CARTESIAN_POINT ( 'NONE',  ( 0.9968887458511672683, 25.59699785741785405, 34.43855515351779673 ) ) ;
#58942=ORIENTED_EDGE ( 'NONE', *, *, #25040, .F. ) ;
#58945=CARTESIAN_POINT ( 'NONE',  ( 2.526464513654344213, -17.56107808841279194, -39.22765990515338785 ) ) ;
#58956=ORIENTED_EDGE ( 'NONE', *, *, #45842, .F. ) ;
#58962=ORIENTED_EDGE ( 'NONE', *, *, #15032, .F. ) ;
#58963=CARTESIAN_POINT ( 'NONE',  ( 0.5819845901640485764, -46.14435291605020950, -12.83441129068581965 ) ) ;
#58965=EDGE_CURVE ( 'NONE', #2384, #54909, #30410, .T. ) ;
#58966=DIRECTION ( 'NONE',  ( 0.000000000000000000, 0.000000000000000000, 1.000000000000000000 ) ) ;
#58973=EDGE_CURVE ( 'NONE', #2634, #24857, #22885, .T. ) ;
#58979=CARTESIAN_POINT ( 'NONE',  ( 0.5850706913938534814, -44.31965802246092778, -18.16120156791927798 ) ) ;
#58985=CARTESIAN_POINT ( 'NONE',  ( 0.6067099128993216350, -41.12102523654870367, 24.55985149487306529 ) ) ;
#58991=CARTESIAN_POINT ( 'NONE',  ( 0.9741495583595161101, -26.43366215195285562, 33.79932324264177623 ) ) ;
#58992=( BOUNDED_SURFACE ( )  B_SPLINE_SURFACE ( 3, 1, ( 
 ( #6031, #16092 ),
 ( #2269, #24871 ),
 ( #48666, #25789 ),
 ( #53647, #58660 ) ),
 .UNSPECIFIED., .F., .F., .F. ) 
 B_SPLINE_SURFACE_WITH_KNOTS ( ( 4, 4 ),
 ( 2, 2 ),
 ( 0.000000000000000000, 1.000000000000000000 ),
 ( 0.000000000000000000, 1.000000000000000000 ),
 .UNSPECIFIED. ) 
 GEOMETRIC_REPRESENTATION_ITEM ( )  RATIONAL_B_SPLINE_SURFACE ( (
 ( 1.000000000000000000, 1.000000000000000000),
 ( 0.7269869731126817891, 0.9931720237060910339),
 ( 0.7269869731126817891, 0.9931720237060910339),
 ( 1.000000000000000000, 1.000000000000000000) ) ) 
 REPRESENTATION_ITEM ( '' )  SURFACE ( )  );
#58997=ORIENTED_EDGE ( 'NONE', *, *, #55821, .F. ) ;
#58998=VERTEX_POINT ( 'NONE', #4676 ) ;
#59000=CARTESIAN_POINT ( 'NONE',  ( 2.281351352603291360, -46.66131639318007984, 11.14238889600268934 ) ) ;
#59005=CARTESIAN_POINT ( 'NONE',  ( 3.783198216974389627, 40.39102707215877786, -14.86152287314638620 ) ) ;
#59006=CARTESIAN_POINT ( 'NONE',  ( 2.281351352603298022, 25.11567449372765637, -40.87339198768968629 ) ) ;
#59017=CARTESIAN_POINT ( 'NONE',  ( 0.5809828226811553087, 6.791453954330313181, 47.41188724015881917 ) ) ;
#59024=CARTESIAN_POINT ( 'NONE',  ( 0.5838002273316442725, 44.30203797796963272, -18.20308624554782639 ) ) ;
#59033=FACE_OUTER_BOUND ( 'NONE', #8742, .T. ) ;
#59038=CARTESIAN_POINT ( 'NONE',  ( 5.860006189529234355, -43.26650951066853423, -21.31760477694627554 ) ) ;
#59039=ORIENTED_EDGE ( 'NONE', *, *, #3890, .T. ) ;
#59046=CARTESIAN_POINT ( 'NONE',  ( 0.5809828226811544205, 5.711058609466008740, -47.55412398569200150 ) ) ;
#59048=CARTESIAN_POINT ( 'NONE',  ( 0.5827359174754830340, 46.35666395585288058, -12.04517879102088429 ) ) ;
#59052=DIRECTION ( 'NONE',  ( 0.000000000000000000, 0.000000000000000000, 1.000000000000000000 ) ) ;
#59056=EDGE_LOOP ( 'NONE', ( #28265, #47742, #34223, #568 ) ) ;
#59058=CARTESIAN_POINT ( 'NONE',  ( 0.8557997880470697982, -13.27832040216607190, -46.03118133706039572 ) ) ;
#59061=CARTESIAN_POINT ( 'NONE',  ( 0.5850706913938534814, 41.38834827854241638, -24.10530971368245190 ) ) ;
#59065=LINE ( 'NONE', #40013, #28726 ) ;
#59070=CARTESIAN_POINT ( 'NONE',  ( 4.303969348037258058, -40.54345935592797900, 25.89994482339355386 ) ) ;
#59072=CARTESIAN_POINT ( 'NONE',  ( 3.407937589446174087, -13.69123696618924058, -0.4592810312473414314 ) ) ;
#59077=CARTESIAN_POINT ( 'NONE',  ( 4.967162193818130511, -42.34252806656598977, 7.970725651239652265 ) ) ;
#59080=ORIENTED_EDGE ( 'NONE', *, *, #51270, .F. ) ;
#59085=ORIENTED_EDGE ( 'NONE', *, *, #5654, .T. ) ;
#59086=B_SPLINE_CURVE_WITH_KNOTS ( 'NONE', 3,
 ( #44226, #1254, #24463, #5026 ),
 .UNSPECIFIED., .F., .F.,
 ( 4, 4 ),
 ( 1.962615573354719267E-17, 0.005004741218457437087 ),
 .UNSPECIFIED. ) ;
#59087=CARTESIAN_POINT ( 'NONE',  ( 4.967162193818130511, 28.07411493385295032, 32.68434214048178177 ) ) ;
#59089=ORIENTED_EDGE ( 'NONE', *, *, #28002, .T. ) ;
#59093=VERTEX_POINT ( 'NONE', #9713 ) ;
#59100=CARTESIAN_POINT ( 'NONE',  ( 0.5809828226811553087, 41.20389530892342833, -24.41822904836879715 ) ) ;
#59104=ORIENTED_EDGE ( 'NONE', *, *, #48234, .T. ) ;
#59114=VERTEX_POINT ( 'NONE', #19139 ) ;
#59115=CARTESIAN_POINT ( 'NONE',  ( 0.5827357941260221663, 6.611647889511194087, 47.43746130990116683 ) ) ;
#59120=EDGE_CURVE ( 'NONE', #30566, #60037, #59474, .T. ) ;
#59135=CARTESIAN_POINT ( 'NONE',  ( 0.5807400328401637335, 24.41979442053227700, -41.20655774452942666 ) ) ;
#59142=CARTESIAN_POINT ( 'NONE',  ( 0.7762783648524369529, -5.369627767360159787, 47.60264408896662047 ) ) ;
#59154=CARTESIAN_POINT ( 'NONE',  ( 0.9740398440564311811, -39.79907313245119838, -16.03656236596792084 ) ) ;
#59162=B_SPLINE_CURVE_WITH_KNOTS ( 'NONE', 3,
 ( #42261, #15202, #18432, #34310 ),
 .UNSPECIFIED., .F., .F.,
 ( 4, 4 ),
 ( 0.000000000000000000, 0.005004741218457402392 ),
 .UNSPECIFIED. ) ;
#59165=VERTEX_POINT ( 'NONE', #38249 ) ;
#59171=VERTEX_POINT ( 'NONE', #2460 ) ;
#59172=CARTESIAN_POINT ( 'NONE',  ( 5.960721111146673579, 12.49016043756471284, -16.28787783074214701 ) ) ;
#59174=CARTESIAN_POINT ( 'NONE',  ( 5.981074661064941900, 14.50705827991446029, -14.51919955600720513 ) ) ;
#59175=CARTESIAN_POINT ( 'NONE',  ( 0.5850706913938534814, 41.56998471741228229, 23.79070617305396240 ) ) ;
#59181=( BOUNDED_SURFACE ( )  B_SPLINE_SURFACE ( 3, 1, ( 
 ( #30888, #2372 ),
 ( #29970, #35302 ),
 ( #12122, #50004 ),
 ( #53746, #21491 ) ),
 .UNSPECIFIED., .F., .F., .F. ) 
 B_SPLINE_SURFACE_WITH_KNOTS ( ( 4, 4 ),
 ( 2, 2 ),
 ( 0.000000000000000000, 1.000000000000000000 ),
 ( 0.000000000000000000, 1.000000000000000000 ),
 .UNSPECIFIED. ) 
 GEOMETRIC_REPRESENTATION_ITEM ( )  RATIONAL_B_SPLINE_SURFACE ( (
 ( 1.000000000000000000, 1.000000000000000000),
 ( 0.9953390228620291325, 0.8624445117760984880),
 ( 0.9953390228620291325, 0.8624445117760984880),
 ( 1.000000000000000000, 1.000000000000000000) ) ) 
 REPRESENTATION_ITEM ( '' )  SURFACE ( )  );
#59183=ORIENTED_EDGE ( 'NONE', *, *, #16413, .T. ) ;
#59185=ORIENTED_EDGE ( 'NONE', *, *, #3762, .T. ) ;
#59187=LINE ( 'NONE', #20378, #29374 ) ;
#59188=CARTESIAN_POINT ( 'NONE',  ( 0.5827357941260210561, 33.60975216782532016, -34.12346967353423821 ) ) ;
#59191=ORIENTED_EDGE ( 'NONE', *, *, #28786, .T. ) ;
#59192=LINE ( 'NONE', #53868, #42668 ) ;
#59198=CARTESIAN_POINT ( 'NONE',  ( 4.956653778116981712, -42.88673967249145846, 21.75875759808692322 ) ) ;
#59200=ORIENTED_EDGE ( 'NONE', *, *, #19156, .F. ) ;
#59203=DIRECTION ( 'NONE',  ( -0.07836865515943411409, -0.1223011693452919629, 0.9893941468723553845 ) ) ;
#59217=FACE_OUTER_BOUND ( 'NONE', #23278, .T. ) ;
#59218=CARTESIAN_POINT ( 'NONE',  ( 5.959547316686252039, -19.82530672674358385, -5.315863417546260905 ) ) ;
#59221=CARTESIAN_POINT ( 'NONE',  ( 5.981074661064941900, -7.862380442164262462, 18.95903134304776216 ) ) ;
#59223=ORIENTED_EDGE ( 'NONE', *, *, #27516, .T. ) ;
#59224=CARTESIAN_POINT ( 'NONE',  ( 4.956653778116991482, -8.845409907520609849, -47.27023054223761989 ) ) ;
#59236=CARTESIAN_POINT ( 'NONE',  ( 0.5800708057587358191, -41.16170989303188321, -24.48933404430302829 ) ) ;
#59238=ORIENTED_EDGE ( 'NONE', *, *, #5069, .T. ) ;
#59239=ADVANCED_FACE ( 'NONE', ( #54772 ), #41557, .F. ) ;
#59250=EDGE_CURVE ( 'NONE', #55904, #48168, #53836, .T. ) ;
#59253=( BOUNDED_SURFACE ( )  B_SPLINE_SURFACE ( 3, 1, ( 
 ( #39317, #58377 ),
 ( #14897, #12052 ),
 ( #21423, #6986 ),
 ( #26121, #31126 ) ),
 .UNSPECIFIED., .F., .F., .F. ) 
 B_SPLINE_SURFACE_WITH_KNOTS ( ( 4, 4 ),
 ( 2, 2 ),
 ( 0.000000000000000000, 1.000000000000000000 ),
 ( 0.000000000000000000, 1.000000000000000000 ),
 .UNSPECIFIED. ) 
 GEOMETRIC_REPRESENTATION_ITEM ( )  RATIONAL_B_SPLINE_SURFACE ( (
 ( 1.000000000000000000, 1.000000000000000000),
 ( 0.9953390228620291325, 0.8624445117760984880),
 ( 0.9953390228620291325, 0.8624445117760984880),
 ( 1.000000000000000000, 1.000000000000000000) ) ) 
 REPRESENTATION_ITEM ( '' )  SURFACE ( )  );
#59254=VERTEX_POINT ( 'NONE', #58854 ) ;
#59257=FACE_OUTER_BOUND ( 'NONE', #54132, .T. ) ;
#59260=EDGE_LOOP ( 'NONE', ( #55543, #43330, #5143, #29322 ) ) ;
#59261=VERTEX_POINT ( 'NONE', #1844 ) ;
#59262=AXIS2_PLACEMENT_3D ( 'NONE', #43627, #20416, #29804 ) ;
#59267=ORIENTED_EDGE ( 'NONE', *, *, #32038, .T. ) ;
#59274=CARTESIAN_POINT ( 'NONE',  ( 4.303969348037258058, 46.98258166031690308, 10.35452842635859483 ) ) ;
#59284=CARTESIAN_POINT ( 'NONE',  ( 1.227938101723756947, 22.18841447410719780, 36.73927144310519566 ) ) ;
#59286=CARTESIAN_POINT ( 'NONE',  ( 0.5807400328401574052, -38.33001520688970487, 28.72484455891627775 ) ) ;
#59302=CARTESIAN_POINT ( 'NONE',  ( 5.974727161628369032, -16.27409205901367883, -12.50710176110002081 ) ) ;
#59303=ORIENTED_EDGE ( 'NONE', *, *, #41489, .F. ) ;
#59309=VERTEX_POINT ( 'NONE', #51307 ) ;
#59314=EDGE_CURVE ( 'NONE', #52304, #46447, #4096, .T. ) ;
#59316=ORIENTED_EDGE ( 'NONE', *, *, #31343, .F. ) ;
#59323=CARTESIAN_POINT ( 'NONE',  ( 0.9722240741986369894, -10.54237114526854313, -41.59310805473380412 ) ) ;
#59333=CARTESIAN_POINT ( 'NONE',  ( 0.8551540677456834771, -33.23105123575924580, 34.52115452272916940 ) ) ;
#59335=CARTESIAN_POINT ( 'NONE',  ( 0.5832366564991499081, 12.13301812590415096, -46.33368520589904449 ) ) ;
#59339=CARTESIAN_POINT ( 'NONE',  ( 0.9754402186311951217, -21.61645729243085867, -37.06569162601120127 ) ) ;
#59349=CARTESIAN_POINT ( 'NONE',  ( 0.8551540677456739292, 47.61725548905997840, -5.348818140990426073 ) ) ;
#59350=B_SPLINE_CURVE_WITH_KNOTS ( 'NONE', 3,
 ( #32304, #19142, #3764, #61391 ),
 .UNSPECIFIED., .F., .F.,
 ( 4, 4 ),
 ( 0.000000000000000000, 0.005004741218457427546 ),
 .UNSPECIFIED. ) ;
#59359=DIRECTION ( 'NONE',  ( 0.07836865515943411409, -0.9649662368512254007, 0.2503967164834362547 ) ) ;
#59363=CARTESIAN_POINT ( 'NONE',  ( 0.6846871229502899947, -5.395516691087521188, 47.60345020167350327 ) ) ;
#59364=CARTESIAN_POINT ( 'NONE',  ( 1.227938101723748288, -17.20315230597871903, 39.32113113558960293 ) ) ;
#59379=CARTESIAN_POINT ( 'NONE',  ( 2.624215991343620935, 32.93378783738897653, -34.92983774302933142 ) ) ;
#59380=CARTESIAN_POINT ( 'NONE',  ( 0.5807400328401574052, 37.66660715020866945, 29.58941477093028283 ) ) ;
#59383=CARTESIAN_POINT ( 'NONE',  ( 0.5832366564991514624, -47.44984844891991571, 6.521686574605942255 ) ) ;
#59385=EDGE_CURVE ( 'NONE', #39205, #12115, #52707, .T. ) ;
#59391=CARTESIAN_POINT ( 'NONE',  ( 0.5800708057587399269, 41.78924035064556364, -23.40241940841912793 ) ) ;
#59393=EDGE_CURVE ( 'NONE', #20504, #35226, #45319, .T. ) ;
#59398=B_SPLINE_CURVE_WITH_KNOTS ( 'NONE', 3,
 ( #17306, #13536, #2566, #41439, #59892, #45514, #21687, #55185, #12307, #31398, #46136, #50495, #7568, #45829, #41135, #642, #24462, #19169, #57331 ),
 .UNSPECIFIED., .F., .F.,
 ( 4, 3, 3, 3, 3, 3, 4 ),
 ( 9.813676791237319219E-18, 0.0002724573126191738581, 0.0004086839781548292326, 0.0005449106435901659821, 0.0006811373090491345443, 0.0008459866663933557135, 0.001010840725717199705 ),
 .UNSPECIFIED. ) ;
#59401=CARTESIAN_POINT ( 'NONE',  ( 0.9752570700956809668, 41.50550328400882449, -10.88256294660668821 ) ) ;
#59403=CARTESIAN_POINT ( 'NONE',  ( 0.9722240741986376555, -33.68410525900265640, -26.58024228478330286 ) ) ;
#59404=EDGE_CURVE ( 'NONE', #22913, #18160, #50689, .T. ) ;
#59405=FACE_OUTER_BOUND ( 'NONE', #45272, .T. ) ;
#59409=CARTESIAN_POINT ( 'NONE',  ( 1.088313998177381281, 42.64115081428570875, -4.827222641554805627 ) ) ;
#59416=ORIENTED_EDGE ( 'NONE', *, *, #29011, .T. ) ;
#59419=CARTESIAN_POINT ( 'NONE',  ( 0.5839879327111946461, -18.24507200299072807, 44.28486549479615775 ) ) ;
#59424=VERTEX_POINT ( 'NONE', #8710 ) ;
#59426=CARTESIAN_POINT ( 'NONE',  ( 0.6846871229502899947, 33.25969555998791094, -34.48177377577800939 ) ) ;
#59431=CARTESIAN_POINT ( 'NONE',  ( 4.956653778116975495, 15.97476558431885252, 45.35992544608534160 ) ) ;
#59439=CARTESIAN_POINT ( 'NONE',  ( 0.7762777257811900311, -23.17763256463740973, -41.92424087089334961 ) ) ;
#59446=CARTESIAN_POINT ( 'NONE',  ( 4.303969348037246512, 43.57722561725959309, 20.38638383586135561 ) ) ;
#59450=DIRECTION ( 'NONE',  ( -0.07439287786467652097, -0.9665813013808162157, -0.2453289374370237197 ) ) ;
#59461=EDGE_CURVE ( 'NONE', #1494, #58012, #24542, .T. ) ;
#59464=CARTESIAN_POINT ( 'NONE',  ( 0.9730545539215883499, -25.71816799638755668, -34.34678117142582465 ) ) ;
#59465=CARTESIAN_POINT ( 'NONE',  ( 1.154321485836932393, -25.46626718279332025, 34.54400167111891307 ) ) ;
#59469=CARTESIAN_POINT ( 'NONE',  ( 0.8557997880470697982, 17.48760788519276943, -44.60232077416669227 ) ) ;
#59474=B_SPLINE_CURVE_WITH_KNOTS ( 'NONE', 3,
 ( #42947, #57604, #9953, #606 ),
 .UNSPECIFIED., .F., .F.,
 ( 4, 4 ),
 ( 0.000000000000000000, 0.005004741218457415403 ),
 .UNSPECIFIED. ) ;
#59481=EDGE_LOOP ( 'NONE', ( #47286, #50940, #5708, #23403 ) ) ;
#59484=CARTESIAN_POINT ( 'NONE',  ( 2.624215991343608501, -34.92983774302990696, 32.93378783738836546 ) ) ;
#59486=ORIENTED_EDGE ( 'NONE', *, *, #3246, .F. ) ;
#59487=EDGE_CURVE ( 'NONE', #17561, #50265, #46749, .T. ) ;
#59493=VERTEX_POINT ( 'NONE', #15282 ) ;
#59494=CARTESIAN_POINT ( 'NONE',  ( 0.9757619758474602722, -0.06449181910561185838, -42.90842306541549078 ) ) ;
#59502=CARTESIAN_POINT ( 'NONE',  ( 4.967162193818130511, 43.02067033766018511, 2.375726030842731706 ) ) ;
#59503=CONICAL_SURFACE ( 'NONE', #32524, 43.08621763946400307, 1.568696531533066763 ) ;
#59506=CARTESIAN_POINT ( 'NONE',  ( 2.526552050251863690, -36.59987178591165957, -22.53110080776695412 ) ) ;
#59517=ADVANCED_FACE ( 'NONE', ( #5531 ), #52341, .F. ) ;
#59528=CARTESIAN_POINT ( 'NONE',  ( 5.959547316686252039, -2.675599016784684814, 20.35048796920732173 ) ) ;
#59529=CARTESIAN_POINT ( 'NONE',  ( 4.956653778116988818, -43.37017594958040689, -20.77844580450608447 ) ) ;
#59531=CARTESIAN_POINT ( 'NONE',  ( 4.963659409799330291, 14.83726297270280092, 42.22332985082316270 ) ) ;
#59532=CARTESIAN_POINT ( 'NONE',  ( 0.9722240741986373225, -37.44729083276440207, 20.94823706911186534 ) ) ;
#59537=ADVANCED_FACE ( 'NONE', ( #29059 ), #31609, .T. ) ;
#59538=CARTESIAN_POINT ( 'NONE',  ( 4.303969348037258058, 16.39840148505153650, -45.22910199346958393 ) ) ;
#59543=CARTESIAN_POINT ( 'NONE',  ( 5.959547316686252039, -18.96456592444106448, 7.851524054666073837 ) ) ;
#59547=CARTESIAN_POINT ( 'NONE',  ( 5.860006189529234355, -9.426589201135168850, -47.30296539008834600 ) ) ;
#59554=CARTESIAN_POINT ( 'NONE',  ( 4.967162193818130511, 42.16965968614205451, -8.839793687084773310 ) ) ;
#59555=ORIENTED_EDGE ( 'NONE', *, *, #6397, .T. ) ;
#59557=VERTEX_POINT ( 'NONE', #59087 ) ;
#59560=ORIENTED_EDGE ( 'NONE', *, *, #27240, .F. ) ;
#59570=B_SPLINE_CURVE_WITH_KNOTS ( 'NONE', 3,
 ( #2572, #16080, #6950, #45223, #2257, #21387 ),
 .UNSPECIFIED., .F., .F.,
 ( 4, 2, 4 ),
 ( 1.523643551133495791E-16, 0.0002445252820015197861, 0.0004890505640028871333 ),
 .UNSPECIFIED. ) ;
#59581=DIRECTION ( 'NONE',  ( 0.000000000000000000, 0.000000000000000000, 1.000000000000000000 ) ) ;
#59585=AXIS2_PLACEMENT_3D ( 'NONE', #3694, #18137, #32865 ) ;
#59590=ADVANCED_FACE ( 'NONE', ( #12133 ), #42622, .T. ) ;
#59595=LINE ( 'NONE', #12027, #38126 ) ;
#59599=ADVANCED_FACE ( 'NONE', ( #39406 ), #53973, .F. ) ;
#59602=CARTESIAN_POINT ( 'NONE',  ( 4.967162193818130511, 7.970725651240403664, -42.34252806656584056 ) ) ;
#59615=B_SPLINE_CURVE_WITH_KNOTS ( 'NONE', 3,
 ( #2190, #51044, #31338, #60140 ),
 .UNSPECIFIED., .F., .F.,
 ( 4, 4 ),
 ( 7.589415207398531038E-19, 0.004444878191957666105 ),
 .UNSPECIFIED. ) ;
#59617=CARTESIAN_POINT ( 'NONE',  ( 4.956653778116966613, 0.000000000000000000, 0.000000000000000000 ) ) ;
#59620=ORIENTED_EDGE ( 'NONE', *, *, #14476, .T. ) ;
#59626=VERTEX_POINT ( 'NONE', #3005 ) ;
#59647=DIRECTION ( 'NONE',  ( -1.000000000000000000, -0.000000000000000000, -0.000000000000000000 ) ) ;
#59651=CARTESIAN_POINT ( 'NONE',  ( 0.9752132459055864455, -21.65565338840788812, -37.04276540031529663 ) ) ;
#59652=ORIENTED_EDGE ( 'NONE', *, *, #17944, .T. ) ;
#59653=CARTESIAN_POINT ( 'NONE',  ( 0.6846871229502932144, 46.49193983736607549, -11.56285438919583797 ) ) ;
#59655=DIRECTION ( 'NONE',  ( 0.000000000000000000, 0.000000000000000000, 1.000000000000000000 ) ) ;
#59658=CARTESIAN_POINT ( 'NONE',  ( 0.8551540677456834771, -24.74404575822746466, -41.03346287276453097 ) ) ;
#59673=DIRECTION ( 'NONE',  ( -1.000000000000000000, -0.000000000000000000, -0.000000000000000000 ) ) ;
#59677=EDGE_CURVE ( 'NONE', #35241, #31407, #15344, .T. ) ;
#59678=CARTESIAN_POINT ( 'NONE',  ( 5.959828726073459926, 17.77343634131827699, 10.26672511661762144 ) ) ;
#59690=ORIENTED_EDGE ( 'NONE', *, *, #20257, .T. ) ;
#59691=ORIENTED_EDGE ( 'NONE', *, *, #20881, .T. ) ;
#59692=FACE_OUTER_BOUND ( 'NONE', #12662, .T. ) ;
#59698=B_SPLINE_CURVE_WITH_KNOTS ( 'NONE', 3,
 ( #28185, #60450, #47015, #27269 ),
 .UNSPECIFIED., .F., .F.,
 ( 4, 4 ),
 ( 8.355534721610420292E-17, 0.005004741218457496935 ),
 .UNSPECIFIED. ) ;
#59703=CARTESIAN_POINT ( 'NONE',  ( 5.974727161628369032, 7.868887636447618128, -18.95664195401509744 ) ) ;
#59712=CARTESIAN_POINT ( 'NONE',  ( 1.227938101723748288, -29.74462687941204209, -30.94118573761343782 ) ) ;
#59717=CARTESIAN_POINT ( 'NONE',  ( 0.5807400328401574052, -0.5448834511086588783, -47.89582301953904420 ) ) ;
#59733=CARTESIAN_POINT ( 'NONE',  ( 0.5832367798473394593, -18.58036934788106009, 44.14510605973673307 ) ) ;
#59739=ORIENTED_EDGE ( 'NONE', *, *, #8000, .F. ) ;
#59746=ORIENTED_EDGE ( 'NONE', *, *, #57454, .F. ) ;
#59753=EDGE_LOOP ( 'NONE', ( #40492, #18269, #51795, #17205 ) ) ;
#59761=CARTESIAN_POINT ( 'NONE',  ( 5.974727161628369032, 19.82156119440438147, 5.327229920347495096 ) ) ;
#59765=CARTESIAN_POINT ( 'NONE',  ( 2.624215991343620935, 28.09277600149274789, -38.92973006074482356 ) ) ;
#59778=CARTESIAN_POINT ( 'NONE',  ( 2.526464513654345545, 12.29060355381851188, 41.18424249084321076 ) ) ;
#59783=CARTESIAN_POINT ( 'NONE',  ( 2.526552050251864134, 29.52128340070600743, 31.23611603144874493 ) ) ;
#59788=CARTESIAN_POINT ( 'NONE',  ( 0.9752132459055863345, -26.30543738863321579, -33.89922943039202607 ) ) ;
#59789=CARTESIAN_POINT ( 'NONE',  ( 1.088908134280557105, -25.50067491870061431, 34.51503525510842962 ) ) ;
#59792=FACE_OUTER_BOUND ( 'NONE', #24471, .T. ) ;
#59793=CARTESIAN_POINT ( 'NONE',  ( 5.959547316686252039, 14.51128755440541340, -14.51632612601513728 ) ) ;
#59794=VECTOR ( 'NONE', #57419, 1000.000000000000114 ) ;
#59802=ORIENTED_EDGE ( 'NONE', *, *, #39719, .F. ) ;
#59807=ORIENTED_EDGE ( 'NONE', *, *, #13193, .F. ) ;
#59817=CARTESIAN_POINT ( 'NONE',  ( 0.6846871229502932144, 33.25969555998742777, 34.48177377577847835 ) ) ;
#59830=CARTESIAN_POINT ( 'NONE',  ( -18.11268303252489176, -12.32233744059949743, 2.099999999999994760 ) ) ;
#59833=ORIENTED_EDGE ( 'NONE', *, *, #36070, .F. ) ;
#59835=ORIENTED_EDGE ( 'NONE', *, *, #18507, .F. ) ;
#59838=FACE_OUTER_BOUND ( 'NONE', #47491, .T. ) ;
#59839=B_SPLINE_CURVE_WITH_KNOTS ( 'NONE', 3,
 ( #39182, #4370, #23507, #23825 ),
 .UNSPECIFIED., .F., .F.,
 ( 4, 4 ),
 ( 7.351626287044712563E-17, 0.005004741218457496067 ),
 .UNSPECIFIED. ) ;
#59842=EDGE_LOOP ( 'NONE', ( #40769, #12132, #16281, #31549 ) ) ;
#59843=CARTESIAN_POINT ( 'NONE',  ( 0.9745511491811745808, 21.74846188963830329, -36.98831798234355972 ) ) ;
#59847=CARTESIAN_POINT ( 'NONE',  ( 0.9752132459055847802, 37.04276540031541742, -21.65565338840778153 ) ) ;
#59849=CARTESIAN_POINT ( 'NONE',  ( 0.9730545539215883499, 33.73144377768558400, 26.52009130076782739 ) ) ;
#59851=CARTESIAN_POINT ( 'NONE',  ( 0.8557997880470599172, 7.156447707086380561, -47.37054680076698077 ) ) ;
#59852=CARTESIAN_POINT ( 'NONE',  ( 0.5832366564991513513, -29.37287047358855574, -37.83193087518338160 ) ) ;
#59865=CARTESIAN_POINT ( 'NONE',  ( 0.9754402186311948997, -41.49454543482922730, -10.92425836141462803 ) ) ;
#59867=CARTESIAN_POINT ( 'NONE',  ( 0.5850706913938534814, -47.46255051844958217, 6.431767090162647804 ) ) ;
#59871=CARTESIAN_POINT ( 'NONE',  ( 0.9752132459055846692, -5.369621847647896296, 42.57112816680952960 ) ) ;
#59873=FACE_OUTER_BOUND ( 'NONE', #26204, .T. ) ;
#59879=CARTESIAN_POINT ( 'NONE',  ( 0.9756008150404598123, 16.55159915785279168, 39.58764833544681494 ) ) ;
#59884=CARTESIAN_POINT ( 'NONE',  ( 0.8557997880470599172, 11.51622788066458369, 46.50333260518563350 ) ) ;
#59886=VECTOR ( 'NONE', #13643, 1000.000000000000000 ) ;
#59889=CARTESIAN_POINT ( 'NONE',  ( 0.5836750258453349272, 44.18029554260635194, 18.49664649301206509 ) ) ;
#59890=VERTEX_POINT ( 'NONE', #59017 ) ;
#59892=CARTESIAN_POINT ( 'NONE',  ( 0.9754402186311939005, 26.26956909363317294, 33.92707563620654554 ) ) ;
#59908=B_SPLINE_CURVE_WITH_KNOTS ( 'NONE', 3,
 ( #13884, #48304, #38615, #43319, #14494, #61447 ),
 .UNSPECIFIED., .F., .F.,
 ( 4, 2, 4 ),
 ( 1.015220885719448636E-17, 0.0002291978881530203343, 0.0004583957763060304770 ),
 .UNSPECIFIED. ) ;
#59914=LINE ( 'NONE', #46458, #15847 ) ;
#59921=CARTESIAN_POINT ( 'NONE',  ( 1.227938101723756947, 42.65467462194918369, 4.762198645644581951 ) ) ;
#59922=CARTESIAN_POINT ( 'NONE',  ( 4.956653778116966613, 0.000000000000000000, 0.000000000000000000 ) ) ;
#59925=CARTESIAN_POINT ( 'NONE',  ( 5.965394784446460541, -18.95742317323939830, -7.868087674480889859 ) ) ;
#59929=ORIENTED_EDGE ( 'NONE', *, *, #14859, .T. ) ;
#59930=ORIENTED_EDGE ( 'NONE', *, *, #44868, .T. ) ;
#59941=ORIENTED_EDGE ( 'NONE', *, *, #14553, .F. ) ;
#59942=CARTESIAN_POINT ( 'NONE',  ( 0.5837374860065638327, 47.89569815517037199, -0.1816420316517112499 ) ) ;
#59953=ORIENTED_EDGE ( 'NONE', *, *, #14428, .F. ) ;
#59955=ORIENTED_EDGE ( 'NONE', *, *, #48321, .F. ) ;
#59957=CARTESIAN_POINT ( 'NONE',  ( 5.974727161628367256, 7.840226266082543916, -18.96851388233650582 ) ) ;
#59964=ORIENTED_EDGE ( 'NONE', *, *, #15560, .T. ) ;
#59981=CARTESIAN_POINT ( 'NONE',  ( 1.088313998177378172, -15.69908095455125796, -39.93881167962116052 ) ) ;
#59983=CARTESIAN_POINT ( 'NONE',  ( 0.5807400328401637335, 11.87003418057307869, -46.40483864045133089 ) ) ;
#59984=CARTESIAN_POINT ( 'NONE',  ( 0.7762783648524387292, -47.60264408896656363, -5.369627767360320547 ) ) ;
#59986=CARTESIAN_POINT ( 'NONE',  ( 0.5827357941260205010, 38.21849163199676980, 28.86820951701446702 ) ) ;
#59987=CARTESIAN_POINT ( 'NONE',  ( 0.7762777257811908083, -19.15108781300962448, 43.90991299786893620 ) ) ;
#59994=CARTESIAN_POINT ( 'NONE',  ( 0.5850706913938533704, 41.56998471741261625, -23.79070617305337976 ) ) ;
#60003=AXIS2_PLACEMENT_3D ( 'NONE', #6724, #40614, #25867 ) ;
#60007=ORIENTED_EDGE ( 'NONE', *, *, #29011, .F. ) ;
#60022=B_SPLINE_CURVE_WITH_KNOTS ( 'NONE', 3,
 ( #41814, #23003, #42132, #17999 ),
 .UNSPECIFIED., .F., .F.,
 ( 4, 4 ),
 ( 1.843143693225357538E-18, 0.004444878191957663503 ),
 .UNSPECIFIED. ) ;
#60028=ADVANCED_FACE ( 'NONE', ( #7626 ), #28600, .T. ) ;
#60037=VERTEX_POINT ( 'NONE', #13282 ) ;
#60044=ORIENTED_EDGE ( 'NONE', *, *, #45600, .F. ) ;
#60059=CARTESIAN_POINT ( 'NONE',  ( 0.8557997880470599172, 17.48760788519217257, 44.60232077416692675 ) ) ;
#60060=CARTESIAN_POINT ( 'NONE',  ( 0.5809828226811617480, -6.791453954330657794, 47.41188724015877654 ) ) ;
#60066=CARTESIAN_POINT ( 'NONE',  ( 4.967162193818130511, 38.83676580803792433, -18.65818244221215849 ) ) ;
#60068=CARTESIAN_POINT ( 'NONE',  ( 0.9758171775293914552, -30.33669560438090684, 30.34506652060231602 ) ) ;
#60069=CARTESIAN_POINT ( 'NONE',  ( 4.956653778116973719, 27.17045123668471973, 39.67974989265048436 ) ) ;
#60075=CARTESIAN_POINT ( 'NONE',  ( 0.8551540677456715978, -43.91216198251552072, 19.17641535420838039 ) ) ;
#60088=VECTOR ( 'NONE', #26565, 1000.000000000000000 ) ;
#60089=ORIENTED_EDGE ( 'NONE', *, *, #43894, .F. ) ;
#60092=CARTESIAN_POINT ( 'NONE',  ( 0.9730545539215883499, -25.71816799638802920, 34.34678117142546938 ) ) ;
#60093=ORIENTED_EDGE ( 'NONE', *, *, #56624, .T. ) ;
#60102=ORIENTED_EDGE ( 'NONE', *, *, #39057, .F. ) ;
#60107=CARTESIAN_POINT ( 'NONE',  ( 0.6846871229502899947, 28.47437962186182858, -38.52803883689271203 ) ) ;
#60116=B_SPLINE_CURVE_WITH_KNOTS ( 'NONE', 3,
 ( #51516, #23043, #8606, #23960, #38389, #18974 ),
 .UNSPECIFIED., .F., .F.,
 ( 4, 2, 4 ),
 ( 9.745765416140531346E-18, 0.0002291978881530150488, 0.0004583957763060203397 ),
 .UNSPECIFIED. ) ;
#60122=CARTESIAN_POINT ( 'NONE',  ( 5.958863334805807099, -19.82594244347349033, -5.313608583996449752 ) ) ;
#60125=CARTESIAN_POINT ( 'NONE',  ( 0.9749527285493316819, 10.82939760924503680, 41.51939261707886430 ) ) ;
#60132=CARTESIAN_POINT ( 'NONE',  ( 2.624215991343608501, -42.26352390376111856, 22.77108897942121857 ) ) ;
#60133=ORIENTED_EDGE ( 'NONE', *, *, #43869, .F. ) ;
#60138=ORIENTED_EDGE ( 'NONE', *, *, #16286, .F. ) ;
#60139=LINE ( 'NONE', #25396, #21366 ) ;
#60140=CARTESIAN_POINT ( 'NONE',  ( 4.956653778116974607, -32.11725092155068495, 35.79382859084104496 ) ) ;
#60144=EDGE_CURVE ( 'NONE', #57948, #25296, #35427, .T. ) ;
#60147=DIRECTION ( 'NONE',  ( -1.000000000000000000, -0.000000000000000000, -0.000000000000000000 ) ) ;
#60150=CARTESIAN_POINT ( 'NONE',  ( 0.9730545539215883499, -33.73144377768539215, -26.52009130076805832 ) ) ;
#60151=CARTESIAN_POINT ( 'NONE',  ( 4.956653778116975495, -35.79382859084138602, 32.11725092155030836 ) ) ;
#60168=ORIENTED_EDGE ( 'NONE', *, *, #39856, .T. ) ;
#60170=CARTESIAN_POINT ( 'NONE',  ( 0.9749527285493289064, -41.37154756071288375, -11.38116287125098047 ) ) ;
#60176=ORIENTED_EDGE ( 'NONE', *, *, #22806, .T. ) ;
#60177=EDGE_CURVE ( 'NONE', #12115, #17815, #43970, .T. ) ;
#60179=CARTESIAN_POINT ( 'NONE',  ( 0.9730545539215883499, -5.099196237955184507, 42.60426903087352457 ) ) ;
#60187=EDGE_CURVE ( 'NONE', #14690, #3069, #24191, .T. ) ;
#60188=FACE_OUTER_BOUND ( 'NONE', #26075, .T. ) ;
#60191=ORIENTED_EDGE ( 'NONE', *, *, #1552, .T. ) ;
#60198=VERTEX_POINT ( 'NONE', #39885 ) ;
#60215=FACE_OUTER_BOUND ( 'NONE', #5173, .T. ) ;
#60218=CARTESIAN_POINT ( 'NONE',  ( 5.974727161628367256, 20.34732802718247768, -2.694421823322708853 ) ) ;
#60225=B_SPLINE_CURVE_WITH_KNOTS ( 'NONE', 3,
 ( #10146, #58654, #29242, #44005 ),
 .UNSPECIFIED., .F., .F.,
 ( 4, 4 ),
 ( 1.084202172485504434E-18, 0.004048833967417089959 ),
 .UNSPECIFIED. ) ;
#60226=ORIENTED_EDGE ( 'NONE', *, *, #50907, .F. ) ;
#60227=CARTESIAN_POINT ( 'NONE',  ( 4.956653778116982600, -47.05699031914957686, 9.917440902360995736 ) ) ;
#60230=EDGE_LOOP ( 'NONE', ( #43231, #43657, #29387, #47821 ) ) ;
#60231=ORIENTED_EDGE ( 'NONE', *, *, #55941, .F. ) ;
#60233=CARTESIAN_POINT ( 'NONE',  ( 4.960156602257181468, -20.99019478193080701, 41.40608197274629276 ) ) ;
#60238=CARTESIAN_POINT ( 'NONE',  ( 4.956653778116990594, -35.79382859084093127, -32.11725092155079864 ) ) ;
#60241=ORIENTED_EDGE ( 'NONE', *, *, #60365, .T. ) ;
#60243=CONICAL_SURFACE ( 'NONE', #59262, 43.08621763946400307, 1.568696531533066763 ) ;
#60247=B_SPLINE_CURVE_WITH_KNOTS ( 'NONE', 3,
 ( #59554, #7864, #50771, #26983 ),
 .UNSPECIFIED., .F., .F.,
 ( 4, 4 ),
 ( 0.000000000000000000, 0.005004741218457418005 ),
 .UNSPECIFIED. ) ;
#60252=ORIENTED_EDGE ( 'NONE', *, *, #58097, .F. ) ;
#60253=CARTESIAN_POINT ( 'NONE',  ( 0.9730545539215883499, 21.01499094264601908, -37.40983423658450846 ) ) ;
#60257=CARTESIAN_POINT ( 'NONE',  ( 0.5837374860065633886, 12.22086613152827539, -46.31070423340719344 ) ) ;
#60259=VERTEX_POINT ( 'NONE', #5990 ) ;
#60272=CARTESIAN_POINT ( 'NONE',  ( 0.5850706913938533704, 23.79070617305381319, 41.56998471741236756 ) ) ;
#60277=CARTESIAN_POINT ( 'NONE',  ( 0.9757402383260949108, 42.90839848328079853, 0.08489923450653533155 ) ) ;
#60279=CARTESIAN_POINT ( 'NONE',  ( 0.6846871229502932144, 11.56285438919632469, 46.49193983736596181 ) ) ;
#60282=ORIENTED_EDGE ( 'NONE', *, *, #22373, .F. ) ;
#60284=LINE ( 'NONE', #17396, #53905 ) ;
#60285=CARTESIAN_POINT ( 'NONE',  ( 3.660087539127302669, -16.63102164621066237, 45.06758728829461802 ) ) ;
#60286=CARTESIAN_POINT ( 'NONE',  ( 0.7056555295713298204, -0.8411712675124666250, -47.89404551051137560 ) ) ;
#60293=B_SPLINE_CURVE_WITH_KNOTS ( 'NONE', 3,
 ( #5223, #39712, #15276, #24354 ),
 .UNSPECIFIED., .F., .F.,
 ( 4, 4 ),
 ( 0.000000000000000000, 0.005004741218457427546 ),
 .UNSPECIFIED. ) ;
#60294=ADVANCED_FACE ( 'NONE', ( #42570 ), #54561, .T. ) ;
#60295=CARTESIAN_POINT ( 'NONE',  ( 4.956653778116994147, 35.79382859084161339, -32.11725092155005967 ) ) ;
#60307=ORIENTED_EDGE ( 'NONE', *, *, #26746, .T. ) ;
#60313=ORIENTED_EDGE ( 'NONE', *, *, #4711, .T. ) ;
#60315=CARTESIAN_POINT ( 'NONE',  ( 0.5786265663353153954, 47.58023467411538121, 5.535668456754111233 ) ) ;
#60317=EDGE_CURVE ( 'NONE', #11680, #40793, #54131, .T. ) ;
#60319=CARTESIAN_POINT ( 'NONE',  ( 0.8557997880470599172, 33.22501220301901270, 34.51495345639560952 ) ) ;
#60324=CARTESIAN_POINT ( 'NONE',  ( 1.227938101723748288, -26.79402671879349640, 33.52879263017854328 ) ) ;
#60328=ADVANCED_FACE ( 'NONE', ( #46650 ), #8562, .T. ) ;
#60333=CARTESIAN_POINT ( 'NONE',  ( 0.5827357941260191687, 41.65958460246774564, 23.63272379758808484 ) ) ;
#60334=ORIENTED_EDGE ( 'NONE', *, *, #29222, .T. ) ;
#60343=CARTESIAN_POINT ( 'NONE',  ( 5.959828726073459926, -14.51699876360210162, 14.51059719297091455 ) ) ;
#60344=CARTESIAN_POINT ( 'NONE',  ( 4.967162193818129623, -43.02067033766018511, 2.375726030842427061 ) ) ;
#60347=ORIENTED_EDGE ( 'NONE', *, *, #9987, .T. ) ;
#60353=EDGE_LOOP ( 'NONE', ( #20367, #20074, #33276, #30799 ) ) ;
#60358=CARTESIAN_POINT ( 'NONE',  ( 0.9752570700956799676, -30.50353876750651949, 30.17732761204926817 ) ) ;
#60362=CARTESIAN_POINT ( 'NONE',  ( 5.981074661064941900, -12.50143471347293556, 16.27808421740004619 ) ) ;
#60365=EDGE_CURVE ( 'NONE', #23595, #1395, #51941, .T. ) ;
#60367=DIRECTION ( 'NONE',  ( -1.000000000000000000, -0.000000000000000000, -0.000000000000000000 ) ) ;
#60374=VECTOR ( 'NONE', #6573, 1000.000000000000114 ) ;
#60375=LINE ( 'NONE', #12499, #8450 ) ;
#60381=CARTESIAN_POINT ( 'NONE',  ( 0.9722240750034563117, 37.44729079646494796, 20.94823713380351293 ) ) ;
#60385=ORIENTED_EDGE ( 'NONE', *, *, #47192, .F. ) ;
#60388=CARTESIAN_POINT ( 'NONE',  ( 0.8557997880470599172, -41.93815086860273311, 23.15977007032308421 ) ) ;
#60393=CARTESIAN_POINT ( 'NONE',  ( 3.660087539127331535, -45.06758728829456828, -16.63102164621081158 ) ) ;
#60399=DIRECTION ( 'NONE',  ( -0.07439287786467649322, -0.3693942911085712488, 0.9262902123089757911 ) ) ;
#60407=ORIENTED_EDGE ( 'NONE', *, *, #18507, .T. ) ;
#60415=ORIENTED_EDGE ( 'NONE', *, *, #23663, .F. ) ;
#60422=CARTESIAN_POINT ( 'NONE',  ( 0.9730545539215883499, 42.47233286818616449, 6.101350888304794218 ) ) ;
#60425=ORIENTED_EDGE ( 'NONE', *, *, #21775, .F. ) ;
#60426=CARTESIAN_POINT ( 'NONE',  ( 0.8557997880470690211, 43.90420959842208504, -19.17299735371961944 ) ) ;
#60429=CARTESIAN_POINT ( 'NONE',  ( 0.5839879882012686263, 47.48621496524031471, 6.251648354650349404 ) ) ;
#60447=CARTESIAN_POINT ( 'NONE',  ( 0.9736507210033059634, 37.38294557109065863, -21.06291100879400702 ) ) ;
#60450=CARTESIAN_POINT ( 'NONE',  ( 4.960156602257180580, -34.56254177294248109, -30.99165383632803028 ) ) ;
#60452=( BOUNDED_SURFACE ( )  B_SPLINE_SURFACE ( 3, 1, ( 
 ( #52282, #47294 ),
 ( #51981, #42610 ),
 ( #4343, #61671 ),
 ( #37927, #56984 ) ),
 .UNSPECIFIED., .F., .F., .F. ) 
 B_SPLINE_SURFACE_WITH_KNOTS ( ( 4, 4 ),
 ( 2, 2 ),
 ( 0.000000000000000000, 1.000000000000000000 ),
 ( 0.000000000000000000, 1.000000000000000000 ),
 .UNSPECIFIED. ) 
 GEOMETRIC_REPRESENTATION_ITEM ( )  RATIONAL_B_SPLINE_SURFACE ( (
 ( 1.000000000000000000, 1.000000000000000000),
 ( 0.7269869731126817891, 0.9931720237060910339),
 ( 0.7269869731126817891, 0.9931720237060910339),
 ( 1.000000000000000000, 1.000000000000000000) ) ) 
 REPRESENTATION_ITEM ( '' )  SURFACE ( )  );
#60453=VECTOR ( 'NONE', #21264, 1000.000000000000227 ) ;
#60459=CARTESIAN_POINT ( 'NONE',  ( 0.5807400328401637335, 44.04145271122591510, -18.83234461715135311 ) ) ;
#60465=B_SPLINE_CURVE_WITH_KNOTS ( 'NONE', 3,
 ( #20338, #53514, #33830, #10629, #10317, #29411 ),
 .UNSPECIFIED., .F., .F.,
 ( 4, 2, 4 ),
 ( 7.023086426956682172E-18, 0.0002445244328975388660, 0.0004890488657950706848 ),
 .UNSPECIFIED. ) ;
#60468=CARTESIAN_POINT ( 'NONE',  ( 0.7762777257811930287, -33.23866587527452054, -34.49689427664301888 ) ) ;
#60479=CARTESIAN_POINT ( 'NONE',  ( 0.5786265663353196143, 5.535668456753938038, 47.58023467411540963 ) ) ;
#60483=ADVANCED_FACE ( 'NONE', ( #26209 ), #61656, .F. ) ;
#60484=CARTESIAN_POINT ( 'NONE',  ( 0.9756354156337433414, 16.29989858042629791, 39.69194847698937423 ) ) ;
#60490=ORIENTED_EDGE ( 'NONE', *, *, #29681, .F. ) ;
#60491=CARTESIAN_POINT ( 'NONE',  ( 0.5839879882012700696, 44.25011577017269815, 18.32896541547087566 ) ) ;
#60494=ORIENTED_EDGE ( 'NONE', *, *, #38994, .F. ) ;
#60506=CARTESIAN_POINT ( 'NONE',  ( 5.960721111146673579, 18.96557324978287085, -7.848955554238317589 ) ) ;
#60524=CARTESIAN_POINT ( 'NONE',  ( 2.526464513654347321, 27.11556434133549232, 33.34586834545783773 ) ) ;
#60526=CARTESIAN_POINT ( 'NONE',  ( 3.783278058412226752, 9.462251542474405142, -41.98530666033905590 ) ) ;
#60527=CARTESIAN_POINT ( 'NONE',  ( 5.960221823109900008, 10.26751639438368180, -17.77295928189545648 ) ) ;
#60532=CARTESIAN_POINT ( 'NONE',  ( 0.9730545539215892381, 39.83279466599039154, 15.95224156741843835 ) ) ;
#60535=EDGE_CURVE ( 'NONE', #35558, #9042, #13650, .T. ) ;
#60545=VERTEX_POINT ( 'NONE', #44735 ) ;
#60549=CARTESIAN_POINT ( 'NONE',  ( 0.9756008150404614776, -41.40938772927938061, 11.24277293639973507 ) ) ;
#60552=CARTESIAN_POINT ( 'NONE',  ( 4.956653778116966613, 0.000000000000000000, 0.000000000000000000 ) ) ;
#60567=CIRCLE ( 'NONE', #18559, 48.09070567114147110 ) ;
#60576=CARTESIAN_POINT ( 'NONE',  ( 0.9752132459055858904, 30.50512806189410497, 30.17566824627255428 ) ) ;
#60586=CARTESIAN_POINT ( 'NONE',  ( 0.9756354156337447847, -5.471460801653127426, -42.55820231551296473 ) ) ;
#60587=CARTESIAN_POINT ( 'NONE',  ( 4.967162193818130511, 38.44485641567072776, 19.45289607368836116 ) ) ;
#60589=CARTESIAN_POINT ( 'NONE',  ( 0.5837374860065639437, 38.10878877974146661, 29.01294733976374474 ) ) ;
#60600=CARTESIAN_POINT ( 'NONE',  ( 3.783198216974391404, 3.901161703632050504, 42.86118135813606500 ) ) ;
#60630=ORIENTED_EDGE ( 'NONE', *, *, #18755, .T. ) ;
#60634=CARTESIAN_POINT ( 'NONE',  ( 1.227938101723756947, 10.28900963485438425, -41.66816631169181306 ) ) ;
#60638=FACE_OUTER_BOUND ( 'NONE', #18426, .T. ) ;
#60639=CARTESIAN_POINT ( 'NONE',  ( 0.5837374860065626114, 41.56971235019486244, 23.79054246377985038 ) ) ;
#60645=ADVANCED_FACE ( 'NONE', ( #23070 ), #15225, .F. ) ;
#60646=AXIS2_PLACEMENT_3D ( 'NONE', #57880, #29086, #6170 ) ;
#60647=VERTEX_POINT ( 'NONE', #36255 ) ;
#60669=CARTESIAN_POINT ( 'NONE',  ( 0.5786265663353196143, 18.99608782658092920, -43.97352617418595599 ) ) ;
#60670=CARTESIAN_POINT ( 'NONE',  ( 4.963659409799330291, 25.25989740981497889, 36.94443854030229346 ) ) ;
#60674=CARTESIAN_POINT ( 'NONE',  ( 0.5850706913938533704, -6.071602062250300413, -47.50996714391789055 ) ) ;
#60683=CARTESIAN_POINT ( 'NONE',  ( 5.960721111146673579, 7.848955554238242982, 18.96557324978290282 ) ) ;
#60695=CARTESIAN_POINT ( 'NONE',  ( 0.9730545539215883499, -39.44597740938048958, -16.88610103448599986 ) ) ;
#60700=ORIENTED_EDGE ( 'NONE', *, *, #50841, .T. ) ;
#60705=CARTESIAN_POINT ( 'NONE',  ( 0.5807400328401637335, -33.48217046439086175, -34.25275203086271603 ) ) ;
#60707=CARTESIAN_POINT ( 'NONE',  ( 3.660087539127329759, -42.51124390328615732, -22.37124151181823706 ) ) ;
#60717=CARTESIAN_POINT ( 'NONE',  ( 3.270143674763207553, -3.806843787665823431, -13.14781761974173335 ) ) ;
#60719=CARTESIAN_POINT ( 'NONE',  ( 0.5838002273316430513, -37.91535410490848079, -29.26514720557058880 ) ) ;
#60720=ORIENTED_EDGE ( 'NONE', *, *, #22407, .F. ) ;
#60740=EDGE_CURVE ( 'NONE', #35873, #18521, #31637, .T. ) ;
#60743=CARTESIAN_POINT ( 'NONE',  ( 0.7762777257811932508, 34.49689427664313257, -33.23866587527439265 ) ) ;
#60756=CARTESIAN_POINT ( 'NONE',  ( 0.6846871229502932144, 7.109010606688070055, -47.37786444808385511 ) ) ;
#60768=CARTESIAN_POINT ( 'NONE',  ( 0.5809828226811553087, -29.58751527316153940, -37.66417181417581617 ) ) ;
#60770=CARTESIAN_POINT ( 'NONE',  ( 3.407937589446174087, -7.243367523631106586, 11.62731850632881780 ) ) ;
#60771=CARTESIAN_POINT ( 'NONE',  ( 5.959547316686252039, 17.77749189599203206, 10.25972575517536178 ) ) ;
#60774=ORIENTED_EDGE ( 'NONE', *, *, #58097, .T. ) ;
#60777=SURFACE_STYLE_FILL_AREA ( #8462 ) ;
#60779=CARTESIAN_POINT ( 'NONE',  ( 4.967162193818130511, -2.375726030842277403, -43.02067033766020643 ) ) ;
#60796=EDGE_LOOP ( 'NONE', ( #61536, #26182, #47040, #51038 ) ) ;
#60797=ADVANCED_FACE ( 'NONE', ( #6077 ), #21620, .F. ) ;
#60814=EDGE_LOOP ( 'NONE', ( #33746, #41673, #48928, #56428 ) ) ;
#60815=CARTESIAN_POINT ( 'NONE',  ( 0.5832366564991500191, -46.33368520589909423, -12.13301812590398931 ) ) ;
#60822=CARTESIAN_POINT ( 'NONE',  ( 0.9757787079277453479, -16.45683390770812338, 39.62711913632693239 ) ) ;
#60826=( BOUNDED_SURFACE ( )  B_SPLINE_SURFACE ( 3, 1, ( 
 ( #60362, #26564 ),
 ( #17478, #55984 ),
 ( #31894, #59765 ),
 ( #36600, #50975 ) ),
 .UNSPECIFIED., .F., .F., .F. ) 
 B_SPLINE_SURFACE_WITH_KNOTS ( ( 4, 4 ),
 ( 2, 2 ),
 ( 0.000000000000000000, 1.000000000000000000 ),
 ( 0.000000000000000000, 1.000000000000000000 ),
 .UNSPECIFIED. ) 
 GEOMETRIC_REPRESENTATION_ITEM ( )  RATIONAL_B_SPLINE_SURFACE ( (
 ( 1.000000000000000000, 1.000000000000000000),
 ( 0.7269869731126817891, 0.9931720237060910339),
 ( 0.7269869731126817891, 0.9931720237060910339),
 ( 1.000000000000000000, 1.000000000000000000) ) ) 
 REPRESENTATION_ITEM ( '' )  SURFACE ( )  );
#60851=CARTESIAN_POINT ( 'NONE',  ( 0.7762777257811945830, -34.49689427664289809, 33.23866587527464844 ) ) ;
#60853=ORIENTED_EDGE ( 'NONE', *, *, #36439, .F. ) ;
#60863=EDGE_LOOP ( 'NONE', ( #2506, #31124, #11659, #21805 ) ) ;
#60865=B_SPLINE_CURVE_WITH_KNOTS ( 'NONE', 3,
 ( #31316, #45744, #2794, #21926 ),
 .UNSPECIFIED., .F., .F.,
 ( 4, 4 ),
 ( 0.000000000000000000, 0.005004741218457433617 ),
 .UNSPECIFIED. ) ;
#60871=CIRCLE ( 'NONE', #6845, 48.09070567114147110 ) ;
#60872=ORIENTED_EDGE ( 'NONE', *, *, #6308, .T. ) ;
#60874=FACE_OUTER_BOUND ( 'NONE', #32034, .T. ) ;
#60877=CARTESIAN_POINT ( 'NONE',  ( 1.227938101723756947, 20.72293514920803048, -37.58536632582757875 ) ) ;
#60892=CARTESIAN_POINT ( 'NONE',  ( 0.9756008150404603674, 30.44122083654219679, 30.24019526051556639 ) ) ;
#60894=B_SPLINE_CURVE_WITH_KNOTS ( 'NONE', 3,
 ( #27689, #28916, #57096, #8889 ),
 .UNSPECIFIED., .F., .F.,
 ( 4, 4 ),
 ( 1.192622389734054685E-18, 0.004444878191957673044 ),
 .UNSPECIFIED. ) ;
#60901=CARTESIAN_POINT ( 'NONE',  ( 5.860006189529246790, 36.25227510158463673, 31.81514841426769635 ) ) ;
#60911=CARTESIAN_POINT ( 'NONE',  ( 0.7056555295713303755, 11.58338207350465154, -46.47980662829223064 ) ) ;
#60915=DIRECTION ( 'NONE',  ( -1.000000000000000000, -0.000000000000000000, -0.000000000000000000 ) ) ;
#60921=EDGE_CURVE ( 'NONE', #27918, #37400, #60022, .T. ) ;
#60923=VECTOR ( 'NONE', #36619, 1000.000000000000114 ) ;
#60930=CARTESIAN_POINT ( 'NONE',  ( 5.860006189529246790, -43.25137511473236174, -21.34829429597512629 ) ) ;
#60932=( BOUNDED_SURFACE ( )  B_SPLINE_SURFACE ( 3, 1, ( 
 ( #34950, #44362 ),
 ( #44065, #43434 ),
 ( #33718, #6382 ),
 ( #1093, #6082 ) ),
 .UNSPECIFIED., .F., .F., .F. ) 
 B_SPLINE_SURFACE_WITH_KNOTS ( ( 4, 4 ),
 ( 2, 2 ),
 ( 0.000000000000000000, 1.000000000000000000 ),
 ( 0.000000000000000000, 1.000000000000000000 ),
 .UNSPECIFIED. ) 
 GEOMETRIC_REPRESENTATION_ITEM ( )  RATIONAL_B_SPLINE_SURFACE ( (
 ( 1.000000000000000000, 1.000000000000000000),
 ( 0.7269869731126821222, 0.9931720237060910339),
 ( 0.7269869731126821222, 0.9931720237060910339),
 ( 1.000000000000000000, 1.000000000000000000) ) ) 
 REPRESENTATION_ITEM ( '' )  SURFACE ( )  );
#60955=EDGE_CURVE ( 'NONE', #61570, #50394, #32710, .T. ) ;
#60963=CIRCLE ( 'NONE', #33989, 43.08621763946400307 ) ;
#60966=ORIENTED_EDGE ( 'NONE', *, *, #3890, .F. ) ;
#60975=ADVANCED_FACE ( 'NONE', ( #13293 ), #17660, .T. ) ;
#60977=CARTESIAN_POINT ( 'NONE',  ( -19.26650277682250589, -12.38848617149161946, 1.677297214494516631 ) ) ;
#60978=CARTESIAN_POINT ( 'NONE',  ( 4.960156602257182357, 46.28683144126590321, 3.546989772330050084 ) ) ;
#60980=CARTESIAN_POINT ( 'NONE',  ( 1.227938101723756947, 41.66816631169191965, 10.28900963485394904 ) ) ;
#60981=CARTESIAN_POINT ( 'NONE',  ( 5.958863334805807099, -19.82657410201446524, 5.311251202228508106 ) ) ;
#60986=ORIENTED_EDGE ( 'NONE', *, *, #7189, .F. ) ;
#60987=CARTESIAN_POINT ( 'NONE',  ( 5.959547316686252039, -7.851524054666535690, 18.96456592444086908 ) ) ;
#60989=CARTESIAN_POINT ( 'NONE',  ( 0.5809828226811553087, 18.83114015454698631, 44.03860873105701046 ) ) ;
#60993=CARTESIAN_POINT ( 'NONE',  ( 0.5786265663353153954, -43.97352617418629706, 18.99608782658018313 ) ) ;
#60996=ADVANCED_FACE ( 'NONE', ( #7961 ), #29632, .T. ) ;
#61005=FACE_BOUND ( 'NONE', #9622, .T. ) ;
#61008=ORIENTED_EDGE ( 'NONE', *, *, #27002, .F. ) ;
#61009=CARTESIAN_POINT ( 'NONE',  ( 0.9757892942422827787, 11.05594550521701613, -41.45966865212795938 ) ) ;
#61010=( BOUNDED_SURFACE ( )  B_SPLINE_SURFACE ( 3, 1, ( 
 ( #40592, #39663 ),
 ( #16149, #54321 ),
 ( #30527, #59653 ),
 ( #16767, #29613 ) ),
 .UNSPECIFIED., .F., .F., .F. ) 
 B_SPLINE_SURFACE_WITH_KNOTS ( ( 4, 4 ),
 ( 2, 2 ),
 ( 0.000000000000000000, 1.000000000000000000 ),
 ( 0.000000000000000000, 1.000000000000000000 ),
 .UNSPECIFIED. ) 
 GEOMETRIC_REPRESENTATION_ITEM ( )  RATIONAL_B_SPLINE_SURFACE ( (
 ( 1.000000000000000000, 1.000000000000000000),
 ( 0.9953390228620291325, 0.8624445117761032620),
 ( 0.9953390228620291325, 0.8624445117761032620),
 ( 1.000000000000000000, 1.000000000000000000) ) ) 
 REPRESENTATION_ITEM ( '' )  SURFACE ( )  );
#61026=ORIENTED_EDGE ( 'NONE', *, *, #7412, .T. ) ;
#61027=CARTESIAN_POINT ( 'NONE',  ( 2.281448460670573830, -42.18752512472227068, -22.83953674062058070 ) ) ;
#61042=CARTESIAN_POINT ( 'NONE',  ( 0.8551540677456715978, 47.61725548905997840, -5.348818140990417191 ) ) ;
#61044=CARTESIAN_POINT ( 'NONE',  ( 4.963659409799328515, -40.34793212403981499, 19.36487359954685417 ) ) ;
#61049=EDGE_CURVE ( 'NONE', #53786, #40335, #42864, .T. ) ;
#61052=VERTEX_POINT ( 'NONE', #10124 ) ;
#61055=CARTESIAN_POINT ( 'NONE',  ( 5.960721111146673579, -5.306302591836717930, 19.82781442290488627 ) ) ;
#61059=CARTESIAN_POINT ( 'NONE',  ( 0.5839880159502344181, 47.48028790449886571, 6.296669079378329315 ) ) ;
#61070=CARTESIAN_POINT ( 'NONE',  ( 5.958863334805807099, -7.855954700275743718, 18.96276366205780661 ) ) ;
#61072=CARTESIAN_POINT ( 'NONE',  ( 0.5837374860065636106, 6.071555045025283093, -47.50965286059331305 ) ) ;
#61073=CARTESIAN_POINT ( 'NONE',  ( 5.959547316686252039, 19.82715097195154996, 5.308980600728524735 ) ) ;
#61078=ORIENTED_EDGE ( 'NONE', *, *, #42600, .T. ) ;
#61092=CARTESIAN_POINT ( 'NONE',  ( 1.227938101723748288, -30.94118573761333479, 29.74462687941215222 ) ) ;
#61097=CARTESIAN_POINT ( 'NONE',  ( 0.8557997880470599172, 28.43566216844970640, 38.55640757422448672 ) ) ;
#61105=CARTESIAN_POINT ( 'NONE',  ( 0.9745511491811742477, -16.10518088436877093, -39.77127619790159230 ) ) ;
#61111=ADVANCED_FACE ( 'NONE', ( #53324 ), #42865, .F. ) ;
#61112=CARTESIAN_POINT ( 'NONE',  ( 5.959547316686252039, 12.49803383497728326, 16.28190225198622443 ) ) ;
#61114=CARTESIAN_POINT ( 'NONE',  ( 3.783278058412223643, 22.99727281874625717, 36.37891728069877928 ) ) ;
#61126=CARTESIAN_POINT ( 'NONE',  ( 5.860006189529246790, -43.26650951066883266, 21.31760477694567513 ) ) ;
#61127=CARTESIAN_POINT ( 'NONE',  ( 5.960221823109900008, -12.49086489703216607, -16.28736530777586466 ) ) ;
#61132=CARTESIAN_POINT ( 'NONE',  ( 0.9968887458511642707, 39.89008038581167170, -15.81144734640142424 ) ) ;
#61135=CARTESIAN_POINT ( 'NONE',  ( 5.960721111146673579, 19.82781442290498219, -5.306302591836375981 ) ) ;
#61136=EDGE_CURVE ( 'NONE', #39909, #42030, #14449, .T. ) ;
#61137=CARTESIAN_POINT ( 'NONE',  ( 5.960221823109900008, 5.317678907195162452, 19.82478916873576225 ) ) ;
#61140=CARTESIAN_POINT ( 'NONE',  ( 0.9757402383260949108, 37.11731350497355919, 21.52772413548494868 ) ) ;
#61145=ADVANCED_FACE ( 'NONE', ( #47727 ), #12861, .F. ) ;
#61151=ORIENTED_EDGE ( 'NONE', *, *, #13578, .T. ) ;
#61153=LINE ( 'NONE', #37383, #53502 ) ;
#61155=CARTESIAN_POINT ( 'NONE',  ( 5.958863334805807099, 19.82594244347345480, 5.313608583996586532 ) ) ;
#61156=ORIENTED_EDGE ( 'NONE', *, *, #50417, .F. ) ;
#61160=B_SPLINE_CURVE_WITH_KNOTS ( 'NONE', 3,
 ( #51446, #27971, #38020, #51765 ),
 .UNSPECIFIED., .F., .F.,
 ( 4, 4 ),
 ( 9.813077866773594792E-18, 0.005004741218457441423 ),
 .UNSPECIFIED. ) ;
#61163=VERTEX_POINT ( 'NONE', #25442 ) ;
#61167=CARTESIAN_POINT ( 'NONE',  ( 0.5850706913938534814, -18.49682194437931670, -44.18063951072240769 ) ) ;
#61170=ORIENTED_EDGE ( 'NONE', *, *, #35112, .T. ) ;
#61171=CARTESIAN_POINT ( 'NONE',  ( 0.5839879882012681822, -12.39641777360489350, -46.26394433311397592 ) ) ;
#61172=B_SPLINE_CURVE_WITH_KNOTS ( 'NONE', 3,
 ( #2944, #31461, #12688, #45899 ),
 .UNSPECIFIED., .F., .F.,
 ( 4, 4 ),
 ( 5.421010862427522170E-19, 0.004444878191957664371 ),
 .UNSPECIFIED. ) ;
#61174=CARTESIAN_POINT ( 'NONE',  ( 1.227938101723748288, 11.92353943228006585, -41.23019537246697297 ) ) ;
#61176=CARTESIAN_POINT ( 'NONE',  ( 2.281448460670569389, -45.98107640562105303, 13.68109378871694481 ) ) ;
#61183=ORIENTED_EDGE ( 'NONE', *, *, #27361, .F. ) ;
#61189=EDGE_CURVE ( 'NONE', #24422, #38048, #44904, .T. ) ;
#61195=( BOUNDED_SURFACE ( )  B_SPLINE_SURFACE ( 3, 1, ( 
 ( #36045, #3402 ),
 ( #60122, #36351 ),
 ( #31627, #36652 ),
 ( #7807, #26932 ) ),
 .UNSPECIFIED., .F., .F., .F. ) 
 B_SPLINE_SURFACE_WITH_KNOTS ( ( 4, 4 ),
 ( 2, 2 ),
 ( 0.000000000000000000, 1.000000000000000000 ),
 ( 0.000000000000000000, 1.000000000000000000 ),
 .UNSPECIFIED. ) 
 GEOMETRIC_REPRESENTATION_ITEM ( )  RATIONAL_B_SPLINE_SURFACE ( (
 ( 1.000000000000000000, 1.000000000000000000),
 ( 0.9732289882329797637, 0.9999525324661233672),
 ( 0.9732289882329797637, 0.9999525324661233672),
 ( 1.000000000000000000, 1.000000000000000000) ) ) 
 REPRESENTATION_ITEM ( '' )  SURFACE ( )  );
#61201=CARTESIAN_POINT ( 'NONE',  ( 0.9758171775293917882, 30.34506652060244747, 30.33669560438079316 ) ) ;
#61203=EDGE_LOOP ( 'NONE', ( #4459, #36098, #1165, #57265 ) ) ;
#61204=CARTESIAN_POINT ( 'NONE',  ( 5.959547316686252039, 18.96456592444089395, 7.851524054666477959 ) ) ;
#61205=CARTESIAN_POINT ( 'NONE',  ( 4.960156602257181468, 38.31207700265951388, 26.21519897043440039 ) ) ;
#61208=CARTESIAN_POINT ( 'NONE',  ( 1.227938101723756947, -22.18841447410693846, -36.73927144310534487 ) ) ;
#61209=CARTESIAN_POINT ( 'NONE',  ( 0.9730545539215883499, 42.90536227157002003, 0.5054011016614263774 ) ) ;
#61210=CARTESIAN_POINT ( 'NONE',  ( 2.281351352603276261, 45.98107981851866555, 13.68106635380579661 ) ) ;
#61213=CARTESIAN_POINT ( 'NONE',  ( 5.958863334805807099, 10.26176968287920310, 17.77634700750932595 ) ) ;
#61219=B_SPLINE_CURVE_WITH_KNOTS ( 'NONE', 3,
 ( #55487, #11139, #45825, #30223, #2562, #59889, #17003, #2869, #41434, #60491, #17607, #315, #19461, #57323, #4089, #38580 ),
 .UNSPECIFIED., .F., .F.,
 ( 4, 3, 3, 3, 3, 4 ),
 ( 1.250973872328959318E-17, 0.0002724568934985580949, 0.0004086836638483871400, 0.0005449104342063620671, 0.0008173270854453674322, 0.001089761613562689226 ),
 .UNSPECIFIED. ) ;
#61224=ADVANCED_FACE ( 'NONE', ( #5695 ), #36454, .F. ) ;
#61226=EDGE_CURVE ( 'NONE', #28131, #39143, #19643, .T. ) ;
#61230=ORIENTED_EDGE ( 'NONE', *, *, #1369, .F. ) ;
#61242=ORIENTED_EDGE ( 'NONE', *, *, #6944, .T. ) ;
#61243=CARTESIAN_POINT ( 'NONE',  ( 0.9754402186311947887, 41.49454543482930546, 10.92425836141432960 ) ) ;
#61252=CARTESIAN_POINT ( 'NONE',  ( 0.9972139404380295780, 15.81078898082040674, -39.89035676513719153 ) ) ;
#61260=CARTESIAN_POINT ( 'NONE',  ( 0.9757954354143123510, 0.03224588977124673295, 42.90846090505963417 ) ) ;
#61263=EDGE_CURVE ( 'NONE', #39947, #4978, #40527, .T. ) ;
#61264=EDGE_LOOP ( 'NONE', ( #25438, #56698, #31474, #48823 ) ) ;
#61267=CARTESIAN_POINT ( 'NONE',  ( 1.227938101723748288, -4.762198645644156514, -42.65467462194923343 ) ) ;
#61272=CARTESIAN_POINT ( 'NONE',  ( 0.5827357941260202789, -47.53228940613939812, -5.891356987508117982 ) ) ;
#61276=VERTEX_POINT ( 'NONE', #46742 ) ;
#61291=FACE_OUTER_BOUND ( 'NONE', #40359, .T. ) ;
#61295=CARTESIAN_POINT ( 'NONE',  ( 0.5809828226811553087, -47.89273459658654275, 0.5448590168530708100 ) ) ;
#61305=CARTESIAN_POINT ( 'NONE',  ( 0.8551540677456715978, -44.61036085020937492, -17.49081417858833731 ) ) ;
#61312=ORIENTED_EDGE ( 'NONE', *, *, #37934, .F. ) ;
#61315=DIRECTION ( 'NONE',  ( -1.000000000000000000, -0.000000000000000000, -0.000000000000000000 ) ) ;
#61316=CARTESIAN_POINT ( 'NONE',  ( -19.55483905134862965, -7.879146627487763510, -1.388794482494389637 ) ) ;
#61321=CARTESIAN_POINT ( 'NONE',  ( 3.783198216974389627, 42.86118135813612184, -3.901161703631621958 ) ) ;
#61323=ORIENTED_EDGE ( 'NONE', *, *, #59250, .F. ) ;
#61328=CARTESIAN_POINT ( 'NONE',  ( 0.5809828226811617480, -29.58751527316205809, 37.66417181417541826 ) ) ;
#61331=CARTESIAN_POINT ( 'NONE',  ( 4.967162193818130511, 7.970725651240403664, -42.34252806656584056 ) ) ;
#61332=VECTOR ( 'NONE', #45250, 1000.000000000000000 ) ;
#61335=CARTESIAN_POINT ( 'NONE',  ( 5.960721111146673579, 12.50019045452738276, -16.28018152803680252 ) ) ;
#61340=CARTESIAN_POINT ( 'NONE',  ( 5.959547316686252039, -18.96183906913549322, 7.858107265727412027 ) ) ;
#61341=CARTESIAN_POINT ( 'NONE',  ( 0.9758171775293921213, 34.04519363167634793, 26.11633498242636264 ) ) ;
#61347=B_SPLINE_CURVE_WITH_KNOTS ( 'NONE', 3,
 ( #4376, #23514, #61703, #61097 ),
 .UNSPECIFIED., .F., .F.,
 ( 4, 4 ),
 ( 0.000000000000000000, 0.004446090762761357312 ),
 .UNSPECIFIED. ) ;
#61359=B_SPLINE_CURVE_WITH_KNOTS ( 'NONE', 3,
 ( #2289, #21418, #17342, #8230 ),
 .UNSPECIFIED., .F., .F.,
 ( 4, 4 ),
 ( 0.000000000000000000, 0.005004741218457423209 ),
 .UNSPECIFIED. ) ;
#61363=CARTESIAN_POINT ( 'NONE',  ( 0.8551540677456739292, -44.61036085020961650, 17.49081417858772269 ) ) ;
#61365=ORIENTED_EDGE ( 'NONE', *, *, #21746, .T. ) ;
#61376=CARTESIAN_POINT ( 'NONE',  ( 2.281448460670572054, -1.314143534315570072, -47.95523685111405143 ) ) ;
#61385=CARTESIAN_POINT ( 'NONE',  ( 0.7762783648524379521, 46.03397615175201452, -13.25585403815072105 ) ) ;
#61387=DIRECTION ( 'NONE',  ( 0.000000000000000000, 0.000000000000000000, 1.000000000000000000 ) ) ;
#61389=CARTESIAN_POINT ( 'NONE',  ( 5.860006189529246790, 45.67886430272052678, -15.48781697582000483 ) ) ;
#61391=CARTESIAN_POINT ( 'NONE',  ( 4.956653778116988818, -45.71126949320240840, -14.93973939759935021 ) ) ;
#61393=LINE ( 'NONE', #22597, #17843 ) ;
#61394=VERTEX_POINT ( 'NONE', #4698 ) ;
#61401=ORIENTED_EDGE ( 'NONE', *, *, #30182, .F. ) ;
#61402=CARTESIAN_POINT ( 'NONE',  ( 5.960721111146673579, 16.28018152803692686, -12.50019045452721222 ) ) ;
#61403=CARTESIAN_POINT ( 'NONE',  ( 0.8551540677456739292, -37.45266983663475457, -29.88829867897852921 ) ) ;
#61407=CARTESIAN_POINT ( 'NONE',  ( 5.860006189529234355, -9.393028332205062725, 47.30964106197854591 ) ) ;
#61410=CARTESIAN_POINT ( 'NONE',  ( 0.5836750258453350382, -33.73891062492380399, -33.99574025613945594 ) ) ;
#61413=VERTEX_POINT ( 'NONE', #24451 ) ;
#61417=CARTESIAN_POINT ( 'NONE',  ( 2.526552050251864578, 12.29062829844035498, -41.18423939305552040 ) ) ;
#61426=CARTESIAN_POINT ( 'NONE',  ( 0.6846871229502899947, 38.52803883689301756, 28.47437962186140226 ) ) ;
#61431=CARTESIAN_POINT ( 'NONE',  ( 0.5839879882012696255, -46.26394433311389065, 12.39641777360504449 ) ) ;
#61444=CARTESIAN_POINT ( 'NONE',  ( 0.5786265663353153954, 34.37803667029811550, 33.35675271369551353 ) ) ;
#61445=VECTOR ( 'NONE', #8184, 1000.000000000000114 ) ;
#61447=CARTESIAN_POINT ( 'NONE',  ( 0.9730545539215883499, 34.34678117142556175, 25.71816799638790840 ) ) ;
#61448=CARTESIAN_POINT ( 'NONE',  ( 0.9757892942422831117, 39.66188497122492151, 16.37293303864320038 ) ) ;
#61449=ORIENTED_EDGE ( 'NONE', *, *, #16443, .T. ) ;
#61456=CARTESIAN_POINT ( 'NONE',  ( 0.5827359174754810356, -34.12345922495634909, 33.60976280407636807 ) ) ;
#61459=EDGE_LOOP ( 'NONE', ( #17151, #20896, #35426, #36347 ) ) ;
#61461=CARTESIAN_POINT ( 'NONE',  ( 0.9756950546413923897, -11.19893879603418974, -41.42124338356090618 ) ) ;
#61462=ORIENTED_EDGE ( 'NONE', *, *, #4409, .F. ) ;
#61465=B_SPLINE_CURVE_WITH_KNOTS ( 'NONE', 3,
 ( #54503, #11631, #34206, #34827, #54193, #5954 ),
 .UNSPECIFIED., .F., .F.,
 ( 4, 2, 4 ),
 ( 0.000000000000000000, 0.0002291966416970797290, 0.0004583932833941594580 ),
 .UNSPECIFIED. ) ;
#61472=CARTESIAN_POINT ( 'NONE',  ( 0.8557997880470697982, -46.03118133706034598, 13.27832040216623355 ) ) ;
#61473=VERTEX_POINT ( 'NONE', #53258 ) ;
#61474=B_SPLINE_CURVE_WITH_KNOTS ( 'NONE', 3,
 ( #60227, #6978, #59000, #36154 ),
 .UNSPECIFIED., .F., .F.,
 ( 4, 4 ),
 ( 0.000000000000000000, 0.004446090762761366853 ),
 .UNSPECIFIED. ) ;
#61478=EDGE_LOOP ( 'NONE', ( #39344, #4554, #61462, #29575 ) ) ;
#61480=EDGE_CURVE ( 'NONE', #19687, #39282, #39200, .T. ) ;
#61485=CARTESIAN_POINT ( 'NONE',  ( 0.9757954354143116849, 5.207268878499845415E-15, 42.90846090505964128 ) ) ;
#61488=ADVANCED_FACE ( 'NONE', ( #10673 ), #21257, .F. ) ;
#61494=MECHANICAL_DESIGN_GEOMETRIC_PRESENTATION_REPRESENTATION('',(#48506),#36545);
#61511=CARTESIAN_POINT ( 'NONE',  ( 0.7057020205115021039, 47.59410670607645955, -5.417413437617099703 ) ) ;
#61524=CARTESIAN_POINT ( 'NONE',  ( 0.5786265663353196143, 0.7221568112313164756, -47.89572889566445468 ) ) ;
#61530=ORIENTED_EDGE ( 'NONE', *, *, #28006, .T. ) ;
#61532=CARTESIAN_POINT ( 'NONE',  ( 1.227938101723756947, -42.91134962331487657, 0.8460948827223682134 ) ) ;
#61536=ORIENTED_EDGE ( 'NONE', *, *, #6981, .F. ) ;
#61563=EDGE_CURVE ( 'NONE', #39811, #46967, #46359, .T. ) ;
#61565=VERTEX_POINT ( 'NONE', #41359 ) ;
#61570=VERTEX_POINT ( 'NONE', #27541 ) ;
#61579=ADVANCED_FACE ( 'NONE', ( #50420 ), #51233, .F. ) ;
#61580=CARTESIAN_POINT ( 'NONE',  ( 0.9730545539215892381, 26.52009130076819687, -33.73144377768529978 ) ) ;
#61584=EDGE_CURVE ( 'NONE', #4220, #59114, #60865, .T. ) ;
#61588=VERTEX_POINT ( 'NONE', #17229 ) ;
#61594=CARTESIAN_POINT ( 'NONE',  ( 0.5827359174754840332, 0.3632382226757386867, -47.89462060834301127 ) ) ;
#61597=CARTESIAN_POINT ( 'NONE',  ( 0.9730545539215883499, 41.57420493492400482, -10.61654491617520080 ) ) ;
#61599=CARTESIAN_POINT ( 'NONE',  ( 0.5809828226811617480, 47.41188724015879785, 6.791453954330491705 ) ) ;
#61600=CARTESIAN_POINT ( 'NONE',  ( 0.5807400328401637335, -44.04145271122577299, 18.83234461715167640 ) ) ;
#61610=CARTESIAN_POINT ( 'NONE',  ( 0.9722240750034575330, 30.74950257331021319, 29.92651530838598717 ) ) ;
#61611=CYLINDRICAL_SURFACE ( 'NONE', #43728, 12.50000000000000000 ) ;
#61615=CARTESIAN_POINT ( 'NONE',  ( 5.974727161628369032, 18.95664195401506191, 7.868887636447684741 ) ) ;
#61621=CARTESIAN_POINT ( 'NONE',  ( 1.227938101723748288, 41.23019537246709376, 11.92353943227963597 ) ) ;
#61631=CARTESIAN_POINT ( 'NONE',  ( 0.5836750258453364815, -38.10871351907207583, 29.01293504009526103 ) ) ;
#61646=CARTESIAN_POINT ( 'NONE',  ( 0.9730545539215883499, 34.34678117142556175, 25.71816799638790840 ) ) ;
#61656=( BOUNDED_SURFACE ( )  B_SPLINE_SURFACE ( 3, 1, ( 
 ( #50027, #2395 ),
 ( #45350, #1464 ),
 ( #30917, #54388 ),
 ( #49401, #2077 ) ),
 .UNSPECIFIED., .F., .F., .F. ) 
 B_SPLINE_SURFACE_WITH_KNOTS ( ( 4, 4 ),
 ( 2, 2 ),
 ( 0.000000000000000000, 1.000000000000000000 ),
 ( 0.000000000000000000, 1.000000000000000000 ),
 .UNSPECIFIED. ) 
 GEOMETRIC_REPRESENTATION_ITEM ( )  RATIONAL_B_SPLINE_SURFACE ( (
 ( 1.000000000000000000, 1.000000000000000000),
 ( 0.7269869731126817891, 0.9931720237060910339),
 ( 0.7269869731126817891, 0.9931720237060910339),
 ( 1.000000000000000000, 1.000000000000000000) ) ) 
 REPRESENTATION_ITEM ( '' )  SURFACE ( )  );
#61661=ORIENTED_EDGE ( 'NONE', *, *, #49945, .F. ) ;
#61662=ADVANCED_FACE ( 'NONE', ( #46667 ), #12487, .F. ) ;
#61665=DIRECTION ( 'NONE',  ( -0.07439287786467650709, -0.9161872986448725831, 0.3937848822959336137 ) ) ;
#61671=CARTESIAN_POINT ( 'NONE',  ( 2.624215991343620935, 1.411420423865478613, 47.98682984381861871 ) ) ;
#61673=CARTESIAN_POINT ( 'NONE',  ( 5.860006189529234355, 47.30964106197858854, 9.393028332204897524 ) ) ;
#61674=CARTESIAN_POINT ( 'NONE',  ( 0.5850706913938534814, -41.38834827854224585, 24.10530971368273612 ) ) ;
#61678=CARTESIAN_POINT ( 'NONE',  ( 0.8551540677456715978, -11.51835730326512142, 46.51172240253117707 ) ) ;
#61679=B_SPLINE_CURVE_WITH_KNOTS ( 'NONE', 3,
 ( #12081, #54319, #1394, #49033 ),
 .UNSPECIFIED., .F., .F.,
 ( 4, 4 ),
 ( 4.336808689942017120E-17, 0.005004741218457454434 ),
 .UNSPECIFIED. ) ;
#61680=ADVANCED_FACE ( 'NONE', ( #23157 ), #10460, .F. ) ;
#61683=CARTESIAN_POINT ( 'NONE',  ( 0.9972139404380295780, -39.89035676513721285, -15.81078898082028594 ) ) ;
#61686=LINE ( 'NONE', #8456, #16737 ) ;
#61703=CARTESIAN_POINT ( 'NONE',  ( 2.281351352603289584, 28.15073776031364972, 38.84542754822333421 ) ) ;
#61705=CARTESIAN_POINT ( 'NONE',  ( 2.526464513654346877, -12.29060355381822056, -41.18424249084328181 ) ) ;
#61706=CARTESIAN_POINT ( 'NONE',  ( 4.967162193818130511, 14.26841313271282097, 40.65506779172170582 ) ) ;
#61707=CARTESIAN_POINT ( 'NONE',  ( 5.960721111146673579, -18.96073515164554379, 7.860635756377555516 ) ) ;
#61709=EDGE_LOOP ( 'NONE', ( #16696, #2937, #1779, #54805 ) ) ;
#61712=AXIS2_PLACEMENT_3D ( 'NONE', #16300, #58567, #25383 ) ;
#61722=CARTESIAN_POINT ( 'NONE',  ( 0.5800708119828332787, 47.56394195701287231, 5.628966929617906345 ) ) ;
#61724=ORIENTED_EDGE ( 'NONE', *, *, #14585, .F. ) ;
#61729=DIRECTION ( 'NONE',  ( 0.000000000000000000, 0.000000000000000000, 1.000000000000000000 ) ) ;
#61734=CARTESIAN_POINT ( 'NONE',  ( 2.281351352603289584, 4.956540261593756824, 47.71649595778612962 ) ) ;
#61738=CARTESIAN_POINT ( 'NONE',  ( 0.5827357941260210561, -44.38787053017136230, -17.99287562175633681 ) ) ;
#61741=CARTESIAN_POINT ( 'NONE',  ( 0.5839879327111935359, -46.24044206955225889, 12.48412918464419974 ) ) ;
#61749=CARTESIAN_POINT ( 'NONE',  ( 0.9754402186311941225, 37.25324696807229685, 21.29160191075010644 ) ) ;
#61751=CARTESIAN_POINT ( 'NONE',  ( 0.9730545539215883499, -37.40983423658458662, -21.01499094264588763 ) ) ;
#61761=ORIENTED_EDGE ( 'NONE', *, *, #28444, .T. ) ;
#61762=CARTESIAN_POINT ( 'NONE',  ( 0.5839880159502345292, -33.89965136132169476, 33.83547574026613347 ) ) ;
#61763=CARTESIAN_POINT ( 'NONE',  ( 0.5786265663353153954, 37.55861529268594268, -29.72999788434255564 ) ) ;
#61766=CARTESIAN_POINT ( 'NONE',  ( 0.9756008150404589241, -11.24277293639960362, -41.40938772927945877 ) ) ;
#61767=VERTEX_POINT ( 'NONE', #35264 ) ;
#61770=CARTESIAN_POINT ( 'NONE',  ( 0.9730545539215883499, -41.57420493492393376, 10.61654491617549034 ) ) ;
#61772=ORIENTED_EDGE ( 'NONE', *, *, #41027, .T. ) ;
#61777=B_SPLINE_CURVE_WITH_KNOTS ( 'NONE', 3,
 ( #47239, #42550, #18733, #14047, #50677, #7767 ),
 .UNSPECIFIED., .F., .F.,
 ( 4, 2, 4 ),
 ( 6.256513556477135401E-18, 0.0002445244328975379445, 0.0004890488657950697090 ),
 .UNSPECIFIED. ) ;
#61781=CARTESIAN_POINT ( 'NONE',  ( 0.8551540677456834771, 24.74404575822774888, 41.03346287276437465 ) ) ;
#61793=EDGE_LOOP ( 'NONE', ( #2072, #44190, #53263, #49690 ) ) ;
#61803=AXIS2_PLACEMENT_3D ( 'NONE', #4080, #52014, #30830 ) ;
#61807=CARTESIAN_POINT ( 'NONE',  ( 0.5807400328401637335, -44.04145271122550298, -18.83234461715230168 ) ) ;
#61809=DIRECTION ( 'NONE',  ( 0.000000000000000000, 0.000000000000000000, 1.000000000000000000 ) ) ;
#61814=FACE_OUTER_BOUND ( 'NONE', #48745, .T. ) ;
#61826=CARTESIAN_POINT ( 'NONE',  ( 1.154321485836935057, -39.32643515542047652, 17.18284940416437223 ) ) ;
#61829=CARTESIAN_POINT ( 'NONE',  ( 0.5834872094924179464, 12.17696997821523119, 46.32218741137602080 ) ) ;
#61832=CARTESIAN_POINT ( 'NONE',  ( 4.963659409799330291, 3.403493583737315475, 44.62477100936217056 ) ) ;
#61834=EDGE_LOOP ( 'NONE', ( #29216, #40610, #54856, #317 ) ) ;
#61846=CARTESIAN_POINT ( 'NONE',  ( 0.9730545539215892381, 29.98130006528861813, 30.69604515769660935 ) ) ;
#61847=EDGE_CURVE ( 'NONE', #44407, #45339, #3873, .T. ) ;
#61854=CARTESIAN_POINT ( 'NONE',  ( 5.959547316686252039, 2.675599016784261597, 20.35048796920737857 ) ) ;
#61865=CYLINDRICAL_SURFACE ( 'NONE', #9383, 2.099999999999996092 ) ;
#61874=CYLINDRICAL_SURFACE ( 'NONE', #57520, 2.099999999999996092 ) ;
#61875=ORIENTED_EDGE ( 'NONE', *, *, #36439, .T. ) ;
#61879=CARTESIAN_POINT ( 'NONE',  ( 0.5839254288179551722, -47.47429404163003142, -6.341681103465038660 ) ) ;
#61888=CARTESIAN_POINT ( 'NONE',  ( 0.5809828226811548646, -47.41188724015884048, 6.791453954330148868 ) ) ;
#61898=CARTESIAN_POINT ( 'NONE',  ( 2.526464513654346877, 34.82216969498465176, 25.19161096467240313 ) ) ;
#61904=( BOUNDED_SURFACE ( )  B_SPLINE_SURFACE ( 3, 1, ( 
 ( #61335, #22836 ),
 ( #51325, #56334 ),
 ( #61946, #14074 ),
 ( #19084, #33176 ) ),
 .UNSPECIFIED., .F., .F., .F. ) 
 B_SPLINE_SURFACE_WITH_KNOTS ( ( 4, 4 ),
 ( 2, 2 ),
 ( 0.000000000000000000, 1.000000000000000000 ),
 ( 0.000000000000000000, 1.000000000000000000 ),
 .UNSPECIFIED. ) 
 GEOMETRIC_REPRESENTATION_ITEM ( )  RATIONAL_B_SPLINE_SURFACE ( (
 ( 1.000000000000000000, 1.000000000000000000),
 ( 0.9953390228620291325, 0.8624445117760984880),
 ( 0.9953390228620291325, 0.8624445117760984880),
 ( 1.000000000000000000, 1.000000000000000000) ) ) 
 REPRESENTATION_ITEM ( '' )  SURFACE ( )  );
#61913=EDGE_CURVE ( 'NONE', #48862, #41443, #52660, .T. ) ;
#61920=CARTESIAN_POINT ( 'NONE',  ( 5.965394784446460541, 18.95742317323934145, 7.868087674481023086 ) ) ;
#61927=CARTESIAN_POINT ( 'NONE',  ( 5.974727161628369032, -12.48248968439917661, -16.29297756969643984 ) ) ;
#61928=CARTESIAN_POINT ( 'NONE',  ( 0.5819845901640491315, 47.54333976522124772, -5.801229454883471526 ) ) ;
#61938=EDGE_LOOP ( 'NONE', ( #17820, #27254, #1327, #2156 ) ) ;
#61942=CARTESIAN_POINT ( 'NONE',  ( 4.956653778116971054, 42.88673967249130925, 21.75875759808722876 ) ) ;
#61943=ORIENTED_EDGE ( 'NONE', *, *, #23429, .F. ) ;
#61945=ORIENTED_EDGE ( 'NONE', *, *, #42616, .T. ) ;
#61946=CARTESIAN_POINT ( 'NONE',  ( 5.959828726073459926, 12.49879082830568144, -16.28130559351252060 ) ) ;
#61947=ORIENTED_EDGE ( 'NONE', *, *, #21148, .F. ) ;
#61952=CARTESIAN_POINT ( 'NONE',  ( 0.9740398440564311811, 34.29238484271531462, 25.79088785828992769 ) ) ;
#61959=ORIENTED_EDGE ( 'NONE', *, *, #11790, .F. ) ;
#61960=FILL_AREA_STYLE_COLOUR ( '', #459 ) ;
#61967=EDGE_LOOP ( 'NONE', ( #40259, #27142, #18518, #7857, #38882, #55800, #9705, #38762, #39476, #58088, #20620, #26425, #61761, #20996, #575, #41043, #42244, #28354, #53320, #36175, #60307, #18395, #23613, #11346, #24064, #23231, #43220, #1753, #3621, #20898, #6616, #21061, #136, #33313, #21228, #28659, #55640, #57438, #18453, #11485, #23743, #10822, #54724, #29693, #56027, #48969, #33307, #54145, #5633, #24206, #32010, #42514, #17242, #20427, #47196, #10266, #40939, #42544, #24686, #3290, #19303, #26507, #27877, #5371, #24009, #38644, #12371, #33935, #53142, #61530, #35419, #13596, #6286, #15120, #33210, #16049, #42123, #4790, #26535, #28772, #18542, #23829, #38428, #33995, #41801, #22837, #47890, #13341, #60168, #8005, #32934, #18303, #22015, #29217, #18824, #43336, #22203, #28823, #55126, #30212, #57708, #14934, #55956, #45427, #36627, #59555, #30526, #1924, #24490, #18835, #61078, #25982, #49409, #21618, #7928, #17473, #1214, #19308, #5574, #23470, #34188, #12907, #42891, #16721, #51015, #17338, #45891, #56455, #54286, #13608, #1767, #15610, #24363, #12050, #6882, #27970, #44137, #40213, #43580, #49647, #37751, #26984, #18218, #14820, #59223, #3676, #46808, #29919 ) ) ;
ENDSEC;
END-ISO-10303-21;
